ISO-10303-21;
HEADER;
FILE_DESCRIPTION (('STEP AP214'),
    '1' );
FILE_NAME ('Airflow Sleeve.step',
    '2026-10-05T22:38:29',
    ( '' ),
    ( '' ),
    'SwSTEP 2.0',
    'SolidWorks 2020',
    '' );
FILE_SCHEMA (( 'AUTOMOTIVE_DESIGN' ));
ENDSEC;

DATA;
#11=CARTESIAN_POINT ( 'NONE',  ( 17.93538082550040613, 0.4959841406075952142, -12.68696163625449991 ) ) ;
#12=CARTESIAN_POINT ( 'NONE',  ( 12.26368341514758420, 2.812488373142785214, -12.37327521544950670 ) ) ;
#22=CARTESIAN_POINT ( 'NONE',  ( 18.07822721942927302, 2.978550302103497138, 12.24288824562991351 ) ) ;
#27=CARTESIAN_POINT ( 'NONE',  ( 12.80505043854146940, -1.875000000000000444, 13.78631952119025605 ) ) ;
#29=FACE_OUTER_BOUND ( 'NONE', #10230, .T. ) ;
#39=CARTESIAN_POINT ( 'NONE',  ( 43.76123417800000226, 13.94845324556000143, -4.312847325879000770 ) ) ;
#40=CARTESIAN_POINT ( 'NONE',  ( 12.29711362085063797, 1.966768764679983184, 12.44555721978031038 ) ) ;
#48=CARTESIAN_POINT ( 'NONE',  ( 12.27854653041788957, 2.836954440259892962, 12.36664979425441580 ) ) ;
#51=CARTESIAN_POINT ( 'NONE',  ( 12.25734197670618641, 0.3012394090295977822, 12.69519438487549756 ) ) ;
#55=CARTESIAN_POINT ( 'NONE',  ( 12.37605701841387607, -2.954974367521621570, 13.56637846613975107 ) ) ;
#56=CARTESIAN_POINT ( 'NONE',  ( 12.19373784185879472, 2.630112414937235688, 13.64494795218897671 ) ) ;
#63=AXIS2_PLACEMENT_3D ( 'NONE', #33493, #16702, #6562 ) ;
#64=CARTESIAN_POINT ( 'NONE',  ( 17.89568490471441820, 3.024116370425395939, -12.31388631808444600 ) ) ;
#66=DIRECTION ( 'NONE',  ( 0.000000000000000000, -1.000000000000000000, 0.000000000000000000 ) ) ;
#90=CARTESIAN_POINT ( 'NONE',  ( 12.26246717640210626, 0.3103928943003824159, -13.89533876751735342 ) ) ;
#93=VERTEX_POINT ( 'NONE', #24168 ) ;
#99=CARTESIAN_POINT ( 'NONE',  ( 18.17480529351248109, -2.583342416263718633, -12.43177882285068137 ) ) ;
#103=CARTESIAN_POINT ( 'NONE',  ( 12.21303990359567848, -0.2014071429975183569, 13.89805485625563541 ) ) ;
#120=CARTESIAN_POINT ( 'NONE',  ( 12.27869449350093056, -2.837185661390559499, 13.59614283363490905 ) ) ;
#138=CARTESIAN_POINT ( 'NONE',  ( 18.16648463825930548, 2.629536981073587132, -12.42046771373108172 ) ) ;
#145=CARTESIAN_POINT ( 'NONE',  ( 17.65093666542126272, 1.765655615500123954, 12.47567830514603671 ) ) ;
#147=CARTESIAN_POINT ( 'NONE',  ( 12.18127380957210093, 0.04040257046694419041, -12.69991905489011685 ) ) ;
#156=EDGE_CURVE ( 'NONE', #45407, #3060, #52452, .T. ) ;
#164=CARTESIAN_POINT ( 'NONE',  ( 18.14041819333145966, 2.719953065120093161, -13.62436182279261132 ) ) ;
#166=DIRECTION ( 'NONE',  ( -1.000000000000000000, -0.000000000000000000, -0.000000000000000000 ) ) ;
#169=ORIENTED_EDGE ( 'NONE', *, *, #59426, .T. ) ;
#179=ORIENTED_EDGE ( 'NONE', *, *, #15611, .T. ) ;
#184=CARTESIAN_POINT ( 'NONE',  ( 17.79602238657566105, -1.801771354310902185, -12.47051018296933833 ) ) ;
#198=CARTESIAN_POINT ( 'NONE',  ( 12.37517135966887061, 2.046199321548339611, -13.75929785978299158 ) ) ;
#201=CARTESIAN_POINT ( 'NONE',  ( 17.81345962944524075, -0.5694488842926289651, 13.88429844810378277 ) ) ;
#204=CARTESIAN_POINT ( 'NONE',  ( 4.599999999999999645, 0.7302158263239199032, -13.98094363220830871 ) ) ;
#207=CARTESIAN_POINT ( 'NONE',  ( 18.00676300522524897, -0.4321619634102875085, -13.89096157872279313 ) ) ;
#217=CARTESIAN_POINT ( 'NONE',  ( 18.17882706751078814, 0.04040257046694405857, 12.69991905489010442 ) ) ;
#236=CARTESIAN_POINT ( 'NONE',  ( 18.05312913029195698, 3.003720153666129100, -12.23674614497118718 ) ) ;
#249=DIRECTION ( 'NONE',  ( 1.000000000000000000, 0.000000000000000000, 0.000000000000000000 ) ) ;
#256=CARTESIAN_POINT ( 'NONE',  ( 12.39106450428430328, 2.968342857027793880, -12.33004038639662525 ) ) ;
#263=CARTESIAN_POINT ( 'NONE',  ( 17.74546162999697074, 0.7003689475978067680, 12.58057160030229227 ) ) ;
#266=CARTESIAN_POINT ( 'NONE',  ( 12.19523649643098295, -2.361571219431551238, -12.48275271858022073 ) ) ;
#271=CARTESIAN_POINT ( 'NONE',  ( 12.33310466175879938, -1.963577280744732700, -13.86161695422964435 ) ) ;
#275=CARTESIAN_POINT ( 'NONE',  ( 18.18412234634031677, -2.838955764657545178, 12.27602435542072001 ) ) ;
#283=LINE ( 'NONE', #64587, #6388 ) ;
#294=CARTESIAN_POINT ( 'NONE',  ( 12.24435292127285457, -0.2761699508452415963, 12.69595998167824114 ) ) ;
#298=B_SPLINE_SURFACE_WITH_KNOTS ( 'NONE', 1, 3, ( 
 ( #36914, #9639, #20138, #1143, #64749, #9988, #794, #31326, #57534, #6370, #16864, #59521, #32957, #54271, #27720, #57888, #22453, #65093, #20482, #63112, #9292, #51944, #4044, #25381, #52296, #62775, #14897, #4393, #15239, #52637, #4732, #26076, #47405, #68709, #1833, #12323, #28061, #7414, #23497, #39935, #7767, #45525, #50766, #66835, #61253, #28763, #39582, #7071, #28408, #13371, #17570, #39237, #38897, #60218, #33306, #59864, #8114, #17919, #23151, #49371, #23845, #50076, #49724, #34696, #11970, #18262, #44500, #1485, #60562, #33654, #18608, #56007, #65793, #24188, #18947, #29458, #12669, #2860, #33999, #54624, #55317, #6721, #2182, #22801, #65450, #44838, #54971, #44152, #66144, #60906 ),
 ( #29109, #13023, #34350, #55669, #50415, #2518, #45180, #66485, #25906, #31169, #47237, #41642, #61593, #9821, #57367, #30471, #51446, #52472, #29803, #67171, #13710, #15071, #51786, #19981, #25565, #35039, #4570, #62947, #20315, #4228, #51107, #8800, #61938, #3883, #35716, #8459, #14734, #14051, #68540, #36397, #40276, #67515, #41303, #57033, #19636, #46892, #56353, #3209, #24536, #3541, #46208, #62612, #40610, #30140, #45862, #57713, #19285, #35379, #36052, #9134, #14399, #46554, #56700, #9471, #24878, #40957, #62280, #25216, #67857, #30813, #68196, #52124, #20662, #41988, #52823, #26256, #53164, #64672, #63295, #53849, #54188, #15423, #5947, #5265, #36748, #31501, #714, #58069, #6287, #27634 ) ),
 .UNSPECIFIED., .F., .F., .F.,
 ( 2, 2 ),
 ( 4, 2, 2, 2, 2, 2, 2, 2, 2, 2, 2, 2, 2, 2, 2, 2, 2, 2, 2, 2, 2, 2, 2, 2, 2, 2, 2, 2, 2, 2, 2, 2, 2, 2, 2, 2, 2, 2, 2, 2, 2, 2, 2, 2, 4 ),
 ( 0.000000000000000000, 1.000000000000000000 ),
 ( 0.000000000000000000, 7.143002489358809843E-05, 0.0001428600497871761969, 0.0002142900746807642953, 0.0002857200995743523937, 0.0003214351120211464429, 0.0003571501244679404921, 0.0003928651369147345414, 0.0004285801493615285906, 0.0005000101742551166890, 0.0005357251867019107924, 0.0005714401991487047874, 0.0006071552115954987824, 0.0006428702240422928859, 0.0007143002489358809843, 0.0007857302738294690827, 0.0008214452862762631861, 0.0008571602987230571812, 0.0009285903236166452796, 0.001000020348510233378, 0.001071450373403821585, 0.001142880398297409575, 0.001214310423190997565, 0.001285740448084585772, 0.001321455460531379984, 0.001357170472978173979, 0.001428600497871761969, 0.001500030522765349959, 0.001535745535212143954, 0.001571460547658938165, 0.001607175560105732377, 0.001642890572552526372, 0.001714320597446114362, 0.001750035609892908357, 0.001785750622339702352, 0.001821465634786496347, 0.001857180647233290559, 0.001928610672126878766, 0.001964325684573672761, 0.002000040697020466756, 0.002035755709467261185, 0.002071470721914055180, 0.002142900746807643170, 0.002214330771701231160, 0.002285760796594819150 ),
 .UNSPECIFIED. ) ;
#304=CARTESIAN_POINT ( 'NONE',  ( 18.12478797189196555, 2.757742546077707857, 13.61537068597721856 ) ) ;
#308=ORIENTED_EDGE ( 'NONE', *, *, #5264, .T. ) ;
#314=CARTESIAN_POINT ( 'NONE',  ( 17.55505043854144276, -0.6250000000000001110, -25.00000000000000000 ) ) ;
#318=CARTESIAN_POINT ( 'NONE',  ( 17.60327209889956279, -1.789008353514938809, -13.88522434179080101 ) ) ;
#322=ORIENTED_EDGE ( 'NONE', *, *, #42337, .T. ) ;
#337=CARTESIAN_POINT ( 'NONE',  ( 12.50285324413422394, 1.826185914346435180, -12.46695919779662098 ) ) ;
#340=CARTESIAN_POINT ( 'NONE',  ( 18.17508454104003945, 2.579277621789493047, -13.65633006993505205 ) ) ;
#345=CARTESIAN_POINT ( 'NONE',  ( 12.58137933218757887, -3.164643396295688138, -12.19610741112356678 ) ) ;
#351=CARTESIAN_POINT ( 'NONE',  ( 17.77734287254348544, -0.6847469513499682137, -12.58138041838080490 ) ) ;
#353=EDGE_CURVE ( 'NONE', #93, #10401, #47217, .T. ) ;
#354=CARTESIAN_POINT ( 'NONE',  ( 12.37651575364836098, 2.955073904862975720, -12.33383124654925567 ) ) ;
#359=AXIS2_PLACEMENT_3D ( 'NONE', #39, #4584, #43386 ) ;
#365=CARTESIAN_POINT ( 'NONE',  ( 18.17347573203822009, 2.104651709959050265, 12.42298141210392970 ) ) ;
#366=DIRECTION ( 'NONE',  ( 0.000000000000000000, -0.7198977633594745296, 0.6940801180771755119 ) ) ;
#370=ORIENTED_EDGE ( 'NONE', *, *, #4078, .T. ) ;
#371=CARTESIAN_POINT ( 'NONE',  ( 12.27369669298503574, -2.970039040581493595, 12.24495604130071946 ) ) ;
#378=CARTESIAN_POINT ( 'NONE',  ( 12.61757266016683410, 0.6952251598378623720, 12.58080715426405938 ) ) ;
#381=CARTESIAN_POINT ( 'NONE',  ( 12.58060354176263296, 1.796139714418076627, 12.47132288122299570 ) ) ;
#383=PLANE ( 'NONE',  #54416 ) ;
#390=CARTESIAN_POINT ( 'NONE',  ( 18.16002653637816167, -0.1622975230824323101, 12.69869204565316601 ) ) ;
#393=CARTESIAN_POINT ( 'NONE',  ( 12.76469316422328859, 0.6249999999999994449, 12.67928922306548145 ) ) ;
#395=CARTESIAN_POINT ( 'NONE',  ( 18.00086602808685754, -0.5750310236731011049, -12.58704914195511293 ) ) ;
#397=CARTESIAN_POINT ( 'NONE',  ( 12.21870270123690183, -2.283379404039359351, 13.71702370352176104 ) ) ;
#408=CARTESIAN_POINT ( 'NONE',  ( 17.72806902343758040, 3.100663240735257897, -12.29112607895898890 ) ) ;
#416=CARTESIAN_POINT ( 'NONE',  ( 21.60000021221999944, -12.84999978760999895, -2.874109817690000262E-09 ) ) ;
#417=DIRECTION ( 'NONE',  ( -0.000000000000000000, 0.6555644356537908557, 0.7551392392836745460 ) ) ;
#424=CARTESIAN_POINT ( 'NONE',  ( 17.57587793826700562, -3.124999446933518943, 13.52084426442465315 ) ) ;
#429=CIRCLE ( 'NONE', #68538, 2.000000000000001776 ) ;
#430=DIRECTION ( 'NONE',  ( 0.9999999999999473754, 3.241492201312155981E-07, 2.435229255853115792E-09 ) ) ;
#433=CARTESIAN_POINT ( 'NONE',  ( 12.60522794377905775, 0.5937363472582638524, -13.88293910736286030 ) ) ;
#444=CARTESIAN_POINT ( 'NONE',  ( 18.09708155689165565, -2.811828937043457266, -12.37344130164188805 ) ) ;
#446=DIRECTION ( 'NONE',  ( 1.000000000000000000, 0.000000000000000000, 0.000000000000000000 ) ) ;
#449=CARTESIAN_POINT ( 'NONE',  ( 12.18127378141864980, 0.04040202251154181162, 13.89992604541790477 ) ) ;
#465=CARTESIAN_POINT ( 'NONE',  ( 12.71012035425584763, 0.7146386402729469900, 12.57972080578532470 ) ) ;
#483=CARTESIAN_POINT ( 'NONE',  ( 17.63847140754354470, 3.120744938278101177, -12.28504437646774328 ) ) ;
#489=EDGE_CURVE ( 'NONE', #48158, #58325, #17998, .T. ) ;
#493=CARTESIAN_POINT ( 'NONE',  ( 12.52804317529069955, 0.5603556898929429320, -12.68335562943301476 ) ) ;
#501=CARTESIAN_POINT ( 'NONE',  ( 18.17180710799850374, 0.1030387083473175008, 12.69945707558845704 ) ) ;
#508=CARTESIAN_POINT ( 'NONE',  ( 17.92121436125177070, 3.006915247989151219, -13.55278817016120740 ) ) ;
#510=CARTESIAN_POINT ( 'NONE',  ( 4.599999999999999645, 1.875000000000000000, -13.78631952119025073 ) ) ;
#524=AXIS2_PLACEMENT_3D ( 'NONE', #22459, #44507, #60569 ) ;
#526=DIRECTION ( 'NONE',  ( 0.000000000000000000, 0.9553735099700838562, 0.2954005017724949944 ) ) ;
#530=CARTESIAN_POINT ( 'NONE',  ( 17.97864539808068329, 0.4596704780454121120, -13.88977177191355139 ) ) ;
#541=ORIENTED_EDGE ( 'NONE', *, *, #19877, .T. ) ;
#546=CARTESIAN_POINT ( 'NONE',  ( 12.61254665343898651, 3.094705746550272529, -13.52917745889216228 ) ) ;
#549=CARTESIAN_POINT ( 'NONE',  ( 17.65768761389442787, -0.6168528257048858654, 13.88157091029611045 ) ) ;
#552=B_SPLINE_CURVE_WITH_KNOTS ( 'NONE', 3,
 ( #4825, #10765, #5523, #63558 ),
 .UNSPECIFIED., .F., .F.,
 ( 4, 4 ),
 ( 0.000000000000000000, 1.000000000000000000 ),
 .UNSPECIFIED. ) ;
#554=CARTESIAN_POINT ( 'NONE',  ( 12.53086501621864635, 0.5620205154750185228, 13.88470856849518675 ) ) ;
#558=EDGE_CURVE ( 'NONE', #9109, #56864, #53026, .T. ) ;
#559=ADVANCED_FACE ( 'NONE', ( #55130 ), #12482, .F. ) ;
#568=CARTESIAN_POINT ( 'NONE',  ( 17.93538082550040613, -0.4959841406075954362, 12.68696163625449103 ) ) ;
#582=CARTESIAN_POINT ( 'NONE',  ( 12.53842182639420244, -0.6689867242971878625, -12.58222862546947241 ) ) ;
#584=CARTESIAN_POINT ( 'NONE',  ( 17.81282484970910573, 3.152868460668829975, -12.19915726504404851 ) ) ;
#585=CARTESIAN_POINT ( 'NONE',  ( 5.596495275685874127, 12.13697930370352296, 3.751366953416817029 ) ) ;
#598=CARTESIAN_POINT ( 'NONE',  ( 17.81326568215976636, -0.5695321295966285779, -13.88429381145914299 ) ) ;
#614=CARTESIAN_POINT ( 'NONE',  ( 12.55381283423609418, -1.927626388171778116, -12.56664888159296112 ) ) ;
#620=CARTESIAN_POINT ( 'NONE',  ( 12.15267534726965337, -2.198616041048526704, -13.82629894333309295 ) ) ;
#624=CARTESIAN_POINT ( 'NONE',  ( 18.25535445515778576, -2.667446342172965501, 12.31441698789904393 ) ) ;
#645=ADVANCED_FACE ( 'NONE', ( #36905 ), #41460, .T. ) ;
#652=CARTESIAN_POINT ( 'NONE',  ( 18.08647318473500221, 2.829117779091812501, 13.59807435138920617 ) ) ;
#666=CARTESIAN_POINT ( 'NONE',  ( 18.27992102884633141, -2.544330805874861934, -13.76687901878135278 ) ) ;
#686=CARTESIAN_POINT ( 'NONE',  ( 12.15211780798802188, 2.166395227764201792, -12.41237995041120712 ) ) ;
#689=CARTESIAN_POINT ( 'NONE',  ( 18.07075314651731546, 2.853223032301765105, -13.59217294861458036 ) ) ;
#694=CARTESIAN_POINT ( 'NONE',  ( 12.50326937753805190, -3.134539878383340472, -12.20388000700442355 ) ) ;
#702=CARTESIAN_POINT ( 'NONE',  ( 17.65049462686344128, -0.7131288892044901351, -12.57980326738671906 ) ) ;
#713=CARTESIAN_POINT ( 'NONE',  ( 18.16391642019718944, 2.089583161048361060, 12.42552483951006614 ) ) ;
#714=CARTESIAN_POINT ( 'NONE',  ( 12.70945613931266394, 1.793774045999471989, 13.88460948128834538 ) ) ;
#719=CARTESIAN_POINT ( 'NONE',  ( 12.63802361681261743, -3.180808137691513604, 12.19190235712762416 ) ) ;
#726=CARTESIAN_POINT ( 'NONE',  ( 12.08617037725598031, 0.09400131084486976207, 12.59965472429368916 ) ) ;
#729=CARTESIAN_POINT ( 'NONE',  ( 12.20420485406508782, 2.672372548754606836, 12.40973746665996025 ) ) ;
#734=CARTESIAN_POINT ( 'NONE',  ( 17.55505043854143565, 1.875000000000000000, -13.78631952119025073 ) ) ;
#736=CARTESIAN_POINT ( 'NONE',  ( 12.35392836371782188, 2.932699513109607192, 12.34015408322985863 ) ) ;
#738=ORIENTED_EDGE ( 'NONE', *, *, #19532, .T. ) ;
#739=CARTESIAN_POINT ( 'NONE',  ( 12.38151466835624070, 0.4597251443544757565, 12.68880184500992137 ) ) ;
#745=CARTESIAN_POINT ( 'NONE',  ( 12.08613047971140020, -2.614761652440403150, 13.75367554324229680 ) ) ;
#748=ORIENTED_EDGE ( 'NONE', *, *, #51140, .F. ) ;
#754=CARTESIAN_POINT ( 'NONE',  ( 17.81575242098903544, 1.931873426913545355, -12.56596755615859884 ) ) ;
#771=CARTESIAN_POINT ( 'NONE',  ( 18.00577237252833385, -2.933105347812601238, 13.57200668515162434 ) ) ;
#781=AXIS2_PLACEMENT_3D ( 'NONE', #36370, #52797, #57683 ) ;
#791=CARTESIAN_POINT ( 'NONE',  ( 17.77739983953771841, -3.084473828682777974, -12.29598274197197760 ) ) ;
#793=DIRECTION ( 'NONE',  ( 0.000000000000000000, -0.7270098363383266094, 0.6866270442294852838 ) ) ;
#794=CARTESIAN_POINT ( 'NONE',  ( 12.64146116164745060, 3.103558470340185504, 13.52669597090169695 ) ) ;
#797=CARTESIAN_POINT ( 'NONE',  ( 12.30917092924265077, -0.3809766167652373636, 13.89298487834589402 ) ) ;
#814=CARTESIAN_POINT ( 'NONE',  ( 17.55505043854147118, -3.248109929747637903, 13.61799478206225444 ) ) ;
#827=CARTESIAN_POINT ( 'NONE',  ( 5.568708401995168700, -12.91387459874235688, -2.616215378977960970 ) ) ;
#838=CARTESIAN_POINT ( 'NONE',  ( 12.66237550623657704, 0.6088395004560429591, -12.68034807294329980 ) ) ;
#840=CARTESIAN_POINT ( 'NONE',  ( 5.500000000000000000, 12.87590651766999983, 2.791353855799999728 ) ) ;
#843=EDGE_LOOP ( 'NONE', ( #8756, #37718, #39211, #61668 ) ) ;
#854=CARTESIAN_POINT ( 'NONE',  ( 17.55505043854143565, 3.125000000000000000, -13.52084414783465505 ) ) ;
#862=CARTESIAN_POINT ( 'NONE',  ( 18.11689826751305787, 0.2739464174175113564, -12.69602652205120208 ) ) ;
#863=AXIS2_PLACEMENT_3D ( 'NONE', #9240, #47006, #61366 ) ;
#874=AXIS2_PLACEMENT_3D ( 'NONE', #61387, #34827, #56139 ) ;
#879=CARTESIAN_POINT ( 'NONE',  ( 18.13610176147147257, 0.2304125752724597853, -13.89743363615660776 ) ) ;
#892=CARTESIAN_POINT ( 'NONE',  ( 12.21987570834413006, 2.720459983100028012, -13.62424277487875024 ) ) ;
#896=CARTESIAN_POINT ( 'NONE',  ( 18.16408159376649323, -0.1418539764880170639, 13.89904537328360767 ) ) ;
#902=CARTESIAN_POINT ( 'NONE',  ( 12.24303834293817417, 0.2736100116213214806, 13.89637849652254609 ) ) ;
#903=CARTESIAN_POINT ( 'NONE',  ( 12.32624190542397891, -0.4017285589307944549, -13.89218662323934339 ) ) ;
#905=CARTESIAN_POINT ( 'NONE',  ( 17.82908354277550700, -0.5620915422472464451, -13.88470483921558341 ) ) ;
#914=CARTESIAN_POINT ( 'NONE',  ( 18.17477462772146524, -0.08167875237853229609, 12.69965198491186342 ) ) ;
#929=CARTESIAN_POINT ( 'NONE',  ( 12.13954479299508904, 0.2856017019952032387, -12.59676745213710447 ) ) ;
#945=CARTESIAN_POINT ( 'NONE',  ( 12.80505043854146940, -3.166049082260463443, -13.55318600037536747 ) ) ;
#946=CARTESIAN_POINT ( 'NONE',  ( 18.16373243908211776, -0.1422577892986764680, -13.89902525486550289 ) ) ;
#951=DIRECTION ( 'NONE',  ( 0.000000000000000000, -1.000000000000000000, 0.000000000000000000 ) ) ;
#957=CARTESIAN_POINT ( 'NONE',  ( 17.94049251029959535, -1.899108762321214394, 13.87060088084272458 ) ) ;
#964=CARTESIAN_POINT ( 'NONE',  ( 12.18778960455906635, -2.401422506651156752, -12.47398279053984282 ) ) ;
#968=FACE_OUTER_BOUND ( 'NONE', #9546, .T. ) ;
#969=CARTESIAN_POINT ( 'NONE',  ( 12.30654613137385489, -1.987682873648405124, -13.85818111229402838 ) ) ;
#972=CARTESIAN_POINT ( 'NONE',  ( 17.81328364446397927, -1.807903055951888938, 12.46962321666120665 ) ) ;
#983=VECTOR ( 'NONE', #46111, 1000.000000000000227 ) ;
#984=CARTESIAN_POINT ( 'NONE',  ( 18.00454058110402755, -1.908039605442538145, -12.45487753843153200 ) ) ;
#1000=CARTESIAN_POINT ( 'NONE',  ( 18.18012160401607957, 2.482106737233722882, 13.67720576235794638 ) ) ;
#1015=CARTESIAN_POINT ( 'NONE',  ( 18.26357562437061688, -2.673039206754515007, -13.74245258260623714 ) ) ;
#1029=CARTESIAN_POINT ( 'NONE',  ( 17.92302462182508194, 1.881539600493004061, 13.87303898715941486 ) ) ;
#1031=ORIENTED_EDGE ( 'NONE', *, *, #60303, .F. ) ;
#1035=CARTESIAN_POINT ( 'NONE',  ( 12.80505043854143388, 1.874999999999999556, -12.57545641911172751 ) ) ;
#1042=ORIENTED_EDGE ( 'NONE', *, *, #49334, .T. ) ;
#1053=CARTESIAN_POINT ( 'NONE',  ( 17.95964167607823114, -0.4764818960106708690, -12.68796903437993606 ) ) ;
#1058=DIRECTION ( 'NONE',  ( -1.000000000000000000, 0.000000000000000000, 0.000000000000000000 ) ) ;
#1059=B_SPLINE_CURVE_WITH_KNOTS ( 'NONE', 3,
 ( #43938, #50214, #65243, #60353 ),
 .UNSPECIFIED., .F., .F.,
 ( 4, 4 ),
 ( 0.000000000000000000, 1.000000000000000000 ),
 .UNSPECIFIED. ) ;
#1063=CARTESIAN_POINT ( 'NONE',  ( 18.20581337561478108, 2.797825772877919004, 12.28545032770987078 ) ) ;
#1069=CARTESIAN_POINT ( 'NONE',  ( 12.15211780798805385, -2.166395227764209341, 12.41237995041120712 ) ) ;
#1074=CARTESIAN_POINT ( 'NONE',  ( 12.08961557973415779, -0.1170514037749869340, 12.59946170170351643 ) ) ;
#1077=CARTESIAN_POINT ( 'NONE',  ( 12.18120961385783829, 2.543048387066358274, 12.44145101111442742 ) ) ;
#1081=CARTESIAN_POINT ( 'NONE',  ( 18.22927867710214045, -0.2646961475753731308, 12.59722401988189411 ) ) ;
#1084=CARTESIAN_POINT ( 'NONE',  ( 17.69617877293821451, -0.6091736731909352942, 12.68032649603923545 ) ) ;
#1091=CARTESIAN_POINT ( 'NONE',  ( 18.20209611037771325, 2.854851737536822753, -12.27307487513336959 ) ) ;
#1095=CARTESIAN_POINT ( 'NONE',  ( 12.21493840618619053, -2.942228658260931162, 13.68734401625692954 ) ) ;
#1098=ORIENTED_EDGE ( 'NONE', *, *, #66211, .F. ) ;
#1106=CARTESIAN_POINT ( 'NONE',  ( 18.00740283128405395, 2.068595914410284120, -12.54170588102538808 ) ) ;
#1118=CARTESIAN_POINT ( 'NONE',  ( 17.84291783703838874, -3.054853729147657848, 13.53999333998545218 ) ) ;
#1120=ORIENTED_EDGE ( 'NONE', *, *, #39328, .F. ) ;
#1125=CARTESIAN_POINT ( 'NONE',  ( 12.70654069053541768, -3.248070099070596850, -13.61800428248625572 ) ) ;
#1143=CARTESIAN_POINT ( 'NONE',  ( 12.72201428491563746, 3.119809216722633227, 13.52222099568140479 ) ) ;
#1144=CARTESIAN_POINT ( 'NONE',  ( 17.57589479786111042, -1.875260891896569415, 12.57541370809468972 ) ) ;
#1147=CARTESIAN_POINT ( 'NONE',  ( 12.70241326318844877, 0.6168528257048850882, 13.88157091029611045 ) ) ;
#1154=DIRECTION ( 'NONE',  ( -1.000000000000000000, 0.000000000000000000, 0.000000000000000000 ) ) ;
#1172=CARTESIAN_POINT ( 'NONE',  ( 5.700000000000001954, -13.02829083177932823, 1.966948496269156132 ) ) ;
#1175=CARTESIAN_POINT ( 'NONE',  ( 12.80505043854146940, -1.787797342887047947, -13.88538010501570774 ) ) ;
#1179=VECTOR ( 'NONE', #6236, 1000.000000000000000 ) ;
#1189=CARTESIAN_POINT ( 'NONE',  ( 12.72228957558485618, 1.874999999999999778, -13.78631905550013137 ) ) ;
#1191=CARTESIAN_POINT ( 'NONE',  ( 5.568708408617618844, 12.91387460240243357, 2.616215362094806540 ) ) ;
#1196=CARTESIAN_POINT ( 'NONE',  ( 18.09779212070452914, 0.3101159434603414367, 12.69490728026488569 ) ) ;
#1200=CARTESIAN_POINT ( 'NONE',  ( 5.634824896760862067, 12.09997259267891678, -3.741298181620886343 ) ) ;
#1215=CARTESIAN_POINT ( 'NONE',  ( 17.71800267517521377, -3.104751769966808794, -13.52637079326617453 ) ) ;
#1221=CARTESIAN_POINT ( 'NONE',  ( 18.10291897067260436, 0.3009486140249941211, -13.89561788111246621 ) ) ;
#1227=AXIS2_PLACEMENT_3D ( 'NONE', #62461, #20852, #62798 ) ;
#1228=EDGE_CURVE ( 'NONE', #12996, #40006, #20300, .T. ) ;
#1230=CARTESIAN_POINT ( 'NONE',  ( 12.80505043854144276, 0.6249999999999994449, 13.88107975066923316 ) ) ;
#1232=DIRECTION ( 'NONE',  ( 1.000000000000000000, 0.000000000000000000, 0.000000000000000000 ) ) ;
#1235=CARTESIAN_POINT ( 'NONE',  ( 12.18088137079341671, 2.461818645006701445, -13.68150212747531214 ) ) ;
#1238=CARTESIAN_POINT ( 'NONE',  ( 17.99694095195319221, -0.5793931417437904186, 13.98801390351337659 ) ) ;
#1239=CARTESIAN_POINT ( 'NONE',  ( 17.89454199030562620, 0.5248377731126082635, 13.88666204734250620 ) ) ;
#1243=CARTESIAN_POINT ( 'NONE',  ( 12.76469414187607399, -0.6250000000000007772, 13.88107975724713761 ) ) ;
#1244=CARTESIAN_POINT ( 'NONE',  ( 12.31443335387396054, -0.3873583148778746987, -13.89273910399192147 ) ) ;
#1246=CARTESIAN_POINT ( 'NONE',  ( 17.72543224073729817, -0.6019432101965236370, -13.88245510388864012 ) ) ;
#1254=CARTESIAN_POINT ( 'NONE',  ( 18.06292190248829499, -0.3644117276601269717, 12.69296657371243953 ) ) ;
#1256=CARTESIAN_POINT ( 'NONE',  ( 17.59643454745107505, -3.124999999999999556, -12.28373095898681910 ) ) ;
#1269=CARTESIAN_POINT ( 'NONE',  ( 12.13047558099394863, 0.2638285456865417933, -12.59724228039519822 ) ) ;
#1271=CONICAL_SURFACE ( 'NONE', #33670, 2.100040596737999810, 0.7853981633972997312 ) ;
#1275=ORIENTED_EDGE ( 'NONE', *, *, #68206, .F. ) ;
#1287=CARTESIAN_POINT ( 'NONE',  ( 12.15658143857204898, 2.853298863252174744, -12.27345178217327160 ) ) ;
#1289=CARTESIAN_POINT ( 'NONE',  ( 18.17902784157848473, -0.04113803725886195500, -13.89993798560270122 ) ) ;
#1298=CARTESIAN_POINT ( 'NONE',  ( 12.30950027206278818, -2.881007065227998876, -13.58518188446750230 ) ) ;
#1300=CARTESIAN_POINT ( 'NONE',  ( 17.55505043854144631, 0.7192913403693005359, 12.57945229203838267 ) ) ;
#1302=CARTESIAN_POINT ( 'NONE',  ( 12.61159012396490731, -1.905606515074950602, -12.57035430044310331 ) ) ;
#1308=CARTESIAN_POINT ( 'NONE',  ( 12.80505043854146940, -3.199751711897561801, 12.18694338143115452 ) ) ;
#1309=CARTESIAN_POINT ( 'NONE',  ( 17.75769270374273390, -3.091259753241552222, 12.29395838111495465 ) ) ;
#1324=FACE_BOUND ( 'NONE', #36148, .T. ) ;
#1338=CARTESIAN_POINT ( 'NONE',  ( 17.94528078231815371, 2.988314720655957935, 13.55762497744564321 ) ) ;
#1351=CARTESIAN_POINT ( 'NONE',  ( 17.57920283571460374, -1.787797991197240366, -13.88537998700429910 ) ) ;
#1373=CARTESIAN_POINT ( 'NONE',  ( 12.54706542093073018, 3.153101027525006650, -12.19910009420586050 ) ) ;
#1391=CARTESIAN_POINT ( 'NONE',  ( 18.17180462559269571, -0.1017072266180428924, -12.69945743039636099 ) ) ;
#1392=CARTESIAN_POINT ( 'NONE',  ( 12.19259201841741813, 2.624586292379584851, -12.42169361725944832 ) ) ;
#1400=CARTESIAN_POINT ( 'NONE',  ( 18.20050923854813263, 2.808308534135711909, 12.28305809155435924 ) ) ;
#1408=CARTESIAN_POINT ( 'NONE',  ( 12.15953697780020093, -2.808329718129386254, 12.28305324893824313 ) ) ;
#1414=CARTESIAN_POINT ( 'NONE',  ( 12.08472055051101890, 0.08234928811776985602, 12.59973629603894096 ) ) ;
#1419=CARTESIAN_POINT ( 'NONE',  ( 12.59749754106150554, 3.089553852145856983, 12.29445441479364831 ) ) ;
#1434=CARTESIAN_POINT ( 'NONE',  ( 17.92003806247919329, 0.6285461057906830407, -12.58436427553157166 ) ) ;
#1437=CARTESIAN_POINT ( 'NONE',  ( 12.18685148345903890, -2.135865664097126526, 13.83612956354244083 ) ) ;
#1450=CARTESIAN_POINT ( 'NONE',  ( 18.03475265876376810, 2.099231872491031936, -12.53598779768163318 ) ) ;
#1462=CARTESIAN_POINT ( 'NONE',  ( 18.17918265292645685, -2.461360938835027934, 13.68159685767607137 ) ) ;
#1476=VERTEX_POINT ( 'NONE', #44240 ) ;
#1480=CARTESIAN_POINT ( 'NONE',  ( 17.79074592071068039, -3.210128306667220155, -13.62701119231860680 ) ) ;
#1483=CARTESIAN_POINT ( 'NONE',  ( 12.80505043854144276, 0.7192913403693015351, 12.57945229203838267 ) ) ;
#1484=EDGE_CURVE ( 'NONE', #44214, #24573, #12032, .T. ) ;
#1485=CARTESIAN_POINT ( 'NONE',  ( 12.39041931600610091, 2.032227219086496284, 13.76156428297225709 ) ) ;
#1488=CARTESIAN_POINT ( 'NONE',  ( 12.78475401282448942, 0.6249999999999995559, -12.67928921589118474 ) ) ;
#1490=CARTESIAN_POINT ( 'NONE',  ( 12.57146999070152837, 0.6916885356983997202, 13.98290438115173551 ) ) ;
#1501=PLANE ( 'NONE',  #44912 ) ;
#1502=LINE ( 'NONE', #17589, #63425 ) ;
#1532=CARTESIAN_POINT ( 'NONE',  ( 12.80505043854143388, 1.760910691117811844, 12.47634535983622861 ) ) ;
#1535=CARTESIAN_POINT ( 'NONE',  ( 12.12622056954395156, -0.2566959043864930345, -13.99765098363215365 ) ) ;
#1543=CARTESIAN_POINT ( 'NONE',  ( 18.15689837892989544, 2.331154328543900700, -13.70782442673660384 ) ) ;
#1550=CARTESIAN_POINT ( 'NONE',  ( 17.85612272126378031, 0.5477996803047007202, -12.68409554377638315 ) ) ;
#1555=CARTESIAN_POINT ( 'NONE',  ( 18.11165249910125752, -2.784436927218168378, -13.60895423192975073 ) ) ;
#1557=VERTEX_POINT ( 'NONE', #58926 ) ;
#1560=ORIENTED_EDGE ( 'NONE', *, *, #37783, .F. ) ;
#1562=CARTESIAN_POINT ( 'NONE',  ( 17.95087979294698499, -3.083166700081136025, -12.21696069964854559 ) ) ;
#1569=ADVANCED_FACE ( 'NONE', ( #51195 ), #60302, .T. ) ;
#1576=CARTESIAN_POINT ( 'NONE',  ( 12.39110436774224588, 2.968713941934965295, -13.56281002627123122 ) ) ;
#1579=CARTESIAN_POINT ( 'NONE',  ( 17.96724268330523344, 0.4699225802676941233, 13.88930950616752114 ) ) ;
#1581=CARTESIAN_POINT ( 'NONE',  ( 17.82908354283126329, 0.5620915422200578604, 13.88470483921787135 ) ) ;
#1585=CARTESIAN_POINT ( 'NONE',  ( 12.27345183621622837, -0.3288514424339070708, 13.89476819318031708 ) ) ;
#1587=CARTESIAN_POINT ( 'NONE',  ( 12.70148458876750652, -0.6166668696418402540, -13.88158203759318887 ) ) ;
#1594=CYLINDRICAL_SURFACE ( 'NONE', #31758, 0.6250000000000005551 ) ;
#1598=CARTESIAN_POINT ( 'NONE',  ( 17.83205770179218774, 0.5603556898929425989, 12.68335562943300232 ) ) ;
#1601=CARTESIAN_POINT ( 'NONE',  ( 18.16712151970202882, -2.626596269781440007, -12.42116978061999433 ) ) ;
#1606=CARTESIAN_POINT ( 'NONE',  ( 12.70155625791299947, -1.883284863834662648, 13.78507964965113963 ) ) ;
#1615=CARTESIAN_POINT ( 'NONE',  ( 12.08146954708834997, 0.04649795050485474451, -12.59991969135870526 ) ) ;
#1632=CARTESIAN_POINT ( 'NONE',  ( 12.80505043854146763, -3.248147246781390329, -13.61798588129781074 ) ) ;
#1634=CARTESIAN_POINT ( 'NONE',  ( 18.06311169547815254, -0.3645810575750400573, -13.89357890581303501 ) ) ;
#1636=CARTESIAN_POINT ( 'NONE',  ( 12.80505043854143388, 2.499999999999999556, -25.00000000000000000 ) ) ;
#1643=CARTESIAN_POINT ( 'NONE',  ( 12.60065541204594908, -3.091968277195503489, -13.52988132686527756 ) ) ;
#1646=CARTESIAN_POINT ( 'NONE',  ( 18.27990737420073586, -0.1887961029072405539, 12.59999260960568535 ) ) ;
#1655=CARTESIAN_POINT ( 'NONE',  ( 17.67525416028805552, -1.770698066894643041, 12.47496018400917173 ) ) ;
#1660=AXIS2_PLACEMENT_3D ( 'NONE', #51724, #24478, #3819 ) ;
#1686=CARTESIAN_POINT ( 'NONE',  ( 17.81289281796187751, 1.835117743393749334, 13.87920855489149297 ) ) ;
#1694=LINE ( 'NONE', #40142, #5609 ) ;
#1696=DIRECTION ( 'NONE',  ( 0.000000000000000000, 0.000000000000000000, -1.000000000000000000 ) ) ;
#1697=CARTESIAN_POINT ( 'NONE',  ( 18.25518009351767645, -2.707823354518777759, -13.73564093574334422 ) ) ;
#1715=CARTESIAN_POINT ( 'NONE',  ( 17.92207321737432579, 3.154877352444517058, 13.63994794764266238 ) ) ;
#1719=CARTESIAN_POINT ( 'NONE',  ( 12.75668783919146954, 3.198551280946738018, -12.18725874734144021 ) ) ;
#1727=CARTESIAN_POINT ( 'NONE',  ( 12.58710648703388912, -3.166459836794174088, -12.19563591444343054 ) ) ;
#1728=AXIS2_PLACEMENT_3D ( 'NONE', #29476, #67188, #24555 ) ;
#1734=CARTESIAN_POINT ( 'NONE',  ( 12.76344776297779227, -3.123961325724114779, -13.52107359494106475 ) ) ;
#1735=CARTESIAN_POINT ( 'NONE',  ( 18.15003166281171332, 0.1916424759571789538, -12.69805926625132919 ) ) ;
#1746=CARTESIAN_POINT ( 'NONE',  ( 17.78706641053893378, 1.919568985577240872, 12.56801103569107703 ) ) ;
#1748=LINE ( 'NONE', #49993, #6009 ) ;
#1753=CARTESIAN_POINT ( 'NONE',  ( 12.13935791461259583, -2.765884558748030742, 12.29268093925658079 ) ) ;
#1756=ADVANCED_FACE ( 'NONE', ( #59868 ), #10064, .T. ) ;
#1763=CARTESIAN_POINT ( 'NONE',  ( 12.16000645811907255, -0.3284204639250598023, 12.59572022474404562 ) ) ;
#1767=CARTESIAN_POINT ( 'NONE',  ( 12.27327344217065175, 2.829024202110181907, 12.36880877243790700 ) ) ;
#1777=CIRCLE ( 'NONE', #55376, 12.79999953825000070 ) ;
#1782=CARTESIAN_POINT ( 'NONE',  ( 17.92356899887492006, 1.853474162671549852, -12.46298541230188128 ) ) ;
#1784=CARTESIAN_POINT ( 'NONE',  ( 12.78422499708368321, -3.124999410541265732, 13.52084427634422603 ) ) ;
#1805=CARTESIAN_POINT ( 'NONE',  ( 12.54534433730547782, -3.068834427903050610, 12.30067458026101157 ) ) ;
#1809=CARTESIAN_POINT ( 'NONE',  ( 17.81506173200510190, -3.068442049787682979, 13.53632421860061008 ) ) ;
#1811=EDGE_LOOP ( 'NONE', ( #40604, #36803, #47897, #42745, #14625 ) ) ;
#1814=LINE ( 'NONE', #8440, #31130 ) ;
#1815=VECTOR ( 'NONE', #20909, 1000.000000000000000 ) ;
#1817=CARTESIAN_POINT ( 'NONE',  ( 12.70934146430499290, -1.792598170651241052, -13.88476440023862324 ) ) ;
#1819=CARTESIAN_POINT ( 'NONE',  ( 17.78803358707871851, 0.6812425322175482689, -12.58157083403807341 ) ) ;
#1833=CARTESIAN_POINT ( 'NONE',  ( 12.23130451870204460, 2.748081639521271935, 13.61765624098743821 ) ) ;
#1838=CARTESIAN_POINT ( 'NONE',  ( 12.08961512266909999, 0.1188263301541283151, 13.99950072926553446 ) ) ;
#1839=VERTEX_POINT ( 'NONE', #27292 ) ;
#1860=ORIENTED_EDGE ( 'NONE', *, *, #13240, .F. ) ;
#1880=EDGE_CURVE ( 'NONE', #56864, #16266, #33714, .T. ) ;
#1887=CARTESIAN_POINT ( 'NONE',  ( 17.55505043854143565, 3.248109929747637903, -13.61799478206225444 ) ) ;
#1888=CARTESIAN_POINT ( 'NONE',  ( 12.08146951720330087, -0.04720351400547519866, -13.99992551180917211 ) ) ;
#1896=CARTESIAN_POINT ( 'NONE',  ( 17.79021264935886748, 3.209040350003987463, -13.62725621160039324 ) ) ;
#1909=CARTESIAN_POINT ( 'NONE',  ( 18.08703349542470917, -2.171337119009642436, 13.73770667395803358 ) ) ;
#1917=CARTESIAN_POINT ( 'NONE',  ( 18.14595306053284318, -2.897894011715727025, -12.26224306838060585 ) ) ;
#1927=CARTESIAN_POINT ( 'NONE',  ( 12.80505043854143388, 3.124999999999999556, -13.52084414783465505 ) ) ;
#1929=CARTESIAN_POINT ( 'NONE',  ( 12.19536857401206831, 2.360987227094834218, -13.70197821715308706 ) ) ;
#1933=CARTESIAN_POINT ( 'NONE',  ( 17.98979471028674126, 0.4491394412341184750, 13.89023495843590439 ) ) ;
#1934=CARTESIAN_POINT ( 'NONE',  ( 17.92176811213217036, 0.5062908249625720503, 13.88759084002720989 ) ) ;
#1936=ORIENTED_EDGE ( 'NONE', *, *, #20827, .T. ) ;
#1946=CARTESIAN_POINT ( 'NONE',  ( 12.80505043854143388, 2.499999999999999556, -25.00000000000000000 ) ) ;
#1950=CARTESIAN_POINT ( 'NONE',  ( 17.56537431432192164, 0.6249999662751106744, 12.67928921590351798 ) ) ;
#1952=CARTESIAN_POINT ( 'NONE',  ( 18.06413707771143606, -2.862722769407199053, -12.35962335206856544 ) ) ;
#1955=CARTESIAN_POINT ( 'NONE',  ( 12.08078742596668675, -2.670354628853650603, -12.31525682383281506 ) ) ;
#1959=CARTESIAN_POINT ( 'NONE',  ( 18.18005043799233178, 2.500000011518615395, -12.45159158845316405 ) ) ;
#1963=VERTEX_POINT ( 'NONE', #42677 ) ;
#1966=CARTESIAN_POINT ( 'NONE',  ( 12.23004733766516949, -0.4382646521645954252, -12.59237917444261434 ) ) ;
#1967=CARTESIAN_POINT ( 'NONE',  ( 12.63917144501162326, -1.891830949829975461, -12.57269938248998642 ) ) ;
#1984=CARTESIAN_POINT ( 'NONE',  ( 17.94354858665103336, -0.4896942981276207196, -13.88839019180475809 ) ) ;
#1990=CARTESIAN_POINT ( 'NONE',  ( 18.16257472060389233, -2.647071732840386549, 12.41611113220489138 ) ) ;
#2004=CARTESIAN_POINT ( 'NONE',  ( 17.60337015074825828, -1.762344248314565931, 12.47614295832086206 ) ) ;
#2019=EDGE_CURVE ( 'NONE', #25814, #56658, #66265, .T. ) ;
#2038=CARTESIAN_POINT ( 'NONE',  ( 18.07920178076626883, 2.013390639430577167, 13.85446980737596157 ) ) ;
#2066=ORIENTED_EDGE ( 'NONE', *, *, #34743, .F. ) ;
#2073=CARTESIAN_POINT ( 'NONE',  ( 12.61213290433100553, 1.905496177770260591, -12.57041190218061288 ) ) ;
#2082=CARTESIAN_POINT ( 'NONE',  ( 17.65273365043483977, -0.7301396911442770143, 13.98094760870049136 ) ) ;
#2084=CARTESIAN_POINT ( 'NONE',  ( 12.25620353052270595, -2.010025970016508623, -12.43864443381842833 ) ) ;
#2091=CARTESIAN_POINT ( 'NONE',  ( 12.78422293702846524, -3.124999446934218383, -13.52078617650838943 ) ) ;
#2092=CARTESIAN_POINT ( 'NONE',  ( 18.00459872918310822, -0.4343244881883122632, -12.69000555157927934 ) ) ;
#2093=CARTESIAN_POINT ( 'NONE',  ( 12.18033843151448181, 2.521515055313179321, -12.44655896212864121 ) ) ;
#2103=CARTESIAN_POINT ( 'NONE',  ( 17.84319482158666048, 1.945290144093657192, 12.56363827966045932 ) ) ;
#2110=CARTESIAN_POINT ( 'NONE',  ( 12.60227161487513747, -1.908786995848724022, 12.56986146204938137 ) ) ;
#2115=CARTESIAN_POINT ( 'NONE',  ( 12.45211143562937650, -0.6284163952874709524, 12.58432055988358123 ) ) ;
#2118=CARTESIAN_POINT ( 'NONE',  ( 12.39760546513563533, 2.025954772141363769, 12.54945441499613068 ) ) ;
#2124=CARTESIAN_POINT ( 'NONE',  ( 17.96217742534082618, -0.4744044027482017256, 12.68807559256817008 ) ) ;
#2131=CARTESIAN_POINT ( 'NONE',  ( 18.10276869593483440, -2.801190086625830133, 13.60495303825237023 ) ) ;
#2133=CARTESIAN_POINT ( 'NONE',  ( 12.09915596617140920, -2.684647274610782119, 13.74018952919733572 ) ) ;
#2134=FACE_BOUND ( 'NONE', #12463, .T. ) ;
#2141=DIRECTION ( 'NONE',  ( 0.000000000000000000, 0.9772984074130801613, 0.2118674653358960658 ) ) ;
#2142=CARTESIAN_POINT ( 'NONE',  ( 17.63765675162811419, 1.874999999999999778, -13.78631904427533428 ) ) ;
#2148=CARTESIAN_POINT ( 'NONE',  ( 21.59999953993000332, 7.283063041541000399E-14, -6.705747068735999778E-14 ) ) ;
#2156=CARTESIAN_POINT ( 'NONE',  ( 12.19483627255733893, -2.635236895375446586, 12.41905446230203758 ) ) ;
#2161=CARTESIAN_POINT ( 'NONE',  ( 18.07092639204462259, -2.147008627175521767, 13.74201915664823659 ) ) ;
#2176=ORIENTED_EDGE ( 'NONE', *, *, #18228, .F. ) ;
#2182=CARTESIAN_POINT ( 'NONE',  ( 12.61244651655885640, 1.905326457160023690, 13.78169738549997092 ) ) ;
#2187=CARTESIAN_POINT ( 'NONE',  ( 12.57519714614618778, -0.5812901181791702010, 13.88363587338390381 ) ) ;
#2202=DIRECTION ( 'NONE',  ( 0.7071058580589949516, -0.7071077043128949358, 4.007459190705968920E-09 ) ) ;
#2233=CARTESIAN_POINT ( 'NONE',  ( 12.63955452181609296, -0.7113363331415235580, -13.98191770012930135 ) ) ;
#2242=CARTESIAN_POINT ( 'NONE',  ( 18.10320344748333454, 2.199570933858661981, -13.73260621368703660 ) ) ;
#2250=CARTESIAN_POINT ( 'NONE',  ( 17.88362877544205176, 0.5317665474480599563, -12.68501283761906251 ) ) ;
#2254=CARTESIAN_POINT ( 'NONE',  ( 18.05135021981381982, -2.880031268720636195, -13.58542674995411126 ) ) ;
#2255=CARTESIAN_POINT ( 'NONE',  ( 17.72013721777323880, -1.891648809703187606, 13.78386988244476008 ) ) ;
#2260=CARTESIAN_POINT ( 'NONE',  ( 18.03534466112218482, -3.019381283786360282, -12.23288205540259099 ) ) ;
#2269=CARTESIAN_POINT ( 'NONE',  ( 18.18005044388383240, -2.499999700414728743, -12.45156116530568902 ) ) ;
#2270=CARTESIAN_POINT ( 'NONE',  ( 12.37945077454910781, 1.926407208811268257, -13.86683589633374147 ) ) ;
#2273=CARTESIAN_POINT ( 'NONE',  ( 17.55505043854144276, 0.6250000000000001110, 13.88107975066923316 ) ) ;
#2280=CARTESIAN_POINT ( 'NONE',  ( 12.41737190950597736, -0.4903666733423311941, 13.88835870178277965 ) ) ;
#2281=CARTESIAN_POINT ( 'NONE',  ( 12.19329716804611508, -2.371658047293454530, 13.69984404025631441 ) ) ;
#2292=CARTESIAN_POINT ( 'NONE',  ( 12.33488707410255714, -0.4118223544696936744, 12.69101228723419261 ) ) ;
#2293=CARTESIAN_POINT ( 'NONE',  ( 18.15140653325676467, -2.687261711676918630, -12.40596587103102522 ) ) ;
#2305=ORIENTED_EDGE ( 'NONE', *, *, #61446, .T. ) ;
#2306=CARTESIAN_POINT ( 'NONE',  ( 12.33591545429644398, -0.5485298171727041039, -12.58805670501782004 ) ) ;
#2307=CARTESIAN_POINT ( 'NONE',  ( 12.30490414479101524, -2.123060221858890095, -12.53148904351019866 ) ) ;
#2316=EDGE_LOOP ( 'NONE', ( #27031, #25592, #43397, #31222 ) ) ;
#2323=CARTESIAN_POINT ( 'NONE',  ( 17.99694095195319576, 0.5793931417437954146, -13.98801390351337837 ) ) ;
#2337=CARTESIAN_POINT ( 'NONE',  ( 12.80505043854146940, -1.787816316115923287, 13.88537766212463076 ) ) ;
#2341=CARTESIAN_POINT ( 'NONE',  ( 4.699998537092440642, 13.17499999999999893, 0.000000000000000000 ) ) ;
#2344=CARTESIAN_POINT ( 'NONE',  ( 12.27392385059252966, -0.3300666952397324216, -13.89473968862477449 ) ) ;
#2345=CARTESIAN_POINT ( 'NONE',  ( 17.74784205817680061, -3.094544633123687660, 12.29297002796977800 ) ) ;
#2369=CARTESIAN_POINT ( 'NONE',  ( 17.87583791501560526, -0.6451567829544473387, 12.58347320810647929 ) ) ;
#2376=CARTESIAN_POINT ( 'NONE',  ( 18.21591247723851481, 2.819087736749464224, 13.71325046847544016 ) ) ;
#2386=CARTESIAN_POINT ( 'NONE',  ( 18.08585342091144099, -3.015868411947693950, -13.67131429327874947 ) ) ;
#2398=DIRECTION ( 'NONE',  ( 0.000000000000000000, 1.000000000000000000, 0.000000000000000000 ) ) ;
#2409=CARTESIAN_POINT ( 'NONE',  ( 12.17614882354824068, 2.839252809666478861, -12.27595571488803650 ) ) ;
#2414=ORIENTED_EDGE ( 'NONE', *, *, #57925, .F. ) ;
#2418=CARTESIAN_POINT ( 'NONE',  ( 12.33234491188480320, -1.934664193338951899, -12.45058764867823164 ) ) ;
#2425=CARTESIAN_POINT ( 'NONE',  ( 18.13994946422174337, 0.2205037192104047084, -12.69742880170240085 ) ) ;
#2426=B_SPLINE_CURVE_WITH_KNOTS ( 'NONE', 3,
 ( #61022, #4256, #60674, #7885, #19054, #34468, #41669, #31196, #50876, #7527, #25934, #25594, #29219, #52501, #12788, #4598, #34117, #41330, #68223, #29574, #2973, #44953, #45640, #14762, #62975, #50531, #66943, #2292, #46919, #47263, #30841, #15100, #45294, #36424, #66257, #28882, #66601, #57739, #9850, #34805, #18719, #50192, #36080, #18378, #39700, #13484, #40053, #56115, #13139, #61364, #15786, #27662, #43399, #10882, #22052, #43044, #32561, #58774, #21710, #51, #64010, #10198, #37798, #21035, #64348, #53874, #59121, #48981, #11224, #26284, #58095, #42019, #739, #16466, #32228, #68919, #38134, #59462, #5974, #36773, #27314, #20690, #32903, #63321, #48639, #64698, #53540, #5631, #42368, #15449, #5293, #393, #31876 ),
 .UNSPECIFIED., .F., .F.,
 ( 4, 2, 2, 2, 2, 2, 2, 2, 2, 1, 1, 2, 2, 2, 2, 2, 2, 2, 2, 2, 2, 2, 2, 2, 2, 2, 2, 2, 2, 2, 2, 2, 2, 1, 1, 2, 2, 2, 2, 1, 2, 2, 2, 2, 2, 2, 2, 2, 4 ),
 ( 0.000000000000000000, 0.03124999999999071576, 0.06249999999998143152, 0.09374999999997214728, 0.1093749999999674982, 0.1249999999999628630, 0.1562499999999562850, 0.1718749999999529821, 0.1874999999999496791, 0.2031249999999463762, 0.2109374999999447109, 0.2148437499999447942, 0.2187499999999448774, 0.2499999999999507061, 0.2656249999999529265, 0.2734374999999541478, 0.2812499999999553135, 0.2968749999999561462, 0.3124999999999569789, 0.3437499999999587552, 0.3593749999999590883, 0.3749999999999593658, 0.4062499999999609757, 0.4374999999999625300, 0.4999999999999656941, 0.5312499999999672484, 0.5624999999999689138, 0.5937499999999704681, 0.6093749999999715783, 0.6249999999999726885, 0.6562499999999740208, 0.6718749999999746869, 0.6874999999999753530, 0.7031249999999760192, 0.7109374999999763522, 0.7148437499999772404, 0.7187499999999782396, 0.7499999999999861222, 0.7656249999999907851, 0.7734374999999930056, 0.7773437499999942268, 0.7812499999999953371, 0.7968749999999964473, 0.8124999999999974465, 0.8437499999999995559, 0.8593750000000005551, 0.8750000000000015543, 0.9375000000000007772, 1.000000000000000000 ),
 .UNSPECIFIED. ) ;
#2427=AXIS2_PLACEMENT_3D ( 'NONE', #6372, #7417, #38191 ) ;
#2432=CYLINDRICAL_SURFACE ( 'NONE', #23842, 13.17499999999999893 ) ;
#2434=CARTESIAN_POINT ( 'NONE',  ( 17.55505043854143565, 3.199698446519374073, 12.18695736643652516 ) ) ;
#2444=CARTESIAN_POINT ( 'NONE',  ( 12.30671156051923809, -2.122656121997153367, 12.53154589464477731 ) ) ;
#2450=CARTESIAN_POINT ( 'NONE',  ( 12.76392908090536515, 0.6239794389693666954, 12.67935706666152740 ) ) ;
#2453=CARTESIAN_POINT ( 'NONE',  ( 12.21847001913369191, 2.284010606415769029, 12.49926433191011377 ) ) ;
#2466=CARTESIAN_POINT ( 'NONE',  ( 18.04063798913343675, -0.3934994367753943956, -12.69179478357233748 ) ) ;
#2468=CARTESIAN_POINT ( 'NONE',  ( 17.59634971247464819, -3.125000000000000444, 13.52084437902333391 ) ) ;
#2470=CARTESIAN_POINT ( 'NONE',  ( 17.59662294266148663, -1.876036575741765189, -13.78611707749648119 ) ) ;
#2490=DIRECTION ( 'NONE',  ( 0.000000000000000000, -1.000000000000000000, 0.000000000000000000 ) ) ;
#2492=CARTESIAN_POINT ( 'NONE',  ( 12.18009334795439003, -2.513081858656105450, 12.44854102044225463 ) ) ;
#2495=CARTESIAN_POINT ( 'NONE',  ( 18.22053876895019542, -2.807780685761766204, 13.71555663160087057 ) ) ;
#2507=CARTESIAN_POINT ( 'NONE',  ( 17.60275121352128025, 0.7181168112306527407, -12.57951960855069551 ) ) ;
#2510=DIRECTION ( 'NONE',  ( -1.000000000000000000, 0.000000000000000000, 0.000000000000000000 ) ) ;
#2518=CARTESIAN_POINT ( 'NONE',  ( 12.63832872341678204, 3.228981699441171305, 13.62254385108541754 ) ) ;
#2521=CARTESIAN_POINT ( 'NONE',  ( 12.60485626873164300, 0.5921620643864188294, -12.68141136813213166 ) ) ;
#2522=CARTESIAN_POINT ( 'NONE',  ( 12.76393046405280174, -0.6239795106976188110, 13.88114172264461210 ) ) ;
#2524=ORIENTED_EDGE ( 'NONE', *, *, #11348, .F. ) ;
#2528=FACE_OUTER_BOUND ( 'NONE', #28917, .T. ) ;
#2532=FACE_OUTER_BOUND ( 'NONE', #25345, .T. ) ;
#2533=CARTESIAN_POINT ( 'NONE',  ( 12.65065493613386138, 3.183300664725533746, 12.19125106909030798 ) ) ;
#2550=CYLINDRICAL_SURFACE ( 'NONE', #39808, 0.6250000000000005551 ) ;
#2557=CARTESIAN_POINT ( 'NONE',  ( 17.65148079338494824, 1.767134912084544318, -12.47546541983269286 ) ) ;
#2567=CARTESIAN_POINT ( 'NONE',  ( 12.44165070291072261, -0.6323113780857178012, -13.98571806661953332 ) ) ;
#2572=CARTESIAN_POINT ( 'NONE',  ( 4.599999999999999645, -1.760910691117812954, -12.47634535983622861 ) ) ;
#2576=CARTESIAN_POINT ( 'NONE',  ( 18.14815926393670154, 2.301857555364728913, -13.71350736626465405 ) ) ;
#2592=ORIENTED_EDGE ( 'NONE', *, *, #2620, .T. ) ;
#2594=CARTESIAN_POINT ( 'NONE',  ( 18.27407156835994684, -2.576234207239483709, -12.33383912514346648 ) ) ;
#2597=FACE_OUTER_BOUND ( 'NONE', #58221, .T. ) ;
#2607=CARTESIAN_POINT ( 'NONE',  ( 12.25852519399115614, 2.998253127629454617, -13.67519035003951267 ) ) ;
#2608=CIRCLE ( 'NONE', #35015, 12.60000000000000142 ) ;
#2611=CARTESIAN_POINT ( 'NONE',  ( 18.18333308066189247, -0.3651687365794509810, 13.99525266148724256 ) ) ;
#2612=CARTESIAN_POINT ( 'NONE',  ( 18.17891623994083616, -2.457256301358912154, 12.46146663849685865 ) ) ;
#2617=CARTESIAN_POINT ( 'NONE',  ( 12.18408897593004347, -2.571470745484657261, 13.65804488218840618 ) ) ;
#2618=DIRECTION ( 'NONE',  ( 0.7071074108314172602, 0.7071061515411172227, -4.731322706660111483E-09 ) ) ;
#2620=EDGE_CURVE ( 'NONE', #53074, #40500, #38204, .T. ) ;
#2624=( GEOMETRIC_REPRESENTATION_CONTEXT ( 3 ) GLOBAL_UNCERTAINTY_ASSIGNED_CONTEXT ( ( #31116 ) ) GLOBAL_UNIT_ASSIGNED_CONTEXT ( ( #41969, #4210, #20298 ) ) REPRESENTATION_CONTEXT ( 'NONE', 'WORKASPACE' ) );
#2627=ADVANCED_FACE ( 'NONE', ( #54464, #1324, #48188, #65291 ), #53088, .T. ) ;
#2629=VECTOR ( 'NONE', #3454, 1000.000000000000000 ) ;
#2632=CARTESIAN_POINT ( 'NONE',  ( 17.66769993992418364, 0.6148490057825420907, 12.67995724530759816 ) ) ;
#2637=CARTESIAN_POINT ( 'NONE',  ( 12.70687399449098365, -1.760978113263731881, -12.47633584387829941 ) ) ;
#2645=CARTESIAN_POINT ( 'NONE',  ( 12.38211335778635558, 0.5846869236304474970, -12.58643362292763612 ) ) ;
#2663=CARTESIAN_POINT ( 'NONE',  ( 18.14440149583523620, -0.4259565731506483321, -13.99353270933016979 ) ) ;
#2666=ORIENTED_EDGE ( 'NONE', *, *, #6462, .F. ) ;
#2679=ORIENTED_EDGE ( 'NONE', *, *, #61365, .T. ) ;
#2681=AXIS2_PLACEMENT_3D ( 'NONE', #41221, #24456, #29722 ) ;
#2687=CARTESIAN_POINT ( 'NONE',  ( 12.18006450918421812, 0.02080959496298997666, -13.89999914846831075 ) ) ;
#2688=CARTESIAN_POINT ( 'NONE',  ( 17.98541303540595493, -2.046657644932490250, 12.54573712159721133 ) ) ;
#2693=VERTEX_POINT ( 'NONE', #7952 ) ;
#2701=ORIENTED_EDGE ( 'NONE', *, *, #68552, .T. ) ;
#2713=CARTESIAN_POINT ( 'NONE',  ( 18.26375634269466275, -0.1521017209118873392, 12.59908727444663867 ) ) ;
#2719=CARTESIAN_POINT ( 'NONE',  ( 18.26096953105663800, 2.684662952176594786, 13.74018646639511942 ) ) ;
#2730=CARTESIAN_POINT ( 'NONE',  ( 18.20591985607871521, -2.840417715854227421, -13.70884684492145134 ) ) ;
#2734=ORIENTED_EDGE ( 'NONE', *, *, #50915, .F. ) ;
#2753=CARTESIAN_POINT ( 'NONE',  ( 12.21314472040064913, 2.700933736278044339, -12.40250870093142410 ) ) ;
#2762=ORIENTED_EDGE ( 'NONE', *, *, #33583, .T. ) ;
#2764=CARTESIAN_POINT ( 'NONE',  ( 12.08005347077625835, -2.506700685333587586, -12.34815832536655833 ) ) ;
#2770=CARTESIAN_POINT ( 'NONE',  ( 12.80505043854146763, -3.125000000000000444, -13.52078605991414761 ) ) ;
#2777=CARTESIAN_POINT ( 'NONE',  ( 17.71800267521794936, 3.104751769958197016, 13.52637079326926539 ) ) ;
#2781=CARTESIAN_POINT ( 'NONE',  ( 17.74512657133769622, 3.174942931788175216, 12.19343219266723821 ) ) ;
#2786=CARTESIAN_POINT ( 'NONE',  ( 12.17998194132763423, -2.482033040872618113, 12.45578191469033413 ) ) ;
#2793=CARTESIAN_POINT ( 'NONE',  ( 12.23161381921988422, 0.2487950381773037789, 12.69672507751632118 ) ) ;
#2796=CARTESIAN_POINT ( 'NONE',  ( 12.18110988575100251, 2.462234709496985197, 12.46028276222759068 ) ) ;
#2807=CARTESIAN_POINT ( 'NONE',  ( 17.91195086072671572, -0.5131995813064865741, -12.68604179104344531 ) ) ;
#2809=CARTESIAN_POINT ( 'NONE',  ( 18.12459608108212805, -2.757432806210013521, 13.61548201701218197 ) ) ;
#2811=CARTESIAN_POINT ( 'NONE',  ( 12.70947385406810604, -3.242135136469473267, 13.61941870117945186 ) ) ;
#2815=ORIENTED_EDGE ( 'NONE', *, *, #35366, .F. ) ;
#2819=LINE ( 'NONE', #30103, #37991 ) ;
#2835=CARTESIAN_POINT ( 'NONE',  ( 12.27931543957927119, -2.838108479055812872, 12.36635919027515307 ) ) ;
#2838=CARTESIAN_POINT ( 'NONE',  ( 17.92019487611651485, -3.148838011673614101, 13.64129243465967356 ) ) ;
#2844=CARTESIAN_POINT ( 'NONE',  ( 12.80505043854143388, 3.174834474598374090, -12.21921104873077013 ) ) ;
#2858=DIRECTION ( 'NONE',  ( 0.000000000000000000, 0.7198977633594747516, -0.6940801180771756229 ) ) ;
#2860=CARTESIAN_POINT ( 'NONE',  ( 12.54499921992989719, 1.931577877770959573, 13.77766407476416077 ) ) ;
#2863=CARTESIAN_POINT ( 'NONE',  ( 12.20957360716226248, -0.1900975198226042273, -12.69808960362384553 ) ) ;
#2864=CARTESIAN_POINT ( 'NONE',  ( 12.75722769875344476, 0.7290248443971270031, 13.98100598729141097 ) ) ;
#2873=ADVANCED_FACE ( 'NONE', ( #41483 ), #46734, .F. ) ;
#2879=CARTESIAN_POINT ( 'NONE',  ( 12.34734069910707710, 3.038294257956348776, 12.22819623478419260 ) ) ;
#2882=LINE ( 'NONE', #8478, #57051 ) ;
#2894=DIRECTION ( 'NONE',  ( 1.000000000000000000, 0.000000000000000000, 0.000000000000000000 ) ) ;
#2899=CARTESIAN_POINT ( 'NONE',  ( 18.28003019995797018, 2.460172313524571663, -12.35749544995779559 ) ) ;
#2909=CARTESIAN_POINT ( 'NONE',  ( 12.25919481816069734, -0.4811670829680815276, -13.99174107639406373 ) ) ;
#2918=CARTESIAN_POINT ( 'NONE',  ( 17.55505043854143565, 1.875000000000000000, -13.78631952119025250 ) ) ;
#2919=VERTEX_POINT ( 'NONE', #41146 ) ;
#2926=CARTESIAN_POINT ( 'NONE',  ( 17.77470270344264947, 0.5852243768386650169, -12.68184418015340142 ) ) ;
#2931=CARTESIAN_POINT ( 'NONE',  ( 18.16451541384049051, -2.360124911643264323, 13.70214797745214241 ) ) ;
#2938=CARTESIAN_POINT ( 'NONE',  ( 18.27884988594220772, -2.529462001843207464, -12.34351620764206814 ) ) ;
#2947=CARTESIAN_POINT ( 'NONE',  ( 12.51458961313711171, 3.187047769811530706, -13.63241538057482671 ) ) ;
#2951=CARTESIAN_POINT ( 'NONE',  ( 18.08442884140762175, 0.4994936913945440815, 13.99109680828866153 ) ) ;
#2970=CARTESIAN_POINT ( 'NONE',  ( 12.43999839839561794, -0.6380582630144968626, 13.98550026811445157 ) ) ;
#2972=CARTESIAN_POINT ( 'NONE',  ( 17.89428234746476676, 0.5250240499537031091, 12.68539034781188413 ) ) ;
#2973=CARTESIAN_POINT ( 'NONE',  ( 12.41699802712859224, -0.4899468514546045372, 12.68727699266409203 ) ) ;
#2983=VERTEX_POINT ( 'NONE', #15602 ) ;
#2984=CARTESIAN_POINT ( 'NONE',  ( 12.50535913667519239, 0.6550687562476287251, -12.58296113213902423 ) ) ;
#2988=CARTESIAN_POINT ( 'NONE',  ( 17.55505043854143565, 3.125000000000000000, 13.52078605991414939 ) ) ;
#3004=CARTESIAN_POINT ( 'NONE',  ( 17.99626221348004407, -0.5795518042670582126, -13.98800095993140857 ) ) ;
#3016=EDGE_CURVE ( 'NONE', #38787, #35474, #57837, .T. ) ;
#3018=AXIS2_PLACEMENT_3D ( 'NONE', #63932, #10799, #5892 ) ;
#3020=EDGE_LOOP ( 'NONE', ( #11322, #30908, #55815, #10074 ) ) ;
#3022=ADVANCED_FACE ( 'NONE', ( #10691 ), #33063, .F. ) ;
#3027=CARTESIAN_POINT ( 'NONE',  ( 12.70241326318844877, -0.6168528257048864205, -13.88157091029610157 ) ) ;
#3028=CARTESIAN_POINT ( 'NONE',  ( 18.16584637247986933, -2.632875908479945348, 12.41964751440798409 ) ) ;
#3051=CARTESIAN_POINT ( 'NONE',  ( 17.81057016328025000, -0.6732419856523113033, 12.58200148172923960 ) ) ;
#3057=CARTESIAN_POINT ( 'NONE',  ( 18.27399547846086136, 2.614774648920893174, 13.75367307402544270 ) ) ;
#3060=VERTEX_POINT ( 'NONE', #58939 ) ;
#3068=CARTESIAN_POINT ( 'NONE',  ( 17.78978190923680458, -3.208919636066283498, -13.62728338959921537 ) ) ;
#3086=ORIENTED_EDGE ( 'NONE', *, *, #37007, .F. ) ;
#3092=CARTESIAN_POINT ( 'NONE',  ( 12.32688384993702080, 2.902596799746486322, -12.34862005174977462 ) ) ;
#3096=ORIENTED_EDGE ( 'NONE', *, *, #37727, .T. ) ;
#3100=CARTESIAN_POINT ( 'NONE',  ( 17.92038287127229523, -0.6379138416578085113, 13.98550699733554303 ) ) ;
#3102=CARTESIAN_POINT ( 'NONE',  ( 12.14402373937352841, -2.776896049134141009, -12.29021278449864774 ) ) ;
#3111=DIRECTION ( 'NONE',  ( -1.000000000000000000, 0.000000000000000000, 0.000000000000000000 ) ) ;
#3112=VECTOR ( 'NONE', #42024, 1000.000000000000227 ) ;
#3117=ORIENTED_EDGE ( 'NONE', *, *, #28669, .T. ) ;
#3120=CARTESIAN_POINT ( 'NONE',  ( 17.96842299895978101, 2.968890910958777773, 13.56270300417350860 ) ) ;
#3123=CARTESIAN_POINT ( 'NONE',  ( 17.87877696946767614, 3.124133162484063586, 12.20654824865394517 ) ) ;
#3129=CARTESIAN_POINT ( 'NONE',  ( 12.47240630447280907, -1.970775872724743749, 12.55927287175691731 ) ) ;
#3136=CARTESIAN_POINT ( 'NONE',  ( 12.18832871607760460, 0.1019009512359494996, 12.69945530929771493 ) ) ;
#3141=CARTESIAN_POINT ( 'NONE',  ( 12.79462099885201454, 1.875000035136120236, 12.57541665307954837 ) ) ;
#3160=DIRECTION ( 'NONE',  ( 0.000000000000000000, 1.000000000000000000, 0.000000000000000000 ) ) ;
#3166=CARTESIAN_POINT ( 'NONE',  ( 7.100000000000000533, 12.50865771883999855, 2.924687089724999911 ) ) ;
#3173=EDGE_CURVE ( 'NONE', #12996, #16254, #43901, .T. ) ;
#3178=AXIS2_PLACEMENT_3D ( 'NONE', #56692, #19974, #15064 ) ;
#3183=CARTESIAN_POINT ( 'NONE',  ( 12.36790781771545689, -2.946786910879655608, 12.33618673617669970 ) ) ;
#3186=CARTESIAN_POINT ( 'NONE',  ( 17.65136412466926075, -3.242045876614692013, 13.61943996000380430 ) ) ;
#3198=CARTESIAN_POINT ( 'NONE',  ( 18.26841343935702255, 0.1288995356414767979, -12.59934597632939735 ) ) ;
#3206=AXIS2_PLACEMENT_3D ( 'NONE', #47649, #30883, #58815 ) ;
#3209=CARTESIAN_POINT ( 'NONE',  ( 12.09560501594671500, 2.367229839359596522, 13.79841893036761213 ) ) ;
#3213=CARTESIAN_POINT ( 'NONE',  ( 12.64392860536586127, 0.6042188441601874516, -12.68064732209416867 ) ) ;
#3218=CARTESIAN_POINT ( 'NONE',  ( 12.80505043854144276, -0.6878608935795337276, 12.61273126665598276 ) ) ;
#3249=CARTESIAN_POINT ( 'NONE',  ( 17.87931509819275888, 1.836668601340711193, -12.46541920085824451 ) ) ;
#3252=CARTESIAN_POINT ( 'NONE',  ( 12.18026105735517461, 2.480641341450430026, -13.67754910896964660 ) ) ;
#3255=EDGE_LOOP ( 'NONE', ( #27597, #8885, #11706, #56447 ) ) ;
#3257=CARTESIAN_POINT ( 'NONE',  ( 12.30932141792787604, 0.5329747956505024309, -13.98985355243729423 ) ) ;
#3260=CARTESIAN_POINT ( 'NONE',  ( 18.18005044388380043, 2.499999700417821380, 12.45156116530496604 ) ) ;
#3265=CARTESIAN_POINT ( 'NONE',  ( 18.05244152647595257, 3.049274110449839092, -13.66389386579125897 ) ) ;
#3285=CARTESIAN_POINT ( 'NONE',  ( 17.63760627221314081, -1.880133632725761172, -12.57457483776005525 ) ) ;
#3286=DIRECTION ( 'NONE',  ( -1.000000000000000000, 0.000000000000000000, 0.000000000000000000 ) ) ;
#3288=DIRECTION ( 'NONE',  ( 0.000000000000000000, -0.6884191022827257367, 0.7253131321107084695 ) ) ;
#3293=CARTESIAN_POINT ( 'NONE',  ( 12.36183802548525179, 3.095880799707793063, -13.65340897264974451 ) ) ;
#3295=CARTESIAN_POINT ( 'NONE',  ( 18.23380192947725575, 0.2577288767859139962, 13.99764474128114600 ) ) ;
#3315=CARTESIAN_POINT ( 'NONE',  ( 12.80505043854143210, 3.248147246781388553, 13.61798588129781251 ) ) ;
#3328=CARTESIAN_POINT ( 'NONE',  ( 12.70960625021945134, 0.7131288892044854721, -12.57980326738671906 ) ) ;
#3345=CARTESIAN_POINT ( 'NONE',  ( 18.18884185737635661, -0.3547769576528466695, -13.99550803169339730 ) ) ;
#3353=CARTESIAN_POINT ( 'NONE',  ( 12.80505043854146940, -3.207073286498425269, 13.58561123731972131 ) ) ;
#3356=CARTESIAN_POINT ( 'NONE',  ( 12.19373784164274532, -2.630112413918074932, -13.64494795241839675 ) ) ;
#3359=CARTESIAN_POINT ( 'NONE',  ( 12.43708913301322028, -1.881554942479412018, 13.87303690248389643 ) ) ;
#3361=CARTESIAN_POINT ( 'NONE',  ( 17.91802112630374211, 0.5089014841412820012, -13.88746088749277874 ) ) ;
#3365=CARTESIAN_POINT ( 'NONE',  ( 12.18528724423033616, -0.08139021474669536071, -13.89968437038779925 ) ) ;
#3366=CARTESIAN_POINT ( 'NONE',  ( 18.13036722553557567, -2.255582932783688488, 12.50519018731260878 ) ) ;
#3367=ORIENTED_EDGE ( 'NONE', *, *, #57684, .T. ) ;
#3371=AXIS2_PLACEMENT_3D ( 'NONE', #67151, #13004, #45839 ) ;
#3390=CARTESIAN_POINT ( 'NONE',  ( 17.91761838490637615, -0.6233258800551685352, 12.58457734799055139 ) ) ;
#3409=CARTESIAN_POINT ( 'NONE',  ( 17.67416556365687441, -3.238622530711267267, -13.62025504818856270 ) ) ;
#3430=CARTESIAN_POINT ( 'NONE',  ( 12.21993702172673757, 2.719929609653445546, -12.39763114037443970 ) ) ;
#3438=CARTESIAN_POINT ( 'NONE',  ( 12.12868457208163520, -2.220738826795313869, -12.40275942113248142 ) ) ;
#3444=CARTESIAN_POINT ( 'NONE',  ( 12.42225061842106903, -2.005837741177418199, -13.76588300560132438 ) ) ;
#3454=DIRECTION ( 'NONE',  ( 1.000000000000000000, 0.000000000000000000, 0.000000000000000000 ) ) ;
#3458=CARTESIAN_POINT ( 'NONE',  ( 17.84326074309960575, 3.054675730970588532, 12.30486402137391977 ) ) ;
#3465=CARTESIAN_POINT ( 'NONE',  ( 12.57303446153997406, -1.919568987556539152, 12.56805043247348941 ) ) ;
#3473=CARTESIAN_POINT ( 'NONE',  ( 12.19601995205470502, -0.1418569258565868241, 12.69895512164409368 ) ) ;
#3477=CARTESIAN_POINT ( 'NONE',  ( 12.73227166903752128, 1.879164230820285608, 12.57473389636349026 ) ) ;
#3489=CARTESIAN_POINT ( 'NONE',  ( 18.01651533331883570, -0.4224082581076209486, -12.69056396411460774 ) ) ;
#3492=CARTESIAN_POINT ( 'NONE',  ( 17.92097848891127398, -3.007049802558098062, 13.55275178750181020 ) ) ;
#3496=DIRECTION ( 'NONE',  ( 1.000000000000000000, 0.000000000000000000, 0.000000000000000000 ) ) ;
#3510=VECTOR ( 'NONE', #19141, 1000.000000000000000 ) ;
#3512=CARTESIAN_POINT ( 'NONE',  ( 18.05145975767274891, 0.3802875570022087870, -13.89301034115781874 ) ) ;
#3517=CARTESIAN_POINT ( 'NONE',  ( 17.88894803995539817, -3.166162608671032608, 13.63728156593011498 ) ) ;
#3525=EDGE_CURVE ( 'NONE', #60760, #68619, #6817, .T. ) ;
#3531=CARTESIAN_POINT ( 'NONE',  ( 18.03319509584025937, 0.5408165383911073265, -12.58839068838662278 ) ) ;
#3539=CARTESIAN_POINT ( 'NONE',  ( 17.60324462842604376, 1.762109595560071851, 12.47617631420775197 ) ) ;
#3541=CARTESIAN_POINT ( 'NONE',  ( 12.10383213726155560, 2.332238815612523553, 13.80437617213671331 ) ) ;
#3544=CARTESIAN_POINT ( 'NONE',  ( 12.29147016624624733, 0.3563519072876710769, -12.69327554148065573 ) ) ;
#3553=AXIS2_PLACEMENT_3D ( 'NONE', #52541, #30884, #4638 ) ;
#3558=CARTESIAN_POINT ( 'NONE',  ( 12.68571266918094764, 3.190282694684578590, 12.18942654693561600 ) ) ;
#3565=CARTESIAN_POINT ( 'NONE',  ( 12.18582115250623055, 2.585797660597818570, 12.43116941330281300 ) ) ;
#3569=DIRECTION ( 'NONE',  ( -1.000000000000000000, 0.000000000000000000, 0.000000000000000000 ) ) ;
#3581=CARTESIAN_POINT ( 'NONE',  ( 18.23147373744589927, 2.220711592698080494, -12.40276429823313897 ) ) ;
#3583=DIRECTION ( 'NONE',  ( -1.000000000000000000, 0.000000000000000000, 0.000000000000000000 ) ) ;
#3586=FACE_OUTER_BOUND ( 'NONE', #23902, .T. ) ;
#3598=CARTESIAN_POINT ( 'NONE',  ( 18.15341532599038032, 2.105586285009647174, -13.84075898842493935 ) ) ;
#3617=ORIENTED_EDGE ( 'NONE', *, *, #3525, .T. ) ;
#3619=CARTESIAN_POINT ( 'NONE',  ( 17.84610786052058984, -3.139226446220204636, -12.20267444563224224 ) ) ;
#3627=DIRECTION ( 'NONE',  ( -0.000000000000000000, -0.000000000000000000, 1.000000000000000000 ) ) ;
#3628=CARTESIAN_POINT ( 'NONE',  ( 12.18865279333483720, 2.902449960337685653, -13.69583488376822800 ) ) ;
#3630=CARTESIAN_POINT ( 'NONE',  ( 18.27886422513980591, 0.04806343339259133707, 13.99993753789458850 ) ) ;
#3660=CARTESIAN_POINT ( 'NONE',  ( 12.76392908090536338, -0.6239794389693680277, -12.67935706666153450 ) ) ;
#3661=CARTESIAN_POINT ( 'NONE',  ( 12.20324964192238326, -2.330992520672867219, -12.48933099340478492 ) ) ;
#3677=CARTESIAN_POINT ( 'NONE',  ( 18.27538073532130980, -0.08359636179364166031, -13.99975542440154541 ) ) ;
#3686=CARTESIAN_POINT ( 'NONE',  ( 17.75789140674246980, -3.091531401859648476, 12.29387995131532918 ) ) ;
#3695=EDGE_LOOP ( 'NONE', ( #8253, #34860, #29460, #42476 ) ) ;
#3701=CARTESIAN_POINT ( 'NONE',  ( 12.19409625758322235, 0.1321590433901056461, -13.89915950722680016 ) ) ;
#3702=CARTESIAN_POINT ( 'NONE',  ( 18.05208962242105741, -2.879457400869560146, 12.35505085550156501 ) ) ;
#3703=ORIENTED_EDGE ( 'NONE', *, *, #25818, .T. ) ;
#3729=CARTESIAN_POINT ( 'NONE',  ( 18.25578817174763202, 0.1860047152749647326, 12.59864695008082336 ) ) ;
#3744=ORIENTED_EDGE ( 'NONE', *, *, #65897, .T. ) ;
#3746=CARTESIAN_POINT ( 'NONE',  ( 21.59999987243000064, 1.172395514003999961E-13, -2.486899575159999765E-14 ) ) ;
#3767=CARTESIAN_POINT ( 'NONE',  ( 12.28024293382672028, 2.160546425968631556, -12.52422939561507675 ) ) ;
#3768=EDGE_CURVE ( 'NONE', #35849, #24800, #24896, .T. ) ;
#3778=CARTESIAN_POINT ( 'NONE',  ( 12.41053097114618708, -2.984774150185583785, -12.32529705072536963 ) ) ;
#3784=CARTESIAN_POINT ( 'NONE',  ( 12.41408225146707522, -2.012274740545227480, -13.76483611190084133 ) ) ;
#3791=EDGE_CURVE ( 'NONE', #45267, #47657, #2882, .T. ) ;
#3794=CARTESIAN_POINT ( 'NONE',  ( 18.17228756840857073, 2.598712620722948508, 13.65197972919175484 ) ) ;
#3797=CARTESIAN_POINT ( 'NONE',  ( 18.00599872992918549, 2.932869382066923603, 12.34010572687589757 ) ) ;
#3808=CARTESIAN_POINT ( 'NONE',  ( 12.18407639872240189, 0.07155418421575378274, 12.69973420405192144 ) ) ;
#3812=DIRECTION ( 'NONE',  ( 0.000000000000000000, 1.000000000000000000, 0.000000000000000000 ) ) ;
#3818=CARTESIAN_POINT ( 'NONE',  ( 17.81540764135917243, 1.931433452195108869, 13.77768866547343407 ) ) ;
#3819=DIRECTION ( 'NONE',  ( 1.000000000000000000, 0.000000000000000000, 0.000000000000000000 ) ) ;
#3830=CARTESIAN_POINT ( 'NONE',  ( 17.96975113184320350, -2.032288328865629268, -13.76155421333986340 ) ) ;
#3840=CARTESIAN_POINT ( 'NONE',  ( 17.95596346641302077, -0.4795055877513557108, 13.88886709645684547 ) ) ;
#3855=CIRCLE ( 'NONE', #524, 1.799999999999999156 ) ;
#3857=CARTESIAN_POINT ( 'NONE',  ( 17.78669369145618973, -1.919420387948956419, 13.77958849407365349 ) ) ;
#3871=CARTESIAN_POINT ( 'NONE',  ( 18.00565376249823046, 0.5635217852606941857, -12.58739276154098086 ) ) ;
#3883=CARTESIAN_POINT ( 'NONE',  ( 12.14431428438022564, 2.818682143830020248, 13.71332026632872747 ) ) ;
#3886=CARTESIAN_POINT ( 'NONE',  ( 12.53084372997124163, 0.5620101267580669413, -12.68326259364286202 ) ) ;
#3887=CARTESIAN_POINT ( 'NONE',  ( 12.08965255773060221, -0.1190513140356090627, 13.99949878896183719 ) ) ;
#3892=DIRECTION ( 'NONE',  ( 1.000000000000000000, 0.000000000000000000, 0.000000000000000000 ) ) ;
#3896=DIRECTION ( 'NONE',  ( -1.000000000000000000, 0.000000000000000000, 0.000000000000000000 ) ) ;
#3898=CARTESIAN_POINT ( 'NONE',  ( 12.08013217067790990, 2.460179751193587006, 12.35749396829501023 ) ) ;
#3913=DIRECTION ( 'NONE',  ( 0.000000000000000000, 1.000000000000000000, 0.000000000000000000 ) ) ;
#3914=CARTESIAN_POINT ( 'NONE',  ( 12.76347793713369505, -1.876036575608651447, 13.78616487348348052 ) ) ;
#3915=CARTESIAN_POINT ( 'NONE',  ( 12.64199182499262619, 3.104696382830980372, 13.52638422211090408 ) ) ;
#3922=CARTESIAN_POINT ( 'NONE',  ( 18.00033872679588498, 1.911966235111669743, -12.45410047071287174 ) ) ;
#3924=CARTESIAN_POINT ( 'NONE',  ( 18.07102077504459814, 2.852831731484589906, 12.36232801722215235 ) ) ;
#3925=CARTESIAN_POINT ( 'NONE',  ( 12.18001976712812073, 2.492954602445635715, -13.67495394283574228 ) ) ;
#3930=CARTESIAN_POINT ( 'NONE',  ( 12.50552075632584170, 0.6654101994098731154, -13.98418081573738903 ) ) ;
#3941=CARTESIAN_POINT ( 'NONE',  ( 18.06104743845536831, 3.040966990778155132, -13.66574534766771798 ) ) ;
#3942=ORIENTED_EDGE ( 'NONE', *, *, #64210, .T. ) ;
#3948=DIRECTION ( 'NONE',  ( -0.000000000000000000, -0.000000000000000000, 1.000000000000000000 ) ) ;
#3958=CARTESIAN_POINT ( 'NONE',  ( 17.59659105803586954, -1.876041592512284195, -12.57524627323323863 ) ) ;
#3965=DIRECTION ( 'NONE',  ( 1.000000000000000000, -4.332706595949694629E-15, 1.401268137124204108E-14 ) ) ;
#3969=CARTESIAN_POINT ( 'NONE',  ( 17.82168025737886197, 0.6791475903683997783, 13.98351814429473094 ) ) ;
#3988=ADVANCED_FACE ( 'NONE', ( #19130 ), #49193, .T. ) ;
#3997=VECTOR ( 'NONE', #8481, 1000.000000000000000 ) ;
#4003=CARTESIAN_POINT ( 'NONE',  ( 12.37030581721858447, -0.4491390935506887616, -12.68931154995402188 ) ) ;
#4004=CARTESIAN_POINT ( 'NONE',  ( 12.42192081635679912, -3.001194947154673276, -12.32076077294284566 ) ) ;
#4022=ORIENTED_EDGE ( 'NONE', *, *, #59036, .T. ) ;
#4027=CARTESIAN_POINT ( 'NONE',  ( 12.80505043854146940, -3.248109929747638347, 13.61799478206225444 ) ) ;
#4030=CARTESIAN_POINT ( 'NONE',  ( 12.18521525456901777, -2.580824918023420622, -13.65593716523674317 ) ) ;
#4037=ORIENTED_EDGE ( 'NONE', *, *, #60012, .F. ) ;
#4039=EDGE_CURVE ( 'NONE', #64156, #1476, #52603, .T. ) ;
#4044=CARTESIAN_POINT ( 'NONE',  ( 12.36880880067034738, 2.947687262017097964, 13.56819815501604509 ) ) ;
#4045=CARTESIAN_POINT ( 'NONE',  ( 17.97023714413482764, -2.032719534845758069, 12.54827100236067494 ) ) ;
#4053=CARTESIAN_POINT ( 'NONE',  ( 12.64132288496826639, 1.896477787946245774, -13.78309086827116658 ) ) ;
#4072=CARTESIAN_POINT ( 'NONE',  ( 17.99694387276892371, 0.5707228546306919448, 12.58707662888204304 ) ) ;
#4078=EDGE_CURVE ( 'NONE', #45774, #15974, #26889, .T. ) ;
#4080=CARTESIAN_POINT ( 'NONE',  ( 17.72083032727074681, 3.229203862303413608, 13.62249117442681978 ) ) ;
#4104=VERTEX_POINT ( 'NONE', #35824 ) ;
#4111=CARTESIAN_POINT ( 'NONE',  ( 12.19547854351943705, 2.361608046327442700, -12.48276200957625548 ) ) ;
#4116=CARTESIAN_POINT ( 'NONE',  ( 17.74278939942546174, -0.6963438834338713246, 12.58074676375308165 ) ) ;
#4119=CARTESIAN_POINT ( 'NONE',  ( 12.57326805540222914, -3.080523641713202476, -12.29716358636311213 ) ) ;
#4126=CARTESIAN_POINT ( 'NONE',  ( 12.48178274919588482, -3.171647819517037892, -13.63600670097294021 ) ) ;
#4133=CARTESIAN_POINT ( 'NONE',  ( 12.70736722663045448, -0.7301396911442795679, -13.98094760870049491 ) ) ;
#4136=CARTESIAN_POINT ( 'NONE',  ( 17.81484293442183997, 3.068795199393538287, 13.53617370486282923 ) ) ;
#4140=CARTESIAN_POINT ( 'NONE',  ( 18.17480529351244201, 2.583342416263719077, 12.43177882285067781 ) ) ;
#4147=CARTESIAN_POINT ( 'NONE',  ( 12.54002611783806387, -3.066051210233500690, 12.30150130090889427 ) ) ;
#4154=CARTESIAN_POINT ( 'NONE',  ( 12.75354487906747991, -0.6229596466635322072, 12.67942438339646571 ) ) ;
#4156=EDGE_CURVE ( 'NONE', #62789, #21338, #9935, .T. ) ;
#4164=ADVANCED_FACE ( 'NONE', ( #56465 ), #15532, .T. ) ;
#4166=CARTESIAN_POINT ( 'NONE',  ( 17.55505043854143565, 1.760845406083394682, -12.47635457398814829 ) ) ;
#4175=CARTESIAN_POINT ( 'NONE',  ( 18.13153191400934716, -2.741475808281053972, 13.61927240699122876 ) ) ;
#4178=CARTESIAN_POINT ( 'NONE',  ( 17.84240044433953543, -3.055120806185296800, -13.53986419860029322 ) ) ;
#4182=VERTEX_POINT ( 'NONE', #30580 ) ;
#4205=CARTESIAN_POINT ( 'NONE',  ( 17.55505043854144276, 0.6250000000000001110, 12.67928921589117586 ) ) ;
#4210=( NAMED_UNIT ( * ) PLANE_ANGLE_UNIT ( ) SI_UNIT ( $, .RADIAN. ) );
#4216=CARTESIAN_POINT ( 'NONE',  ( 18.25212943717077252, 0.1980440493285416381, -12.59844852634975254 ) ) ;
#4227=CARTESIAN_POINT ( 'NONE',  ( 17.94097423839751926, 1.871151600931000081, 12.46029012432409289 ) ) ;
#4228=CARTESIAN_POINT ( 'NONE',  ( 12.18844676753244727, 2.902714632704711750, 13.69578956119810442 ) ) ;
#4232=CARTESIAN_POINT ( 'NONE',  ( 12.27567203567527621, -0.4994936913945440815, 13.99109680828866509 ) ) ;
#4243=CARTESIAN_POINT ( 'NONE',  ( 12.11673986888014376, 2.253747544392081803, 12.39680392560332045 ) ) ;
#4246=CARTESIAN_POINT ( 'NONE',  ( 17.55505043854144276, -0.6250000000000001110, 13.88107975066923494 ) ) ;
#4252=CARTESIAN_POINT ( 'NONE',  ( 12.33152592722388796, 2.090072125033849204, 12.53771354783954983 ) ) ;
#4256=CARTESIAN_POINT ( 'NONE',  ( 12.78475401288254432, -0.6250000000000006661, 12.67928921589117408 ) ) ;
#4263=CARTESIAN_POINT ( 'NONE',  ( 12.66212950609382126, -3.108785237067038576, 13.52531707329824684 ) ) ;
#4264=CARTESIAN_POINT ( 'NONE',  ( 12.23606299695415878, 2.758663578173562669, 13.61513466668993466 ) ) ;
#4266=VERTEX_POINT ( 'NONE', #67971 ) ;
#4267=EDGE_CURVE ( 'NONE', #45407, #63209, #33449, .T. ) ;
#4273=CARTESIAN_POINT ( 'NONE',  ( 18.17639191339633697, 2.431702999347771676, -12.46724561074273296 ) ) ;
#4275=CARTESIAN_POINT ( 'NONE',  ( 18.13163533202872557, 2.741228481653361637, 12.39208274281023847 ) ) ;
#4276=CARTESIAN_POINT ( 'NONE',  ( 12.72306420252682280, 3.125000000000000000, -13.52084465375510014 ) ) ;
#4277=CARTESIAN_POINT ( 'NONE',  ( 4.600000207916445483, 2.033928581112999763E-13, 13.27499874715509698 ) ) ;
#4281=CARTESIAN_POINT ( 'NONE',  ( 12.17125901970652180, 0.3547769576528396196, -13.99550803169339908 ) ) ;
#4289=CARTESIAN_POINT ( 'NONE',  ( 18.17163261364642324, 2.902690589304655955, -13.69579465584391365 ) ) ;
#4300=ORIENTED_EDGE ( 'NONE', *, *, #20293, .T. ) ;
#4301=CYLINDRICAL_SURFACE ( 'NONE', #15353, 1.999999999999999556 ) ;
#4308=CARTESIAN_POINT ( 'NONE',  ( 18.09858302120876772, -2.191289104517299080, -12.51814558466705840 ) ) ;
#4318=CARTESIAN_POINT ( 'NONE',  ( 17.99626221348004051, 0.5795518042670492198, 13.98800095993141390 ) ) ;
#4325=CARTESIAN_POINT ( 'NONE',  ( 12.24837323140831202, -2.784344744657781590, 13.60903177735235836 ) ) ;
#4349=CARTESIAN_POINT ( 'NONE',  ( 17.92307254474012623, 3.107335109280919383, 12.21089239123578984 ) ) ;
#4352=CARTESIAN_POINT ( 'NONE',  ( 12.30864223534303648, 0.3802890292809097961, -12.69234946364261241 ) ) ;
#4353=CARTESIAN_POINT ( 'NONE',  ( 12.23610050202371369, -2.758887154262256391, -12.38747357484177947 ) ) ;
#4360=CARTESIAN_POINT ( 'NONE',  ( 17.98740632563133346, 0.4515327045973433484, 12.68919950483489067 ) ) ;
#4378=CARTESIAN_POINT ( 'NONE',  ( 12.18808187647154817, -2.399650199032397069, -13.69418124938799330 ) ) ;
#4393=CARTESIAN_POINT ( 'NONE',  ( 12.30785086506343795, 2.879247442421004166, 13.58563033715520341 ) ) ;
#4397=ORIENTED_EDGE ( 'NONE', *, *, #33873, .T. ) ;
#4400=CARTESIAN_POINT ( 'NONE',  ( 12.24277986057914980, 2.226901448799673666, -13.72760233995392731 ) ) ;
#4404=CARTESIAN_POINT ( 'NONE',  ( 18.18005043824477696, -1.062925945863725942E-10, 13.90000000153292881 ) ) ;
#4410=EDGE_CURVE ( 'NONE', #46362, #27235, #21791, .T. ) ;
#4419=CARTESIAN_POINT ( 'NONE',  ( 17.63863136176617274, 0.7145943380091432928, 12.57972004139935152 ) ) ;
#4425=CARTESIAN_POINT ( 'NONE',  ( 18.08585342091140546, 3.015868411947682404, 13.67131429327875125 ) ) ;
#4463=CARTESIAN_POINT ( 'NONE',  ( 12.79295051314563203, -1.760910731560545450, -12.47634535177225068 ) ) ;
#4468=CARTESIAN_POINT ( 'NONE',  ( 12.70873338277719711, -3.242082958893204303, -13.61943113270052486 ) ) ;
#4471=ADVANCED_FACE ( 'NONE', ( #55349 ), #38929, .F. ) ;
#4473=CARTESIAN_POINT ( 'NONE',  ( 18.27597346048322535, -2.401680171065127212, 12.36899652916222436 ) ) ;
#4481=CARTESIAN_POINT ( 'NONE',  ( 18.05239999627272951, 2.879049404332129747, 12.35514073459315476 ) ) ;
#4487=EDGE_LOOP ( 'NONE', ( #36704, #63668, #24026, #18587 ) ) ;
#4500=ORIENTED_EDGE ( 'NONE', *, *, #42230, .T. ) ;
#4502=CARTESIAN_POINT ( 'NONE',  ( 18.18005043824377154, 1.329526366183796371E-10, 12.70000000088145420 ) ) ;
#4504=CARTESIAN_POINT ( 'NONE',  ( 12.70917152008051154, -3.194951439751541944, -12.18820651941599387 ) ) ;
#4509=B_SPLINE_CURVE_WITH_KNOTS ( 'NONE', 3,
 ( #36276, #9348, #56917, #41521 ),
 .UNSPECIFIED., .F., .F.,
 ( 4, 4 ),
 ( 0.000000000000000000, 1.000000000000000000 ),
 .UNSPECIFIED. ) ;
#4520=CARTESIAN_POINT ( 'NONE',  ( 18.04548494004250969, -2.887558854919742846, -13.58353091070611107 ) ) ;
#4529=CARTESIAN_POINT ( 'NONE',  ( 18.17906596529827823, -0.04061643729585483892, 13.89993966956888372 ) ) ;
#4539=CARTESIAN_POINT ( 'NONE',  ( 12.08085380679222531, 2.436412096897879298, -12.36221874022169764 ) ) ;
#4543=CARTESIAN_POINT ( 'NONE',  ( 17.84579744522524436, -1.849003904486296701, 13.87736309738764184 ) ) ;
#4544=CARTESIAN_POINT ( 'NONE',  ( 18.16264250269799163, 2.646798803964871549, -13.64122832052404988 ) ) ;
#4557=CARTESIAN_POINT ( 'NONE',  ( 18.24150829797650530, 0.2316996085786106607, -12.59787430930301433 ) ) ;
#4560=CARTESIAN_POINT ( 'NONE',  ( 12.52707377838018132, 3.060156797977223508, -12.30326077405661778 ) ) ;
#4570=CARTESIAN_POINT ( 'NONE',  ( 12.25061842917684451, 2.988573241473608366, 13.67729937646034521 ) ) ;
#4572=CARTESIAN_POINT ( 'NONE',  ( 12.80505043854144276, -0.6250000000000001110, -12.67928921589118652 ) ) ;
#4573=CARTESIAN_POINT ( 'NONE',  ( 12.44248702983405153, -0.6327954766588973490, 13.98569611075749108 ) ) ;
#4575=CARTESIAN_POINT ( 'NONE',  ( 12.56977253056427557, -1.799738463188393256, 12.47080370841241326 ) ) ;
#4580=CARTESIAN_POINT ( 'NONE',  ( 18.18005043824477696, -1.062925945863725942E-10, 13.90000000153292881 ) ) ;
#4582=CARTESIAN_POINT ( 'NONE',  ( 12.16008153508536083, 0.3287229608534073533, 12.59571550161850695 ) ) ;
#4584=DIRECTION ( 'NONE',  ( -1.000000000000000000, 0.000000000000000000, 0.000000000000000000 ) ) ;
#4585=CARTESIAN_POINT ( 'NONE',  ( 12.30575661439779900, 1.958493781132642386, 12.44686177741867006 ) ) ;
#4594=CARTESIAN_POINT ( 'NONE',  ( 12.42192081640602019, 3.001194947204297581, 12.32076077293008076 ) ) ;
#4598=CARTESIAN_POINT ( 'NONE',  ( 12.47604026688563117, -0.5315006617180365600, 12.68502792337811336 ) ) ;
#4606=CARTESIAN_POINT ( 'NONE',  ( 12.30652006878824700, -2.122495540605185749, 13.74632343115108490 ) ) ;
#4607=CARTESIAN_POINT ( 'NONE',  ( 12.80505043854143388, 1.875000000000000000, 13.78627172894481667 ) ) ;
#4614=CARTESIAN_POINT ( 'NONE',  ( 18.17988829291487818, 2.482516021556980590, -12.45565317647434611 ) ) ;
#4622=CARTESIAN_POINT ( 'NONE',  ( 12.80505043854144276, 0.7302158263239216796, -13.98094363220831049 ) ) ;
#4624=DIRECTION ( 'NONE',  ( 0.000000000000000000, 0.9905022095861402143, 0.1374968101629056305 ) ) ;
#4631=CARTESIAN_POINT ( 'NONE',  ( 17.92014050163761496, 1.886715056483305952, -13.87229028472749981 ) ) ;
#4637=CARTESIAN_POINT ( 'NONE',  ( 12.21279768068213656, 0.1999278272693495451, -13.89806912752725232 ) ) ;
#4638=DIRECTION ( 'NONE',  ( 0.000000000000000000, -0.9772984074130801613, -0.2118674653358960658 ) ) ;
#4648=CARTESIAN_POINT ( 'NONE',  ( 18.14141836411850761, -2.283433982113741934, -12.49938471124205641 ) ) ;
#4656=EDGE_CURVE ( 'NONE', #29163, #55276, #16869, .T. ) ;
#4663=ORIENTED_EDGE ( 'NONE', *, *, #6953, .T. ) ;
#4673=EDGE_LOOP ( 'NONE', ( #62440, #23823, #22596, #11693 ) ) ;
#4677=CARTESIAN_POINT ( 'NONE',  ( 12.80505043854143388, 3.166049082260463443, 13.55318600037536925 ) ) ;
#4680=CARTESIAN_POINT ( 'NONE',  ( 17.92118024654437036, 3.006907963399584549, -12.31891425463943079 ) ) ;
#4691=CARTESIAN_POINT ( 'NONE',  ( 12.18006454708593544, -0.02081145935391386093, -12.69999906470294526 ) ) ;
#4692=CARTESIAN_POINT ( 'NONE',  ( 12.35392836372401426, -2.932699513115810230, -12.34015408322826168 ) ) ;
#4715=CARTESIAN_POINT ( 'NONE',  ( 17.86968310087778278, -3.040418749906950158, 12.30910170914067514 ) ) ;
#4725=ORIENTED_EDGE ( 'NONE', *, *, #62270, .T. ) ;
#4728=CARTESIAN_POINT ( 'NONE',  ( 17.74668184667432413, -0.5949840079737200860, -12.68123264482376555 ) ) ;
#4729=CYLINDRICAL_SURFACE ( 'NONE', #47769, 0.6250000000000005551 ) ;
#4732=CARTESIAN_POINT ( 'NONE',  ( 12.26307976823773949, 2.811936524129936998, 13.60229516772050573 ) ) ;
#4738=EDGE_CURVE ( 'NONE', #2693, #5374, #36789, .T. ) ;
#4745=CARTESIAN_POINT ( 'NONE',  ( 18.16373243908211776, 0.1422577892986753023, 13.89902525486551887 ) ) ;
#4749=ORIENTED_EDGE ( 'NONE', *, *, #6953, .F. ) ;
#4761=CARTESIAN_POINT ( 'NONE',  ( 17.97798751929653704, 0.5846869236304546025, 12.58643362292763612 ) ) ;
#4767=CARTESIAN_POINT ( 'NONE',  ( 17.97915611674147129, 3.110288500502087494, 13.65013405122916268 ) ) ;
#4777=CARTESIAN_POINT ( 'NONE',  ( 12.44248249217650937, -0.6233258800551970680, -12.58457734799054784 ) ) ;
#4792=FACE_OUTER_BOUND ( 'NONE', #28827, .T. ) ;
#4800=CARTESIAN_POINT ( 'NONE',  ( 4.599999999999999645, 13.17499999999999893, 0.000000000000000000 ) ) ;
#4804=EDGE_CURVE ( 'NONE', #9530, #53691, #50658, .T. ) ;
#4807=AXIS2_PLACEMENT_3D ( 'NONE', #39918, #13352, #67498 ) ;
#4812=CARTESIAN_POINT ( 'NONE',  ( 12.59749754106154107, -3.089553852145857427, -12.29445441479364654 ) ) ;
#4817=CARTESIAN_POINT ( 'NONE',  ( 12.51441652845170793, -3.187012454917765858, -13.63242365153888613 ) ) ;
#4820=CARTESIAN_POINT ( 'NONE',  ( 18.27887336143460928, -2.529852868668394539, 12.34343546511470890 ) ) ;
#4822=ORIENTED_EDGE ( 'NONE', *, *, #35989, .F. ) ;
#4825=CARTESIAN_POINT ( 'NONE',  ( 12.80505043854144098, -0.7302158263239267866, -13.98094363220830871 ) ) ;
#4829=CARTESIAN_POINT ( 'NONE',  ( 18.15011669908943048, 2.691369836981456487, 12.40492163541245674 ) ) ;
#4835=CARTESIAN_POINT ( 'NONE',  ( 12.32688384993705455, -2.902596799746487211, 12.34862005174977462 ) ) ;
#4845=CARTESIAN_POINT ( 'NONE',  ( 5.602673821509172036, -12.13104802960947914, -3.749633869517229101 ) ) ;
#4857=CARTESIAN_POINT ( 'NONE',  ( 5.629847151468639233, -12.10477468259465184, 3.742618271631878102 ) ) ;
#4867=CARTESIAN_POINT ( 'NONE',  ( 18.15991033943444677, -2.341318227119850270, -13.70580147614464295 ) ) ;
#4887=B_SPLINE_CURVE_WITH_KNOTS ( 'NONE', 1,
 ( #36447, #9875 ),
 .UNSPECIFIED., .F., .F.,
 ( 2, 2 ),
 ( 0.000000000000000000, 1.000000000000000000 ),
 .UNSPECIFIED. ) ;
#4888=CARTESIAN_POINT ( 'NONE',  ( 12.51375467530090191, 1.821335011922586844, -12.46766859972881392 ) ) ;
#4891=AXIS2_PLACEMENT_3D ( 'NONE', #43633, #5526, #27901 ) ;
#4892=CARTESIAN_POINT ( 'NONE',  ( 17.55505043854147118, -1.787816316115923509, 13.88537766212463254 ) ) ;
#4893=CARTESIAN_POINT ( 'NONE',  ( 18.10276869592869176, 2.801190086637412868, -13.60495303824969149 ) ) ;
#4905=CARTESIAN_POINT ( 'NONE',  ( 18.06292190248829499, 0.3644117276601265831, -12.69296657371244841 ) ) ;
#4917=VECTOR ( 'NONE', #23558, 1000.000000000000000 ) ;
#4921=CARTESIAN_POINT ( 'NONE',  ( 12.44873997953563105, -0.5136077743616320745, -12.68601957541463676 ) ) ;
#4925=CARTESIAN_POINT ( 'NONE',  ( 12.51375467530093921, -1.821335011922595282, 12.46766859972881569 ) ) ;
#4931=CARTESIAN_POINT ( 'NONE',  ( 12.09898038912534091, 0.1637242582067924557, 12.59894148523291157 ) ) ;
#4934=CARTESIAN_POINT ( 'NONE',  ( 12.09087492024910304, 2.355317862440506449, 12.37790828721919389 ) ) ;
#4938=B_SPLINE_CURVE_WITH_KNOTS ( 'NONE', 3,
 ( #41648, #20321, #10181, #20670 ),
 .UNSPECIFIED., .F., .F.,
 ( 4, 4 ),
 ( 0.000000000000000000, 1.000000000000000000 ),
 .UNSPECIFIED. ) ;
#4943=CARTESIAN_POINT ( 'NONE',  ( 12.19364288186088352, 2.630035215285695394, 12.42031982010608182 ) ) ;
#4944=DIRECTION ( 'NONE',  ( -1.000000000000000000, 0.000000000000000000, 0.000000000000000000 ) ) ;
#4954=CARTESIAN_POINT ( 'NONE',  ( 12.23531288305056819, -2.757742497410567317, 13.61542453244087270 ) ) ;
#4955=CARTESIAN_POINT ( 'NONE',  ( 12.27940634384846064, 2.838250353088386468, 13.59582428664483267 ) ) ;
#4965=CARTESIAN_POINT ( 'NONE',  ( 17.94557471909616098, 2.987998163485180214, -12.32438680867656444 ) ) ;
#4968=CARTESIAN_POINT ( 'NONE',  ( 18.17221331277271190, 2.599179209401793589, 12.42790858716554858 ) ) ;
#4988=CARTESIAN_POINT ( 'NONE',  ( 12.80505043854144276, 0.6249999999999994449, -13.88107975066922428 ) ) ;
#4991=ORIENTED_EDGE ( 'NONE', *, *, #52011, .F. ) ;
#4998=CARTESIAN_POINT ( 'NONE',  ( 18.11139879660522212, -2.784965558754640913, -12.38059455073776682 ) ) ;
#5026=CARTESIAN_POINT ( 'NONE',  ( 5.500000000000000000, 12.22293095105000127, 3.800428736101999938 ) ) ;
#5031=CARTESIAN_POINT ( 'NONE',  ( 17.86968310086820111, 3.040418749912511487, -12.30910170913888280 ) ) ;
#5044=CARTESIAN_POINT ( 'NONE',  ( 12.20412026884455692, -0.1720826094844762344, -12.69843621396829292 ) ) ;
#5060=CARTESIAN_POINT ( 'NONE',  ( 18.11595230660369538, 2.775896237034515490, -13.61106543307219852 ) ) ;
#5065=CARTESIAN_POINT ( 'NONE',  ( 17.85458012075705270, -0.6654101994098823303, -13.98418081573739080 ) ) ;
#5081=CARTESIAN_POINT ( 'NONE',  ( 17.87873473849108308, -1.836456536727123279, -12.46545041361348716 ) ) ;
#5082=CARTESIAN_POINT ( 'NONE',  ( 17.55505043854147118, -3.125000000000000000, -12.28373071562070074 ) ) ;
#5087=EDGE_CURVE ( 'NONE', #1476, #19317, #59624, .T. ) ;
#5094=CARTESIAN_POINT ( 'NONE',  ( 17.55505043854144276, 0.7192913403693119712, -12.57945229203838267 ) ) ;
#5098=CARTESIAN_POINT ( 'NONE',  ( 17.77562957671592159, -0.5851376999905967269, 13.88342059653409066 ) ) ;
#5100=CARTESIAN_POINT ( 'NONE',  ( 18.18005043854833147, 0.04052532553066783699, 13.90000015527369470 ) ) ;
#5102=CARTESIAN_POINT ( 'NONE',  ( 12.58523710836478138, 0.5851630251601297461, 13.88341719038585076 ) ) ;
#5105=CARTESIAN_POINT ( 'NONE',  ( 17.63844293513428596, -0.6206536994987036371, -13.88134483103688765 ) ) ;
#5111=AXIS2_PLACEMENT_3D ( 'NONE', #54094, #22620, #54442 ) ;
#5113=CARTESIAN_POINT ( 'NONE',  ( 18.27393049982691053, -0.09400131084487256539, 12.59965472429368916 ) ) ;
#5144=CARTESIAN_POINT ( 'NONE',  ( 12.35552214745947275, 1.907986453762813284, -12.45488571128362487 ) ) ;
#5146=CONICAL_SURFACE ( 'NONE', #44250, 12.72499970924999957, 0.7853981386146715593 ) ;
#5152=B_SPLINE_CURVE_WITH_KNOTS ( 'NONE', 3,
 ( #27073, #54319, #49078, #59912, #28460, #49774, #12020, #65844, #33357, #53972, #38949, #64797, #59220, #54671, #33005, #1532 ),
 .UNSPECIFIED., .F., .F.,
 ( 4, 2, 2, 2, 2, 2, 2, 4 ),
 ( 0.000000000000000000, 0.06249999999999997224, 0.1249999999999999445, 0.2499999999999996669, 0.5000000000000002220, 0.7500000000000007772, 0.8750000000000003331, 1.000000000000000000 ),
 .UNSPECIFIED. ) ;
#5153=CARTESIAN_POINT ( 'NONE',  ( 17.85668400807925238, 1.853912555516304739, -13.87670837816644287 ) ) ;
#5154=CARTESIAN_POINT ( 'NONE',  ( 12.47244801656836799, 3.029249266520640305, -12.31238128988859692 ) ) ;
#5161=CONICAL_SURFACE ( 'NONE', #36408, 13.94999927503000059, 0.7853981058017837080 ) ;
#5165=CARTESIAN_POINT ( 'NONE',  ( 12.51734955436001329, -3.054939157457061238, -12.30478592156021200 ) ) ;
#5169=CARTESIAN_POINT ( 'NONE',  ( 12.36102515544325797, -1.940652449090411791, -13.86484480881332892 ) ) ;
#5172=CARTESIAN_POINT ( 'NONE',  ( 18.20249588168630694, -2.156032850912788401, 12.41417075669994219 ) ) ;
#5173=ORIENTED_EDGE ( 'NONE', *, *, #54441, .T. ) ;
#5181=CARTESIAN_POINT ( 'NONE',  ( 18.15916593608967133, 2.338515402758149619, -12.48776758577575308 ) ) ;
#5187=CARTESIAN_POINT ( 'NONE',  ( 12.72186720215638189, -3.119790641632218975, 12.28533200497073885 ) ) ;
#5188=CARTESIAN_POINT ( 'NONE',  ( 4.599999999999999645, 0.000000000000000000, 0.000000000000000000 ) ) ;
#5193=CARTESIAN_POINT ( 'NONE',  ( 12.32802524195760085, -0.4039503557775031561, 12.69135589213615312 ) ) ;
#5194=CARTESIAN_POINT ( 'NONE',  ( 5.600889858811719080, -12.13276343987879002, -3.750125071914726327 ) ) ;
#5202=CARTESIAN_POINT ( 'NONE',  ( 17.83426395974174383, 1.940453161589466458, 13.77628863228519407 ) ) ;
#5206=ORIENTED_EDGE ( 'NONE', *, *, #20932, .T. ) ;
#5211=UNCERTAINTY_MEASURE_WITH_UNIT (LENGTH_MEASURE( 1.000000000000000082E-05 ), #29365, 'distance_accuracy_value', 'NONE');
#5218=CARTESIAN_POINT ( 'NONE',  ( 18.08802622730391008, -2.172927601657333785, -13.73737356033239010 ) ) ;
#5238=CARTESIAN_POINT ( 'NONE',  ( 12.11689977649198191, 2.253070615825692347, -12.39692697851452330 ) ) ;
#5255=CARTESIAN_POINT ( 'NONE',  ( 17.91892138177004412, 0.5082598251325838312, -12.68630931495243530 ) ) ;
#5256=CARTESIAN_POINT ( 'NONE',  ( 12.43937386263551836, 3.007228867379230675, -12.31882001148154515 ) ) ;
#5263=CARTESIAN_POINT ( 'NONE',  ( 18.28023629128824012, 2.459623831379299297, 12.35762167929923017 ) ) ;
#5264=EDGE_CURVE ( 'NONE', #67648, #39916, #49784, .T. ) ;
#5265=CARTESIAN_POINT ( 'NONE',  ( 12.61605721975964478, 1.812633401299055480, 13.88216159563417662 ) ) ;
#5271=CARTESIAN_POINT ( 'NONE',  ( 12.25647171456043694, -2.009180677272478732, 12.43879158508227079 ) ) ;
#5279=CARTESIAN_POINT ( 'NONE',  ( 12.25813800312568880, 2.953224329521587865, 12.24903309118795747 ) ) ;
#5284=EDGE_CURVE ( 'NONE', #59995, #19638, #64099, .T. ) ;
#5288=CARTESIAN_POINT ( 'NONE',  ( 12.22547077881214506, 2.733971791169954813, 12.39396907918110813 ) ) ;
#5293=CARTESIAN_POINT ( 'NONE',  ( 12.72380912721855317, 0.6210782762490741904, 12.67955178808353445 ) ) ;
#5295=CARTESIAN_POINT ( 'NONE',  ( 17.74546162998189658, -0.7003689476013792437, -12.58057160030211108 ) ) ;
#5298=CARTESIAN_POINT ( 'NONE',  ( 12.20019055993962276, -2.341318142288553616, 13.70585175580906245 ) ) ;
#5307=CARTESIAN_POINT ( 'NONE',  ( 18.13036722553554370, 2.255582932783688044, -12.50519018731260168 ) ) ;
#5309=CARTESIAN_POINT ( 'NONE',  ( 18.16243401547605885, 2.647653205692694911, 12.41593780989185092 ) ) ;
#5330=CARTESIAN_POINT ( 'NONE',  ( 12.52211160825347136, 0.5573818238326222474, -13.88495700089724316 ) ) ;
#5338=ORIENTED_EDGE ( 'NONE', *, *, #56125, .T. ) ;
#5341=CARTESIAN_POINT ( 'NONE',  ( 17.84326074309963772, -3.054675730970588532, -12.30486402137391799 ) ) ;
#5346=ADVANCED_FACE ( 'NONE', ( #56140 ), #18747, .F. ) ;
#5348=CARTESIAN_POINT ( 'NONE',  ( 18.10184514650583409, -2.186078922896901755, -12.51950284166921890 ) ) ;
#5350=CARTESIAN_POINT ( 'NONE',  ( 12.29653044000528794, 0.3639325664385079095, 13.89360161040563035 ) ) ;
#5356=DIRECTION ( 'NONE',  ( -1.000000000000000000, -0.000000000000000000, -0.000000000000000000 ) ) ;
#5367=CARTESIAN_POINT ( 'NONE',  ( 12.80505043854146940, -3.125000000000000000, 13.52084414783465860 ) ) ;
#5374=VERTEX_POINT ( 'NONE', #62410 ) ;
#5379=CARTESIAN_POINT ( 'NONE',  ( 5.644459972124513669, -12.96885562507462808, 2.321858007525494205 ) ) ;
#5391=CARTESIAN_POINT ( 'NONE',  ( 12.33468944037056048, 0.4116921281473236438, -12.69102089861180893 ) ) ;
#5402=CARTESIAN_POINT ( 'NONE',  ( 18.04536347373271710, 0.3876168848508783626, 12.69203885981886870 ) ) ;
#5409=CARTESIAN_POINT ( 'NONE',  ( 17.77709566067061786, 3.084588255221574649, -13.53194174261899185 ) ) ;
#5413=CARTESIAN_POINT ( 'NONE',  ( 17.91761384724884110, -0.6327954766588933522, -13.98569611075749464 ) ) ;
#5418=CARTESIAN_POINT ( 'NONE',  ( 12.80505043854146940, -3.199698446519381179, -12.18695736643652516 ) ) ;
#5425=AXIS2_PLACEMENT_3D ( 'NONE', #25816, #21258, #35962 ) ;
#5433=DIRECTION ( 'NONE',  ( 0.000000000000000000, -0.9553735099700839672, 0.2954005017724949389 ) ) ;
#5448=CARTESIAN_POINT ( 'NONE',  ( 18.14018103492323775, 0.2205930660282628131, 13.89766156610768277 ) ) ;
#5453=CARTESIAN_POINT ( 'NONE',  ( 12.64394750688183500, 0.6042238833753180716, 13.88232004407564801 ) ) ;
#5455=CARTESIAN_POINT ( 'NONE',  ( 17.86525158946622938, -0.5426919696322294318, -13.88574006265329963 ) ) ;
#5463=CARTESIAN_POINT ( 'NONE',  ( 18.17902769456078360, -0.04114048977874908142, 12.69993211551498469 ) ) ;
#5482=CARTESIAN_POINT ( 'NONE',  ( 5.634466645576796218, 12.10031501007015819, 3.741403512701362732 ) ) ;
#5498=DIRECTION ( 'NONE',  ( 1.000000000000000000, 0.000000000000000000, 0.000000000000000000 ) ) ;
#5509=CARTESIAN_POINT ( 'NONE',  ( 12.72194006826445545, -1.880463790526825552, -12.57452048663021671 ) ) ;
#5513=CARTESIAN_POINT ( 'NONE',  ( 12.13953890720640416, -2.807801093580551743, -13.71555245415304292 ) ) ;
#5516=CARTESIAN_POINT ( 'NONE',  ( 18.10200918459799979, -2.953257374879731501, 12.24902512628088225 ) ) ;
#5523=CARTESIAN_POINT ( 'NONE',  ( 12.80505043854144276, -0.6600719421079733751, -13.91436771118225302 ) ) ;
#5526=DIRECTION ( 'NONE',  ( -1.000000000000000000, 0.000000000000000000, 0.000000000000000000 ) ) ;
#5538=CARTESIAN_POINT ( 'NONE',  ( 12.58454787187813295, -0.5848996845204778028, 12.68186405703078812 ) ) ;
#5539=CARTESIAN_POINT ( 'NONE',  ( 5.596495275684807424, -12.13697930370502753, -3.751366953416414685 ) ) ;
#5545=CARTESIAN_POINT ( 'NONE',  ( 17.75741541229203335, 3.091422763980662403, 13.53001720626202520 ) ) ;
#5557=CARTESIAN_POINT ( 'NONE',  ( 17.59651852071655753, -3.123961849275329161, -13.52107344427228597 ) ) ;
#5575=CARTESIAN_POINT ( 'NONE',  ( 12.41909388474793019, 1.871095411850174139, -12.46029856231474930 ) ) ;
#5578=CARTESIAN_POINT ( 'NONE',  ( 18.11804139222710219, 2.771758052454487142, -13.61206300403527436 ) ) ;
#5583=CARTESIAN_POINT ( 'NONE',  ( 12.38044747764044651, -3.063579277862365391, -12.22188755179955955 ) ) ;
#5589=CARTESIAN_POINT ( 'NONE',  ( 17.94753454920341795, 0.4864235087029692428, -12.68745975172791240 ) ) ;
#5590=CARTESIAN_POINT ( 'NONE',  ( 12.80505043854144276, 0.7302158263239216796, -13.98094363220830871 ) ) ;
#5599=CARTESIAN_POINT ( 'NONE',  ( 18.26225755805769424, 2.321011060851990493, 12.38438709824086814 ) ) ;
#5609=VECTOR ( 'NONE', #54834, 1000.000000000000000 ) ;
#5610=FACE_OUTER_BOUND ( 'NONE', #36601, .T. ) ;
#5615=CARTESIAN_POINT ( 'NONE',  ( 12.51647491292534475, 0.6599616342124019486, 12.58270523616455705 ) ) ;
#5620=CARTESIAN_POINT ( 'NONE',  ( 12.67305101672400269, 1.772831636685040957, 12.47465725448102170 ) ) ;
#5631=CARTESIAN_POINT ( 'NONE',  ( 12.55586324463467918, 0.5732756864902116556, 12.68257855878055906 ) ) ;
#5635=CARTESIAN_POINT ( 'NONE',  ( 12.54527475442097995, -3.068547466015818070, 13.53629565290702352 ) ) ;
#5636=CARTESIAN_POINT ( 'NONE',  ( 12.21323965715487603, 2.701097325876321786, 13.62869820427204814 ) ) ;
#5643=VECTOR ( 'NONE', #1154, 1000.000000000000000 ) ;
#5644=CARTESIAN_POINT ( 'NONE',  ( 18.17584245753825911, 2.573100139072833414, -12.43426722069302137 ) ) ;
#5649=CARTESIAN_POINT ( 'NONE',  ( 4.599999999999999645, -1.875000000000000000, -13.78627172894481667 ) ) ;
#5669=CARTESIAN_POINT ( 'NONE',  ( 12.39828470357503321, 0.4745495851175757784, -13.88909655036762913 ) ) ;
#5673=ORIENTED_EDGE ( 'NONE', *, *, #4156, .F. ) ;
#5682=CARTESIAN_POINT ( 'NONE',  ( 12.80505043854143388, 3.124999999999999556, -25.00000000000000000 ) ) ;
#5683=CARTESIAN_POINT ( 'NONE',  ( 18.16381471383438395, -2.642962562933662607, -12.41712880859051893 ) ) ;
#5687=CARTESIAN_POINT ( 'NONE',  ( 18.18000379063077787, -2.491959044355968711, -12.45343158201009359 ) ) ;
#5688=CARTESIAN_POINT ( 'NONE',  ( 12.18832812670981092, -0.1018973686818604313, 13.89950237059086291 ) ) ;
#5704=CARTESIAN_POINT ( 'NONE',  ( 17.74675502951912520, -3.228624035270135639, 13.62268076943954753 ) ) ;
#5718=CARTESIAN_POINT ( 'NONE',  ( 18.18005043799233178, 2.500000011518615395, -12.45159158845316405 ) ) ;
#5720=CARTESIAN_POINT ( 'NONE',  ( 17.55505043854143565, 3.125000000000000000, -13.52084414783465682 ) ) ;
#5724=CARTESIAN_POINT ( 'NONE',  ( 17.60407896980289522, 1.760945483361004538, 12.47634044926096308 ) ) ;
#5728=CARTESIAN_POINT ( 'NONE',  ( 12.51886017880454816, 0.5557204214162397848, -12.68363025601217231 ) ) ;
#5732=LINE ( 'NONE', #6077, #6965 ) ;
#5743=CARTESIAN_POINT ( 'NONE',  ( 18.00577237252829832, 2.933105347812601238, -13.57200668515162612 ) ) ;
#5745=CARTESIAN_POINT ( 'NONE',  ( 4.599999999999999645, 3.199698446519375850, 12.18695736643652694 ) ) ;
#5754=FACE_OUTER_BOUND ( 'NONE', #33608, .T. ) ;
#5764=CARTESIAN_POINT ( 'NONE',  ( 4.599999999999999645, 14.00000000000000000, 0.000000000000000000 ) ) ;
#5778=CARTESIAN_POINT ( 'NONE',  ( 12.31461592258503046, 2.887558836668429052, -13.58358613427759209 ) ) ;
#5785=CARTESIAN_POINT ( 'NONE',  ( 12.33489288317251820, 0.4118289862746073449, 13.89178842664828295 ) ) ;
#5787=CARTESIAN_POINT ( 'NONE',  ( 17.55505043854144276, -0.6250000000000001110, -25.00000000000000000 ) ) ;
#5788=CARTESIAN_POINT ( 'NONE',  ( 17.88363324753128580, -0.5317637309696081616, -13.88630818040599202 ) ) ;
#5797=CARTESIAN_POINT ( 'NONE',  ( 17.65692019170432303, -0.6169782284476043044, 12.67981870385669652 ) ) ;
#5809=CARTESIAN_POINT ( 'NONE',  ( 17.55505043854143565, 3.125000000000000000, -12.28374638332999602 ) ) ;
#5817=CARTESIAN_POINT ( 'NONE',  ( 17.70945903195347171, 3.183352579998539156, -12.19123751323113325 ) ) ;
#5820=VERTEX_POINT ( 'NONE', #52798 ) ;
#5831=CARTESIAN_POINT ( 'NONE',  ( 12.15578049617548650, 2.108731457858032066, -12.42302753736613852 ) ) ;
#5833=CARTESIAN_POINT ( 'NONE',  ( 17.69685691690358809, -0.6090406077983145927, -13.88203505342130661 ) ) ;
#5848=CARTESIAN_POINT ( 'NONE',  ( 12.57288091590949897, -1.919630123611445693, -12.56800073041603305 ) ) ;
#5852=CARTESIAN_POINT ( 'NONE',  ( 12.14271297744737232, -2.220151667091626813, -13.82285866607422520 ) ) ;
#5855=CARTESIAN_POINT ( 'NONE',  ( 17.84599613952814678, -3.139413506986239888, 12.20262697555082632 ) ) ;
#5856=ORIENTED_EDGE ( 'NONE', *, *, #156, .F. ) ;
#5859=AXIS2_PLACEMENT_3D ( 'NONE', #65495, #17622, #55021 ) ;
#5869=ADVANCED_FACE ( 'NONE', ( #41278 ), #26231, .F. ) ;
#5884=CARTESIAN_POINT ( 'NONE',  ( 18.14139820495726241, 2.283379482803411076, 13.71697381851087805 ) ) ;
#5892=DIRECTION ( 'NONE',  ( 0.000000000000000000, 0.000000000000000000, 1.000000000000000000 ) ) ;
#5894=ORIENTED_EDGE ( 'NONE', *, *, #43878, .F. ) ;
#5896=CARTESIAN_POINT ( 'NONE',  ( 18.11095118117833636, -2.049130080444088620, -13.84922935676121902 ) ) ;
#5916=CARTESIAN_POINT ( 'NONE',  ( 12.18347802452934658, 2.109676230065139269, -12.42212916133884981 ) ) ;
#5926=ORIENTED_EDGE ( 'NONE', *, *, #2620, .F. ) ;
#5934=CARTESIAN_POINT ( 'NONE',  ( 17.81315952985430329, 0.5693054069933394246, -12.68281928773557787 ) ) ;
#5935=CARTESIAN_POINT ( 'NONE',  ( 12.22109980851669953, 2.722998852138081016, -12.39684006587159892 ) ) ;
#5945=CARTESIAN_POINT ( 'NONE',  ( 18.23116755655858867, 2.220104646260180559, 12.40287289761280576 ) ) ;
#5947=CARTESIAN_POINT ( 'NONE',  ( 12.58164121395688007, 1.823227133926375698, 13.88077287699123197 ) ) ;
#5953=CARTESIAN_POINT ( 'NONE',  ( 12.54706542093076038, -3.153101027525017752, 12.19910009420584984 ) ) ;
#5958=B_SPLINE_CURVE_WITH_KNOTS ( 'NONE', 1,
 ( #4205, #36027 ),
 .UNSPECIFIED., .F., .F.,
 ( 2, 2 ),
 ( 0.000000000000000000, 1.000000000000000000 ),
 .UNSPECIFIED. ) ;
#5960=CARTESIAN_POINT ( 'NONE',  ( 12.27567264278500581, 0.4920215530101147428, 12.59040071882420797 ) ) ;
#5964=CARTESIAN_POINT ( 'NONE',  ( 12.42670498308433658, 2.997500030636911728, 12.32161918487003405 ) ) ;
#5971=CARTESIAN_POINT ( 'NONE',  ( 12.19705744689154692, 2.644897762231630534, 12.41662195483983488 ) ) ;
#5974=CARTESIAN_POINT ( 'NONE',  ( 12.41737000022668269, 0.4903651763005736353, 12.68725775796289312 ) ) ;
#5977=CARTESIAN_POINT ( 'NONE',  ( 17.55505043854143565, 1.760845406083394682, -12.47635457398814829 ) ) ;
#5978=CARTESIAN_POINT ( 'NONE',  ( 12.08002994951554498, -2.497059486053643695, 13.77553160571068247 ) ) ;
#5989=CARTESIAN_POINT ( 'NONE',  ( 17.63816080826976673, 1.880463790428644533, -12.57456020225082582 ) ) ;
#5994=CARTESIAN_POINT ( 'NONE',  ( 12.43754357095653518, 3.154646014582549896, 13.64000194806622090 ) ) ;
#6004=CARTESIAN_POINT ( 'NONE',  ( 17.69878333211500987, -3.108595074582393369, 13.52536937155546681 ) ) ;
#6009=VECTOR ( 'NONE', #17127, 1000.000000000000000 ) ;
#6012=CARTESIAN_POINT ( 'NONE',  ( 12.35751123590698519, -3.100314578187023162, -13.65257769754496842 ) ) ;
#6013=CARTESIAN_POINT ( 'NONE',  ( 12.53102142834153376, 0.5618070542492630270, -13.88471645277093103 ) ) ;
#6020=EDGE_LOOP ( 'NONE', ( #18374, #56308, #11960, #10569, #42336, #27068 ) ) ;
#6024=CARTESIAN_POINT ( 'NONE',  ( 17.96133816917720338, -2.975035784927402283, -12.32810058309830836 ) ) ;
#6030=ADVANCED_BREP_SHAPE_REPRESENTATION ( '', ( #30272, #9676 ), #58898 ) ;
#6031=CARTESIAN_POINT ( 'NONE',  ( 18.17992876607769048, -2.487411392606218463, -12.45448399073205437 ) ) ;
#6032=CARTESIAN_POINT ( 'NONE',  ( 12.26373570557222514, -0.3125842563278225517, 13.89527356689843884 ) ) ;
#6072=B_SPLINE_CURVE_WITH_KNOTS ( 'NONE', 3,
 ( #40112, #66313, #13201, #35210, #14223, #7942, #60732, #49900, #61426, #29632, #34529, #18091, #23331, #50593 ),
 .UNSPECIFIED., .F., .F.,
 ( 4, 2, 2, 2, 2, 2, 4 ),
 ( 0.000000000000000000, 0.2494049090185054274, 0.3741073635277598064, 0.4052829771550735538, 0.4364585907823873012, 0.4676342044097009931, 0.4988098180370147405 ),
 .UNSPECIFIED. ) ;
#6077=CARTESIAN_POINT ( 'NONE',  ( 5.699999772733999492, 12.03770622561999915, 3.722046322334000124 ) ) ;
#6082=CARTESIAN_POINT ( 'NONE',  ( 18.14037995568667583, 0.2193687868415796216, 12.69745523515037711 ) ) ;
#6106=VERTEX_POINT ( 'NONE', #7310 ) ;
#6108=CARTESIAN_POINT ( 'NONE',  ( 18.06139357112843058, 0.3666408745733568675, -13.89349736880774877 ) ) ;
#6120=CARTESIAN_POINT ( 'NONE',  ( 12.23531288305053621, 2.757742497410567317, -13.61542453244087092 ) ) ;
#6123=CARTESIAN_POINT ( 'NONE',  ( 18.17882709566423216, -0.04040202251154500351, 13.89992604541790477 ) ) ;
#6129=CARTESIAN_POINT ( 'NONE',  ( 12.22418139215586486, -0.2308705899090618963, 13.89742331311339818 ) ) ;
#6130=CARTESIAN_POINT ( 'NONE',  ( 12.39787770614147355, -0.4743614816433503467, -13.88910774395701608 ) ) ;
#6132=CARTESIAN_POINT ( 'NONE',  ( 18.18005043824477696, 1.062919176435095297E-10, -13.90000000153291637 ) ) ;
#6140=CARTESIAN_POINT ( 'NONE',  ( 17.78490268980527134, -0.5812897767837150731, 12.68208758371477352 ) ) ;
#6150=DIRECTION ( 'NONE',  ( 1.000000000000000000, 0.000000000000000000, 0.000000000000000000 ) ) ;
#6154=CARTESIAN_POINT ( 'NONE',  ( 12.09857507241188657, 0.1632583333441771367, -12.59896334813831409 ) ) ;
#6156=CARTESIAN_POINT ( 'NONE',  ( 17.74426251268373633, 3.174930969421378091, -12.19343357469032085 ) ) ;
#6171=CARTESIAN_POINT ( 'NONE',  ( 17.55505043854143921, 0.7302158263239216796, -13.98094363220831049 ) ) ;
#6173=CYLINDRICAL_SURFACE ( 'NONE', #15235, 0.6250000000000005551 ) ;
#6188=CARTESIAN_POINT ( 'NONE',  ( 12.24703709751431724, -2.218305284339070482, -12.51274264014588411 ) ) ;
#6192=CARTESIAN_POINT ( 'NONE',  ( 12.08550557360782562, -2.425787521189701756, -13.78826042901831528 ) ) ;
#6194=CARTESIAN_POINT ( 'NONE',  ( 12.70675980919359205, -3.199682200194524651, 12.18696163212649886 ) ) ;
#6195=CARTESIAN_POINT ( 'NONE',  ( 17.63759097916654994, -3.119868145639166812, 12.28530842955781921 ) ) ;
#6208=CARTESIAN_POINT ( 'NONE',  ( 17.60407896982588127, -1.760945483361028074, -12.47634044926095420 ) ) ;
#6221=B_SPLINE_CURVE_WITH_KNOTS ( 'NONE', 3,
 ( #8097, #2844, #45164, #17902 ),
 .UNSPECIFIED., .F., .F.,
 ( 4, 4 ),
 ( 0.000000000000000000, 1.000000000000000000 ),
 .UNSPECIFIED. ) ;
#6227=CARTESIAN_POINT ( 'NONE',  ( 18.02623320712467603, 2.911124530445448499, 13.57757619639374269 ) ) ;
#6236=DIRECTION ( 'NONE',  ( -0.000000000000000000, -0.000000000000000000, 1.000000000000000000 ) ) ;
#6239=CARTESIAN_POINT ( 'NONE',  ( 18.20725128760098244, -2.198916822427667395, -13.82623906782133005 ) ) ;
#6255=EDGE_CURVE ( 'NONE', #40006, #16502, #24005, .T. ) ;
#6261=CARTESIAN_POINT ( 'NONE',  ( 12.49755103297837167, 3.131894283645451971, -12.20455838002552973 ) ) ;
#6265=ORIENTED_EDGE ( 'NONE', *, *, #48657, .F. ) ;
#6276=CARTESIAN_POINT ( 'NONE',  ( 17.84384701673186058, -0.6598665579122044988, -12.58271022457860155 ) ) ;
#6277=CARTESIAN_POINT ( 'NONE',  ( 12.20883946519827390, 2.687526094442107993, -12.40592204487018790 ) ) ;
#6281=B_SPLINE_CURVE_WITH_KNOTS ( 'NONE', 3,
 ( #34595, #45759, #66384, #12915, #13269, #13610, #23399, #55563, #45078, #65694, #35274, #44395, #3100, #55909, #2082, #24434 ),
 .UNSPECIFIED., .F., .F.,
 ( 4, 2, 2, 2, 2, 2, 2, 4 ),
 ( 0.000000000000000000, 0.06249999999999893141, 0.1249999999999978628, 0.2499999999999999445, 0.5000000000000009992, 0.7500000000000019984, 0.8750000000000009992, 1.000000000000000000 ),
 .UNSPECIFIED. ) ;
#6286=CARTESIAN_POINT ( 'NONE',  ( 18.27884988594217219, 2.529462001843210128, 12.34351620764206814 ) ) ;
#6287=CARTESIAN_POINT ( 'NONE',  ( 12.78089695109145119, 1.787798027819076596, 13.88537998392835249 ) ) ;
#6295=CARTESIAN_POINT ( 'NONE',  ( 12.32471554566195238, -3.019419751198730850, 12.23287256106958232 ) ) ;
#6300=CARTESIAN_POINT ( 'NONE',  ( 12.12622238209133840, -0.2528603812084252445, 12.59746735456353051 ) ) ;
#6303=CARTESIAN_POINT ( 'NONE',  ( 12.18425839594605442, 2.573099938722084978, 12.43423733299713341 ) ) ;
#6307=CARTESIAN_POINT ( 'NONE',  ( 18.20534100106117137, -0.3182341284860664143, 12.59598505207571861 ) ) ;
#6312=CARTESIAN_POINT ( 'NONE',  ( 17.90980607979504313, -0.5146431973202493237, 12.68596244101487791 ) ) ;
#6319=CARTESIAN_POINT ( 'NONE',  ( 12.36046591005678685, -1.940744226335692879, 13.86483863263027594 ) ) ;
#6330=CARTESIAN_POINT ( 'NONE',  ( 17.65865034516101773, 1.883559157718814880, -12.57405095325165512 ) ) ;
#6341=DIRECTION ( 'NONE',  ( -1.000000000000000000, 0.000000000000000000, 0.000000000000000000 ) ) ;
#6347=CARTESIAN_POINT ( 'NONE',  ( 18.03303331148768862, -2.902815211882732616, 13.57973159350535752 ) ) ;
#6363=ORIENTED_EDGE ( 'NONE', *, *, #19592, .T. ) ;
#6370=CARTESIAN_POINT ( 'NONE',  ( 12.55449126378680980, 3.072671109762265651, 13.53512077903586075 ) ) ;
#6372=CARTESIAN_POINT ( 'NONE',  ( 5.500000000000000000, 13.94845324556000143, 4.312847325879000770 ) ) ;
#6373=ADVANCED_FACE ( 'NONE', ( #63542 ), #28448, .F. ) ;
#6374=CARTESIAN_POINT ( 'NONE',  ( 12.80505043854144098, 0.6249999999999996669, 13.88107975066923316 ) ) ;
#6376=EDGE_LOOP ( 'NONE', ( #24682, #15427, #61392, #7338 ) ) ;
#6383=FACE_OUTER_BOUND ( 'NONE', #7063, .T. ) ;
#6388=VECTOR ( 'NONE', #42591, 1000.000000000000000 ) ;
#6403=CARTESIAN_POINT ( 'NONE',  ( 17.55505043854143565, 3.199751711897561801, -12.18694338143115452 ) ) ;
#6405=CARTESIAN_POINT ( 'NONE',  ( 5.579147253214326696, -12.92151814423300316, 2.574492151368334536 ) ) ;
#6420=ORIENTED_EDGE ( 'NONE', *, *, #54469, .F. ) ;
#6426=CARTESIAN_POINT ( 'NONE',  ( 5.602978689604023010, 12.13075210502077184, -3.749558893019930839 ) ) ;
#6431=CARTESIAN_POINT ( 'NONE',  ( 17.86097767714751328, 3.045104419577886912, -13.54261379197757087 ) ) ;
#6446=CARTESIAN_POINT ( 'NONE',  ( 17.99248396118099080, -2.946503669276440363, -13.56850299727616260 ) ) ;
#6454=CARTESIAN_POINT ( 'NONE',  ( 17.77313190797698539, -1.794191980291848676, -12.47160287655520428 ) ) ;
#6460=B_SPLINE_SURFACE_WITH_KNOTS ( 'NONE', 1, 3, ( 
 ( #17387, #38717, #29968, #66994, #3027, #35204, #45001, #46024, #14559, #55833, #56171, #8281, #19106, #67332, #62097, #50928, #28937, #50240, #61076, #34523, #8620, #2344, #13193, #7937, #35877, #23664, #46371, #18432, #56513, #57192, #66308, #40428, #51271, #13873, #29624, #3365, #67672, #29273, #24701, #18776, #50587, #2687, #39757, #19452, #61754, #45689, #14215, #3701, #24357, #40772, #35544, #56862, #8959, #45347, #66657, #51604, #19800, #30299, #40105, #25040, #24013, #61419, #41125, #62438, #13537, #34856, #60958, #28110, #6772, #8163, #50465, #17971, #66192, #39290, #44204, #13422, #13073, #34403, #55720, #50127, #65498, #39636, #38591, #17626, #33705, #55024 ),
 ( #45231, #38952, #50815, #28818, #49422, #2233, #60612, #7816, #60269, #12374, #56052, #2567, #29157, #61303, #44555, #23548, #66536, #23896, #2909, #29511, #24238, #18656, #59915, #45576, #17268, #12723, #12024, #33360, #1535, #7125, #54674, #34741, #44888, #18313, #39989, #22853, #28463, #49777, #1888, #23205, #65847, #34054, #55369, #7464, #62330, #35091, #41354, #19332, #52524, #41691, #31218, #24925, #67911, #14446, #46257, #4281, #9874, #36446, #20027, #15126, #45909, #51835, #56752, #24586, #3257, #61640, #62664, #30521, #35765, #52180, #62997, #57081, #14784, #9181, #3930, #46606, #14102, #35427, #20367, #57763, #25267, #8849, #36103, #40321, #66882, #4622 ) ),
 .UNSPECIFIED., .F., .F., .F.,
 ( 2, 2 ),
 ( 4, 2, 2, 2, 2, 2, 2, 2, 2, 2, 2, 2, 2, 2, 2, 2, 2, 2, 2, 2, 2, 2, 2, 2, 2, 2, 2, 2, 2, 2, 2, 2, 2, 2, 2, 2, 2, 2, 2, 2, 2, 2, 4 ),
 ( 0.000000000000000000, 1.000000000000000000 ),
 ( 0.000000000000000000, 7.083094307561114554E-05, 0.0001416618861512222911, 0.0002124928292268334366, 0.0002833237723024445822, 0.0003541547153780557006, 0.0004249856584536668733, 0.0004958166015292780459, 0.0005666475446048891643, 0.0006374784876805002828, 0.0007083094307561114012, 0.0007791403738317225196, 0.0008145558453695280789, 0.0008499713169073337465, 0.0008853867884451394141, 0.0009208022599829449734, 0.0009916332030585560918, 0.001027048674596361651, 0.001062464146134167210, 0.001097879617671972769, 0.001133295089209778329, 0.001204126032285389447, 0.001239541503823195006, 0.001274956975361000566, 0.001310372446898806125, 0.001345787918436611684, 0.001416618861512222802, 0.001487449804587833921, 0.001522865276125639480, 0.001558280747663445039, 0.001629111690739056158, 0.001699942633814667493, 0.001735358105352473052, 0.001770773576890278828, 0.001806189048428084388, 0.001841604519965889947, 0.001912435463041501065, 0.001983266406117112184, 0.002018681877654917960, 0.002054097349192723302, 0.002124928292268334420, 0.002195759235343945539, 0.002266590178419556657 ),
 .UNSPECIFIED. ) ;
#6462=EDGE_CURVE ( 'NONE', #45774, #38751, #64220, .T. ) ;
#6469=CARTESIAN_POINT ( 'NONE',  ( 12.61514273204568859, 1.812907417374174379, -13.88212581052983197 ) ) ;
#6472=CARTESIAN_POINT ( 'NONE',  ( 18.21574553171933886, -0.3008963210924971987, 13.99677033988233354 ) ) ;
#6477=CARTESIAN_POINT ( 'NONE',  ( 12.44245189050256073, -0.5091685952834601459, 13.88744776337617282 ) ) ;
#6490=CARTESIAN_POINT ( 'NONE',  ( 17.71666921258853122, -0.6040886362899380302, 12.68065483099174884 ) ) ;
#6493=CARTESIAN_POINT ( 'NONE',  ( 18.04518119038796442, -2.887943935952099306, -12.35267345331065414 ) ) ;
#6496=CARTESIAN_POINT ( 'NONE',  ( 17.55505043854143565, 1.875000000000000000, -12.57545641911172751 ) ) ;
#6505=CARTESIAN_POINT ( 'NONE',  ( 12.09168743772586296, -0.1288995356414814608, -12.59934597632939735 ) ) ;
#6508=CARTESIAN_POINT ( 'NONE',  ( 18.27038927661324053, 2.598921547761769091, -12.32906097307314219 ) ) ;
#6523=CARTESIAN_POINT ( 'NONE',  ( 18.10142235202799199, -0.3036576181174172051, -13.89554011873102546 ) ) ;
#6539=CARTESIAN_POINT ( 'NONE',  ( 12.54434846374639001, -1.931873423426546443, -12.56592826555433362 ) ) ;
#6544=CARTESIAN_POINT ( 'NONE',  ( 12.08884934673722711, -2.402320636441741541, -13.79236805980801073 ) ) ;
#6548=CARTESIAN_POINT ( 'NONE',  ( 17.57923549477752090, -1.761145725279483987, 12.47631219955854043 ) ) ;
#6562=DIRECTION ( 'NONE',  ( 0.000000000000000000, 1.000000000000000000, 0.000000000000000000 ) ) ;
#6579=CARTESIAN_POINT ( 'NONE',  ( 18.05171780850496788, 2.879539315883434369, 13.58554773987827602 ) ) ;
#6591=CARTESIAN_POINT ( 'NONE',  ( 17.77689708618911268, -3.084393760937525375, -13.53193451522998103 ) ) ;
#6614=CARTESIAN_POINT ( 'NONE',  ( 12.08596835297189287, 2.576236330983344036, -12.33383868535373296 ) ) ;
#6625=CARTESIAN_POINT ( 'NONE',  ( 12.70928935905668489, -3.193791526923299706, -12.18850694772984333 ) ) ;
#6631=DIRECTION ( 'NONE',  ( 0.000000000000000000, -0.9905022095861402143, 0.1374968101629056305 ) ) ;
#6632=CARTESIAN_POINT ( 'NONE',  ( 17.85930819889520649, -0.5460377805369022175, -12.68419612078312220 ) ) ;
#6633=CARTESIAN_POINT ( 'NONE',  ( 12.21329150906689343, 2.701250044071452194, -12.40242623238894559 ) ) ;
#6640=CARTESIAN_POINT ( 'NONE',  ( 18.08635919897130151, 2.970004615628405897, 12.24496439055023700 ) ) ;
#6643=CARTESIAN_POINT ( 'NONE',  ( 12.80505043854144276, -0.7302158263239078018, 13.98094363220830871 ) ) ;
#6646=CARTESIAN_POINT ( 'NONE',  ( 12.12887591290038536, -2.220077349933753830, 12.40287778440552380 ) ) ;
#6650=B_SPLINE_CURVE_WITH_KNOTS ( 'NONE', 1,
 ( #42538, #37290 ),
 .UNSPECIFIED., .F., .F.,
 ( 2, 2 ),
 ( 0.000000000000000000, 1.000000000000000000 ),
 .UNSPECIFIED. ) ;
#6653=CARTESIAN_POINT ( 'NONE',  ( 12.08233499759481155, -0.05827135643915358487, 12.59987075990256677 ) ) ;
#6657=CARTESIAN_POINT ( 'NONE',  ( 12.52646068131086210, 3.059569037265597480, 12.30341205401442473 ) ) ;
#6666=DIRECTION ( 'NONE',  ( -0.000000000000000000, -0.000000000000000000, 1.000000000000000000 ) ) ;
#6673=CARTESIAN_POINT ( 'NONE',  ( 12.25852519399118634, -2.998253127629475046, 13.67519035003951267 ) ) ;
#6682=CARTESIAN_POINT ( 'NONE',  ( 5.599965786763100084, 11.06886219213000011, 1.536526853569999851 ) ) ;
#6683=CARTESIAN_POINT ( 'NONE',  ( 17.74851076052200938, 1.905606517475760597, -12.57039381402181633 ) ) ;
#6690=CARTESIAN_POINT ( 'NONE',  ( 12.80505043854143388, 1.787797342887042840, 13.88538010501570774 ) ) ;
#6691=EDGE_CURVE ( 'NONE', #21149, #66718, #57185, .T. ) ;
#6698=CARTESIAN_POINT ( 'NONE',  ( 18.17999014114401035, -2.522019970189117277, 13.66878426939143587 ) ) ;
#6700=ORIENTED_EDGE ( 'NONE', *, *, #27085, .F. ) ;
#6704=DIRECTION ( 'NONE',  ( 0.000000000000000000, -1.000000000000000000, -0.000000000000000000 ) ) ;
#6708=CARTESIAN_POINT ( 'NONE',  ( 17.82167905068868663, 0.6689867242971743178, -12.58222862546947418 ) ) ;
#6716=ORIENTED_EDGE ( 'NONE', *, *, #43878, .T. ) ;
#6717=CARTESIAN_POINT ( 'NONE',  ( 17.92302462176263944, -1.881539600472786677, -13.87303898716210426 ) ) ;
#6721=CARTESIAN_POINT ( 'NONE',  ( 12.60257768741563567, 1.908613650260960526, 13.78119617999061397 ) ) ;
#6723=CARTESIAN_POINT ( 'NONE',  ( 12.80505043854144276, 0.6249999999999994449, -12.67928921589118652 ) ) ;
#6724=CARTESIAN_POINT ( 'NONE',  ( 12.18532581790793223, -0.08167545936615885904, 13.89968205666727386 ) ) ;
#6731=EDGE_CURVE ( 'NONE', #62111, #57125, #47525, .T. ) ;
#6732=LINE ( 'NONE', #39250, #5643 ) ;
#6738=CARTESIAN_POINT ( 'NONE',  ( 17.65355681326706261, -3.248032782086183179, 13.61801318301550268 ) ) ;
#6740=CARTESIAN_POINT ( 'NONE',  ( 12.44006281456469232, 0.6285461057673268348, 12.58436427553280801 ) ) ;
#6764=CARTESIAN_POINT ( 'NONE',  ( 12.64262999012820998, 0.6038699852804525481, -12.68066884516331783 ) ) ;
#6766=CARTESIAN_POINT ( 'NONE',  ( 12.21880568482660934, 2.282463263829442646, -13.71720984526209364 ) ) ;
#6769=ORIENTED_EDGE ( 'NONE', *, *, #64209, .T. ) ;
#6772=CARTESIAN_POINT ( 'NONE',  ( 12.42469545966024214, 0.4960449563116388627, -13.88808666890936827 ) ) ;
#6779=EDGE_LOOP ( 'NONE', ( #43510, #1120, #19957, #16138, #65081 ) ) ;
#6781=CARTESIAN_POINT ( 'NONE',  ( 18.02738429465118486, 2.090191673117355542, -13.75189211025434410 ) ) ;
#6787=CARTESIAN_POINT ( 'NONE',  ( 17.77845184731630468, 1.823244735605227484, -13.88077056497939665 ) ) ;
#6788=CARTESIAN_POINT ( 'NONE',  ( 17.86524243511767196, 0.5426972542083243756, -12.68439075057428944 ) ) ;
#6794=CARTESIAN_POINT ( 'NONE',  ( 17.98396147894309749, -2.954720660964888168, -13.56638041066537070 ) ) ;
#6802=CARTESIAN_POINT ( 'NONE',  ( 18.26479085099342115, -2.332519703358805874, -12.38222476794584814 ) ) ;
#6806=DIRECTION ( 'NONE',  ( 0.000000000000000000, 1.000000000000000000, 0.000000000000000000 ) ) ;
#6811=ORIENTED_EDGE ( 'NONE', *, *, #48044, .T. ) ;
#6815=CARTESIAN_POINT ( 'NONE',  ( 12.25820678327523616, 2.802802780256932191, -13.60456178155848050 ) ) ;
#6817=B_SPLINE_CURVE_WITH_KNOTS ( 'NONE', 3,
 ( #16200, #48359, #465, #28080, #60929, #6740, #44858, #28785, #17592, #49394, #61274, #7787, #38917, #13391, #13041, #34371 ),
 .UNSPECIFIED., .F., .F.,
 ( 4, 2, 2, 2, 2, 2, 2, 4 ),
 ( 0.000000000000000000, 0.06249999999999897304, 0.1249999999999979461, 0.2499999999999980016, 0.4999999999999981126, 0.7499999999999982236, 0.8749999999999990008, 1.000000000000000000 ),
 .UNSPECIFIED. ) ;
#6819=CARTESIAN_POINT ( 'NONE',  ( 17.75589283472434232, 0.5919407257947367773, 13.88303015925714590 ) ) ;
#6827=CARTESIAN_POINT ( 'NONE',  ( 12.18827041299910796, -0.1029057169788573228, 13.89950510286037044 ) ) ;
#6838=CARTESIAN_POINT ( 'NONE',  ( 18.00459872918310467, 0.4343244881883151498, 12.69000555157926868 ) ) ;
#6845=FACE_OUTER_BOUND ( 'NONE', #36731, .T. ) ;
#6851=CARTESIAN_POINT ( 'NONE',  ( 12.14435919815817932, 0.2964030593063847197, -12.59651778044212556 ) ) ;
#6870=CARTESIAN_POINT ( 'NONE',  ( 18.08578335600534359, -0.3302328523437055852, -13.89472426752320899 ) ) ;
#6879=CARTESIAN_POINT ( 'NONE',  ( 12.27415370856040511, -2.829964016113827530, -13.59786649615824672 ) ) ;
#6887=DIRECTION ( 'NONE',  ( 0.000000000000000000, 0.7198977633594747516, 0.6940801180771756229 ) ) ;
#6892=CARTESIAN_POINT ( 'NONE',  ( 17.65791272883258500, -3.116819718221111035, 12.28623542600055352 ) ) ;
#6895=ORIENTED_EDGE ( 'NONE', *, *, #53701, .F. ) ;
#6924=CARTESIAN_POINT ( 'NONE',  ( 18.11732105061182452, 2.226901518982099759, 13.72755281718821507 ) ) ;
#6933=VERTEX_POINT ( 'NONE', #5590 ) ;
#6934=CARTESIAN_POINT ( 'NONE',  ( 17.55505043854143565, 1.875000000000000000, -25.00000000000000000 ) ) ;
#6935=CARTESIAN_POINT ( 'NONE',  ( 17.92097207270829173, -1.887179018856798507, -13.87222722961340793 ) ) ;
#6953=EDGE_CURVE ( 'NONE', #1839, #15133, #25161, .T. ) ;
#6955=VERTEX_POINT ( 'NONE', #12577 ) ;
#6961=CARTESIAN_POINT ( 'NONE',  ( 12.37983597880427133, 3.063558859249376987, -12.22189795429199144 ) ) ;
#6965=VECTOR ( 'NONE', #12371, 1000.000000000000000 ) ;
#6966=ORIENTED_EDGE ( 'NONE', *, *, #64769, .F. ) ;
#6970=CARTESIAN_POINT ( 'NONE',  ( 12.47126843887709846, -3.119056300612248034, -12.20784669583220072 ) ) ;
#6978=CARTESIAN_POINT ( 'NONE',  ( 12.43888651633847608, -3.006915248264998564, -13.55273156457844230 ) ) ;
#6980=CARTESIAN_POINT ( 'NONE',  ( 17.99001832964330561, -0.4489258298041840511, -12.68932177688765428 ) ) ;
#6981=CARTESIAN_POINT ( 'NONE',  ( 12.20035750765601179, 2.340667166415539402, -12.48730567878040176 ) ) ;
#6989=CARTESIAN_POINT ( 'NONE',  ( 17.60340893540758600, 3.198498114537103199, 12.18727270072288604 ) ) ;
#6995=CARTESIAN_POINT ( 'NONE',  ( 12.29866314003343319, -2.995318252715390095, 12.23879431495722336 ) ) ;
#6998=CARTESIAN_POINT ( 'NONE',  ( 5.599999772733800008, -6.661338147750999827E-14, -1.931788062847999572E-14 ) ) ;
#7002=CARTESIAN_POINT ( 'NONE',  ( 12.44180168752029481, -0.6226057762474820345, 12.58460959628226483 ) ) ;
#7007=CARTESIAN_POINT ( 'NONE',  ( 12.29593341745174584, 2.863102696958911508, 12.35953065740858570 ) ) ;
#7013=CARTESIAN_POINT ( 'NONE',  ( 18.04535692654280155, -0.3877536850946274871, 12.69203640188686144 ) ) ;
#7024=CARTESIAN_POINT ( 'NONE',  ( 12.29779067500862944, -1.996199619003550918, 13.85695719179636853 ) ) ;
#7038=DIRECTION ( 'NONE',  ( 0.000000000000000000, 1.000000000000000000, 0.000000000000000000 ) ) ;
#7041=DIRECTION ( 'NONE',  ( 1.000000000000000000, 0.000000000000000000, 0.000000000000000000 ) ) ;
#7043=CARTESIAN_POINT ( 'NONE',  ( 18.00086112087954149, 0.5837697426924873811, -13.98798827748158580 ) ) ;
#7045=CARTESIAN_POINT ( 'NONE',  ( 12.34817707648056917, -2.926896462556495493, 12.34181790735160256 ) ) ;
#7050=CARTESIAN_POINT ( 'NONE',  ( 17.96876343269825327, -2.968584057511098440, 13.56283743052909152 ) ) ;
#7055=ADVANCED_FACE ( 'NONE', ( #13620 ), #11874, .F. ) ;
#7063=EDGE_LOOP ( 'NONE', ( #28202, #63086, #35856, #21103 ) ) ;
#7066=CARTESIAN_POINT ( 'NONE',  ( 17.74422827376958267, -3.224484589758234598, -13.62361160044833674 ) ) ;
#7071=CARTESIAN_POINT ( 'NONE',  ( 12.19342855462627817, 2.370970601743435324, 13.69993124892199532 ) ) ;
#7075=CARTESIAN_POINT ( 'NONE',  ( 12.70318375531252286, -0.6169787192598757963, 13.88156336867697149 ) ) ;
#7111=VECTOR ( 'NONE', #68108, 1000.000000000000000 ) ;
#7120=CARTESIAN_POINT ( 'NONE',  ( 12.33198418664063034, 2.089544947752365101, -13.75203186101843578 ) ) ;
#7122=CARTESIAN_POINT ( 'NONE',  ( 5.679181296657521472, 13.00268187854355517, 2.124261045359595812 ) ) ;
#7124=CARTESIAN_POINT ( 'NONE',  ( 18.20318779768322770, 2.896782429289181504, -13.69773569390626555 ) ) ;
#7125=CARTESIAN_POINT ( 'NONE',  ( 12.11827043973742590, -0.2342631834278633973, -13.99804438501501203 ) ) ;
#7130=CARTESIAN_POINT ( 'NONE',  ( 5.695116968501675814, 12.04237015855112958, -3.723491068767787127 ) ) ;
#7131=ORIENTED_EDGE ( 'NONE', *, *, #34669, .F. ) ;
#7133=CARTESIAN_POINT ( 'NONE',  ( 17.65136412466922522, 3.242045876614677358, -13.61943996000380785 ) ) ;
#7140=CARTESIAN_POINT ( 'NONE',  ( 17.60314900679412631, 1.789028854058313689, -13.88522169503354142 ) ) ;
#7144=ORIENTED_EDGE ( 'NONE', *, *, #47586, .T. ) ;
#7149=AXIS2_PLACEMENT_3D ( 'NONE', #39235, #45178, #56351 ) ;
#7154=CARTESIAN_POINT ( 'NONE',  ( 18.22068658462134749, -2.765866853816883353, -12.29268492208001362 ) ) ;
#7160=EDGE_LOOP ( 'NONE', ( #179, #67454, #42323, #60090, #9476 ) ) ;
#7165=CARTESIAN_POINT ( 'NONE',  ( 12.60268547648130522, 3.091422767983463604, -13.53007486046832852 ) ) ;
#7168=CARTESIAN_POINT ( 'NONE',  ( 18.03351914841129400, -0.5491314443420109992, 13.98923457196397990 ) ) ;
#7170=CARTESIAN_POINT ( 'NONE',  ( 17.59542397727922847, 0.6250000000000002220, 13.88107975724994958 ) ) ;
#7178=CARTESIAN_POINT ( 'NONE',  ( 12.44983642699930471, -0.5143249053040993557, -13.88719129591020618 ) ) ;
#7190=CARTESIAN_POINT ( 'NONE',  ( 18.11801110581809127, 0.2715269968477682094, 12.69609476950841120 ) ) ;
#7193=CARTESIAN_POINT ( 'NONE',  ( 17.83361872140014270, -3.059864849510719242, -12.30332992014196591 ) ) ;
#7198=CARTESIAN_POINT ( 'NONE',  ( 12.48958479105538011, -1.960066648180105453, 13.77326086059893306 ) ) ;
#7207=CARTESIAN_POINT ( 'NONE',  ( 12.13082219998073086, -0.2646961475753908943, -12.59722401988189588 ) ) ;
#7219=VERTEX_POINT ( 'NONE', #24515 ) ;
#7221=CARTESIAN_POINT ( 'NONE',  ( 12.80505043854146940, -3.125000000000000000, -13.52078605991414761 ) ) ;
#7222=CARTESIAN_POINT ( 'NONE',  ( 17.75589283472434232, -0.5919407257947371104, -13.88303015925713879 ) ) ;
#7227=EDGE_CURVE ( 'NONE', #42472, #10401, #5958, .T. ) ;
#7230=VERTEX_POINT ( 'NONE', #67493 ) ;
#7235=CARTESIAN_POINT ( 'NONE',  ( 4.599999999999999645, 0.6250000000000001110, -13.88107975066922428 ) ) ;
#7236=VERTEX_POINT ( 'NONE', #35356 ) ;
#7243=CARTESIAN_POINT ( 'NONE',  ( 17.92144340210922948, -1.859318429515438353, 12.46206136722991786 ) ) ;
#7246=EDGE_LOOP ( 'NONE', ( #64907, #58050, #4991, #22806, #16389, #37407, #16091, #37478, #48295, #28051, #32225 ) ) ;
#7252=MECHANICAL_DESIGN_GEOMETRIC_PRESENTATION_REPRESENTATION('',(#34362),#57486);
#7273=CARTESIAN_POINT ( 'NONE',  ( 18.17327101506963061, 2.135860178445227575, 13.83613041148202782 ) ) ;
#7303=VERTEX_POINT ( 'NONE', #35695 ) ;
#7307=CARTESIAN_POINT ( 'NONE',  ( 12.78419053748684675, 1.875000590519849908, -12.57545628621518041 ) ) ;
#7310=CARTESIAN_POINT ( 'NONE',  ( 18.18005044575082252, 2.500000006795693785, 13.67340643792831045 ) ) ;
#7315=CARTESIAN_POINT ( 'NONE',  ( 12.13758509790272910, -2.198972988417293273, -12.40663693328272288 ) ) ;
#7323=CARTESIAN_POINT ( 'NONE',  ( 17.81340500845573871, -0.5691963043021742719, -12.68282590392938225 ) ) ;
#7332=CARTESIAN_POINT ( 'NONE',  ( 17.65155715295176719, 3.193702317672029611, 12.18853033496119842 ) ) ;
#7336=CARTESIAN_POINT ( 'NONE',  ( 12.61463924707910245, 0.7003689475937157072, -12.58057160030251254 ) ) ;
#7337=EDGE_CURVE ( 'NONE', #47809, #45267, #59332, .T. ) ;
#7338=ORIENTED_EDGE ( 'NONE', *, *, #19922, .F. ) ;
#7339=CARTESIAN_POINT ( 'NONE',  ( 12.13037555192281047, -2.744322634620805612, 12.29751256722372865 ) ) ;
#7346=CARTESIAN_POINT ( 'NONE',  ( 12.63954751664500442, -0.7006927685644985804, 12.58050281163331796 ) ) ;
#7349=CARTESIAN_POINT ( 'NONE',  ( 12.18021258978585486, 2.482515821435916870, 12.45562150274660596 ) ) ;
#7355=CARTESIAN_POINT ( 'NONE',  ( 17.94896820980294905, -0.4852478459816373935, 12.68752000237651778 ) ) ;
#7360=EDGE_CURVE ( 'NONE', #56202, #38546, #13793, .T. ) ;
#7368=CARTESIAN_POINT ( 'NONE',  ( 12.12494527865627880, -2.264899384641844815, 13.81558393673957141 ) ) ;
#7370=DIRECTION ( 'NONE',  ( 1.000000000000000000, 0.000000000000000000, 0.000000000000000000 ) ) ;
#7378=DIRECTION ( 'NONE',  ( -0.000000000000000000, -0.000000000000000000, 1.000000000000000000 ) ) ;
#7389=VERTEX_POINT ( 'NONE', #48235 ) ;
#7392=CARTESIAN_POINT ( 'NONE',  ( 18.11747123342424715, -2.226643993407489308, 13.72766178540381254 ) ) ;
#7394=ORIENTED_EDGE ( 'NONE', *, *, #40389, .F. ) ;
#7401=FACE_OUTER_BOUND ( 'NONE', #13406, .T. ) ;
#7405=CARTESIAN_POINT ( 'NONE',  ( 7.100000000000000533, -12.59999999999999964, 1.543054966925665076E-15 ) ) ;
#7414=CARTESIAN_POINT ( 'NONE',  ( 12.20116045406118310, 2.662322297126387571, 13.63765712018377663 ) ) ;
#7417=DIRECTION ( 'NONE',  ( 1.000000000000000000, 0.000000000000000000, 0.000000000000000000 ) ) ;
#7418=CARTESIAN_POINT ( 'NONE',  ( 12.08233492791620378, 0.05915529127692535638, 13.99988012777929214 ) ) ;
#7425=DIRECTION ( 'NONE',  ( 0.000000000000000000, 0.000000000000000000, 1.000000000000000000 ) ) ;
#7428=DIRECTION ( 'NONE',  ( -0.000000000000000000, -0.000000000000000000, 1.000000000000000000 ) ) ;
#7430=CARTESIAN_POINT ( 'NONE',  ( 4.599999999999999645, 12.59999999999999964, 0.000000000000000000 ) ) ;
#7464=CARTESIAN_POINT ( 'NONE',  ( 12.08472014176157394, 0.08359636179363652553, -13.99975542440154719 ) ) ;
#7465=CARTESIAN_POINT ( 'NONE',  ( 5.700000000000000178, -13.04986661130000059, 1.811520473896000016 ) ) ;
#7472=CARTESIAN_POINT ( 'NONE',  ( 17.87830683576860125, 3.171613455744695109, -13.63601469363850249 ) ) ;
#7481=CARTESIAN_POINT ( 'NONE',  ( 18.11245859367112132, 0.2828884610753772400, -12.69576253191497983 ) ) ;
#7486=CARTESIAN_POINT ( 'NONE',  ( 18.16706615800142544, -2.626761369726613005, -13.64570327821840579 ) ) ;
#7493=CARTESIAN_POINT ( 'NONE',  ( 18.06564745257667326, -2.991132176950372479, -12.23981809347030847 ) ) ;
#7497=AXIS2_PLACEMENT_3D ( 'NONE', #64328, #22384, #27644 ) ;
#7499=CARTESIAN_POINT ( 'NONE',  ( 4.599999999999999645, 0.6250000000000001110, 13.88107975066923494 ) ) ;
#7505=CARTESIAN_POINT ( 'NONE',  ( 12.19498122944100515, 2.912558373969582171, -13.69368860183518066 ) ) ;
#7508=CARTESIAN_POINT ( 'NONE',  ( 17.63678025734559540, 0.6199690124688018722, 13.88138352397878705 ) ) ;
#7512=CIRCLE ( 'NONE', #781, 13.89999852641999922 ) ;
#7514=CARTESIAN_POINT ( 'NONE',  ( 12.26182380061670152, 0.3097576186857741720, 13.89536933047994083 ) ) ;
#7515=CARTESIAN_POINT ( 'NONE',  ( 12.19113298427591552, -2.617185168745339574, 13.64790684748871818 ) ) ;
#7526=CARTESIAN_POINT ( 'NONE',  ( 17.96738117868769535, 0.4698014501121438591, 12.68830453558791405 ) ) ;
#7527=CARTESIAN_POINT ( 'NONE',  ( 12.58522439494062084, -0.5851582065386651266, 12.68184838022285099 ) ) ;
#7534=CARTESIAN_POINT ( 'NONE',  ( 12.42175510762291779, -2.005905104281934470, 13.76592701692032783 ) ) ;
#7542=ORIENTED_EDGE ( 'NONE', *, *, #3791, .F. ) ;
#7543=CARTESIAN_POINT ( 'NONE',  ( 12.12622238209132419, 0.2528603812084147529, -12.59746735456352873 ) ) ;
#7544=CARTESIAN_POINT ( 'NONE',  ( 12.33152592714634288, -2.090072125112540036, -12.53771354782229963 ) ) ;
#7546=VECTOR ( 'NONE', #14577, 1000.000000000000000 ) ;
#7548=VERTEX_POINT ( 'NONE', #24347 ) ;
#7562=CARTESIAN_POINT ( 'NONE',  ( 18.27544000105305599, 0.08309727575449966930, -13.99975851644561686 ) ) ;
#7564=ORIENTED_EDGE ( 'NONE', *, *, #68206, .T. ) ;
#7576=CARTESIAN_POINT ( 'NONE',  ( 12.42368232297769204, -2.995580128734608660, -13.55572452362624425 ) ) ;
#7587=CONICAL_SURFACE ( 'NONE', #37726, 13.94999927503000059, 0.7853981058017837080 ) ;
#7588=CARTESIAN_POINT ( 'NONE',  ( 17.79082714041179969, -1.799831594964177661, 12.47079078729190904 ) ) ;
#7613=CARTESIAN_POINT ( 'NONE',  ( 18.25212943717076541, -0.1980440493285358372, 12.59844852634975787 ) ) ;
#7621=CARTESIAN_POINT ( 'NONE',  ( 18.26357562437058490, 2.673039206754507902, 13.74245258260623892 ) ) ;
#7644=DIRECTION ( 'NONE',  ( 1.000000000000000000, 0.000000000000000000, 0.000000000000000000 ) ) ;
#7647=DIRECTION ( 'NONE',  ( -1.000000000000000000, 0.000000000000000000, 0.000000000000000000 ) ) ;
#7654=CARTESIAN_POINT ( 'NONE',  ( 12.55399154093075431, 1.927548249315100382, -12.56670145065455380 ) ) ;
#7666=CARTESIAN_POINT ( 'NONE',  ( 12.11673986888017929, -2.253747544392083135, -12.39680392560332223 ) ) ;
#7674=CARTESIAN_POINT ( 'NONE',  ( 18.17005379958825273, -0.1118057330073155969, -12.69934308675517620 ) ) ;
#7675=CARTESIAN_POINT ( 'NONE',  ( 17.55505043854144276, 0.000000000000000000, -25.00000000000000000 ) ) ;
#7682=FILL_AREA_STYLE_COLOUR ( '', #51117 ) ;
#7687=CARTESIAN_POINT ( 'NONE',  ( 17.75782926003066819, 1.908786995103509021, 12.56982197457662842 ) ) ;
#7693=CARTESIAN_POINT ( 'NONE',  ( 12.61213290433104106, -1.905496177770261479, 12.57041190218061644 ) ) ;
#7696=CARTESIAN_POINT ( 'NONE',  ( 4.600000533658372248, 13.89999946622000060, 2.316961247309999772E-09 ) ) ;
#7699=CARTESIAN_POINT ( 'NONE',  ( 12.11457469949691834, -0.2196334679052307781, 12.59809060309703277 ) ) ;
#7703=CARTESIAN_POINT ( 'NONE',  ( 12.76340515712443491, 1.876302067334184809, 12.57520337466226223 ) ) ;
#7710=CARTESIAN_POINT ( 'NONE',  ( 17.81145623641422304, -0.5702806495523290442, 12.68276204030464349 ) ) ;
#7719=FACE_OUTER_BOUND ( 'NONE', #50103, .T. ) ;
#7726=CARTESIAN_POINT ( 'NONE',  ( 18.02726358174409782, 2.088564957010012435, -13.75219797956691714 ) ) ;
#7736=CARTESIAN_POINT ( 'NONE',  ( 17.55505043854147118, -3.125000000000000000, 12.28374638332999780 ) ) ;
#7739=CARTESIAN_POINT ( 'NONE',  ( 12.43937386265613476, -3.007228867393120897, 12.31882001147781658 ) ) ;
#7745=CARTESIAN_POINT ( 'NONE',  ( 18.02597764372135813, -3.073197451853428408, 13.65853278380549085 ) ) ;
#7752=DIRECTION ( 'NONE',  ( 0.000000000000000000, 0.000000000000000000, -1.000000000000000000 ) ) ;
#7767=CARTESIAN_POINT ( 'NONE',  ( 12.18524896721726769, 2.583003884521776872, 13.65547336762760189 ) ) ;
#7770=CARTESIAN_POINT ( 'NONE',  ( 12.61465226482422608, 0.5953800883773135988, -12.68120857324976036 ) ) ;
#7772=CARTESIAN_POINT ( 'NONE',  ( 12.34868974583248580, -0.4275223103465197738, 13.89116040406442565 ) ) ;
#7778=CARTESIAN_POINT ( 'NONE',  ( 4.650000881942629505, 3.375077994860000042E-14, 1.048050535245999973E-13 ) ) ;
#7784=CARTESIAN_POINT ( 'NONE',  ( 12.50326937753801992, 3.134539878383339584, 12.20388000700441999 ) ) ;
#7787=CARTESIAN_POINT ( 'NONE',  ( 12.35923484894147251, -0.5750310236205122827, 12.58704914195723390 ) ) ;
#7797=ADVANCED_FACE ( 'NONE', ( #33032 ), #43171, .F. ) ;
#7801=CARTESIAN_POINT ( 'NONE',  ( 12.37676482144652290, 2.955308392773305926, 13.56622858938220055 ) ) ;
#7807=CARTESIAN_POINT ( 'NONE',  ( 17.75579847504522135, 3.171737058802235776, -12.19426492080490831 ) ) ;
#7816=CARTESIAN_POINT ( 'NONE',  ( 12.57146999070152127, -0.6916885356984082689, -13.98290438115173551 ) ) ;
#7820=EDGE_CURVE ( 'NONE', #35032, #7987, #56204, .T. ) ;
#7822=AXIS2_PLACEMENT_3D ( 'NONE', #21243, #32093, #64222 ) ;
#7830=CARTESIAN_POINT ( 'NONE',  ( 17.96192083627959590, 2.025460433975771579, -13.76272661095429406 ) ) ;
#7849=CARTESIAN_POINT ( 'NONE',  ( 18.25351233825843522, -2.286726172143648483, -12.39076325940497725 ) ) ;
#7851=CARTESIAN_POINT ( 'NONE',  ( 5.500000000000000000, 13.94845324556000143, -4.312847325879000770 ) ) ;
#7860=CARTESIAN_POINT ( 'NONE',  ( 12.80505043854143388, 3.166036643249212634, -13.55322769257718996 ) ) ;
#7861=CARTESIAN_POINT ( 'NONE',  ( 12.09654996457810050, 2.673023974430118521, -13.74245554503370670 ) ) ;
#7864=CIRCLE ( 'NONE', #11194, 12.60000000000000142 ) ;
#7865=CARTESIAN_POINT ( 'NONE',  ( 18.13088524799816881, -0.4443071882833248831, 13.99296005428181644 ) ) ;
#7866=CARTESIAN_POINT ( 'NONE',  ( 18.16418420727211824, -2.358504521599060322, 12.48345420460293376 ) ) ;
#7871=CARTESIAN_POINT ( 'NONE',  ( 12.18033707850589131, -2.521449564331566418, 13.66889060756772167 ) ) ;
#7878=CARTESIAN_POINT ( 'NONE',  ( 12.80505043854143388, 3.174798964346249530, 12.21921514949791820 ) ) ;
#7880=CARTESIAN_POINT ( 'NONE',  ( 12.70736722666912044, 0.7301396911442955551, 13.98094760870049491 ) ) ;
#7884=CARTESIAN_POINT ( 'NONE',  ( 17.91965136929538005, 0.5080407711865452258, 12.68632595416892883 ) ) ;
#7885=CARTESIAN_POINT ( 'NONE',  ( 12.72336162097400880, -0.6199801057863054687, 12.67962184309742923 ) ) ;
#7886=CARTESIAN_POINT ( 'NONE',  ( 18.05156413928683534, -2.879751443183493187, -12.35493952382125116 ) ) ;
#7894=CARTESIAN_POINT ( 'NONE',  ( 4.599999999999999645, 0.000000000000000000, 0.000000000000000000 ) ) ;
#7897=CARTESIAN_POINT ( 'NONE',  ( 12.30935811146625980, -0.3808128809978846840, -12.69231869260113754 ) ) ;
#7901=CARTESIAN_POINT ( 'NONE',  ( 7.100000000000000533, 13.04986661130000059, -1.811520473896000016 ) ) ;
#7916=CARTESIAN_POINT ( 'NONE',  ( 18.10090605892218463, 0.4811670829680798622, -13.99174107639406373 ) ) ;
#7937=CARTESIAN_POINT ( 'NONE',  ( 12.24892445252029205, -0.2854033456632662502, -13.89606078824646929 ) ) ;
#7938=CARTESIAN_POINT ( 'NONE',  ( 18.12481736082888517, -2.757674955237352510, 12.38783183949682787 ) ) ;
#7942=CARTESIAN_POINT ( 'NONE',  ( 18.14117786275468092, 2.282023444416499292, 13.71724589037855502 ) ) ;
#7952=CARTESIAN_POINT ( 'NONE',  ( 17.55505043854143565, 1.760910691117812954, 12.47634535983622861 ) ) ;
#7961=EDGE_CURVE ( 'NONE', #7303, #26199, #34205, .T. ) ;
#7963=CARTESIAN_POINT ( 'NONE',  ( 18.21544979345814141, -0.2970375428997804046, 12.59650273238872487 ) ) ;
#7972=CARTESIAN_POINT ( 'NONE',  ( 18.02709866344912726, 1.963667282347026477, 13.86160417883469975 ) ) ;
#7983=CARTESIAN_POINT ( 'NONE',  ( 18.17146957700712662, -2.902473988487527468, -13.69582979195751271 ) ) ;
#7987=VERTEX_POINT ( 'NONE', #65868 ) ;
#8005=CARTESIAN_POINT ( 'NONE',  ( 12.18117696241645653, 2.542707536216995301, -12.44156325543625385 ) ) ;
#8014=CARTESIAN_POINT ( 'NONE',  ( 12.08892279761561106, -2.366838896507808876, -12.37571060269618961 ) ) ;
#8026=ORIENTED_EDGE ( 'NONE', *, *, #34589, .T. ) ;
#8029=CARTESIAN_POINT ( 'NONE',  ( 18.16596415324148950, 2.632031933676235891, 13.64451525667362652 ) ) ;
#8031=CARTESIAN_POINT ( 'NONE',  ( 17.65794081825375272, 1.883184384514173360, 12.57407373858317712 ) ) ;
#8036=ORIENTED_EDGE ( 'NONE', *, *, #42614, .F. ) ;
#8037=CARTESIAN_POINT ( 'NONE',  ( 12.21195445704744209, -2.302603597045700390, 12.49539791649142373 ) ) ;
#8042=CARTESIAN_POINT ( 'NONE',  ( 12.19409707445300306, 0.1321628250398321214, 12.69908003149455133 ) ) ;
#8046=CARTESIAN_POINT ( 'NONE',  ( 12.18014475499750837, 2.522932601087060966, 12.44621172798972708 ) ) ;
#8050=EDGE_CURVE ( 'NONE', #2983, #7548, #59163, .T. ) ;
#8075=CARTESIAN_POINT ( 'NONE',  ( 17.71608705225915514, -0.6042412280147623216, 13.88231902343041924 ) ) ;
#8086=CARTESIAN_POINT ( 'NONE',  ( 17.65273365045183596, 0.7301396911442742388, -13.98094760870049313 ) ) ;
#8088=CARTESIAN_POINT ( 'NONE',  ( 12.80505043854146940, -3.125000000000000000, 12.28374638332999780 ) ) ;
#8091=CARTESIAN_POINT ( 'NONE',  ( 17.86981019193749631, -1.959656554206103962, 13.77332550900839969 ) ) ;
#8092=CARTESIAN_POINT ( 'NONE',  ( 17.98398272105957219, 2.954699841475006306, -13.56644208774675597 ) ) ;
#8097=CARTESIAN_POINT ( 'NONE',  ( 12.80505043854143388, 3.199751711897557804, -12.18694338143115630 ) ) ;
#8102=CARTESIAN_POINT ( 'NONE',  ( 17.67321935251239751, 0.7100593550699959566, -12.57997761080729582 ) ) ;
#8112=PLANE ( 'NONE',  #7149 ) ;
#8114=CARTESIAN_POINT ( 'NONE',  ( 12.26189125119389978, 2.190632771808445067, 13.73417700668422725 ) ) ;
#8117=CARTESIAN_POINT ( 'NONE',  ( 12.21279950747578269, -0.1999332404816966391, -12.69788654131174610 ) ) ;
#8118=CARTESIAN_POINT ( 'NONE',  ( 12.36315992512968975, 0.5793931417437889753, 13.98801390351337481 ) ) ;
#8135=CARTESIAN_POINT ( 'NONE',  ( 12.80505043854144276, 0.7192913403693124152, -12.57945229203838267 ) ) ;
#8138=CARTESIAN_POINT ( 'NONE',  ( 12.72212784907325833, 1.874999999999999556, 12.57541659658320476 ) ) ;
#8146=CARTESIAN_POINT ( 'NONE',  ( 12.33523313525534526, 2.912685155779578317, 13.57718188376387225 ) ) ;
#8154=CARTESIAN_POINT ( 'NONE',  ( 17.56715138999748760, 1.760845446529456071, -12.47635456592353442 ) ) ;
#8158=CARTESIAN_POINT ( 'NONE',  ( 12.19234151428706880, 2.623341430473556724, -13.64652576295699404 ) ) ;
#8163=CARTESIAN_POINT ( 'NONE',  ( 12.44118158293134613, 0.5082612142235577446, -13.88749228919889767 ) ) ;
#8172=CARTESIAN_POINT ( 'NONE',  ( 17.65776394871754107, 1.883156081309886432, -13.78509897404220830 ) ) ;
#8188=ORIENTED_EDGE ( 'NONE', *, *, #28669, .F. ) ;
#8190=CARTESIAN_POINT ( 'NONE',  ( 18.02641336659269555, -3.027085105403487297, -12.23097768044556055 ) ) ;
#8202=CARTESIAN_POINT ( 'NONE',  ( 12.08142877465142107, 2.567860614650635753, -13.76250926564159016 ) ) ;
#8206=CARTESIAN_POINT ( 'NONE',  ( 18.26845486291481535, -0.1306247939804510705, 13.99939550958098522 ) ) ;
#8212=CARTESIAN_POINT ( 'NONE',  ( 12.41737123621465599, -2.003119782556758821, 13.76653501053765716 ) ) ;
#8214=ADVANCED_FACE ( 'NONE', ( #30803 ), #40266, .F. ) ;
#8226=CARTESIAN_POINT ( 'NONE',  ( 17.63732991102260073, 0.6196453797482972536, 12.67964297675817598 ) ) ;
#8235=EDGE_CURVE ( 'NONE', #58563, #44202, #11644, .T. ) ;
#8239=CARTESIAN_POINT ( 'NONE',  ( 12.74530398939899634, 0.7169431667913611639, -12.57958639523259059 ) ) ;
#8243=CARTESIAN_POINT ( 'NONE',  ( 4.700001368028300597, 0.000000000000000000, 0.000000000000000000 ) ) ;
#8253=ORIENTED_EDGE ( 'NONE', *, *, #27478, .F. ) ;
#8256=CARTESIAN_POINT ( 'NONE',  ( 18.24552752486710716, 0.2229649748661320929, -13.99822903660538564 ) ) ;
#8269=CARTESIAN_POINT ( 'NONE',  ( 12.15512143695920599, -2.141660958086382127, 13.83591020989070053 ) ) ;
#8281=CARTESIAN_POINT ( 'NONE',  ( 12.49177480397739615, -0.5412024733746028105, -13.88582008197801976 ) ) ;
#8282=CARTESIAN_POINT ( 'NONE',  ( 18.17519250343470461, -2.421563205337722291, 12.46952409297816544 ) ) ;
#8299=DIRECTION ( 'NONE',  ( -1.000000000000000000, 0.000000000000000000, 0.000000000000000000 ) ) ;
#8312=CARTESIAN_POINT ( 'NONE',  ( 18.26224557552276551, 2.355566563843568773, 13.80042983216602259 ) ) ;
#8319=VECTOR ( 'NONE', #166, 1000.000000000000000 ) ;
#8340=EDGE_LOOP ( 'NONE', ( #21266, #32630, #60473, #25648, #49451 ) ) ;
#8347=CARTESIAN_POINT ( 'NONE',  ( 12.30671156051920612, 2.122656121997152479, -12.53154589464477553 ) ) ;
#8357=CARTESIAN_POINT ( 'NONE',  ( 12.37879419969807415, -1.897860824706870453, -12.45625557883630208 ) ) ;
#8364=CARTESIAN_POINT ( 'NONE',  ( 12.47278092208625999, -3.029458323191939861, -13.54674174801984066 ) ) ;
#8369=EDGE_CURVE ( 'NONE', #33960, #7236, #24446, .T. ) ;
#8375=CARTESIAN_POINT ( 'NONE',  ( 18.18005044575082252, 2.500000006795693785, 13.67340643792831045 ) ) ;
#8378=CARTESIAN_POINT ( 'NONE',  ( 17.67527538783543406, 3.190136231796164346, 12.18946489087518970 ) ) ;
#8384=CARTESIAN_POINT ( 'NONE',  ( 12.24230779986662476, -2.227307356672650229, 12.51097363402015361 ) ) ;
#8389=CARTESIAN_POINT ( 'NONE',  ( 12.47502136616923529, 0.5311517451680617397, 12.68505220952105184 ) ) ;
#8392=CARTESIAN_POINT ( 'NONE',  ( 12.43764207941351607, 1.993980486415519726, 12.55516735266245298 ) ) ;
#8404=CARTESIAN_POINT ( 'NONE',  ( 17.93438960660997950, -0.4968201169902036751, -12.68691926186208541 ) ) ;
#8410=CARTESIAN_POINT ( 'NONE',  ( 17.77733961940316121, -1.915504334253006036, -13.78014422891541813 ) ) ;
#8417=CARTESIAN_POINT ( 'NONE',  ( 18.08703349541059424, 2.171337118988397208, -13.73770667396175149 ) ) ;
#8423=CARTESIAN_POINT ( 'NONE',  ( 4.599999999999999645, -0.7192913403693119712, -12.57945229203838267 ) ) ;
#8429=CARTESIAN_POINT ( 'NONE',  ( 12.80505043854143388, 1.836948468694464820, -12.54242247073720051 ) ) ;
#8431=CARTESIAN_POINT ( 'NONE',  ( 12.30936054504846311, -2.880824963478894052, 12.35466577905677354 ) ) ;
#8433=ORIENTED_EDGE ( 'NONE', *, *, #23039, .T. ) ;
#8434=CARTESIAN_POINT ( 'NONE',  ( 17.87830683576864033, -3.171613455744689336, 13.63601469363850072 ) ) ;
#8440=CARTESIAN_POINT ( 'NONE',  ( 4.599999999999999645, -1.787816316115923509, 13.88537766212462898 ) ) ;
#8445=EDGE_CURVE ( 'NONE', #16254, #7548, #9041, .T. ) ;
#8446=CARTESIAN_POINT ( 'NONE',  ( 18.18333067157144001, -0.3597103837128303727, -12.59488153751295769 ) ) ;
#8456=DIRECTION ( 'NONE',  ( 1.000000000000000000, 0.000000000000000000, 0.000000000000000000 ) ) ;
#8459=CARTESIAN_POINT ( 'NONE',  ( 12.12605828839490663, 2.774939115234940967, 13.72225238672862346 ) ) ;
#8462=CARTESIAN_POINT ( 'NONE',  ( 12.26246716472426712, -0.3103928899670306274, -12.69489813901335573 ) ) ;
#8463=CARTESIAN_POINT ( 'NONE',  ( 12.13047358906991846, 0.2678304234473986578, 13.99744223245316199 ) ) ;
#8475=CARTESIAN_POINT ( 'NONE',  ( 12.58710648703385360, 3.166459836794169647, 12.19563591444343231 ) ) ;
#8478=CARTESIAN_POINT ( 'NONE',  ( 18.18005043854143565, 2.500000000000000000, -25.00000000000000000 ) ) ;
#8481=DIRECTION ( 'NONE',  ( -0.000000000000000000, -0.000000000000000000, 1.000000000000000000 ) ) ;
#8482=CARTESIAN_POINT ( 'NONE',  ( 12.18001542466622844, 2.493364570375297795, 12.45310825070289340 ) ) ;
#8490=ADVANCED_FACE ( 'NONE', ( #67757 ), #43028, .T. ) ;
#8496=CARTESIAN_POINT ( 'NONE',  ( 17.91108626730879649, 1.853415294216377962, -12.46294044425349945 ) ) ;
#8504=CARTESIAN_POINT ( 'NONE',  ( 17.74431590774614165, 1.811500042942241873, -13.88231098336932590 ) ) ;
#8512=AXIS2_PLACEMENT_3D ( 'NONE', #46241, #67204, #18297 ) ;
#8514=CARTESIAN_POINT ( 'NONE',  ( 17.97976423439214955, 3.110159202364623621, -13.65016833014880859 ) ) ;
#8522=CARTESIAN_POINT ( 'NONE',  ( 4.600000207916445483, 13.27499874714999883, 0.000000000000000000 ) ) ;
#8528=CARTESIAN_POINT ( 'NONE',  ( 18.14066966380071833, -2.280775195390137178, 13.71753029190269046 ) ) ;
#8534=CARTESIAN_POINT ( 'NONE',  ( 17.86252378965070164, -3.131846597291660927, -12.20457061699601375 ) ) ;
#8544=CARTESIAN_POINT ( 'NONE',  ( 12.12630585043895159, 2.775512167237635275, -13.72213635400578191 ) ) ;
#8548=CARTESIAN_POINT ( 'NONE',  ( 17.67321579093595219, 0.7208442004938064862, 13.98143072948223775 ) ) ;
#8549=VECTOR ( 'NONE', #31731, 999.9999999999998863 ) ;
#8551=ORIENTED_EDGE ( 'NONE', *, *, #69048, .T. ) ;
#8555=CARTESIAN_POINT ( 'NONE',  ( 12.21945847189276435, -2.718477924323257966, 13.62469170132030705 ) ) ;
#8568=DIRECTION ( 'NONE',  ( 0.000000000000000000, -0.6195591179857913300, 0.7849499979748191247 ) ) ;
#8574=DIRECTION ( 'NONE',  ( 0.000000000000000000, -1.000000000000000000, 0.000000000000000000 ) ) ;
#8578=CARTESIAN_POINT ( 'NONE',  ( 12.41659929819182473, -0.4896501542853357036, -12.68729270499358108 ) ) ;
#8579=SHAPE_REPRESENTATION ( 'Airflow Sleeve', ( #9676 ), #58898 ) ;
#8580=CARTESIAN_POINT ( 'NONE',  ( 5.700000000000000178, 13.04986661130000059, 1.811520473896000016 ) ) ;
#8587=CARTESIAN_POINT ( 'NONE',  ( 17.63677106488414026, 0.6210356003491741550, 12.67955509032280048 ) ) ;
#8597=CARTESIAN_POINT ( 'NONE',  ( 18.21571869486623996, -0.3016537271415190569, -13.99676704218776813 ) ) ;
#8604=CARTESIAN_POINT ( 'NONE',  ( 17.92118024654466168, -3.006907963399408690, 12.31891425463948941 ) ) ;
#8605=ORIENTED_EDGE ( 'NONE', *, *, #56125, .F. ) ;
#8612=VECTOR ( 'NONE', #58961, 1000.000000000000000 ) ;
#8615=CARTESIAN_POINT ( 'NONE',  ( 17.69809243813181254, 0.6087680664020044263, -13.88205110007294607 ) ) ;
#8620=CARTESIAN_POINT ( 'NONE',  ( 12.29653044000528617, -0.3639325664385079095, -13.89360161040561970 ) ) ;
#8621=CARTESIAN_POINT ( 'NONE',  ( 18.17458387927301899, -2.583096938294931366, 12.43185036011799305 ) ) ;
#8644=CARTESIAN_POINT ( 'NONE',  ( 18.10028187597347582, -0.4746736627229541927, 12.59106879393900513 ) ) ;
#8652=CARTESIAN_POINT ( 'NONE',  ( 17.55505043854143565, 3.125000000000000000, 13.52078605991414939 ) ) ;
#8686=CARTESIAN_POINT ( 'NONE',  ( 12.42174667009958533, 2.006228232438482362, -12.55302761990816407 ) ) ;
#8699=CARTESIAN_POINT ( 'NONE',  ( 12.48081329218153002, -1.836727633573115970, -12.46541050266128181 ) ) ;
#8706=CARTESIAN_POINT ( 'NONE',  ( 12.43989325004536362, -3.148871498663014634, -13.64128470488402201 ) ) ;
#8714=CARTESIAN_POINT ( 'NONE',  ( 18.01235687062835567, 2.926439070439386558, 13.57366610795702755 ) ) ;
#8718=CARTESIAN_POINT ( 'NONE',  ( 18.02661896923962104, 2.910306870311579530, 12.34644497411517428 ) ) ;
#8723=CARTESIAN_POINT ( 'NONE',  ( 12.36741688735896361, -2.053674487412247451, 12.54445365011033608 ) ) ;
#8730=CARTESIAN_POINT ( 'NONE',  ( 12.33502333850778143, 0.4124490627810437071, 12.69099791225215235 ) ) ;
#8733=CARTESIAN_POINT ( 'NONE',  ( 12.38986377076836476, 2.032719501308456245, 12.54823268863295382 ) ) ;
#8744=CARTESIAN_POINT ( 'NONE',  ( 17.77478288653529503, -0.5854877331960374187, -12.68183053514018077 ) ) ;
#8747=CARTESIAN_POINT ( 'NONE',  ( 17.63932472559630327, -3.120604413325592130, 13.52206336586401569 ) ) ;
#8756=ORIENTED_EDGE ( 'NONE', *, *, #11001, .F. ) ;
#8777=CARTESIAN_POINT ( 'NONE',  ( 17.60330540716448411, -3.246896514464381767, 13.61828436941213205 ) ) ;
#8787=CARTESIAN_POINT ( 'NONE',  ( 18.20001934199752824, 0.3287229608534117942, -12.59571550161850340 ) ) ;
#8800=CARTESIAN_POINT ( 'NONE',  ( 12.15975302296892124, 2.850959433913112129, 13.70664605376239287 ) ) ;
#8804=CARTESIAN_POINT ( 'NONE',  ( 12.27274573043892580, 0.3283020094446014170, -12.69430739907382488 ) ) ;
#8814=CARTESIAN_POINT ( 'NONE',  ( 12.51412939328308305, 3.139365204187051006, 12.20263940233110489 ) ) ;
#8824=ORIENTED_EDGE ( 'NONE', *, *, #60613, .T. ) ;
#8835=EDGE_CURVE ( 'NONE', #12254, #47064, #47439, .T. ) ;
#8840=CARTESIAN_POINT ( 'NONE',  ( 18.27533594408734530, 2.564445959844773526, -12.33627802783496286 ) ) ;
#8848=CARTESIAN_POINT ( 'NONE',  ( -17.56123417799999942, -11.06886219213000011, -1.536526853569999851 ) ) ;
#8849=CARTESIAN_POINT ( 'NONE',  ( 12.68688508614694044, 0.7208442004938129255, -13.98143072948223775 ) ) ;
#8852=CARTESIAN_POINT ( 'NONE',  ( 18.17882542848376559, 2.459571230201114567, 12.46089164816697270 ) ) ;
#8858=CARTESIAN_POINT ( 'NONE',  ( 18.25624423923968109, 2.332236704353569223, -13.80437652844153718 ) ) ;
#8879=CARTESIAN_POINT ( 'NONE',  ( 17.81550493765278986, -1.931762299006051897, -12.56594712229140143 ) ) ;
#8885=ORIENTED_EDGE ( 'NONE', *, *, #46673, .F. ) ;
#8886=CARTESIAN_POINT ( 'NONE',  ( 4.600000207916445483, 2.033928581112999763E-13, -2.806643806251999915E-13 ) ) ;
#8889=CARTESIAN_POINT ( 'NONE',  ( 12.10494519979306460, 2.707806787687952799, -13.73564420130114172 ) ) ;
#8890=CARTESIAN_POINT ( 'NONE',  ( 18.27044831935228686, 0.1190513140356058014, 13.99949878896183719 ) ) ;
#8896=DIRECTION ( 'NONE',  ( -1.000000000000000000, 0.000000000000000000, 0.000000000000000000 ) ) ;
#8897=CARTESIAN_POINT ( 'NONE',  ( 12.22548351784305432, -2.734003476492731899, 13.62103941681218267 ) ) ;
#8902=CARTESIAN_POINT ( 'NONE',  ( 21.35000154058000277, 0.000000000000000000, 0.000000000000000000 ) ) ;
#8911=DIRECTION ( 'NONE',  ( 1.000000000000000000, 0.000000000000000000, 1.094362695702000107E-14 ) ) ;
#8922=CARTESIAN_POINT ( 'NONE',  ( 12.58275800453940185, 0.6847469513499626625, -12.58138041838080490 ) ) ;
#8923=CARTESIAN_POINT ( 'NONE',  ( 12.30934879319026720, -2.881204795959748211, -12.35454860660538579 ) ) ;
#8940=CARTESIAN_POINT ( 'NONE',  ( 18.26845486291482601, 0.1306247939804529856, -13.99939550958098344 ) ) ;
#8946=CARTESIAN_POINT ( 'NONE',  ( 17.59622528268192099, -3.125000000000000444, 12.28374666422326378 ) ) ;
#8959=CARTESIAN_POINT ( 'NONE',  ( 12.21991984215965310, 0.2205930660282648670, -13.89766156610767034 ) ) ;
#8960=CARTESIAN_POINT ( 'NONE',  ( 18.17829451895835291, -2.452078260301032930, 12.46263202712693996 ) ) ;
#8983=CARTESIAN_POINT ( 'NONE',  ( 17.57898592363197210, 0.7189971323193946606, 12.57946912511938109 ) ) ;
#9020=CARTESIAN_POINT ( 'NONE',  ( 17.55505043854147118, -1.787816316115923954, 13.88537766212463254 ) ) ;
#9023=CARTESIAN_POINT ( 'NONE',  ( 12.23541831425119675, 2.757387829712824701, -12.38789221355391312 ) ) ;
#9031=CARTESIAN_POINT ( 'NONE',  ( 12.46441593768246570, -3.024116347931780524, -12.31386760464157781 ) ) ;
#9037=CARTESIAN_POINT ( 'NONE',  ( 12.33410680267665960, -3.073228032305979962, -13.65852590327789962 ) ) ;
#9040=VECTOR ( 'NONE', #14418, 1000.000000000000000 ) ;
#9041=LINE ( 'NONE', #56602, #983 ) ;
#9044=CARTESIAN_POINT ( 'NONE',  ( 12.75652363867719252, 0.7301778992647915967, -13.98094561311457440 ) ) ;
#9047=CARTESIAN_POINT ( 'NONE',  ( 18.16759718491386977, 2.624144391529842579, 13.64629239149777185 ) ) ;
#9051=CARTESIAN_POINT ( 'NONE',  ( 18.13653212795700753, 2.729361600744797389, 12.39516738912175597 ) ) ;
#9059=CARTESIAN_POINT ( 'NONE',  ( 12.47244801656840174, -3.029249266520640305, 12.31238128988859515 ) ) ;
#9065=CARTESIAN_POINT ( 'NONE',  ( 12.24445512745668019, 0.2765170649790821833, 12.69595318831094133 ) ) ;
#9070=ORIENTED_EDGE ( 'NONE', *, *, #54469, .T. ) ;
#9074=ADVANCED_FACE ( 'NONE', ( #59230 ), #15085, .T. ) ;
#9079=ORIENTED_EDGE ( 'NONE', *, *, #7961, .T. ) ;
#9087=CARTESIAN_POINT ( 'NONE',  ( 12.30746066369764691, -3.049480053538148105, 13.66385627579028039 ) ) ;
#9096=CARTESIAN_POINT ( 'NONE',  ( 5.699999545467999695, 0.000000000000000000, 0.000000000000000000 ) ) ;
#9109=VERTEX_POINT ( 'NONE', #34420 ) ;
#9110=CARTESIAN_POINT ( 'NONE',  ( 18.21576355877877162, -2.818661318639680058, 13.71332454644887200 ) ) ;
#9123=CARTESIAN_POINT ( 'NONE',  ( 18.20808481425077474, -0.3124912280145399346, -12.59612551846059780 ) ) ;
#9130=DIRECTION ( 'NONE',  ( 1.000000000000000000, 0.000000000000000000, 0.000000000000000000 ) ) ;
#9133=EDGE_CURVE ( 'NONE', #18819, #12380, #38609, .T. ) ;
#9134=CARTESIAN_POINT ( 'NONE',  ( 12.20666462242724215, 2.105579624229084068, 13.84076000201157974 ) ) ;
#9138=CARTESIAN_POINT ( 'NONE',  ( 12.29580549756552088, 0.3624889076790000497, -12.69304043452270214 ) ) ;
#9139=CARTESIAN_POINT ( 'NONE',  ( 12.22983020848964486, -0.4451122480341178633, 13.99293440828418866 ) ) ;
#9157=CARTESIAN_POINT ( 'NONE',  ( 12.48752230519103357, 1.955425561929305056, 12.56195022952150353 ) ) ;
#9174=CARTESIAN_POINT ( 'NONE',  ( 18.27898910297786372, 2.436826214745338337, -12.36212035235843487 ) ) ;
#9177=CARTESIAN_POINT ( 'NONE',  ( 12.27869449350294850, 2.837185661393637481, -13.59614283363436549 ) ) ;
#9181=CARTESIAN_POINT ( 'NONE',  ( 12.48412837678613485, 0.6552116771452474175, -13.98466387211990281 ) ) ;
#9189=CARTESIAN_POINT ( 'NONE',  ( 17.90989566141528755, 3.154773125069392670, -13.63992084652273817 ) ) ;
#9206=CARTESIAN_POINT ( 'NONE',  ( 17.83404768640024685, -1.940633243441993505, -12.56443520114847345 ) ) ;
#9208=ADVANCED_FACE ( 'NONE', ( #15823 ), #10922, .F. ) ;
#9219=CARTESIAN_POINT ( 'NONE',  ( 18.26841422636658052, 0.1308528744652167064, 13.99939340647621044 ) ) ;
#9221=CARTESIAN_POINT ( 'NONE',  ( 17.55505043854147118, -1.875000000000000000, 12.57545641911172396 ) ) ;
#9222=ORIENTED_EDGE ( 'NONE', *, *, #65897, .F. ) ;
#9225=CARTESIAN_POINT ( 'NONE',  ( 5.599999772733800008, -6.661338147750999827E-14, -1.931788062847999572E-14 ) ) ;
#9240=CARTESIAN_POINT ( 'NONE',  ( 7.100000000000000533, -13.94845324556000143, -4.312847325879000770 ) ) ;
#9250=CARTESIAN_POINT ( 'NONE',  ( 12.42472005158248294, -0.4959841406075989889, -12.68696163625449813 ) ) ;
#9251=CARTESIAN_POINT ( 'NONE',  ( 12.20227052514783672, -2.665223630829422596, -12.41153314577902833 ) ) ;
#9259=CARTESIAN_POINT ( 'NONE',  ( 17.75512362461813964, 0.5924617913754783860, 12.68139389762679770 ) ) ;
#9274=CARTESIAN_POINT ( 'NONE',  ( 17.55505043854147118, -3.125000000000000000, 12.28374638332999780 ) ) ;
#9279=CARTESIAN_POINT ( 'NONE',  ( 12.30281274453381535, -2.118998859563833381, -13.74704000636702084 ) ) ;
#9289=DIRECTION ( 'NONE',  ( 1.000000000000000000, 0.000000000000000000, 0.000000000000000000 ) ) ;
#9292=CARTESIAN_POINT ( 'NONE',  ( 12.39133745138800613, 2.968584063660573147, 13.56278128057737042 ) ) ;
#9294=CARTESIAN_POINT ( 'NONE',  ( 17.75825915738909444, -1.908867900852240673, 12.56984843829418885 ) ) ;
#9295=EDGE_CURVE ( 'NONE', #48911, #19729, #69100, .T. ) ;
#9318=CARTESIAN_POINT ( 'NONE',  ( 18.22962529608892623, 0.2638285456865405720, 12.59724228039519645 ) ) ;
#9325=FACE_BOUND ( 'NONE', #33574, .T. ) ;
#9333=CARTESIAN_POINT ( 'NONE',  ( 18.20209611035324926, -2.854851737566545644, 12.27307487512611317 ) ) ;
#9335=ADVANCED_FACE ( 'NONE', ( #7401 ), #7587, .T. ) ;
#9344=VERTEX_POINT ( 'NONE', #60203 ) ;
#9348=CARTESIAN_POINT ( 'NONE',  ( 12.80505043854146940, -1.845932447629014872, -13.81930785430178155 ) ) ;
#9355=CARTESIAN_POINT ( 'NONE',  ( 12.27338658866627341, 2.829189413748181003, -12.36878769217040741 ) ) ;
#9361=LINE ( 'NONE', #42239, #40220 ) ;
#9363=CARTESIAN_POINT ( 'NONE',  ( 12.33364337825308965, -2.910866508044257728, -12.34629936699908015 ) ) ;
#9369=CARTESIAN_POINT ( 'NONE',  ( 12.70233692021773564, -1.883156082608298032, -13.78505115204619713 ) ) ;
#9374=CARTESIAN_POINT ( 'NONE',  ( 17.72109462663384605, -3.180738073285652945, 12.19192004217518743 ) ) ;
#9378=CARTESIAN_POINT ( 'NONE',  ( 12.61731565722499759, 0.7069209314914761677, -13.98214394338181954 ) ) ;
#9385=CARTESIAN_POINT ( 'NONE',  ( 18.12879050829617711, 2.748092781515380612, 12.39029782533441093 ) ) ;
#9390=CARTESIAN_POINT ( 'NONE',  ( 12.43857111758547163, -3.006687177877844785, 12.31897860641675635 ) ) ;
#9400=CARTESIAN_POINT ( 'NONE',  ( 12.26373771493048181, 0.3125877143166541638, 12.69482668528968183 ) ) ;
#9401=VECTOR ( 'NONE', #7647, 1000.000000000000000 ) ;
#9402=CARTESIAN_POINT ( 'NONE',  ( 5.664191326654759884, -12.07183080424680988, -3.732901064427135207 ) ) ;
#9418=CARTESIAN_POINT ( 'NONE',  ( 18.14647333850305699, -2.702177529538977829, 13.62849908381775066 ) ) ;
#9421=CARTESIAN_POINT ( 'NONE',  ( 18.17537806675986545, -2.421014888063410808, -13.68986186821174122 ) ) ;
#9430=VECTOR ( 'NONE', #10990, 1000.000000000000000 ) ;
#9431=CARTESIAN_POINT ( 'NONE',  ( 18.11727536438081643, -0.2737665426917151312, 13.89638618295341743 ) ) ;
#9446=CARTESIAN_POINT ( 'NONE',  ( 17.83317199299634126, 3.060086213980319769, -13.53858764060185216 ) ) ;
#9458=CARTESIAN_POINT ( 'NONE',  ( 18.26152580467100250, -0.1632583333441851581, -12.59896334813831409 ) ) ;
#9459=CARTESIAN_POINT ( 'NONE',  ( 12.27407495021074801, 2.829836729549234153, -12.36860105340628557 ) ) ;
#9470=CARTESIAN_POINT ( 'NONE',  ( 17.91028475965235600, 1.853043856158717251, 12.46299565389693065 ) ) ;
#9471=CARTESIAN_POINT ( 'NONE',  ( 12.25717089523534753, 2.039201503940123228, 13.85070424198621097 ) ) ;
#9476=ORIENTED_EDGE ( 'NONE', *, *, #7337, .F. ) ;
#9488=CARTESIAN_POINT ( 'NONE',  ( 12.08128888832027137, 2.529854562579153754, 12.34343511423995388 ) ) ;
#9506=CARTESIAN_POINT ( 'NONE',  ( 12.60268547648134074, -3.091422767983464492, 13.53007486046831964 ) ) ;
#9514=CARTESIAN_POINT ( 'NONE',  ( 18.28010889142759865, 2.506697083851606056, -12.34815906022513410 ) ) ;
#9516=CARTESIAN_POINT ( 'NONE',  ( 17.76019544538929296, 3.091716410417681526, 12.29381940408887530 ) ) ;
#9519=CARTESIAN_POINT ( 'NONE',  ( 12.21427240567356876, 2.704226675929312762, -13.62802533659631798 ) ) ;
#9527=CARTESIAN_POINT ( 'NONE',  ( 18.05693606621465719, 2.118559450777698583, 12.53247283884194019 ) ) ;
#9530=VERTEX_POINT ( 'NONE', #32517 ) ;
#9532=CARTESIAN_POINT ( 'NONE',  ( 18.20564091649229610, 2.840274733304992694, -13.70886432971491509 ) ) ;
#9533=ORIENTED_EDGE ( 'NONE', *, *, #26406, .T. ) ;
#9546=EDGE_LOOP ( 'NONE', ( #25218, #26804, #17563, #18813 ) ) ;
#9553=CARTESIAN_POINT ( 'NONE',  ( 18.04714676118040018, -2.114551447792224703, -12.53305202231724635 ) ) ;
#9565=CARTESIAN_POINT ( 'NONE',  ( 17.93787990420808853, 0.6205713442106982614, 13.98624562867391496 ) ) ;
#9568=ORIENTED_EDGE ( 'NONE', *, *, #67246, .T. ) ;
#9585=CARTESIAN_POINT ( 'NONE',  ( 18.17508965101259832, -2.579233224755918208, -12.43275545427360385 ) ) ;
#9586=CARTESIAN_POINT ( 'NONE',  ( 18.17514718081074676, 2.578773340588377483, -12.43289648652257995 ) ) ;
#9598=CARTESIAN_POINT ( 'NONE',  ( 12.25868397512095243, -0.3036663359794735673, -12.69511825016613749 ) ) ;
#9599=CARTESIAN_POINT ( 'NONE',  ( 12.18024789519250284, -2.481080537702162303, -12.45595244967812576 ) ) ;
#9607=CARTESIAN_POINT ( 'NONE',  ( 17.95718847840442578, 0.4784641824370373109, 12.68786700119948208 ) ) ;
#9622=CARTESIAN_POINT ( 'NONE',  ( 18.07108758008967442, -2.852736468728856778, 12.36237742789788641 ) ) ;
#9625=CARTESIAN_POINT ( 'NONE',  ( 12.19454236345195852, -2.633904201044235727, -13.64409272160013487 ) ) ;
#9639=CARTESIAN_POINT ( 'NONE',  ( 12.78422293702843326, 3.124999446934218383, 13.52078617650838055 ) ) ;
#9643=EDGE_LOOP ( 'NONE', ( #60801, #5206, #17017, #32786 ) ) ;
#9647=CARTESIAN_POINT ( 'NONE',  ( 12.23409240334733461, 2.245563803222850208, -13.72414218390522578 ) ) ;
#9658=CARTESIAN_POINT ( 'NONE',  ( 17.55505043854144276, 0.6250000000000001110, -12.67928921589118474 ) ) ;
#9664=CARTESIAN_POINT ( 'NONE',  ( 17.55505043854144276, -0.6250000000000001110, 12.67928921589117586 ) ) ;
#9676=AXIS2_PLACEMENT_3D ( 'NONE', #40345, #19020, #18341 ) ;
#9682=LINE ( 'NONE', #47799, #15249 ) ;
#9715=CARTESIAN_POINT ( 'NONE',  ( 12.27327344217068905, -2.829024202110182351, -12.36880877243790344 ) ) ;
#9719=CARTESIAN_POINT ( 'NONE',  ( 12.39818000720382152, -2.025460462753591706, -13.76267819017275329 ) ) ;
#9724=ORIENTED_EDGE ( 'NONE', *, *, #22195, .T. ) ;
#9732=CARTESIAN_POINT ( 'NONE',  ( 18.16381471383434487, 2.642962562933662163, 12.41712880859051893 ) ) ;
#9740=CARTESIAN_POINT ( 'NONE',  ( 12.55417570215098166, -3.072462724870960393, 12.29958987976102058 ) ) ;
#9748=CARTESIAN_POINT ( 'NONE',  ( 12.30864223534304003, -0.3802890292809111283, 12.69234946364259287 ) ) ;
#9757=CARTESIAN_POINT ( 'NONE',  ( 17.55505043854143921, -0.7302158263239086899, 13.98094363220831049 ) ) ;
#9769=CARTESIAN_POINT ( 'NONE',  ( 18.06966903239552735, -2.854820418091305712, -13.59172178685414245 ) ) ;
#9780=CARTESIAN_POINT ( 'NONE',  ( 17.96719322784330330, -0.4698824116306926091, 13.88931020049250087 ) ) ;
#9792=CARTESIAN_POINT ( 'NONE',  ( 12.08521996405947974, 2.390121770085890329, -12.37125191860131324 ) ) ;
#9797=CARTESIAN_POINT ( 'NONE',  ( 18.16658511877958659, -2.125673232124642986, 13.83768827471936547 ) ) ;
#9798=CARTESIAN_POINT ( 'NONE',  ( 18.13153191398660624, 2.741475808336658382, -13.61927240697805175 ) ) ;
#9810=CARTESIAN_POINT ( 'NONE',  ( 18.22055608408779648, -0.2856017019952077352, -12.59676745213710447 ) ) ;
#9820=CARTESIAN_POINT ( 'NONE',  ( 17.88934697238257243, 1.841816770035708872, 12.46465977041040141 ) ) ;
#9821=CARTESIAN_POINT ( 'NONE',  ( 12.45019282332726185, 3.154806840457482053, 13.63991304855491649 ) ) ;
#9824=CARTESIAN_POINT ( 'NONE',  ( 12.41737000014478376, -0.4903651762333725017, -12.68725775796614741 ) ) ;
#9825=CARTESIAN_POINT ( 'NONE',  ( 12.25981791760051465, -0.4818816852691660824, 13.99171642476389721 ) ) ;
#9839=CARTESIAN_POINT ( 'NONE',  ( 12.40831127361655462, 1.878029834076329951, 12.45925554172551486 ) ) ;
#9846=CARTESIAN_POINT ( 'NONE',  ( 18.05195279573837297, -0.3792326064291314247, 12.69238213821911643 ) ) ;
#9850=CARTESIAN_POINT ( 'NONE',  ( 12.24304070173655390, -0.2736148577199287724, 12.69603606445621402 ) ) ;
#9856=CARTESIAN_POINT ( 'NONE',  ( 12.21305109721492066, -2.701423549395647328, 13.62869161905334181 ) ) ;
#9857=CARTESIAN_POINT ( 'NONE',  ( 12.25785601946420478, 2.186712656649328235, 13.73518136001305479 ) ) ;
#9867=CARTESIAN_POINT ( 'NONE',  ( 17.77721830936820879, 3.084271799839128914, -12.29605728393571873 ) ) ;
#9869=CARTESIAN_POINT ( 'NONE',  ( 7.100000000000000533, 0.000000000000000000, 0.000000000000000000 ) ) ;
#9870=CARTESIAN_POINT ( 'NONE',  ( 17.55505043854143565, 3.248147246781390329, 13.61798588129781074 ) ) ;
#9874=CARTESIAN_POINT ( 'NONE',  ( 12.17712534909926170, 0.3652063536484317918, -13.99523956222174448 ) ) ;
#9875=CARTESIAN_POINT ( 'NONE',  ( 17.55505043854143565, 3.199698446519375850, 12.18695736643652694 ) ) ;
#9885=CARTESIAN_POINT ( 'NONE',  ( 18.13175260058826055, 2.961013189755318908, -13.68330200419957166 ) ) ;
#9893=CARTESIAN_POINT ( 'NONE',  ( 12.18105065344216165, 0.04081304491956393166, -13.89993877190634564 ) ) ;
#9905=CARTESIAN_POINT ( 'NONE',  ( 17.85706045311523127, -3.134356930968903665, -12.20392612899626528 ) ) ;
#9919=EDGE_CURVE ( 'NONE', #54460, #35032, #23204, .T. ) ;
#9935=LINE ( 'NONE', #63055, #21316 ) ;
#9938=CARTESIAN_POINT ( 'NONE',  ( 18.15933590956319321, 2.660621712302206454, -12.41273490623410858 ) ) ;
#9947=CARTESIAN_POINT ( 'NONE',  ( 21.60000000000000142, 0.000000000000000000, 0.000000000000000000 ) ) ;
#9948=CARTESIAN_POINT ( 'NONE',  ( 5.500000000000000000, 12.87590651766999983, -2.791353855799999728 ) ) ;
#9951=CARTESIAN_POINT ( 'NONE',  ( 12.37753504985973940, 0.4560270868711863157, -12.68898073362801071 ) ) ;
#9952=CARTESIAN_POINT ( 'NONE',  ( 12.27854653042187039, -2.836954440265831767, -12.36664979425283839 ) ) ;
#9974=CARTESIAN_POINT ( 'NONE',  ( 12.80505043854146940, -3.125000000000000000, 13.52084414783465860 ) ) ;
#9988=CARTESIAN_POINT ( 'NONE',  ( 12.66131753640901714, 3.108595072584060315, 13.52531149670803501 ) ) ;
#9995=FACE_OUTER_BOUND ( 'NONE', #65288, .T. ) ;
#10003=CARTESIAN_POINT ( 'NONE',  ( 12.72336452611786051, 0.6199804606742643776, 13.88138355690256276 ) ) ;
#10010=CARTESIAN_POINT ( 'NONE',  ( 12.43804048110095017, 3.154843637346236740, -13.63995574168323266 ) ) ;
#10014=CARTESIAN_POINT ( 'NONE',  ( 18.28003407448206730, -0.02395120399003650841, 12.59999907117300033 ) ) ;
#10030=CARTESIAN_POINT ( 'NONE',  ( 12.75734966356159994, -0.7181168112306600682, -12.57951960855069551 ) ) ;
#10049=CARTESIAN_POINT ( 'NONE',  ( 17.75641289383300148, 0.5920240553917505144, -13.88302649426327307 ) ) ;
#10060=DIRECTION ( 'NONE',  ( 1.000000000000000000, 0.000000000000000000, 0.000000000000000000 ) ) ;
#10061=CARTESIAN_POINT ( 'NONE',  ( 18.00096484318083867, -0.5748214922774377289, 12.58705572532630157 ) ) ;
#10064=B_SPLINE_SURFACE_WITH_KNOTS ( 'NONE', 1, 3, ( 
 ( #6374, #54274, #22114, #16182, #1147, #32960, #64404, #10940, #11973, #42418, #37168, #48004, #38545, #16870, #54628, #53592, #43459, #63725, #32285, #43102, #5350, #27030, #11620, #22456, #64752, #28065, #15837, #21766, #38193, #59524, #27724, #58488, #49038, #59179, #43801, #65096, #37508, #37854, #449, #16528, #17220, #10592, #31934, #49374, #6724, #5688, #48343, #58832, #21092, #53244, #26689, #103, #11278, #32618, #53929, #21420, #6032, #42757, #27370, #48696, #797, #24193, #7772, #45530, #54976, #56011, #49728, #60566, #45184, #44504, #60910, #29464, #29808, #28767, #66840, #2187, #18612, #17924, #39587, #29113, #50419, #7075, #61258, #2522, #18951, #40280 ),
 ( #55674, #61597, #2864, #50080, #35043, #50770, #34700, #1490, #39241, #23849, #39940, #44155, #13028, #22805, #8118, #17574, #38902, #23501, #65453, #44842, #13375, #60223, #66148, #23155, #12327, #13714, #56358, #8463, #66491, #65798, #33658, #28415, #18266, #12674, #1838, #34005, #55323, #7418, #34354, #46896, #20666, #14404, #52130, #24541, #40962, #3887, #35383, #57037, #41645, #31173, #25571, #58073, #45866, #51790, #68199, #20318, #62952, #67175, #15074, #19986, #9139, #9825, #4232, #62616, #62285, #36400, #57717, #57371, #52476, #63299, #51451, #36753, #4573, #25910, #46212, #67863, #30475, #25222, #47241, #19289, #40614, #10176, #68544, #35720, #46558, #24882 ) ),
 .UNSPECIFIED., .F., .F., .F.,
 ( 2, 2 ),
 ( 4, 2, 2, 2, 2, 2, 2, 2, 2, 2, 2, 2, 2, 2, 2, 2, 2, 2, 2, 2, 2, 2, 2, 2, 2, 2, 2, 2, 2, 2, 2, 2, 2, 2, 2, 2, 2, 2, 2, 2, 2, 2, 4 ),
 ( 0.000000000000000000, 1.000000000000000000 ),
 ( 0.000000000000000000, 7.083094307561015621E-05, 0.0001416618861512203124, 0.0002124928292268304822, 0.0002833237723024406248, 0.0003541547153780508217, 0.0004249856584536609643, 0.0004958166015292711070, 0.0005666475446048812497, 0.0006374784876804913923, 0.0007083094307561016434, 0.0007791403738317117860, 0.0008145558453695168032, 0.0008499713169073219287, 0.0008853867884451270542, 0.0009208022599829320714, 0.0009916332030585422140, 0.001027048674596347340, 0.001062464146134152465, 0.001097879617671957374, 0.001133295089209762499, 0.001204126032285372534, 0.001239541503823177659, 0.001274956975360982785, 0.001310372446898787910, 0.001345787918436593036, 0.001416618861512203287, 0.001487449804587813538, 0.001522865276125618447, 0.001558280747663423572, 0.001629111690739033606, 0.001699942633814643857, 0.001735358105352448983, 0.001770773576890254108, 0.001806189048428059017, 0.001841604519965864143, 0.001912435463041474177, 0.001983266406117084428, 0.002018681877654889337, 0.002054097349192694679, 0.002124928292268304930, 0.002195759235343914748, 0.002266590178419524999 ),
 .UNSPECIFIED. ) ;
#10065=CARTESIAN_POINT ( 'NONE',  ( 12.67305101672403822, -1.772831636685044066, -12.47465725448102170 ) ) ;
#10069=CARTESIAN_POINT ( 'NONE',  ( 12.61244651655888838, -1.905326457160024356, -13.78169738549997447 ) ) ;
#10072=CARTESIAN_POINT ( 'NONE',  ( 18.20615948710265286, -2.797893282243149038, 12.28544817418252677 ) ) ;
#10074=ORIENTED_EDGE ( 'NONE', *, *, #53898, .T. ) ;
#10080=CARTESIAN_POINT ( 'NONE',  ( 17.63823367518480367, 3.119790641614041959, 12.28531617466518355 ) ) ;
#10083=CARTESIAN_POINT ( 'NONE',  ( 17.55505043854147118, -3.199698446519375850, -12.18695736643652694 ) ) ;
#10090=CARTESIAN_POINT ( 'NONE',  ( 12.76336819523230126, -3.123957167202323859, 12.28406425424631898 ) ) ;
#10098=CARTESIAN_POINT ( 'NONE',  ( 12.51886017880454816, -0.5557204214162426714, 12.68363025601216520 ) ) ;
#10102=ORIENTED_EDGE ( 'NONE', *, *, #51141, .F. ) ;
#10106=CARTESIAN_POINT ( 'NONE',  ( 17.59662294266145466, 1.876036575741765189, 13.78611707749647763 ) ) ;
#10119=CARTESIAN_POINT ( 'NONE',  ( 18.16762906240597530, -2.624018810214523434, 13.64637396502913269 ) ) ;
#10122=CARTESIAN_POINT ( 'NONE',  ( 17.83426395974178291, -1.940453161589465791, -13.77628863228519229 ) ) ;
#10140=ORIENTED_EDGE ( 'NONE', *, *, #6731, .T. ) ;
#10143=CARTESIAN_POINT ( 'NONE',  ( 12.07997135281818579, 2.506142839463715521, -12.34827158344147868 ) ) ;
#10147=CARTESIAN_POINT ( 'NONE',  ( 18.12530810765561640, -2.066994332627602571, 13.84657437950017744 ) ) ;
#10148=CARTESIAN_POINT ( 'NONE',  ( 18.02549019385832096, 2.911978589154019748, -13.57741733930033590 ) ) ;
#10160=CARTESIAN_POINT ( 'NONE',  ( 18.02507753857510764, 0.4124490627810463161, -12.69099791225217189 ) ) ;
#10162=CARTESIAN_POINT ( 'NONE',  ( 12.25778805736141841, 2.802014929491043471, -12.37607946563925942 ) ) ;
#10175=ADVANCED_FACE ( 'NONE', ( #40769 ), #4729, .F. ) ;
#10176=CARTESIAN_POINT ( 'NONE',  ( 12.68688508614694044, -0.7208442004938080405, 13.98143072948223953 ) ) ;
#10181=CARTESIAN_POINT ( 'NONE',  ( 12.80505043854143388, 1.845938772038641318, -13.81933890150171074 ) ) ;
#10184=CARTESIAN_POINT ( 'NONE',  ( 12.50564389185357683, 0.6551943188411649688, 12.58295456804123091 ) ) ;
#10187=CARTESIAN_POINT ( 'NONE',  ( 12.22840029456386723, 2.917071392396657803, 12.25769309035714727 ) ) ;
#10194=DIRECTION ( 'NONE',  ( 0.000000000000000000, -0.9549051095262108824, 0.2969111513580035000 ) ) ;
#10197=ORIENTED_EDGE ( 'NONE', *, *, #52103, .F. ) ;
#10198=CARTESIAN_POINT ( 'NONE',  ( 12.27345231316480678, 0.3288522286145963980, 12.69427358703447695 ) ) ;
#10202=DIRECTION ( 'NONE',  ( 0.000000000000000000, -1.000000000000000000, 0.000000000000000000 ) ) ;
#10203=CARTESIAN_POINT ( 'NONE',  ( 12.27908368890585322, -2.837770472453527315, 13.59599796867854593 ) ) ;
#10211=CARTESIAN_POINT ( 'NONE',  ( 18.01290626049236820, 2.925915981747411632, -12.34209597222820776 ) ) ;
#10213=CARTESIAN_POINT ( 'NONE',  ( 18.16637421239960659, 2.630058152923315351, 12.42030992595579697 ) ) ;
#10228=DIRECTION ( 'NONE',  ( 1.000000000000000000, 0.000000000000000000, 0.000000000000000000 ) ) ;
#10230=EDGE_LOOP ( 'NONE', ( #29275, #51325, #23557, #24081 ) ) ;
#10238=EDGE_LOOP ( 'NONE', ( #2734, #29714, #41854, #20895 ) ) ;
#10245=CARTESIAN_POINT ( 'NONE',  ( 17.69900574642235824, -3.108543425041114805, -12.28872856983836748 ) ) ;
#10254=LINE ( 'NONE', #36834, #30671 ) ;
#10281=CARTESIAN_POINT ( 'NONE',  ( 17.71828964454860511, 3.103661179295900574, -12.29022416950854613 ) ) ;
#10289=CARTESIAN_POINT ( 'NONE',  ( 5.700000000000000178, 13.02829083129866738, -1.966948499731759448 ) ) ;
#10291=ORIENTED_EDGE ( 'NONE', *, *, #46673, .T. ) ;
#10292=CARTESIAN_POINT ( 'NONE',  ( 12.19409707445299773, -0.1321628250398325377, -12.69908003149456377 ) ) ;
#10298=DIRECTION ( 'NONE',  ( 0.000000000000000000, -0.000000000000000000, 1.000000000000000000 ) ) ;
#10300=CARTESIAN_POINT ( 'NONE',  ( 18.06139130780318780, 0.3666439886240649426, 12.69288249683096303 ) ) ;
#10307=CARTESIAN_POINT ( 'NONE',  ( 17.57587793826696299, 3.124999446933518943, -13.52084426442464604 ) ) ;
#10327=CARTESIAN_POINT ( 'NONE',  ( 17.98741890681814937, 0.4515201818990199345, -13.89013314509501917 ) ) ;
#10331=CYLINDRICAL_SURFACE ( 'NONE', #42162, 2.000000000000000444 ) ;
#10332=FACE_OUTER_BOUND ( 'NONE', #3255, .T. ) ;
#10345=CARTESIAN_POINT ( 'NONE',  ( 18.08617702649035763, -0.3300666952397341425, 13.89473968862478870 ) ) ;
#10346=CARTESIAN_POINT ( 'NONE',  ( 18.08719402100870610, 0.3285636529947569273, 13.89479065952357573 ) ) ;
#10348=CARTESIAN_POINT ( 'NONE',  ( 12.29146891697695132, 0.3563501258281275286, 13.89385640120309340 ) ) ;
#10351=CARTESIAN_POINT ( 'NONE',  ( 18.12515256033828592, -0.2563263767734609844, -13.89682277887181527 ) ) ;
#10360=CARTESIAN_POINT ( 'NONE',  ( 17.74345815918222158, 0.6949735217938506349, 12.58082105808780682 ) ) ;
#10368=ORIENTED_EDGE ( 'NONE', *, *, #11992, .F. ) ;
#10375=CARTESIAN_POINT ( 'NONE',  ( 17.55505043854147118, -1.760845406083394682, 12.47635457398814829 ) ) ;
#10391=EDGE_CURVE ( 'NONE', #37575, #36489, #64832, .T. ) ;
#10397=CARTESIAN_POINT ( 'NONE',  ( 12.66109513597118408, 3.108543426238434382, -12.28874474902926117 ) ) ;
#10401=VERTEX_POINT ( 'NONE', #22885 ) ;
#10406=CARTESIAN_POINT ( 'NONE',  ( 12.47303194318978647, -3.029615900428510589, -12.31225512782602927 ) ) ;
#10410=CARTESIAN_POINT ( 'NONE',  ( 12.38020518697568839, -1.926193139504583707, -13.86686096623706987 ) ) ;
#10413=CARTESIAN_POINT ( 'NONE',  ( 18.22257245894170907, -2.198943951577552625, 12.40664208059732410 ) ) ;
#10423=CARTESIAN_POINT ( 'NONE',  ( 18.10184288977456646, 2.186031417495633455, -12.51954808657351848 ) ) ;
#10425=CARTESIAN_POINT ( 'NONE',  ( 18.20426522488219589, -2.108767964861150368, -12.42302121882717536 ) ) ;
#10428=CARTESIAN_POINT ( 'NONE',  ( 12.55891702277100563, -3.074517471785633838, 12.29897628258782483 ) ) ;
#10437=CARTESIAN_POINT ( 'NONE',  ( 12.70247988648369386, -0.6166112555940445050, 12.67984200623734381 ) ) ;
#10444=CARTESIAN_POINT ( 'NONE',  ( 17.55505043854143565, 1.874999999999999556, 13.78627172894481667 ) ) ;
#10455=CARTESIAN_POINT ( 'NONE',  ( 18.17602379430269011, -2.571655014620207069, 13.65800652342065469 ) ) ;
#10458=CARTESIAN_POINT ( 'NONE',  ( 17.91230600709726772, -3.012931617833825904, -13.55113455194569028 ) ) ;
#10467=CARTESIAN_POINT ( 'NONE',  ( 17.96365918304935860, -0.4729502184326867531, 13.88916975807169862 ) ) ;
#10481=CARTESIAN_POINT ( 'NONE',  ( 12.80505043854143388, 1.760845406083386910, -12.47635457398815007 ) ) ;
#10485=CARTESIAN_POINT ( 'NONE',  ( 17.74403704562418937, -1.812651413143275381, 13.88215924362445897 ) ) ;
#10486=CARTESIAN_POINT ( 'NONE',  ( 18.16582246963814384, 2.632686764026700654, -13.64442020596820271 ) ) ;
#10490=ORIENTED_EDGE ( 'NONE', *, *, #3768, .F. ) ;
#10497=CARTESIAN_POINT ( 'NONE',  ( 17.86760901219547293, 0.5416145769730069670, -12.68445494689095732 ) ) ;
#10520=CARTESIAN_POINT ( 'NONE',  ( 12.34976886901036863, 0.5598083480993562011, 12.58755849294668394 ) ) ;
#10524=CARTESIAN_POINT ( 'NONE',  ( 12.08005347077622460, 2.506700685333588918, 12.34815832536655655 ) ) ;
#10526=CARTESIAN_POINT ( 'NONE',  ( 5.700000000000000178, -13.04986661130000059, -1.811520473896000016 ) ) ;
#10532=CARTESIAN_POINT ( 'NONE',  ( 12.20453436425304261, 2.673271222929743285, 12.40950569879642629 ) ) ;
#10541=CARTESIAN_POINT ( 'NONE',  ( 12.18763606713065073, -2.400822034753087753, 13.69401148367744270 ) ) ;
#10551=CARTESIAN_POINT ( 'NONE',  ( 18.17995611468269246, 2.522932803854499806, -12.44624262618112631 ) ) ;
#10554=CARTESIAN_POINT ( 'NONE',  ( 18.15140653315626196, 2.687261712024030746, 12.40596587094356984 ) ) ;
#10569=ORIENTED_EDGE ( 'NONE', *, *, #34743, .T. ) ;
#10585=VECTOR ( 'NONE', #27843, 1000.000000000000000 ) ;
#10589=CARTESIAN_POINT ( 'NONE',  ( 18.11597065765687375, -2.775858272760586498, -12.38300578299706345 ) ) ;
#10592=CARTESIAN_POINT ( 'NONE',  ( 12.18006450918421990, -0.02080959496299183628, 13.89999914846831963 ) ) ;
#10599=AXIS2_PLACEMENT_3D ( 'NONE', #37506, #793, #446 ) ;
#10621=CARTESIAN_POINT ( 'NONE',  ( 17.88880419370435604, 3.028786488651918685, -12.31252201556902470 ) ) ;
#10633=CARTESIAN_POINT ( 'NONE',  ( 12.18407639872240189, -0.07155418421575461541, -12.69973420405193032 ) ) ;
#10642=CARTESIAN_POINT ( 'NONE',  ( 18.08681263782093396, 0.3285869677314403048, 12.69428288850128084 ) ) ;
#10648=CARTESIAN_POINT ( 'NONE',  ( 18.06424752491733798, 2.862976204506490596, -13.58975765073224551 ) ) ;
#10652=CIRCLE ( 'NONE', #35277, 2.000000000000000444 ) ;
#10664=EDGE_CURVE ( 'NONE', #59800, #9344, #18000, .T. ) ;
#10668=LINE ( 'NONE', #5764, #11927 ) ;
#10669=CARTESIAN_POINT ( 'NONE',  ( 18.01649462541978508, 0.4224288466528487440, -13.89137824132244425 ) ) ;
#10682=CARTESIAN_POINT ( 'NONE',  ( 12.47202999840589754, 1.970716439074157611, -13.77157652140723165 ) ) ;
#10685=CARTESIAN_POINT ( 'NONE',  ( 17.91964795130430588, -0.5080432161604405694, 13.88750743611951854 ) ) ;
#10691=FACE_OUTER_BOUND ( 'NONE', #44640, .T. ) ;
#10700=CARTESIAN_POINT ( 'NONE',  ( 18.15003166281171332, -0.1916424759571756231, 12.69805926625132209 ) ) ;
#10714=CARTESIAN_POINT ( 'NONE',  ( 12.47371306568758875, -0.6398865404514904043, -12.58374251866278648 ) ) ;
#10716=CARTESIAN_POINT ( 'NONE',  ( 17.85685707441188086, 3.134587784889869333, -12.20386770240991581 ) ) ;
#10717=CARTESIAN_POINT ( 'NONE',  ( 5.624287198480771188, 12.11015306275865733, 3.744045437480294947 ) ) ;
#10734=VECTOR ( 'NONE', #59322, 1000.000000000000000 ) ;
#10737=CARTESIAN_POINT ( 'NONE',  ( 17.55505043854143565, 1.875000000000000000, 12.57541666120756041 ) ) ;
#10738=DIRECTION ( 'NONE',  ( 0.000000000000000000, -0.7198977633594745296, 0.6940801180771756229 ) ) ;
#10740=CARTESIAN_POINT ( 'NONE',  ( 12.43857111758543788, 3.006687177877848338, -12.31897860641675102 ) ) ;
#10755=CARTESIAN_POINT ( 'NONE',  ( 12.54752909501217673, -1.835309592424128056, -13.87918066653183224 ) ) ;
#10758=CARTESIAN_POINT ( 'NONE',  ( 17.94028104512299393, -3.089952709746686121, 12.21524586714252969 ) ) ;
#10762=VERTEX_POINT ( 'NONE', #33912 ) ;
#10765=CARTESIAN_POINT ( 'NONE',  ( 12.80505043854144276, -0.6951438842159466391, -13.94765567169527998 ) ) ;
#10780=CARTESIAN_POINT ( 'NONE',  ( 12.20096618732085680, -0.1616215023347950530, 12.69863621249087871 ) ) ;
#10790=CARTESIAN_POINT ( 'NONE',  ( 17.78650313621483647, 3.080655036186602302, 13.53295239609827050 ) ) ;
#10799=DIRECTION ( 'NONE',  ( 1.000000000000000000, 0.000000000000000000, 0.000000000000000000 ) ) ;
#10804=CARTESIAN_POINT ( 'NONE',  ( 17.86935674558758080, -3.040604463256959544, -13.54376658945627021 ) ) ;
#10829=CARTESIAN_POINT ( 'NONE',  ( 18.13616101482883636, 2.730220173529687600, -13.62193317606529241 ) ) ;
#10834=FACE_OUTER_BOUND ( 'NONE', #3695, .T. ) ;
#10840=LINE ( 'NONE', #38094, #61709 ) ;
#10842=CARTESIAN_POINT ( 'NONE',  ( 17.77532606275349636, 0.5849872192492382439, -12.68185863724643170 ) ) ;
#10851=CARTESIAN_POINT ( 'NONE',  ( 18.26132062505687159, 2.644858796842615156, 12.31930452622237127 ) ) ;
#10861=DIRECTION ( 'NONE',  ( 1.000000000000000000, 0.000000000000000000, 0.000000000000000000 ) ) ;
#10869=CARTESIAN_POINT ( 'NONE',  ( 12.09902206169133265, 2.644659774828324039, 12.31933076163361207 ) ) ;
#10882=CARTESIAN_POINT ( 'NONE',  ( 12.20957360714451490, 0.1900975197669926287, 12.69808960362405870 ) ) ;
#10885=CARTESIAN_POINT ( 'NONE',  ( 17.60358162561344741, 0.7192569394295647012, -12.57945425907935366 ) ) ;
#10888=CARTESIAN_POINT ( 'NONE',  ( 12.49074413817431406, -3.040604467177681958, 13.54382360563873000 ) ) ;
#10889=CARTESIAN_POINT ( 'NONE',  ( 12.18428608238131794, 2.573446268032343998, 13.65756128989349349 ) ) ;
#10898=CARTESIAN_POINT ( 'NONE',  ( 17.86072591669549681, 3.045244688009580702, -12.30767216807748810 ) ) ;
#10922=CYLINDRICAL_SURFACE ( 'NONE', #3206, 0.6250000000000005551 ) ;
#10923=CARTESIAN_POINT ( 'NONE',  ( 12.33073330736950268, 0.4072264705458581990, -13.89197624348239479 ) ) ;
#10935=CARTESIAN_POINT ( 'NONE',  ( 17.96903643132316475, -2.968342805378974436, -12.33002008018445039 ) ) ;
#10939=CARTESIAN_POINT ( 'NONE',  ( 18.17813554645151797, -2.450019327192359597, -12.46306814186711520 ) ) ;
#10940=CARTESIAN_POINT ( 'NONE',  ( 12.60368798324988582, 0.5920240553917486270, 13.88302649426328372 ) ) ;
#10942=CARTESIAN_POINT ( 'NONE',  ( 5.699999772733999492, -12.03770622561999915, -3.722046322334000124 ) ) ;
#10956=CARTESIAN_POINT ( 'NONE',  ( 18.00383897971941138, -1.936685752059260190, 13.86556672038733851 ) ) ;
#10972=CARTESIAN_POINT ( 'NONE',  ( 18.08168818186308258, 2.836704670500534764, -12.36674034546831891 ) ) ;
#10979=CARTESIAN_POINT ( 'NONE',  ( 18.20426522485155729, 2.108767964823663910, 12.42302121883312793 ) ) ;
#10981=CARTESIAN_POINT ( 'NONE',  ( 12.18004360525213414, 0.009762034906139017282, -12.70000045436731995 ) ) ;
#10990=DIRECTION ( 'NONE',  ( -0.000000000000000000, -0.000000000000000000, 1.000000000000000000 ) ) ;
#10991=CARTESIAN_POINT ( 'NONE',  ( 17.55505043854144276, 0.7192913403693119712, -12.57945229203838267 ) ) ;
#11001=EDGE_CURVE ( 'NONE', #4266, #7303, #68797, .T. ) ;
#11005=CARTESIAN_POINT ( 'NONE',  ( 17.55505043854143565, 1.760845406083394682, -12.47635457398814829 ) ) ;
#11012=DIRECTION ( 'NONE',  ( 1.000000000000000000, 0.000000000000000000, 0.000000000000000000 ) ) ;
#11019=CARTESIAN_POINT ( 'NONE',  ( 18.04536508902295822, 0.3876148459518023448, -13.89272660623100641 ) ) ;
#11027=B_SPLINE_CURVE_WITH_KNOTS ( 'NONE', 3,
 ( #62769, #29963, #30980, #8615, #52291, #47054, #47398, #20475, #14210, #19445, #56508, #41803, #68704, #51265, #3361, #24696, #46019, #40768, #62090, #56857, #48081, #530, #10327, #10669, #27447, #49110, #11019, #26418, #6108, #53672, #32693, #64830, #58565, #1221, #48771, #31664, #879, #53330, #37930, #47745, #43178, #27107, #52984, #21844, #36908, #22194 ),
 .UNSPECIFIED., .F., .F.,
 ( 4, 2, 2, 2, 2, 2, 2, 2, 2, 2, 2, 2, 2, 2, 1, 2, 2, 2, 2, 2, 1, 2, 2, 4 ),
 ( 0.000000000000000000, 0.06247329711229584331, 0.09370994566844376150, 0.1249465942245916866, 0.1405649185026656423, 0.1561832427807396118, 0.1874198913368828046, 0.2030382156149564132, 0.2186565398930300219, 0.2264657020320668679, 0.2342748641711037416, 0.2498931884491772670, 0.2811298370053271767, 0.2889389991443658823, 0.2967481612834046989, 0.3123664855614854408, 0.3279848098395661271, 0.3436031341176468690, 0.3748397826738083527, 0.3904581069518891501, 0.4060764312299698364, 0.4373130797861328189, 0.4685497283422958015, 0.4997863768984587285 ),
 .UNSPECIFIED. ) ;
#11033=CARTESIAN_POINT ( 'NONE',  ( 12.27207468729462647, 2.172927540677619174, -13.73742275803506274 ) ) ;
#11037=CARTESIAN_POINT ( 'NONE',  ( 18.18003636789866917, 0.02080959496299054218, 13.89999914846831963 ) ) ;
#11038=CARTESIAN_POINT ( 'NONE',  ( 18.12515256038028255, 0.2563263766789344866, 13.89682277887403394 ) ) ;
#11039=ORIENTED_EDGE ( 'NONE', *, *, #64174, .F. ) ;
#11046=CARTESIAN_POINT ( 'NONE',  ( 18.03457755495272252, -0.4008875276241527508, -13.89221989487475639 ) ) ;
#11053=B_SPLINE_CURVE_WITH_KNOTS ( 'NONE', 1,
 ( #40090, #56497 ),
 .UNSPECIFIED., .F., .F.,
 ( 2, 2 ),
 ( 0.000000000000000000, 1.000000000000000000 ),
 .UNSPECIFIED. ) ;
#11054=CARTESIAN_POINT ( 'NONE',  ( 18.17808098948988516, 0.05063260980701757286, 12.69986973508908079 ) ) ;
#11057=DIRECTION ( 'NONE',  ( -1.000000000000000000, 0.000000000000000000, 0.000000000000000000 ) ) ;
#11058=EDGE_LOOP ( 'NONE', ( #53324, #19136, #44323, #22552 ) ) ;
#11070=CARTESIAN_POINT ( 'NONE',  ( 18.25535445515775024, 2.667446342172959728, -12.31441698789904393 ) ) ;
#11082=ORIENTED_EDGE ( 'NONE', *, *, #51959, .T. ) ;
#11085=CARTESIAN_POINT ( 'NONE',  ( 18.17481363285255469, 0.08139021474669749789, -13.89968437038779570 ) ) ;
#11104=CARTESIAN_POINT ( 'NONE',  ( 12.68590879673673477, -1.797325930449588327, -13.88415075348993710 ) ) ;
#11108=CARTESIAN_POINT ( 'NONE',  ( 18.24534165125343677, -2.701041880525442807, 12.30709158425920613 ) ) ;
#11112=ORIENTED_EDGE ( 'NONE', *, *, #38625, .F. ) ;
#11136=CARTESIAN_POINT ( 'NONE',  ( 6.166666667074697905, 12.50864792167083017, -2.924697251373290730 ) ) ;
#11138=CARTESIAN_POINT ( 'NONE',  ( 18.17921951168938932, 2.461818733276640803, 13.68145094671735329 ) ) ;
#11143=CARTESIAN_POINT ( 'NONE',  ( 5.619239821438371862, -12.11503533078118622, 3.745341923022787789 ) ) ;
#11151=CARTESIAN_POINT ( 'NONE',  ( 18.25665235842816259, -2.332587565413964725, -13.80433135817204793 ) ) ;
#11172=CARTESIAN_POINT ( 'NONE',  ( 18.04486049886915211, 2.888348857507973211, -13.58339007192517656 ) ) ;
#11177=CARTESIAN_POINT ( 'NONE',  ( 12.30701392268165684, -3.003682976637727098, -12.23675526868967545 ) ) ;
#11180=EDGE_CURVE ( 'NONE', #38546, #55988, #56789, .T. ) ;
#11185=CARTESIAN_POINT ( 'NONE',  ( 18.08473038518646092, -0.4912829912815128153, -12.59042165808840252 ) ) ;
#11194=AXIS2_PLACEMENT_3D ( 'NONE', #9096, #68500, #68850 ) ;
#11195=CARTESIAN_POINT ( 'NONE',  ( 18.27054884872053009, 2.599315299774881627, 12.32899436121337189 ) ) ;
#11202=CARTESIAN_POINT ( 'NONE',  ( 12.51396835178763034, -3.139274738718787816, 12.20266202197805150 ) ) ;
#11211=CARTESIAN_POINT ( 'NONE',  ( 12.80505043854144276, 0.7192913403693016461, 12.57945229203838444 ) ) ;
#11214=CARTESIAN_POINT ( 'NONE',  ( 12.21328932544278523, 2.701359397734038215, 12.40237271074985159 ) ) ;
#11215=FACE_OUTER_BOUND ( 'NONE', #62166, .T. ) ;
#11221=CARTESIAN_POINT ( 'NONE',  ( 18.09811783085022441, -0.3100350603877315425, 12.69492243000587983 ) ) ;
#11224=CARTESIAN_POINT ( 'NONE',  ( 12.32101752301072572, 0.3953985757077859708, 12.69171505958679802 ) ) ;
#11228=CARTESIAN_POINT ( 'NONE',  ( 17.55505043854143565, 3.199751711897561801, -12.18694338143115452 ) ) ;
#11229=CARTESIAN_POINT ( 'NONE',  ( 12.28091743413951953, -2.013400871504821943, 13.85446832019263219 ) ) ;
#11238=CARTESIAN_POINT ( 'NONE',  ( 18.02812495262682901, 2.091428156338118960, -12.53745402072848947 ) ) ;
#11246=LINE ( 'NONE', #37139, #60043 ) ;
#11252=CARTESIAN_POINT ( 'NONE',  ( 18.14140153244920839, -2.282676164818131515, 13.71717056020691317 ) ) ;
#11262=CARTESIAN_POINT ( 'NONE',  ( 12.24298788029395268, 0.2740979065993932040, -13.89637745338620967 ) ) ;
#11271=LINE ( 'NONE', #5682, #64880 ) ;
#11272=CARTESIAN_POINT ( 'NONE',  ( 18.17545025690713345, -2.421661855460688351, -12.46948612151124358 ) ) ;
#11278=CARTESIAN_POINT ( 'NONE',  ( 12.21991984215965132, -0.2205930660282666711, 13.89766156610768277 ) ) ;
#11290=CIRCLE ( 'NONE', #34776, 2.000000000000001332 ) ;
#11292=LINE ( 'NONE', #32632, #38900 ) ;
#11293=CARTESIAN_POINT ( 'NONE',  ( 18.00257402908058424, -3.100282954733041940, 13.65258486500941970 ) ) ;
#11322=ORIENTED_EDGE ( 'NONE', *, *, #21785, .T. ) ;
#11326=CARTESIAN_POINT ( 'NONE',  ( 18.04063798880599379, 0.3934994371746786679, 12.69179478355544255 ) ) ;
#11348=EDGE_CURVE ( 'NONE', #31306, #6106, #6072, .T. ) ;
#11355=CARTESIAN_POINT ( 'NONE',  ( 17.60324462842607929, -1.762109595560080066, -12.47617631420775197 ) ) ;
#11361=DIRECTION ( 'NONE',  ( 0.000000000000000000, 0.9553735099700839672, -0.2954005017724949389 ) ) ;
#11367=CARTESIAN_POINT ( 'NONE',  ( 12.80505043854143388, 3.124999999999999556, -13.52084414783465505 ) ) ;
#11370=CARTESIAN_POINT ( 'NONE',  ( 17.93599053679681887, -0.4959091552601235242, 13.88809952003718351 ) ) ;
#11374=CARTESIAN_POINT ( 'NONE',  ( 12.57406875486398867, 0.5808247544327472811, 13.88366201036104641 ) ) ;
#11375=CARTESIAN_POINT ( 'NONE',  ( 12.80505043854144276, -0.6250000000000001110, -13.88107975066922428 ) ) ;
#11377=CARTESIAN_POINT ( 'NONE',  ( 17.85613310409923216, -0.5477939754333960298, -13.88547043407233694 ) ) ;
#11387=CARTESIAN_POINT ( 'NONE',  ( 17.57569811463524445, -0.6249994333735310326, 12.67928921956170996 ) ) ;
#11401=EDGE_LOOP ( 'NONE', ( #63628, #27117, #5673, #10197 ) ) ;
#11402=CARTESIAN_POINT ( 'NONE',  ( 12.38296014331786843, -0.5849390254007856838, -12.58641711472857772 ) ) ;
#11404=CARTESIAN_POINT ( 'NONE',  ( 18.17205452211569749, 2.859046691836176546, -12.27135926524918474 ) ) ;
#11405=CARTESIAN_POINT ( 'NONE',  ( 5.642739276337785270, 12.09235441392603150, 3.739144582074417578 ) ) ;
#11419=CARTESIAN_POINT ( 'NONE',  ( 17.57569738523962144, -0.6249994334955764064, -13.88107975403457495 ) ) ;
#11428=VERTEX_POINT ( 'NONE', #51277 ) ;
#11435=ORIENTED_EDGE ( 'NONE', *, *, #20125, .T. ) ;
#11436=CARTESIAN_POINT ( 'NONE',  ( 12.37468788209173809, -2.046657606614539660, -12.54569895759545517 ) ) ;
#11440=CARTESIAN_POINT ( 'NONE',  ( 12.22832816813801315, -2.961039467707567319, -13.68329631872640917 ) ) ;
#11444=CARTESIAN_POINT ( 'NONE',  ( 17.86958940788779771, -3.040180081688693470, 12.30916660591379674 ) ) ;
#11449=VECTOR ( 'NONE', #21248, 1000.000000000000000 ) ;
#11471=CARTESIAN_POINT ( 'NONE',  ( 7.100000000000000533, 12.50865771883999855, -2.924687089724999911 ) ) ;
#11473=CARTESIAN_POINT ( 'NONE',  ( 18.02766551172499376, 2.090896903265579976, 13.75171326662667504 ) ) ;
#11485=CARTESIAN_POINT ( 'NONE',  ( 18.27121482242689865, -2.402104771923907034, -13.79240553248645718 ) ) ;
#11504=CARTESIAN_POINT ( 'NONE',  ( 12.15953697780016540, 2.808329718129376928, -12.28305324893824668 ) ) ;
#11513=VERTEX_POINT ( 'NONE', #5094 ) ;
#11514=CARTESIAN_POINT ( 'NONE',  ( 12.48183889708585426, -3.124385432114249461, -12.20648365185189022 ) ) ;
#11521=CARTESIAN_POINT ( 'NONE',  ( 17.95947714806422368, 0.4766234715920644738, -12.68796191786314154 ) ) ;
#11522=CARTESIAN_POINT ( 'NONE',  ( 12.21202437720863010, 2.301604982166983948, -12.49562318899369018 ) ) ;
#11533=CARTESIAN_POINT ( 'NONE',  ( 18.24677884388063021, 2.264233918701648474, 12.39489312188808334 ) ) ;
#11539=CARTESIAN_POINT ( 'NONE',  ( 12.07997135281821954, -2.506142839463719962, 12.34827158344147335 ) ) ;
#11545=CARTESIAN_POINT ( 'NONE',  ( 12.13954479299509615, -0.2856017019952157288, 12.59676745213710625 ) ) ;
#11548=CARTESIAN_POINT ( 'NONE',  ( 17.55505043854143565, 1.787797342887044394, 13.88538010501570952 ) ) ;
#11549=CARTESIAN_POINT ( 'NONE',  ( 12.19026796737403195, 2.613005292445991223, 12.42452312575879070 ) ) ;
#11552=CARTESIAN_POINT ( 'NONE',  ( 18.16427545049632286, -0.3901114995139697283, 12.59396323349878166 ) ) ;
#11564=CARTESIAN_POINT ( 'NONE',  ( 12.30643338748587468, -1.987817336848023198, 13.85816184334709433 ) ) ;
#11575=CARTESIAN_POINT ( 'NONE',  ( 17.60707724214342917, 1.877081947552195151, -12.57511531410870731 ) ) ;
#11590=CARTESIAN_POINT ( 'NONE',  ( 17.86097767714754525, -3.045104419577887800, 13.54261379197756732 ) ) ;
#11598=CARTESIAN_POINT ( 'NONE',  ( 12.80505043854144098, -0.7302158263239267866, -13.98094363220830871 ) ) ;
#11612=CARTESIAN_POINT ( 'NONE',  ( 18.14016391943236073, -2.719929439268203630, -12.39760446975600416 ) ) ;
#11620=CARTESIAN_POINT ( 'NONE',  ( 12.26342747050452076, 0.3125520594525317275, 13.89528657259775102 ) ) ;
#11644=B_SPLINE_CURVE_WITH_KNOTS ( 'NONE', 3,
 ( #61929, #62940, #14726, #40603 ),
 .UNSPECIFIED., .F., .F.,
 ( 4, 4 ),
 ( 0.000000000000000000, 1.000000000000000000 ),
 .UNSPECIFIED. ) ;
#11665=ORIENTED_EDGE ( 'NONE', *, *, #68167, .T. ) ;
#11693=ORIENTED_EDGE ( 'NONE', *, *, #39881, .F. ) ;
#11698=CARTESIAN_POINT ( 'NONE',  ( 17.72120476622717433, -1.779652109340960520, -12.47368672373263898 ) ) ;
#11705=CARTESIAN_POINT ( 'NONE',  ( 12.80505043854144098, 0.7302158263239095781, 13.98094363220830871 ) ) ;
#11706=ORIENTED_EDGE ( 'NONE', *, *, #55803, .F. ) ;
#11710=CARTESIAN_POINT ( 'NONE',  ( 12.29628962427834793, 2.863168005537269689, -13.58969864530831728 ) ) ;
#11713=CARTESIAN_POINT ( 'NONE',  ( 18.17001922193489705, 0.1119984579798026098, 13.89939774083726576 ) ) ;
#11718=CARTESIAN_POINT ( 'NONE',  ( 12.23148617193598220, 0.2485195352681210113, 13.89701485918539170 ) ) ;
#11719=CARTESIAN_POINT ( 'NONE',  ( 12.41700012673178044, -0.4899485148888237940, -13.88837626668755831 ) ) ;
#11720=DIRECTION ( 'NONE',  ( -0.000000000000000000, -0.000000000000000000, 1.000000000000000000 ) ) ;
#11732=CARTESIAN_POINT ( 'NONE',  ( 18.01141060613106148, -0.4275228316712903487, 12.69032453495386292 ) ) ;
#11735=EDGE_LOOP ( 'NONE', ( #7144, #4725, #36956, #66556 ) ) ;
#11747=CARTESIAN_POINT ( 'NONE',  ( 12.20907020345897642, -0.4097539338085484095, -12.59333942654355809 ) ) ;
#11749=CARTESIAN_POINT ( 'NONE',  ( 18.26836321268585195, 2.610382005543650408, -12.32663954618810820 ) ) ;
#11750=CARTESIAN_POINT ( 'NONE',  ( 5.500000000000000000, 12.22293095105000127, 3.800428736101999938 ) ) ;
#11762=VERTEX_POINT ( 'NONE', #42848 ) ;
#11765=CARTESIAN_POINT ( 'NONE',  ( 17.72054635526678368, 0.7113363331415119006, -13.98191770012930135 ) ) ;
#11768=FACE_OUTER_BOUND ( 'NONE', #36207, .T. ) ;
#11773=AXIS2_PLACEMENT_3D ( 'NONE', #26344, #3627, #25651 ) ;
#11776=CARTESIAN_POINT ( 'NONE',  ( 18.02697970389229454, -1.963589444787183558, 13.86161523094991210 ) ) ;
#11783=CARTESIAN_POINT ( 'NONE',  ( 12.27169925567833175, -2.173540117687664974, -12.52166307684904112 ) ) ;
#11788=CARTESIAN_POINT ( 'NONE',  ( 12.14431428438026472, -2.818682143830034015, -13.71332026632872036 ) ) ;
#11791=CARTESIAN_POINT ( 'NONE',  ( 12.61539589083637658, -1.784264304828792058, 12.47303049908514438 ) ) ;
#11792=CARTESIAN_POINT ( 'NONE',  ( 17.68706105916313120, -1.772767334361405211, 12.47466639265151755 ) ) ;
#11822=CARTESIAN_POINT ( 'NONE',  ( 18.06381123663115673, 2.863168028152634825, 13.58964369048649701 ) ) ;
#11825=ORIENTED_EDGE ( 'NONE', *, *, #21653, .T. ) ;
#11833=CARTESIAN_POINT ( 'NONE',  ( 18.27869735329875311, -2.567871808703005243, -13.76250717860552264 ) ) ;
#11850=DIRECTION ( 'NONE',  ( -1.000000000000000000, 0.000000000000000000, 0.000000000000000000 ) ) ;
#11855=CARTESIAN_POINT ( 'NONE',  ( 12.48129647765398076, 3.124180215534350769, -12.20653620603297362 ) ) ;
#11872=CARTESIAN_POINT ( 'NONE',  ( 17.91965136929538005, -0.5080407711865443376, -12.68632595416894837 ) ) ;
#11874=CYLINDRICAL_SURFACE ( 'NONE', #35253, 0.6250000000000005551 ) ;
#11884=CARTESIAN_POINT ( 'NONE',  ( 18.18389880332053465, 2.839229093938504089, 12.27596119698807620 ) ) ;
#11890=CARTESIAN_POINT ( 'NONE',  ( 12.78084111884637331, -3.199751093817833958, 12.18694350317452724 ) ) ;
#11898=CARTESIAN_POINT ( 'NONE',  ( 12.72146951531671455, -0.7145943380091435149, 12.57972004139935152 ) ) ;
#11900=CARTESIAN_POINT ( 'NONE',  ( 17.55505043854143565, 1.875000000000000000, 13.78627172894481667 ) ) ;
#11901=CARTESIAN_POINT ( 'NONE',  ( 12.78418764580518108, 3.124999405572221445, 12.28373085793388064 ) ) ;
#11912=VERTEX_POINT ( 'NONE', #2269 ) ;
#11919=CARTESIAN_POINT ( 'NONE',  ( 12.15420371307394909, -2.840396063362202295, 13.70885132993088007 ) ) ;
#11921=CARTESIAN_POINT ( 'NONE',  ( 12.80505043854143388, 1.816864895258029522, 13.85234397965874464 ) ) ;
#11927=VECTOR ( 'NONE', #20474, 1000.000000000000000 ) ;
#11946=CARTESIAN_POINT ( 'NONE',  ( 17.80560960443414942, -3.072671113640228491, 13.53517819557379376 ) ) ;
#11960=ORIENTED_EDGE ( 'NONE', *, *, #10391, .T. ) ;
#11966=CARTESIAN_POINT ( 'NONE',  ( 17.92207321742860415, -3.154877352415835556, -13.63994794764937701 ) ) ;
#11969=CARTESIAN_POINT ( 'NONE',  ( 12.80505043854144276, -0.6250000000000001110, 13.88107975066923316 ) ) ;
#11970=CARTESIAN_POINT ( 'NONE',  ( 12.34634080959761171, 2.074995934380768237, 13.75442486551246013 ) ) ;
#11971=CARTESIAN_POINT ( 'NONE',  ( 17.71905360607588875, -1.896551502301641712, 12.57190390430904436 ) ) ;
#11973=CARTESIAN_POINT ( 'NONE',  ( 12.58447130036695327, 0.5851376999905932852, 13.88342059653409066 ) ) ;
#11992=EDGE_CURVE ( 'NONE', #10762, #22430, #28509, .T. ) ;
#12018=CARTESIAN_POINT ( 'NONE',  ( 12.24279999538062924, 2.226287937568673936, -13.72772666894336879 ) ) ;
#12020=CARTESIAN_POINT ( 'NONE',  ( 12.35662541760398625, 3.053258836637784857, 12.22465729757279185 ) ) ;
#12024=CARTESIAN_POINT ( 'NONE',  ( 12.13954239761512177, -0.2899337805559861203, -13.99700184298317396 ) ) ;
#12029=CARTESIAN_POINT ( 'NONE',  ( 5.685751648549689286, 12.05129647863442344, -3.726325695169643737 ) ) ;
#12032=B_SPLINE_CURVE_WITH_KNOTS ( 'NONE', 3,
 ( #11705, #38630, #33044, #1230 ),
 .UNSPECIFIED., .F., .F.,
 ( 4, 4 ),
 ( 0.000000000000000000, 1.000000000000000000 ),
 .UNSPECIFIED. ) ;
#12034=CARTESIAN_POINT ( 'NONE',  ( 18.11747123342421162, 2.226643993407489308, -13.72766178540381077 ) ) ;
#12044=DIRECTION ( 'NONE',  ( 0.000000000000000000, 0.000000000000000000, 1.000000000000000000 ) ) ;
#12047=CARTESIAN_POINT ( 'NONE',  ( 18.01235687061446455, -2.926439070453491720, -13.57366610795276962 ) ) ;
#12055=CARTESIAN_POINT ( 'NONE',  ( 18.27054884872056206, -2.599315299774876298, -12.32899436121337189 ) ) ;
#12060=EDGE_CURVE ( 'NONE', #19784, #12411, #20940, .T. ) ;
#12065=LINE ( 'NONE', #18010, #21375 ) ;
#12068=CARTESIAN_POINT ( 'NONE',  ( 12.18824001706381210, 2.602861674270835923, -13.65112526288234029 ) ) ;
#12071=CARTESIAN_POINT ( 'NONE',  ( 18.25578913467702336, -0.1888260363403085340, 13.99874504378992590 ) ) ;
#12073=ORIENTED_EDGE ( 'NONE', *, *, #40020, .F. ) ;
#12076=CARTESIAN_POINT ( 'NONE',  ( 12.29062815680005549, -0.3550741891739155331, 13.89389891666938226 ) ) ;
#12090=CARTESIAN_POINT ( 'NONE',  ( 18.17981518646734784, 0.01996654564806146087, 12.69998441237379083 ) ) ;
#12093=CARTESIAN_POINT ( 'NONE',  ( 18.13624051180335783, -2.730018211839375208, -12.39499564932253328 ) ) ;
#12105=ORIENTED_EDGE ( 'NONE', *, *, #60303, .T. ) ;
#12107=CARTESIAN_POINT ( 'NONE',  ( 12.08612546794235421, 0.09367178904473767720, -12.59965724591066660 ) ) ;
#12109=CARTESIAN_POINT ( 'NONE',  ( 18.08628618592427273, 2.970581112497161502, -12.24483314193592776 ) ) ;
#12123=CARTESIAN_POINT ( 'NONE',  ( 12.70675980919426173, 3.199682200193715520, -12.18696163212671024 ) ) ;
#12125=CARTESIAN_POINT ( 'NONE',  ( 18.14018103492323419, -0.2205930660282629796, -13.89766156610767034 ) ) ;
#12135=CARTESIAN_POINT ( 'NONE',  ( 12.28991563251189945, -2.854049639552650675, -13.59191281878594992 ) ) ;
#12137=CARTESIAN_POINT ( 'NONE',  ( 17.65223863462161802, 0.7192245859873318548, 12.57945610904469724 ) ) ;
#12139=CARTESIAN_POINT ( 'NONE',  ( 12.58248715490569047, -1.915879699765342892, -12.56863216566091168 ) ) ;
#12145=CARTESIAN_POINT ( 'NONE',  ( 12.70945613931270124, -1.793774045999469102, -13.88460948128834360 ) ) ;
#12150=CARTESIAN_POINT ( 'NONE',  ( 17.92103372721324561, -3.006741473881710647, 12.31895748915803424 ) ) ;
#12151=ORIENTED_EDGE ( 'NONE', *, *, #47373, .T. ) ;
#12161=ORIENTED_EDGE ( 'NONE', *, *, #24662, .F. ) ;
#12165=DIRECTION ( 'NONE',  ( 0.000000000000000000, -0.9549051095262108824, 0.2969111513580035000 ) ) ;
#12179=CARTESIAN_POINT ( 'NONE',  ( 18.01397738364135392, 2.075598766708242060, 13.75431519107023526 ) ) ;
#12192=CARTESIAN_POINT ( 'NONE',  ( 18.10325613414707746, -2.040025360435032464, -13.85057320474804854 ) ) ;
#12213=CARTESIAN_POINT ( 'NONE',  ( 12.13935791461255675, 2.765884558748026301, -12.29268093925658434 ) ) ;
#12228=ADVANCED_FACE ( 'NONE', ( #52560 ), #51870, .F. ) ;
#12230=CARTESIAN_POINT ( 'NONE',  ( 12.72201428491567121, -3.119809216722634115, -13.52222099568139413 ) ) ;
#12232=CARTESIAN_POINT ( 'NONE',  ( 18.14710087547455331, -0.2005123242923291527, -12.69787478206145259 ) ) ;
#12243=CARTESIAN_POINT ( 'NONE',  ( 18.06564745257664129, 2.991132176950368482, 12.23981809347030847 ) ) ;
#12249=CARTESIAN_POINT ( 'NONE',  ( 12.10442723766657025, -2.667336250084669125, 12.31445622895738978 ) ) ;
#12254=VERTEX_POINT ( 'NONE', #52911 ) ;
#12255=CARTESIAN_POINT ( 'NONE',  ( 12.15201606283211788, -0.3124912280145362153, 12.59612551846059780 ) ) ;
#12258=CARTESIAN_POINT ( 'NONE',  ( 12.43906710990142628, 3.006741445058540574, 12.31893827218670445 ) ) ;
#12264=CARTESIAN_POINT ( 'NONE',  ( 18.02801395638694260, -0.4085932595162927727, 12.69115266611978043 ) ) ;
#12269=ORIENTED_EDGE ( 'NONE', *, *, #26043, .F. ) ;
#12278=CARTESIAN_POINT ( 'NONE',  ( 12.50306195774383333, -1.853743832531306701, 13.87673314481786058 ) ) ;
#12288=DIRECTION ( 'NONE',  ( 0.000000000000000000, 0.000000000000000000, 1.000000000000000000 ) ) ;
#12289=CARTESIAN_POINT ( 'NONE',  ( 17.84375123822102438, 1.945578272181329504, -12.56362807389522374 ) ) ;
#12294=CARTESIAN_POINT ( 'NONE',  ( 17.78891907839554420, -0.6928235585744062508, -13.98285841810580443 ) ) ;
#12296=CARTESIAN_POINT ( 'NONE',  ( 12.76376210869972105, -3.125000000000000444, 12.28374662615010671 ) ) ;
#12300=CARTESIAN_POINT ( 'NONE',  ( 18.11136953712603059, -2.785023373216928277, 13.60886753798840765 ) ) ;
#12302=ORIENTED_EDGE ( 'NONE', *, *, #25080, .F. ) ;
#12307=CARTESIAN_POINT ( 'NONE',  ( 12.56925896339910764, -1.825837054118446323, -13.88044190432301406 ) ) ;
#12319=DIRECTION ( 'NONE',  ( 0.000000000000000000, -0.7916053084224905501, -0.6110327615417471270 ) ) ;
#12323=CARTESIAN_POINT ( 'NONE',  ( 12.21968270649327870, 2.719953125373911096, 13.62430835208223101 ) ) ;
#12327=CARTESIAN_POINT ( 'NONE',  ( 12.15456646199064217, 0.3226776716457197547, 13.99628514671256241 ) ) ;
#12369=CARTESIAN_POINT ( 'NONE',  ( 12.19329716805284036, 2.371658047258630830, -13.69984404026345004 ) ) ;
#12371=DIRECTION ( 'NONE',  ( 1.000000000000000000, 0.000000000000000000, 0.000000000000000000 ) ) ;
#12374=CARTESIAN_POINT ( 'NONE',  ( 12.50529577747503929, -0.6653129401483898198, -13.98418548573915743 ) ) ;
#12375=CARTESIAN_POINT ( 'NONE',  ( 17.55505043854147118, -1.875000000000000000, 13.78631952119024895 ) ) ;
#12376=CARTESIAN_POINT ( 'NONE',  ( 7.100000000000000533, -13.94845324556000143, 4.312847325879000770 ) ) ;
#12379=CARTESIAN_POINT ( 'NONE',  ( 5.641095281750911461, 12.09393047400991783, -3.739612655151742793 ) ) ;
#12380=VERTEX_POINT ( 'NONE', #4580 ) ;
#12382=CARTESIAN_POINT ( 'NONE',  ( 17.74765434492527660, 1.905326452124538550, -13.78174529102851231 ) ) ;
#12396=CARTESIAN_POINT ( 'NONE',  ( 18.12992444764572042, -2.745380825951750037, -13.61829546699563664 ) ) ;
#12404=CARTESIAN_POINT ( 'NONE',  ( 18.28006803703877026, -2.506146490485266387, -12.34827083869107156 ) ) ;
#12411=VERTEX_POINT ( 'NONE', #25226 ) ;
#12412=CARTESIAN_POINT ( 'NONE',  ( 5.499988390671900262, -12.65264562523000080, 3.063511175100999573 ) ) ;
#12416=CARTESIAN_POINT ( 'NONE',  ( 12.27908368890581947, 2.837770472453523318, -13.59599796867854238 ) ) ;
#12420=CARTESIAN_POINT ( 'NONE',  ( 17.77532102045679352, 0.5849891190461627977, 13.88342664904964430 ) ) ;
#12426=CARTESIAN_POINT ( 'NONE',  ( 12.44874774240861903, -0.5136130429876892833, 13.88722741725485221 ) ) ;
#12437=CARTESIAN_POINT ( 'NONE',  ( 18.06356912472852727, 0.3639343692979884470, 12.69299665021504531 ) ) ;
#12439=CARTESIAN_POINT ( 'NONE',  ( 17.96110074834193426, -2.975239710472639132, -12.32804434199374377 ) ) ;
#12444=CARTESIAN_POINT ( 'NONE',  ( 12.52583694058618136, -1.940453150098577106, 13.77633667721135780 ) ) ;
#12451=CARTESIAN_POINT ( 'NONE',  ( 12.21591953885793735, -0.4193891200559257126, -12.59302195412780456 ) ) ;
#12454=CARTESIAN_POINT ( 'NONE',  ( 12.80505043854144276, 0.7192913403693124152, -12.57945229203838267 ) ) ;
#12463=EDGE_LOOP ( 'NONE', ( #23014, #322, #45433, #19466 ) ) ;
#12469=CARTESIAN_POINT ( 'NONE',  ( 18.17180502197784975, 0.1017048024284007979, -13.89950429703524293 ) ) ;
#12482=PLANE ( 'NONE',  #22536 ) ;
#12490=CARTESIAN_POINT ( 'NONE',  ( 17.65148079338498022, -1.767134912084536325, 12.47546541983269286 ) ) ;
#12523=CARTESIAN_POINT ( 'NONE',  ( 18.18532329594571095, 2.156378744708868922, 13.83294935661368541 ) ) ;
#12537=CARTESIAN_POINT ( 'NONE',  ( 18.03607885879101147, -1.971554139641146230, -13.86048489721954624 ) ) ;
#12556=CARTESIAN_POINT ( 'NONE',  ( 17.55505043854143565, 1.875000000000000000, 12.57541666120756041 ) ) ;
#12558=CARTESIAN_POINT ( 'NONE',  ( 12.51396835178759659, 3.139274738718781599, -12.20266202197804972 ) ) ;
#12568=CARTESIAN_POINT ( 'NONE',  ( 12.08013217067794720, -2.460179751193595887, -12.35749396829501023 ) ) ;
#12575=CARTESIAN_POINT ( 'NONE',  ( 12.49024380163862169, -3.040024005673539254, -13.54391858567109885 ) ) ;
#12576=CARTESIAN_POINT ( 'NONE',  ( 18.18005727183074782, -0.009762034906138482987, -12.70000045436731995 ) ) ;
#12577=CARTESIAN_POINT ( 'NONE',  ( 17.55505043854143565, 1.875000000000000000, -13.78631952119025073 ) ) ;
#12581=SURFACE_STYLE_USAGE ( .BOTH. , #27975 ) ;
#12587=CARTESIAN_POINT ( 'NONE',  ( 18.08809746899275694, 2.173637705205955228, 12.52162896472547082 ) ) ;
#12594=CARTESIAN_POINT ( 'NONE',  ( 12.43939714311205336, -3.101706251878837861, 12.21226669259267439 ) ) ;
#12600=CARTESIAN_POINT ( 'NONE',  ( 12.36315700431396714, -0.5707228546306997163, 12.58707662888204304 ) ) ;
#12603=CARTESIAN_POINT ( 'NONE',  ( 12.51734955435997598, 3.054939157457059906, 12.30478592156021378 ) ) ;
#12609=CARTESIAN_POINT ( 'NONE',  ( 18.02496081276520101, -0.4121104631841241983, 12.69099970360672458 ) ) ;
#12616=CARTESIAN_POINT ( 'NONE',  ( 18.05125194753120965, -2.880159329997852069, 13.58544989777342415 ) ) ;
#12620=CARTESIAN_POINT ( 'NONE',  ( 12.75683046442385482, -1.789027279909009227, 13.88522190323555350 ) ) ;
#12623=CARTESIAN_POINT ( 'NONE',  ( 17.55505043854143565, 3.125000000000000000, -13.52084414783465682 ) ) ;
#12633=CARTESIAN_POINT ( 'NONE',  ( 17.71905360607584967, 1.896551502301641934, -12.57190390430904436 ) ) ;
#12638=CARTESIAN_POINT ( 'NONE',  ( 18.28019269455629114, 0.1906559479335279972, -14.00000681886699105 ) ) ;
#12640=CARTESIAN_POINT ( 'NONE',  ( 12.64175205087593490, -3.104634757607365625, 12.28992885563596360 ) ) ;
#12646=CARTESIAN_POINT ( 'NONE',  ( 18.06424752491737706, -2.862976204506491484, 13.58975765073224906 ) ) ;
#12654=CARTESIAN_POINT ( 'NONE',  ( 12.43754357087991202, -3.154646014561297562, -13.64000194807119826 ) ) ;
#12669=CARTESIAN_POINT ( 'NONE',  ( 12.52647507922620562, 1.940423270478297102, 13.77628945559399121 ) ) ;
#12674=CARTESIAN_POINT ( 'NONE',  ( 12.09164601416806306, 0.1306247939804469627, 13.99939550958098522 ) ) ;
#12679=CARTESIAN_POINT ( 'NONE',  ( 4.599999999999999645, -1.875000000000000000, 13.78631952119025073 ) ) ;
#12723=CARTESIAN_POINT ( 'NONE',  ( 12.14435534536353600, -0.3008963210925020837, -13.99677033988233354 ) ) ;
#12727=CARTESIAN_POINT ( 'NONE',  ( 18.18005044212792143, 2.500000099754956739, -13.67345740034994250 ) ) ;
#12729=CARTESIAN_POINT ( 'NONE',  ( 5.699999545467999695, 12.03770622561999915, -3.722046322334000124 ) ) ;
#12732=CARTESIAN_POINT ( 'NONE',  ( 18.17918265292642488, 2.461360938835027934, -13.68159685767606781 ) ) ;
#12738=CARTESIAN_POINT ( 'NONE',  ( 17.78989870834643483, 1.827084948615273818, -13.88026577095109815 ) ) ;
#12745=CARTESIAN_POINT ( 'NONE',  ( 18.09739622856945118, -2.188708726578779906, 13.73458559203602469 ) ) ;
#12751=CARTESIAN_POINT ( 'NONE',  ( 18.26225755805772977, -2.321011060852003371, -12.38438709824086459 ) ) ;
#12760=CARTESIAN_POINT ( 'NONE',  ( 5.599959403262399604, 11.06886219213000011, -1.536526853569999851 ) ) ;
#12762=B_SPLINE_CURVE_WITH_KNOTS ( 'NONE', 3,
 ( #30657, #68047, #41488, #25755 ),
 .UNSPECIFIED., .F., .F.,
 ( 4, 4 ),
 ( 0.000000000000000000, 1.000000000000000000 ),
 .UNSPECIFIED. ) ;
#12765=CARTESIAN_POINT ( 'NONE',  ( 12.29779067500859568, 1.996199619003542258, -13.85695719179637031 ) ) ;
#12768=CARTESIAN_POINT ( 'NONE',  ( 17.81326568215976636, 0.5695321295966297992, 13.88429381145915542 ) ) ;
#12771=VERTEX_POINT ( 'NONE', #16143 ) ;
#12774=CARTESIAN_POINT ( 'NONE',  ( 12.19608251854004166, 0.1421750971580202361, 13.89904149565881575 ) ) ;
#12776=CARTESIAN_POINT ( 'NONE',  ( 12.18865263574115509, -2.603587051922128914, 13.65094575296205903 ) ) ;
#12788=CARTESIAN_POINT ( 'NONE',  ( 12.49451986944247217, -0.5425047576885997369, 12.68440192076777961 ) ) ;
#12795=CARTESIAN_POINT ( 'NONE',  ( 12.43812277102956010, -1.993632728549934230, 13.76791003216514575 ) ) ;
#12799=B_SPLINE_SURFACE_WITH_KNOTS ( 'NONE', 1, 3, ( 
 ( #11211, #32547, #62959, #63656, #58415, #64333, #378, #27299, #16452, #53525, #37438, #5615, #10184, #26617, #59105, #16112, #20326, #21020, #47596, #15086, #20674, #63994, #10520, #26267, #42005, #47937, #63307, #5960, #26958, #31181, #48623, #31513, #25919, #47249, #52486, #68904, #53175, #4582, #42686, #37781, #53860, #41653, #15772, #36411, #48272, #15434, #52835, #4931, #65378, #43383, #65726, #726, #1414, #27995, #64683, #48966, #44429, #17500, #6653, #22387, #28335, #1074, #55598, #33928, #38121, #7699, #38473, #6300, #27646, #11545, #49302, #12255, #32889, #1763, #18192, #44771, #23432, #22730, #39513, #33584, #54199, #49655, #60491, #38823, #16793, #39168, #59448, #12600, #17140, #23082, #43726, #7002, #2115, #54901, #59794, #44080, #34278, #65024, #60149, #17850, #22037, #55249, #7346, #28691, #50004, #33236, #11898, #29040, #66071, #60837, #12950, #54556 ),
 ( #24466, #66766, #2450, #61185, #62543, #24810, #56283, #35651, #46135, #14328, #50350, #18881, #30072, #23775, #56963, #14664, #8389, #29732, #51375, #35308, #46478, #41233, #45109, #35980, #66417, #67440, #30404, #57298, #8730, #18536, #19212, #67786, #51036, #19908, #39865, #9400, #19563, #61525, #9065, #40209, #2793, #34627, #13305, #50696, #13640, #34966, #51716, #55940, #8042, #29385, #3136, #67104, #3808, #25147, #24118, #45452, #40885, #62206, #45791, #40538, #56626, #61862, #13983, #3473, #10780, #37699, #32125, #69165, #47859, #21276, #47165, #15690, #294, #26531, #30743, #31432, #57997, #25494, #9748, #5193, #47511, #36678, #52403, #58333, #31096, #16370, #63915, #68129, #59029, #68466, #36327, #57642, #41571, #10098, #42272, #62881, #31777, #48192, #5538, #53441, #52749, #21614, #63576, #15001, #10437, #42604, #26185, #4154, #16027, #46823, #37356, #20589 ) ),
 .UNSPECIFIED., .F., .F., .F.,
 ( 2, 2 ),
 ( 4, 2, 2, 2, 2, 2, 2, 2, 2, 2, 2, 2, 2, 2, 2, 2, 2, 2, 2, 2, 2, 2, 2, 2, 2, 2, 2, 2, 2, 2, 2, 2, 2, 2, 2, 2, 2, 2, 2, 2, 2, 2, 2, 2, 2, 2, 2, 2, 2, 2, 2, 2, 2, 2, 2, 4 ),
 ( 0.000000000000000000, 1.000000000000000000 ),
 ( 0.000000000000000000, 7.083325941644275862E-05, 0.0001416665188328855172, 0.0002124997782493282623, 0.0002479164079575496213, 0.0002833330376657710345, 0.0003187496673739924477, 0.0003541662970822138067, 0.0004249995564986565246, 0.0004604161862068778836, 0.0004781245010609885631, 0.0004958328159150992426, 0.0005312494456233207100, 0.0005666660753315420690, 0.0006374993347479848953, 0.0006729159644562062543, 0.0007083325941644276133, 0.0007437492238726489723, 0.0007791658535808703313, 0.0008145824832890916902, 0.0008499991129973130492, 0.0008854157427055344082, 0.0009208323724137557672, 0.0009562490021219771262, 0.0009916656318301984852, 0.001027082261538419953, 0.001062498891246641420, 0.001133332150663084138, 0.001168748780371305605, 0.001204165410079526856, 0.001239582039787748323, 0.001274998669495969791, 0.001345831928912412509, 0.001381248558620633976, 0.001416665188328855227, 0.001452081818037076477, 0.001469790132891187102, 0.001487498447745297945, 0.001558331707161740663, 0.001629164966578183380, 0.001664581596286404848, 0.001699998225994626098, 0.001735414855702847349, 0.001770831485411068816, 0.001841664744827511534, 0.001877081374535732785, 0.001912498004243954252, 0.001947914633952175720, 0.001983331263660396970, 0.002018747893368618221, 0.002054164523076839905, 0.002124997782493282840, 0.002160414412201504090, 0.002195831041909725341, 0.002231247671617946592, 0.002266664301326168276 ),
 .UNSPECIFIED. ) ;
#12803=CARTESIAN_POINT ( 'NONE',  ( 12.21516876105738092, 0.4188397444781323808, -12.59305179380755035 ) ) ;
#12817=EDGE_LOOP ( 'NONE', ( #32319, #19812, #56249, #2815 ) ) ;
#12822=CARTESIAN_POINT ( 'NONE',  ( 18.26841422636659118, -0.1308528744652316944, -13.99939340647621222 ) ) ;
#12828=CARTESIAN_POINT ( 'NONE',  ( 18.15150620825778205, -2.686947401731335283, 12.40607332096686655 ) ) ;
#12831=CARTESIAN_POINT ( 'NONE',  ( 12.47184101605662931, -3.029124285173875997, -13.54683579967691998 ) ) ;
#12833=CARTESIAN_POINT ( 'NONE',  ( 17.55505043854147118, -1.875000000000000000, 12.57545641911172396 ) ) ;
#12837=CARTESIAN_POINT ( 'NONE',  ( 5.700000000000000178, 11.06886219213000011, 1.536526853569999851 ) ) ;
#12842=CARTESIAN_POINT ( 'NONE',  ( 17.72806902343761948, -3.100663240735258341, 12.29112607895899068 ) ) ;
#12864=AXIS2_PLACEMENT_3D ( 'NONE', #24271, #6806, #56085 ) ;
#12874=CARTESIAN_POINT ( 'NONE',  ( 17.65774109649147050, 3.116847231231422821, 13.52303903038508182 ) ) ;
#12885=CARTESIAN_POINT ( 'NONE',  ( 17.96944589180085572, -3.117220005880608547, -13.64855254614797531 ) ) ;
#12908=CARTESIAN_POINT ( 'NONE',  ( 12.50301483199531916, 3.134404823497599413, -12.20391382861247287 ) ) ;
#12915=CARTESIAN_POINT ( 'NONE',  ( 17.74278521987943336, 0.7069209314886554241, 13.98214394338196165 ) ) ;
#12917=CARTESIAN_POINT ( 'NONE',  ( 12.11850681454236245, -2.712075317534410335, -12.30466467946555653 ) ) ;
#12925=CARTESIAN_POINT ( 'NONE',  ( 12.39904396558118016, -2.975276281382168264, -13.56103672317925124 ) ) ;
#12926=CARTESIAN_POINT ( 'NONE',  ( 18.17808098948988516, -0.05063260980701731612, -12.69986973508909323 ) ) ;
#12935=CARTESIAN_POINT ( 'NONE',  ( 17.74796797082749578, 1.905496177146738690, 12.57037238745254726 ) ) ;
#12940=B_SPLINE_CURVE_WITH_KNOTS ( 'NONE', 1,
 ( #34302, #33610 ),
 .UNSPECIFIED., .F., .F.,
 ( 2, 2 ),
 ( 0.000000000000000000, 1.000000000000000000 ),
 .UNSPECIFIED. ) ;
#12944=CARTESIAN_POINT ( 'NONE',  ( 12.27200335545532894, -2.173637791136410424, 12.52166559990193662 ) ) ;
#12950=CARTESIAN_POINT ( 'NONE',  ( 12.79307474260548538, -0.7192913015564696977, 12.57945229205062709 ) ) ;
#12959=ADVANCED_FACE ( 'NONE', ( #65759 ), #38865, .F. ) ;
#12972=CARTESIAN_POINT ( 'NONE',  ( 5.700000000000000178, -13.94845324556000143, -4.312847325879000770 ) ) ;
#12975=CARTESIAN_POINT ( 'NONE',  ( 12.47175297079834699, -3.166474622353419921, 13.63720910406326858 ) ) ;
#12983=CARTESIAN_POINT ( 'NONE',  ( 17.75510503588994737, -0.5924680672155933081, 13.88300198247031503 ) ) ;
#12995=CARTESIAN_POINT ( 'NONE',  ( 12.22895615649426482, -2.742396662243991035, 12.39180484751770095 ) ) ;
#12996=VERTEX_POINT ( 'NONE', #57675 ) ;
#13000=CARTESIAN_POINT ( 'NONE',  ( 17.67504841906449897, -3.238437383711913586, 13.62029908313571980 ) ) ;
#13004=DIRECTION ( 'NONE',  ( -0.000000000000000000, -0.000000000000000000, 1.000000000000000000 ) ) ;
#13023=CARTESIAN_POINT ( 'NONE',  ( 12.78089176142232475, 3.248146600645739124, 13.61798599873023363 ) ) ;
#13028=CARTESIAN_POINT ( 'NONE',  ( 12.42135566322309614, 0.6200266137005038258, 13.98626978124057807 ) ) ;
#13041=CARTESIAN_POINT ( 'NONE',  ( 12.70786224245961904, -0.7192245859873329650, 12.57945610904470080 ) ) ;
#13058=CARTESIAN_POINT ( 'NONE',  ( 12.47184101605659912, 3.029124285173875997, 13.54683579967692530 ) ) ;
#13070=PLANE ( 'NONE',  #67244 ) ;
#13073=CARTESIAN_POINT ( 'NONE',  ( 12.58477985662609022, 0.5849891190461610213, -13.88342664904962831 ) ) ;
#13081=CARTESIAN_POINT ( 'NONE',  ( 17.86981019193746079, 1.959656554206103962, -13.77332550900839969 ) ) ;
#13088=CARTESIAN_POINT ( 'NONE',  ( 17.72542258366203072, 0.6019459914113660659, -12.68079480699871020 ) ) ;
#13092=CARTESIAN_POINT ( 'NONE',  ( 18.14119057082517017, -2.717377330333714536, -13.62490400537736512 ) ) ;
#13101=CARTESIAN_POINT ( 'NONE',  ( 18.20792762907820972, -2.166426970554230724, -12.41237440719186580 ) ) ;
#13107=AXIS2_PLACEMENT_3D ( 'NONE', #6998, #29038, #23430 ) ;
#13117=CARTESIAN_POINT ( 'NONE',  ( 12.23619509269997430, 2.970722878206525142, -13.68118758531137935 ) ) ;
#13120=CARTESIAN_POINT ( 'NONE',  ( 17.91845017417215757, -0.6323113780857052557, 13.98571806661952976 ) ) ;
#13127=CARTESIAN_POINT ( 'NONE',  ( 12.30534114217652686, -2.122480415427712597, 13.74636906787141477 ) ) ;
#13138=CARTESIAN_POINT ( 'NONE',  ( 18.13658048666561484, 0.2292434675627118279, 12.69722039463304775 ) ) ;
#13139=CARTESIAN_POINT ( 'NONE',  ( 12.18105077442922379, 0.04081512046595160009, 12.69993297814735733 ) ) ;
#13154=CARTESIAN_POINT ( 'NONE',  ( 12.34976886901036508, -0.5598083480993675254, -12.58755849294668394 ) ) ;
#13173=CARTESIAN_POINT ( 'NONE',  ( 18.17070062201314684, -0.3858260082455376994, -13.99468631105251681 ) ) ;
#13192=CARTESIAN_POINT ( 'NONE',  ( 5.500000000000000000, 0.000000000000000000, 0.000000000000000000 ) ) ;
#13193=CARTESIAN_POINT ( 'NONE',  ( 12.26342747050452608, -0.3125520594525371676, -13.89528657259774391 ) ) ;
#13196=CARTESIAN_POINT ( 'NONE',  ( 18.11622138774307444, -2.775899412256286780, 12.38303361670990910 ) ) ;
#13201=CARTESIAN_POINT ( 'NONE',  ( 17.88292281839158093, 1.943028894538316065, 13.77656085490136206 ) ) ;
#13218=DIRECTION ( 'NONE',  ( 0.000000000000000000, -1.000000000000000000, 0.000000000000000000 ) ) ;
#13227=CARTESIAN_POINT ( 'NONE',  ( 18.17146957700709464, 2.902473988487531464, 13.69582979195751271 ) ) ;
#13238=CARTESIAN_POINT ( 'NONE',  ( 18.18357137170428928, -2.882057337525668839, -13.70014066609292058 ) ) ;
#13240=EDGE_CURVE ( 'NONE', #21338, #7236, #31084, .T. ) ;
#13258=VECTOR ( 'NONE', #16467, 1000.000000000000000 ) ;
#13261=CARTESIAN_POINT ( 'NONE',  ( 12.22227632225710359, 2.273941840405718562, -12.50139599066423202 ) ) ;
#13269=CARTESIAN_POINT ( 'NONE',  ( 17.78891907840798225, 0.6928235585691923104, 13.98285841810605135 ) ) ;
#13271=CARTESIAN_POINT ( 'NONE',  ( 12.08977223171471493, -2.598917558143528872, -12.32906181315049032 ) ) ;
#13278=CARTESIAN_POINT ( 'NONE',  ( 12.17999522571492399, -2.481546339243234200, -13.67732359575999013 ) ) ;
#13279=CARTESIAN_POINT ( 'NONE',  ( 18.13628167719502216, 0.2299973361971401897, -12.69720198919504739 ) ) ;
#13289=CARTESIAN_POINT ( 'NONE',  ( 18.12992444769444234, 2.745380825832320681, 13.61829546702431948 ) ) ;
#13291=CARTESIAN_POINT ( 'NONE',  ( 17.91340230256478350, 1.987833194700777240, 12.55624649895498202 ) ) ;
#13296=CARTESIAN_POINT ( 'NONE',  ( 12.80505043854144276, 0.7192913403693124152, -12.57945229203838267 ) ) ;
#13297=ORIENTED_EDGE ( 'NONE', *, *, #12060, .F. ) ;
#13298=CARTESIAN_POINT ( 'NONE',  ( 12.28024293382675403, -2.160546425968632445, 12.52422939561507675 ) ) ;
#13305=CARTESIAN_POINT ( 'NONE',  ( 12.22015141286114215, 0.2205037192104031540, 12.69742880170239019 ) ) ;
#13309=CARTESIAN_POINT ( 'NONE',  ( 12.18370898482671727, 2.431702807279747525, 12.46721300078355554 ) ) ;
#13320=CARTESIAN_POINT ( 'NONE',  ( 18.11727294771828412, -0.2737714781793354479, -12.69604447594146812 ) ) ;
#13332=CARTESIAN_POINT ( 'NONE',  ( 17.69809243807087995, -0.6087680664141890130, 13.88205110007296028 ) ) ;
#13344=CARTESIAN_POINT ( 'NONE',  ( 12.18102902120000053, -2.459609776866888087, 12.46092926277264645 ) ) ;
#13347=CARTESIAN_POINT ( 'NONE',  ( 17.93785022694517295, -2.005837716635007428, 13.76593133495255472 ) ) ;
#13352=DIRECTION ( 'NONE',  ( -1.000000000000000000, 0.000000000000000000, 0.000000000000000000 ) ) ;
#13358=CARTESIAN_POINT ( 'NONE',  ( 17.57900174287143358, 0.7192906882580965000, -12.57945229568000656 ) ) ;
#13362=CARTESIAN_POINT ( 'NONE',  ( 4.599999999999999645, -13.17499999999999893, -1.613472157876637865E-15 ) ) ;
#13369=FACE_OUTER_BOUND ( 'NONE', #6376, .T. ) ;
#13371=CARTESIAN_POINT ( 'NONE',  ( 12.20052126010791405, 2.341019711503390610, 13.70584597024487827 ) ) ;
#13374=CARTESIAN_POINT ( 'NONE',  ( 12.39790242452336244, 0.4743817203469002375, -12.68807659223303475 ) ) ;
#13375=CARTESIAN_POINT ( 'NONE',  ( 12.21516724099300077, 0.4251989115648853179, 13.99355557726514476 ) ) ;
#13387=CYLINDRICAL_SURFACE ( 'NONE', #59408, 0.6250000000000005551 ) ;
#13388=CARTESIAN_POINT ( 'NONE',  ( 12.35197574246970298, 3.042005152232404086, 12.22727356655694386 ) ) ;
#13391=CARTESIAN_POINT ( 'NONE',  ( 12.61463924704883510, -0.7003689475845866763, 12.58057160030299393 ) ) ;
#13406=EDGE_LOOP ( 'NONE', ( #27074, #60718, #41051, #23880 ) ) ;
#13410=CARTESIAN_POINT ( 'NONE',  ( 18.06303038656657733, 1.966720487694622932, -12.44556484937419150 ) ) ;
#13412=DIRECTION ( 'NONE',  ( 0.000000000000000000, -1.000000000000000000, 0.000000000000000000 ) ) ;
#13417=CARTESIAN_POINT ( 'NONE',  ( 12.23612747308697379, 2.758947143663601498, -13.61512400666043376 ) ) ;
#13421=CARTESIAN_POINT ( 'NONE',  ( 18.00257402911388738, 3.100282954702140881, -13.65258486501627466 ) ) ;
#13422=CARTESIAN_POINT ( 'NONE',  ( 12.57519714614618600, 0.5812901181791684246, -13.88363587338389493 ) ) ;
#13424=CARTESIAN_POINT ( 'NONE',  ( 17.88292281824755747, -1.943028894393611372, -13.77656085492286486 ) ) ;
#13431=CARTESIAN_POINT ( 'NONE',  ( 18.06505946208161362, 2.138585121884149398, -13.74350169411782652 ) ) ;
#13451=CARTESIAN_POINT ( 'NONE',  ( 18.13206058706451174, -2.916601882134804313, -12.25780480496326419 ) ) ;
#13459=CARTESIAN_POINT ( 'NONE',  ( 12.80505043854143388, 3.248109929747637015, -13.61799478206225444 ) ) ;
#13460=CARTESIAN_POINT ( 'NONE',  ( 12.15420371307391356, 2.840396063362191192, -13.70885132993087652 ) ) ;
#13465=CARTESIAN_POINT ( 'NONE',  ( 17.97798355280614047, -0.5935699150349393882, 13.98741755999925118 ) ) ;
#13472=CARTESIAN_POINT ( 'NONE',  ( 12.18791262562190525, -2.399397798184976782, 13.69429647073317113 ) ) ;
#13483=CARTESIAN_POINT ( 'NONE',  ( 18.14024703743437072, 0.2197131112048714974, 12.69744725510431493 ) ) ;
#13484=CARTESIAN_POINT ( 'NONE',  ( 12.18394763204575248, -0.08111188042542251397, 12.69973954613695177 ) ) ;
#13488=CARTESIAN_POINT ( 'NONE',  ( 12.15805955563557461, -2.854826764565363106, -12.27308055912475204 ) ) ;
#13493=CARTESIAN_POINT ( 'NONE',  ( 5.699996624164000103, -12.50864642754000045, -2.924703664565999617 ) ) ;
#13496=EDGE_LOOP ( 'NONE', ( #46532, #45250, #61999, #10490 ) ) ;
#13499=CARTESIAN_POINT ( 'NONE',  ( 12.26373771493048181, -0.3125877143166542749, -12.69482668528969604 ) ) ;
#13516=CARTESIAN_POINT ( 'NONE',  ( 18.18333308066189247, 0.3651687365794590856, -13.99525266148724079 ) ) ;
#13523=CARTESIAN_POINT ( 'NONE',  ( 18.16726790532722191, -2.625885335051481029, 12.42137433334730723 ) ) ;
#13529=CARTESIAN_POINT ( 'NONE',  ( 12.61470515270720405, -1.811791595467374671, 13.88227300399886666 ) ) ;
#13537=CARTESIAN_POINT ( 'NONE',  ( 12.37769783401832768, 0.4561791668615491901, -13.88992602861184089 ) ) ;
#13538=CARTESIAN_POINT ( 'NONE',  ( 18.11306383842994450, -2.218305400803588512, 12.51277866499342650 ) ) ;
#13562=CARTESIAN_POINT ( 'NONE',  ( 18.18883553772844408, -0.3494793053307401753, 12.59515668824706580 ) ) ;
#13566=ORIENTED_EDGE ( 'NONE', *, *, #57395, .T. ) ;
#13568=CARTESIAN_POINT ( 'NONE',  ( 18.24660850951283919, 2.298559566806791299, 13.81002375772540880 ) ) ;
#13580=CARTESIAN_POINT ( 'NONE',  ( 17.97915611674150327, -3.110288500502089715, -13.65013405122915913 ) ) ;
#13603=CARTESIAN_POINT ( 'NONE',  ( 12.23131043852896305, 2.748092942712452746, -12.39032383288960482 ) ) ;
#13610=CARTESIAN_POINT ( 'NONE',  ( 17.92010247869879791, 0.6380582630082767270, 13.98550026811474467 ) ) ;
#13612=CARTESIAN_POINT ( 'NONE',  ( 12.17424305300937526, -2.124765750614182824, -12.41957393385126807 ) ) ;
#13618=CARTESIAN_POINT ( 'NONE',  ( 12.33367687689871062, -2.910531109056639920, -13.57771726184491712 ) ) ;
#13620=FACE_OUTER_BOUND ( 'NONE', #20535, .T. ) ;
#13626=CARTESIAN_POINT ( 'NONE',  ( 18.11165249899354635, 2.784436927422415664, 13.60895423188022058 ) ) ;
#13629=CARTESIAN_POINT ( 'NONE',  ( 17.93835418254524328, 2.006228213506225710, 12.55298903047910208 ) ) ;
#13634=ORIENTED_EDGE ( 'NONE', *, *, #8445, .T. ) ;
#13635=CARTESIAN_POINT ( 'NONE',  ( 12.72249460523640963, -1.880133632676047384, 12.57461455596142663 ) ) ;
#13640=CARTESIAN_POINT ( 'NONE',  ( 12.21006921427117398, 0.1916424759571752623, 12.69805926625132209 ) ) ;
#13643=CARTESIAN_POINT ( 'NONE',  ( 12.75302363333805644, 1.877081947669209328, 12.57507557223850903 ) ) ;
#13644=ORIENTED_EDGE ( 'NONE', *, *, #43008, .T. ) ;
#13656=CARTESIAN_POINT ( 'NONE',  ( 18.06967961652323496, -0.3547743934310131353, -12.69333341030272067 ) ) ;
#13658=CARTESIAN_POINT ( 'NONE',  ( 18.07075314650775155, -2.853223032316301033, 13.59217294861099035 ) ) ;
#13660=CARTESIAN_POINT ( 'NONE',  ( 12.32491409494626211, -3.065531103753984077, 13.66026219579215351 ) ) ;
#13666=EDGE_CURVE ( 'NONE', #20140, #63182, #35917, .T. ) ;
#13670=CARTESIAN_POINT ( 'NONE',  ( 17.86532676363442107, -0.5429298016068462296, 13.88573085157524112 ) ) ;
#13672=VERTEX_POINT ( 'NONE', #51495 ) ;
#13674=CARTESIAN_POINT ( 'NONE',  ( 21.54999911806000057, 1.172395514003999961E-13, -2.486899575159999765E-14 ) ) ;
#13682=CARTESIAN_POINT ( 'NONE',  ( 12.18526316314726365, -2.581188759560296919, 12.43231204081571661 ) ) ;
#13685=ORIENTED_EDGE ( 'NONE', *, *, #33147, .T. ) ;
#13686=CARTESIAN_POINT ( 'NONE',  ( 17.81260085050724129, -3.200899519495056023, 13.62917211583034671 ) ) ;
#13687=CARTESIAN_POINT ( 'NONE',  ( 17.71839800377850338, 3.104623491297676452, -13.52646211264892706 ) ) ;
#13698=CARTESIAN_POINT ( 'NONE',  ( 18.27397540914052598, -0.09367178904474234014, -12.59965724591066660 ) ) ;
#13702=ORIENTED_EDGE ( 'NONE', *, *, #58517, .F. ) ;
#13710=CARTESIAN_POINT ( 'NONE',  ( 12.32516769934781209, 3.065409648700728074, 13.66028300215598890 ) ) ;
#13713=CARTESIAN_POINT ( 'NONE',  ( 12.24298814206631825, -0.2740984088879005465, -12.69603503204707096 ) ) ;
#13714=CARTESIAN_POINT ( 'NONE',  ( 12.14435534536354844, 0.3008963210924944232, 13.99677033988233354 ) ) ;
#13719=FACE_OUTER_BOUND ( 'NONE', #58914, .T. ) ;
#13724=CARTESIAN_POINT ( 'NONE',  ( 12.48183889708581695, 3.124385432114247685, 12.20648365185189377 ) ) ;
#13730=CARTESIAN_POINT ( 'NONE',  ( 17.55505043854143565, 3.125000000000000000, -25.00000000000000000 ) ) ;
#13731=CARTESIAN_POINT ( 'NONE',  ( 12.21194436378594972, 2.301855881723279040, 12.49553541603377838 ) ) ;
#13738=CARTESIAN_POINT ( 'NONE',  ( 7.100000000000000533, -13.04986661130000059, 1.811520473896000016 ) ) ;
#13739=CARTESIAN_POINT ( 'NONE',  ( 12.39223264510076561, 2.969378069107369011, 13.56257646889492818 ) ) ;
#13748=CARTESIAN_POINT ( 'NONE',  ( 18.07990072965510464, 1.983698511703259948, -12.44287000959587175 ) ) ;
#13751=CARTESIAN_POINT ( 'NONE',  ( 12.29688428856856852, 2.864514977098406856, -13.58937626179519143 ) ) ;
#13765=CARTESIAN_POINT ( 'NONE',  ( 17.88876975676773640, 1.869670916578580533, -13.87459417580158316 ) ) ;
#13773=CARTESIAN_POINT ( 'NONE',  ( 18.05195279581856127, 0.3792326063240399336, -12.69238213822339567 ) ) ;
#13778=CARTESIAN_POINT ( 'NONE',  ( 17.59614113504008159, -3.125000000000000888, -13.52078631348664217 ) ) ;
#13786=CARTESIAN_POINT ( 'NONE',  ( 17.65794081825379180, -1.883184384514173360, -12.57407373858317534 ) ) ;
#13791=VERTEX_POINT ( 'NONE', #31554 ) ;
#13793=CIRCLE ( 'NONE', #65115, 2.000000000000000444 ) ;
#13796=CARTESIAN_POINT ( 'NONE',  ( 12.11714050632479100, 2.287289704013984792, -13.81189467606769306 ) ) ;
#13800=CARTESIAN_POINT ( 'NONE',  ( 17.55505043854147118, -3.125000000000000000, -12.28373071562070074 ) ) ;
#13821=CARTESIAN_POINT ( 'NONE',  ( 18.11574795581002562, 0.2761699508452412077, 12.69595998167824114 ) ) ;
#13827=EDGE_CURVE ( 'NONE', #46698, #35849, #14104, .T. ) ;
#13833=CARTESIAN_POINT ( 'NONE',  ( 12.72146951531671633, 0.7145943380091474006, -12.57972004139935152 ) ) ;
#13846=VECTOR ( 'NONE', #46382, 1000.000000000000000 ) ;
#13849=ADVANCED_FACE ( 'NONE', ( #62999 ), #15128, .F. ) ;
#13852=CARTESIAN_POINT ( 'NONE',  ( 18.13088524799817947, 0.4443071882833261599, -13.99296005428181466 ) ) ;
#13858=CARTESIAN_POINT ( 'NONE',  ( 18.06426550930201458, -2.862542805000389823, 12.35969564690757316 ) ) ;
#13859=ORIENTED_EDGE ( 'NONE', *, *, #8835, .F. ) ;
#13873=CARTESIAN_POINT ( 'NONE',  ( 12.19004662364084091, -0.1118032413084504434, -13.89939982891984904 ) ) ;
#13874=CARTESIAN_POINT ( 'NONE',  ( 18.16983287387829549, -2.613005487247105574, 12.42455217891717467 ) ) ;
#13875=EDGE_LOOP ( 'NONE', ( #30473, #2066, #68028, #37823 ) ) ;
#13900=CARTESIAN_POINT ( 'NONE',  ( 18.12277215905344363, -0.4475098806653837746, 12.59205372277267898 ) ) ;
#13906=CARTESIAN_POINT ( 'NONE',  ( 18.24298441323063003, 2.287290078788467351, 13.81189461436434307 ) ) ;
#13918=CARTESIAN_POINT ( 'NONE',  ( 18.13115538416117900, -2.961380457613815409, -13.68321312766444997 ) ) ;
#13941=CARTESIAN_POINT ( 'NONE',  ( 12.38992078601020630, 2.032669449810693862, -12.54828005421690307 ) ) ;
#13951=CARTESIAN_POINT ( 'NONE',  ( 12.08128888832030512, -2.529854562579159527, -12.34343511423995743 ) ) ;
#13957=CARTESIAN_POINT ( 'NONE',  ( 12.54499921992993094, -1.931577877770960239, -13.77766407476416077 ) ) ;
#13964=CARTESIAN_POINT ( 'NONE',  ( 18.08141525684210649, 2.837131573407952523, 13.59610056795573740 ) ) ;
#13966=CARTESIAN_POINT ( 'NONE',  ( 4.599999999999999645, 0.000000000000000000, 0.000000000000000000 ) ) ;
#13968=CARTESIAN_POINT ( 'NONE',  ( 17.75808086271924324, 3.091459143609192495, 12.29388367502514257 ) ) ;
#13977=CARTESIAN_POINT ( 'NONE',  ( 12.42174667009962086, -2.006228232438482362, 12.55302761990816052 ) ) ;
#13983=CARTESIAN_POINT ( 'NONE',  ( 12.19004707749462924, -0.1118057330073182615, 12.69934308675516377 ) ) ;
#13986=CARTESIAN_POINT ( 'NONE',  ( 12.20003344249112409, 2.341920628070001342, 12.48700265052702107 ) ) ;
#13998=CARTESIAN_POINT ( 'NONE',  ( 17.59562594683476178, -0.6249999999999998890, -12.67928921589118829 ) ) ;
#14028=ORIENTED_EDGE ( 'NONE', *, *, #33873, .F. ) ;
#14029=CARTESIAN_POINT ( 'NONE',  ( 18.17163261364645876, -2.902690589304653290, 13.69579465584391542 ) ) ;
#14040=CARTESIAN_POINT ( 'NONE',  ( 18.22023691865392081, 0.2863297863804545318, -12.59675086341328232 ) ) ;
#14045=AXIS2_PLACEMENT_3D ( 'NONE', #19625, #30132, #18939 ) ;
#14051=CARTESIAN_POINT ( 'NONE',  ( 12.10457356466339895, 2.707610175640967842, 13.73569711802853099 ) ) ;
#14054=CARTESIAN_POINT ( 'NONE',  ( 12.49451986919435953, 0.5425047575455477222, -12.68440192077494011 ) ) ;
#14062=PLANE ( 'NONE',  #17141 ) ;
#14069=CARTESIAN_POINT ( 'NONE',  ( 12.56995090575619578, 3.160862399908558551, 12.19708787818174400 ) ) ;
#14092=CARTESIAN_POINT ( 'NONE',  ( 17.63759097916651442, 3.119868145639166812, -12.28530842955782099 ) ) ;
#14096=CARTESIAN_POINT ( 'NONE',  ( 12.24478949867863165, 2.777190625918491307, -13.61075457645665665 ) ) ;
#14102=CARTESIAN_POINT ( 'NONE',  ( 12.54953656384602390, 0.6834693007276639865, -13.98330741474946315 ) ) ;
#14104=LINE ( 'NONE', #24927, #62210 ) ;
#14111=CARTESIAN_POINT ( 'NONE',  ( 18.27457017588618271, 2.425781798817260082, -13.78826143416240768 ) ) ;
#14129=CARTESIAN_POINT ( 'NONE',  ( 17.88942345255914645, -3.118753088769716797, -12.20792418036210591 ) ) ;
#14132=ADVANCED_FACE ( 'NONE', ( #64720 ), #30929, .F. ) ;
#14139=CARTESIAN_POINT ( 'NONE',  ( 12.54773036592020574, 3.200672309338199462, -13.62922281487128728 ) ) ;
#14142=CARTESIAN_POINT ( 'NONE',  ( 18.27393099755800421, 0.09542514088231059122, 13.99967976774382272 ) ) ;
#14151=CARTESIAN_POINT ( 'NONE',  ( 12.19221373221769156, -2.622703612849026644, 13.64666901003217703 ) ) ;
#14154=EDGE_CURVE ( 'NONE', #57647, #58563, #30501, .T. ) ;
#14157=LINE ( 'NONE', #26013, #41779 ) ;
#14161=EDGE_CURVE ( 'NONE', #62789, #33960, #7512, .T. ) ;
#14165=CARTESIAN_POINT ( 'NONE',  ( 12.80505043854143388, 3.207098164520926886, 13.58558594083658910 ) ) ;
#14167=LINE ( 'NONE', #45974, #20736 ) ;
#14174=CARTESIAN_POINT ( 'NONE',  ( 12.68606859785048258, 0.7096370184368562262, -12.58000072970462924 ) ) ;
#14175=CARTESIAN_POINT ( 'NONE',  ( 12.21429833793744812, -2.704300905630751206, -12.40162098802949942 ) ) ;
#14177=CARTESIAN_POINT ( 'NONE',  ( 17.55505043854144276, 0.7302158263239086899, 13.98094363220831049 ) ) ;
#14193=CARTESIAN_POINT ( 'NONE',  ( 18.05935379312179734, -0.5247499651446981828, -13.99016470477802443 ) ) ;
#14198=DIRECTION ( 'NONE',  ( 0.000000000000000000, 0.9553735099700839672, -0.2954005017724949389 ) ) ;
#14205=CARTESIAN_POINT ( 'NONE',  ( 12.20052776709553299, -2.340020608624143517, -13.70605490525081827 ) ) ;
#14210=CARTESIAN_POINT ( 'NONE',  ( 17.81163219999022829, 0.5699871459077878733, -13.88426688812565324 ) ) ;
#14215=CARTESIAN_POINT ( 'NONE',  ( 12.19008165514798847, 0.1119984579798066066, -13.89939774083725688 ) ) ;
#14216=CARTESIAN_POINT ( 'NONE',  ( 17.92245882712031246, -1.993980507605455310, 12.55520606452098775 ) ) ;
#14223=CARTESIAN_POINT ( 'NONE',  ( 18.10163077481653104, 2.185641740716382841, 13.73537224937479451 ) ) ;
#14228=CARTESIAN_POINT ( 'NONE',  ( 12.80505043854146940, -1.875000000000000444, -25.00000000000000000 ) ) ;
#14232=CARTESIAN_POINT ( 'NONE',  ( 12.80505043854144276, 0.6249999999999994449, 13.88107975066923316 ) ) ;
#14234=CARTESIAN_POINT ( 'NONE',  ( 5.500000000000000000, -9.503509090790997936E-14, 3.419486915844999993E-14 ) ) ;
#14242=CARTESIAN_POINT ( 'NONE',  ( 18.08473038518645382, 0.4912829912815083744, 12.59042165808839897 ) ) ;
#14284=CARTESIAN_POINT ( 'NONE',  ( 12.17998194132759870, 2.482033040872618113, -12.45578191469033236 ) ) ;
#14288=ORIENTED_EDGE ( 'NONE', *, *, #6731, .F. ) ;
#14293=CARTESIAN_POINT ( 'NONE',  ( 12.68485691281878225, -1.770762539963705695, -12.47495103249912241 ) ) ;
#14300=CARTESIAN_POINT ( 'NONE',  ( 12.68504826104526551, -3.238474326485687449, -13.62029029943391478 ) ) ;
#14310=CARTESIAN_POINT ( 'NONE',  ( 18.15125492461094936, 2.687770500147851571, 13.63179079428598151 ) ) ;
#14317=AXIS2_PLACEMENT_3D ( 'NONE', #6682, #60182, #12288 ) ;
#14320=CARTESIAN_POINT ( 'NONE',  ( 12.18833199825129654, -2.603395164171334653, 12.42692484756187810 ) ) ;
#14328=CARTESIAN_POINT ( 'NONE',  ( 12.58477481432937672, 0.5849872192492359124, 12.68185863724641216 ) ) ;
#14336=PLANE ( 'NONE',  #1660 ) ;
#14341=CARTESIAN_POINT ( 'NONE',  ( 18.08681263786920468, -0.3285869676541873230, -12.69428288850341957 ) ) ;
#14346=CARTESIAN_POINT ( 'NONE',  ( 12.63927634677111733, -3.229167277941582093, 13.62249984660984303 ) ) ;
#14375=CARTESIAN_POINT ( 'NONE',  ( 17.59651827076220343, -1.876037923068245794, 13.78616466676677987 ) ) ;
#14386=CARTESIAN_POINT ( 'NONE',  ( 18.27044763842724251, 0.1172743548790672746, -12.59945959730644205 ) ) ;
#14396=CARTESIAN_POINT ( 'NONE',  ( 17.77313190797694986, 1.794191980291843347, 12.47160287655520428 ) ) ;
#14399=CARTESIAN_POINT ( 'NONE',  ( 12.21346991607042298, 2.095738610141147706, 13.84225324474580354 ) ) ;
#14403=CARTESIAN_POINT ( 'NONE',  ( 12.43800415093376621, 0.5060493093079869720, -12.68643001349182597 ) ) ;
#14404=CARTESIAN_POINT ( 'NONE',  ( 12.08006676141316049, -0.02431279293010735545, 13.99999914078079932 ) ) ;
#14418=DIRECTION ( 'NONE',  ( 1.000000000000000000, 0.000000000000000000, 0.000000000000000000 ) ) ;
#14422=CARTESIAN_POINT ( 'NONE',  ( 12.27188044047571402, 2.173264662094914090, 12.52171693736594271 ) ) ;
#14430=CARTESIAN_POINT ( 'NONE',  ( 12.40004937879930047, 2.976133613074172679, 13.56081502232355795 ) ) ;
#14437=CARTESIAN_POINT ( 'NONE',  ( 17.55505043854143565, 1.760845406083387354, -12.47635457398815362 ) ) ;
#14441=CARTESIAN_POINT ( 'NONE',  ( 12.19818565359414819, 2.649653948234573786, -13.64057837091597669 ) ) ;
#14443=CARTESIAN_POINT ( 'NONE',  ( 12.80505043854146940, -1.760910691117821614, -12.47634535983622683 ) ) ;
#14445=EDGE_CURVE ( 'NONE', #28970, #15559, #14652, .T. ) ;
#14446=CARTESIAN_POINT ( 'NONE',  ( 12.14438218221664378, 0.3016537271415140609, -13.99676704218776813 ) ) ;
#14455=CARTESIAN_POINT ( 'NONE',  ( 18.06209397514826165, 1.995989992690354153, -13.85698731868970590 ) ) ;
#14469=ORIENTED_EDGE ( 'NONE', *, *, #47992, .F. ) ;
#14475=CARTESIAN_POINT ( 'NONE',  ( 18.15975285618101154, -2.341680162859185010, -12.48703895936062480 ) ) ;
#14485=CARTESIAN_POINT ( 'NONE',  ( 12.68593947922891552, 3.238585582162118115, -13.62026383368923454 ) ) ;
#14486=CARTESIAN_POINT ( 'NONE',  ( 18.17070062201315039, 0.3858260082455215456, 13.99468631105251859 ) ) ;
#14505=DIRECTION ( 'NONE',  ( -0.7071058580588949205, 0.7071077043129949669, -4.007463041294969893E-09 ) ) ;
#14516=FACE_OUTER_BOUND ( 'NONE', #27415, .T. ) ;
#14518=ORIENTED_EDGE ( 'NONE', *, *, #25818, .F. ) ;
#14519=CARTESIAN_POINT ( 'NONE',  ( 12.51941477301789973, -0.5560043133243457447, -12.68361349193355103 ) ) ;
#14520=CARTESIAN_POINT ( 'NONE',  ( 12.18869345026739737, -2.603827955476766043, -12.42676989087486206 ) ) ;
#14541=CARTESIAN_POINT ( 'NONE',  ( 4.649999478197480052, 2.033928581112999763E-13, -2.806643806251999915E-13 ) ) ;
#14547=CARTESIAN_POINT ( 'NONE',  ( 12.22895947710367359, -2.742405092547198553, -13.61899867098736472 ) ) ;
#14557=DIRECTION ( 'NONE',  ( 1.000000000000000000, 0.000000000000000000, 0.000000000000000000 ) ) ;
#14559=CARTESIAN_POINT ( 'NONE',  ( 12.58447130036695150, -0.5851376999905949505, -13.88342059653408533 ) ) ;
#14560=CARTESIAN_POINT ( 'NONE',  ( 18.17889124921894961, -2.543048589645668489, 12.44148151073661523 ) ) ;
#14577=DIRECTION ( 'NONE',  ( -0.000000000000000000, -0.000000000000000000, 1.000000000000000000 ) ) ;
#14579=CARTESIAN_POINT ( 'NONE',  ( 12.70933660601936133, 3.243304671732729183, -13.61914346456424951 ) ) ;
#14583=CARTESIAN_POINT ( 'NONE',  ( 17.56702613447739481, 0.7192913015564668111, 12.57945229205062709 ) ) ;
#14590=FACE_BOUND ( 'NONE', #27199, .T. ) ;
#14594=AXIS2_PLACEMENT_3D ( 'NONE', #23164, #55331, #50425 ) ;
#14599=CARTESIAN_POINT ( 'NONE',  ( 17.92356899877518472, -1.853474162636749467, 12.46298541230695456 ) ) ;
#14622=CARTESIAN_POINT ( 'NONE',  ( 12.29460735697731444, 2.139198256859471403, -12.52837235904283908 ) ) ;
#14625=ORIENTED_EDGE ( 'NONE', *, *, #19134, .F. ) ;
#14630=CARTESIAN_POINT ( 'NONE',  ( 12.70218814580029232, -3.116819717849789839, -12.28621950321772616 ) ) ;
#14637=CARTESIAN_POINT ( 'NONE',  ( 12.31340688242393355, -2.113974262928781656, -13.74774419251637880 ) ) ;
#14643=B_SPLINE_CURVE_WITH_KNOTS ( 'NONE', 3,
 ( #56325, #8429, #39554, #34665 ),
 .UNSPECIFIED., .F., .F.,
 ( 4, 4 ),
 ( 0.000000000000000000, 1.000000000000000000 ),
 .UNSPECIFIED. ) ;
#14645=CARTESIAN_POINT ( 'NONE',  ( 12.80505043854144276, 0.7302158263239216796, -13.98094363220830871 ) ) ;
#14650=CARTESIAN_POINT ( 'NONE',  ( 18.17997390458972262, 2.522451123844924759, 12.44632513475228208 ) ) ;
#14652=B_SPLINE_CURVE_WITH_KNOTS ( 'NONE', 3,
 ( #22957, #23999, #39053, #34511 ),
 .UNSPECIFIED., .F., .F.,
 ( 4, 4 ),
 ( 0.000000000000000000, 1.000000000000000000 ),
 .UNSPECIFIED. ) ;
#14654=VECTOR ( 'NONE', #7428, 1000.000000000000000 ) ;
#14657=CARTESIAN_POINT ( 'NONE',  ( 12.39106450428433703, -2.968342857027795656, 12.33004038639663413 ) ) ;
#14664=CARTESIAN_POINT ( 'NONE',  ( 12.49249186488743035, 0.5416145769730058568, 12.68445494689096087 ) ) ;
#14670=DIRECTION ( 'NONE',  ( 0.000000000000000000, 0.000000000000000000, -1.000000000000000000 ) ) ;
#14680=CARTESIAN_POINT ( 'NONE',  ( 18.18005043824376443, -1.329523415562850021E-10, -12.70000000088146486 ) ) ;
#14685=CARTESIAN_POINT ( 'NONE',  ( 17.96899650538952997, -2.968713945236787666, -13.56275387600713067 ) ) ;
#14709=CARTESIAN_POINT ( 'NONE',  ( 17.97988082628308959, -1.926206752467417127, 13.86685907515736638 ) ) ;
#14723=CARTESIAN_POINT ( 'NONE',  ( 18.24522866045827740, 0.2205548374446872906, -12.59807454672508165 ) ) ;
#14726=CARTESIAN_POINT ( 'NONE',  ( 12.80505043854146940, -1.798896937388929640, 12.50938852236267529 ) ) ;
#14733=CARTESIAN_POINT ( 'NONE',  ( 17.81303847540707963, 1.807878129530184896, 12.46962684194071791 ) ) ;
#14734=CARTESIAN_POINT ( 'NONE',  ( 12.11816748453748538, 2.752694035764603253, 13.72673318081622895 ) ) ;
#14737=CARTESIAN_POINT ( 'NONE',  ( 12.18105077442090334, -0.04081512033874237777, -12.69993297814843558 ) ) ;
#14740=CARTESIAN_POINT ( 'NONE',  ( 12.48133867187399915, -1.836397482308033346, 12.46545911376216687 ) ) ;
#14750=CARTESIAN_POINT ( 'NONE',  ( 12.08198123077151287, 2.425144973324804276, 12.36441727636090704 ) ) ;
#14762=CARTESIAN_POINT ( 'NONE',  ( 12.39790242569448075, -0.4743817213088754592, 12.68807659218376571 ) ) ;
#14769=CARTESIAN_POINT ( 'NONE',  ( 12.55463174185022091, -3.072731264995193001, 13.53516186994627013 ) ) ;
#14770=CARTESIAN_POINT ( 'NONE',  ( 12.24260983038582395, 2.772891244655266263, 13.61173698548887501 ) ) ;
#14777=CARTESIAN_POINT ( 'NONE',  ( 18.27458182272986775, 2.390008000232564545, -12.37125705564431577 ) ) ;
#14779=CARTESIAN_POINT ( 'NONE',  ( 18.11161644830704986, 2.784507902010840308, 12.38071508488312844 ) ) ;
#14780=CARTESIAN_POINT ( 'NONE',  ( 5.699999545467999695, -12.03770622561999915, 3.722046322334000124 ) ) ;
#14784=CARTESIAN_POINT ( 'NONE',  ( 12.44248702983404442, 0.6327954766588935742, -13.98569611075749464 ) ) ;
#14787=CARTESIAN_POINT ( 'NONE',  ( 18.14123990138214992, 2.282196115480399801, 12.49965818828386155 ) ) ;
#14789=DIRECTION ( 'NONE',  ( -1.000000000000000000, 0.000000000000000000, 0.000000000000000000 ) ) ;
#14793=CARTESIAN_POINT ( 'NONE',  ( 18.07784313215196903, 3.023931901684152823, -13.66952493495815801 ) ) ;
#14799=CARTESIAN_POINT ( 'NONE',  ( 12.80505043854146940, -3.125000000000000000, -25.00000000000000000 ) ) ;
#14812=CARTESIAN_POINT ( 'NONE',  ( 17.92180752009631561, -1.993817408553323789, -12.55519104945816622 ) ) ;
#14822=CARTESIAN_POINT ( 'NONE',  ( 18.14440149583522199, 0.4259565731506576580, 13.99353270933017335 ) ) ;
#14847=ADVANCED_FACE ( 'NONE', ( #41715 ), #4301, .F. ) ;
#14856=CARTESIAN_POINT ( 'NONE',  ( 12.33502333850778676, -0.4124490627810476484, -12.69099791225217366 ) ) ;
#14857=CARTESIAN_POINT ( 'NONE',  ( 12.20626853909968546, -2.679149498323847300, -12.40801937966050161 ) ) ;
#14869=EDGE_LOOP ( 'NONE', ( #26643, #63699, #15990, #2305 ) ) ;
#14884=CARTESIAN_POINT ( 'NONE',  ( 12.20843209901191884, -2.686266380820965693, -13.63213492619998135 ) ) ;
#14893=CARTESIAN_POINT ( 'NONE',  ( 7.100000000000000533, 0.000000000000000000, 0.000000000000000000 ) ) ;
#14895=FACE_OUTER_BOUND ( 'NONE', #65505, .T. ) ;
#14897=CARTESIAN_POINT ( 'NONE',  ( 12.32706758141025993, 2.902815230603663199, 13.57967619870183640 ) ) ;
#14905=CARTESIAN_POINT ( 'NONE',  ( 12.33243540359735313, 2.090896859126741614, -13.75176201293517586 ) ) ;
#14908=DIRECTION ( 'NONE',  ( -0.000000000000000000, -0.000000000000000000, 1.000000000000000000 ) ) ;
#14910=ORIENTED_EDGE ( 'NONE', *, *, #14161, .F. ) ;
#14919=CARTESIAN_POINT ( 'NONE',  ( 17.55505043854147118, -3.125000000000000000, -13.52078605991414761 ) ) ;
#14921=CARTESIAN_POINT ( 'NONE',  ( 18.02437627528317421, 0.5483668826291584475, 12.58806376549905082 ) ) ;
#14927=CARTESIAN_POINT ( 'NONE',  ( 17.65063036598052548, 3.242172222319704034, 13.61940987276824622 ) ) ;
#14935=ORIENTED_EDGE ( 'NONE', *, *, #57884, .F. ) ;
#14936=CARTESIAN_POINT ( 'NONE',  ( 17.55505043854143565, 1.875000000000000000, 13.78627172894481667 ) ) ;
#14945=AXIS2_PLACEMENT_3D ( 'NONE', #6934, #49589, #1696 ) ;
#14959=CARTESIAN_POINT ( 'NONE',  ( 12.54473519888576050, 3.068232154748442575, -12.30085162971233537 ) ) ;
#14967=CARTESIAN_POINT ( 'NONE',  ( 12.58060354176266493, -1.796139714418076849, -12.47132288122299570 ) ) ;
#14973=CARTESIAN_POINT ( 'NONE',  ( 12.51733672169667422, -1.945066915100360783, -13.77556489992940847 ) ) ;
#14976=CARTESIAN_POINT ( 'NONE',  ( 17.67439832720113557, -3.190335184669550461, 12.18941280901077917 ) ) ;
#14977=ORIENTED_EDGE ( 'NONE', *, *, #56578, .F. ) ;
#14985=CARTESIAN_POINT ( 'NONE',  ( 17.92152980461522560, 3.006687145500352543, 12.31895938800958490 ) ) ;
#14990=ADVANCED_FACE ( 'NONE', ( #60467 ), #17380, .T. ) ;
#14992=CARTESIAN_POINT ( 'NONE',  ( 12.60202002655574205, -3.091459147703856214, 12.29390037902082078 ) ) ;
#15001=CARTESIAN_POINT ( 'NONE',  ( 12.69240093715870010, -0.6148490057825437560, 12.67995724530759816 ) ) ;
#15003=CARTESIAN_POINT ( 'NONE',  ( 5.619729929257407441, -12.11456185543947228, -3.745214083256774629 ) ) ;
#15010=LINE ( 'NONE', #6496, #10585 ) ;
#15021=CARTESIAN_POINT ( 'NONE',  ( 18.15932194375241338, -2.660757699944335197, 13.63806486313331945 ) ) ;
#15024=CARTESIAN_POINT ( 'NONE',  ( 18.09841665128862331, -2.190490658128016577, -13.73421521058128114 ) ) ;
#15047=CARTESIAN_POINT ( 'NONE',  ( 17.88876225154221089, 3.028809290940018162, -13.54697662062381802 ) ) ;
#15055=EDGE_CURVE ( 'NONE', #61133, #49162, #32129, .T. ) ;
#15061=CARTESIAN_POINT ( 'NONE',  ( 18.28003407448208151, 0.02395120399003647718, -12.59999907117299855 ) ) ;
#15064=DIRECTION ( 'NONE',  ( 1.000000000000000000, 0.000000000000000000, 0.000000000000000000 ) ) ;
#15071=CARTESIAN_POINT ( 'NONE',  ( 12.30764200008706766, 3.049303773002893791, 13.66388724637008778 ) ) ;
#15073=CARTESIAN_POINT ( 'NONE',  ( 12.31853785136292956, -0.3923495137057630422, -12.69184251825842757 ) ) ;
#15074=CARTESIAN_POINT ( 'NONE',  ( 12.19581923677613489, -0.3960277493246582847, 13.99440111282555499 ) ) ;
#15085=B_SPLINE_SURFACE_WITH_KNOTS ( 'NONE', 1, 3, ( 
 ( #854, #10307, #43511, #48401, #32674, #69036, #32338, #53647, #5409, #21148, #33016, #42475, #54330, #6431, #21480, #63782, #15894, #508, #53987, #64808, #27426, #16919, #53306, #5743, #16237, #43854, #21823, #52964, #10648, #38250, #42815, #26745, #5060, #43156, #49091, #164, #22511, #64462, #16585, #18664, #60277, #45240, #50137, #61310, #12732, #44897, #34061, #39298, #44563, #39996, #1543, #2576, #65508, #54683, #12034, #2242, #60966, #66546, #45584, #65856, #13431, #33716, #50474, #6781, #55377, #66200, #18322, #22861, #7830, #39645, #34752, #56061, #23556, #50823, #13081, #38960, #23904, #34411, #44213, #55728, #17635, #29165, #12382, #28119, #38602, #8172, #49431, #29521, #33368, #2918 ),
 ( #24247, #55033, #17277, #7133, #59923, #28471, #49786, #1896, #23216, #17979, #60621, #7472, #28826, #9189, #57775, #46614, #36456, #8514, #29862, #51170, #67229, #3265, #3941, #14793, #24597, #19002, #19344, #9885, #20378, #4289, #61998, #25970, #9532, #41702, #30195, #40666, #61652, #66890, #36112, #35775, #67570, #56411, #19696, #57089, #30530, #14111, #35435, #45917, #56761, #8858, #63006, #30877, #40329, #52189, #51843, #62673, #51501, #41016, #62338, #3598, #24934, #15135, #46268, #31227, #52534, #14455, #25279, #67919, #20035, #41364, #25625, #57426, #46953, #68257, #4631, #13765, #35099, #5153, #28478, #65163, #49795, #12738, #6787, #66206, #60974, #38259, #28125, #7140, #39652, #17283 ) ),
 .UNSPECIFIED., .F., .F., .F.,
 ( 2, 2 ),
 ( 4, 2, 2, 2, 2, 2, 2, 2, 2, 2, 2, 2, 2, 2, 2, 2, 2, 2, 2, 2, 2, 2, 2, 2, 2, 2, 2, 2, 2, 2, 2, 2, 2, 2, 2, 2, 2, 2, 2, 2, 2, 2, 2, 2, 4 ),
 ( 0.000000000000000000, 1.000000000000000000 ),
 ( 0.000000000000000000, 7.142752612018008851E-05, 0.0001428550522403601770, 0.0002142825783605402791, 0.0002857101044807203540, 0.0003214238675408103915, 0.0003571376306009004832, 0.0003928513936609905207, 0.0004285651567210805582, 0.0004999926828412606331, 0.0005357064459013507248, 0.0005714202089614407081, 0.0006071339720215306913, 0.0006428477350816207830, 0.0007142752612018009664, 0.0007857027873219810414, 0.0008214165503820710246, 0.0008571303134421611163, 0.0009285578395623411913, 0.0009999853656825212662, 0.001071412891802701450, 0.001142840417922881416, 0.001214267944043061383, 0.001285695470163241566, 0.001321409233223331658, 0.001357122996283421749, 0.001428550522403601933, 0.001499978048523782116, 0.001535691811583872208, 0.001571405574643962083, 0.001607119337704051958, 0.001642833100764142049, 0.001714260626884322233, 0.001749974389944412324, 0.001785688153004502416, 0.001821401916064592508, 0.001857115679124682383, 0.001928543205244862349, 0.001964256968304952441, 0.001999970731365042532, 0.002035684494425132624, 0.002071398257485222716, 0.002142825783605402899, 0.002214253309725583083, 0.002285680835845762832 ),
 .UNSPECIFIED. ) ;
#15086=CARTESIAN_POINT ( 'NONE',  ( 12.36861573454711127, 0.5743932053697951012, 12.58690132123599525 ) ) ;
#15090=CARTESIAN_POINT ( 'NONE',  ( 12.50259176966688379, 1.826373719304920540, 12.46693171540044531 ) ) ;
#15097=CARTESIAN_POINT ( 'NONE',  ( 12.24249432807752314, 2.226917153349847300, 12.51101585363617730 ) ) ;
#15100=CARTESIAN_POINT ( 'NONE',  ( 12.31443506033308921, -0.3873604453481457877, 12.69205253627869823 ) ) ;
#15107=CARTESIAN_POINT ( 'NONE',  ( 12.33386765766683624, -2.911124516513512894, 13.57763168322026459 ) ) ;
#15108=CARTESIAN_POINT ( 'NONE',  ( 12.19290954920418635, 2.626136293140859390, 13.64584403818151337 ) ) ;
#15118=CARTESIAN_POINT ( 'NONE',  ( 17.93339585188538976, 2.997500062648085883, -12.32163866699053401 ) ) ;
#15120=CARTESIAN_POINT ( 'NONE',  ( 18.10295792974228490, 2.800845227017174643, 12.37636719702360288 ) ) ;
#15126=CARTESIAN_POINT ( 'NONE',  ( 12.21569938124765820, 0.4259565731506669839, -13.99353270933016979 ) ) ;
#15128=CYLINDRICAL_SURFACE ( 'NONE', #43250, 1.999999999999999556 ) ;
#15133=VERTEX_POINT ( 'NONE', #28225 ) ;
#15135=CARTESIAN_POINT ( 'NONE',  ( 18.13255570286229101, 2.076448383791616781, -13.84516006853289127 ) ) ;
#15152=CARTESIAN_POINT ( 'NONE',  ( 17.97018005872497426, -2.032669421145251842, -12.54824173908127882 ) ) ;
#15155=CARTESIAN_POINT ( 'NONE',  ( 18.17512443070437200, -2.418970859208086743, -12.47009038069303521 ) ) ;
#15161=CARTESIAN_POINT ( 'NONE',  ( 12.61614725291585160, 3.223296771745986167, -13.62389115065822054 ) ) ;
#15192=DIRECTION ( 'NONE',  ( 1.000000000000000000, 0.000000000000000000, 0.000000000000000000 ) ) ;
#15195=ORIENTED_EDGE ( 'NONE', *, *, #28667, .F. ) ;
#15196=CARTESIAN_POINT ( 'NONE',  ( 12.21300000160833577, 0.2005123242923269322, -12.69787478206145259 ) ) ;
#15197=CARTESIAN_POINT ( 'NONE',  ( 12.29671722858996041, -2.864281468071980807, -12.35920955626405515 ) ) ;
#15199=CARTESIAN_POINT ( 'NONE',  ( 12.80505043854146940, -1.875000000000000444, 13.78631952119025605 ) ) ;
#15204=CARTESIAN_POINT ( 'NONE',  ( 17.55505043854144276, 0.6250000000000001110, 12.67928921589117586 ) ) ;
#15226=CARTESIAN_POINT ( 'NONE',  ( 12.80505043854146940, -1.875000000000000444, -13.78627172894481667 ) ) ;
#15228=ORIENTED_EDGE ( 'NONE', *, *, #47320, .F. ) ;
#15235=AXIS2_PLACEMENT_3D ( 'NONE', #1636, #65600, #48150 ) ;
#15239=CARTESIAN_POINT ( 'NONE',  ( 12.29585337184155946, 2.862976231886636302, 13.58970269765488048 ) ) ;
#15249=VECTOR ( 'NONE', #31032, 1000.000000000000000 ) ;
#15267=CARTESIAN_POINT ( 'NONE',  ( 17.85474174040770023, 0.6550687562476208425, 12.58296113213902245 ) ) ;
#15270=EDGE_CURVE ( 'NONE', #53716, #60760, #43689, .T. ) ;
#15275=CARTESIAN_POINT ( 'NONE',  ( 17.60315097558330777, 3.246934396132593825, 13.61827533163851101 ) ) ;
#15283=ORIENTED_EDGE ( 'NONE', *, *, #25080, .T. ) ;
#15302=CARTESIAN_POINT ( 'NONE',  ( 18.13658220607008786, 0.2292390942789236941, -13.89746050377129905 ) ) ;
#15305=AXIS2_PLACEMENT_3D ( 'NONE', #54239, #6341, #60536 ) ;
#15308=CARTESIAN_POINT ( 'NONE',  ( 12.58270105247233417, 3.084473834238323331, -12.29599965897950220 ) ) ;
#15316=CARTESIAN_POINT ( 'NONE',  ( 12.80505043854143388, 1.760845406083386688, -12.47635457398814829 ) ) ;
#15318=CARTESIAN_POINT ( 'NONE',  ( 12.19649458927093555, -2.642789655208612754, -12.41715525233005479 ) ) ;
#15322=CARTESIAN_POINT ( 'NONE',  ( 12.36790649065927283, -2.053195086250958479, -13.75808315936462023 ) ) ;
#15325=CARTESIAN_POINT ( 'NONE',  ( 18.13174941159754283, -2.917101476509666114, 12.25768593326185396 ) ) ;
#15335=CARTESIAN_POINT ( 'NONE',  ( 18.17921332558106329, 2.461874964459677795, 12.46038192087330643 ) ) ;
#15353=AXIS2_PLACEMENT_3D ( 'NONE', #68266, #43360, #6631 ) ;
#15368=CARTESIAN_POINT ( 'NONE',  ( 18.16732611103527617, -2.625479214373699133, 13.64604457671237014 ) ) ;
#15371=CARTESIAN_POINT ( 'NONE',  ( 17.98404385246625381, -2.954974373217228667, -13.56632247660221324 ) ) ;
#15375=ORIENTED_EDGE ( 'NONE', *, *, #26608, .F. ) ;
#15383=CARTESIAN_POINT ( 'NONE',  ( 18.18005043853800373, -0.02024535602757234626, 13.89999992471014245 ) ) ;
#15390=AXIS2_PLACEMENT_3D ( 'NONE', #41164, #51303, #57571 ) ;
#15397=CARTESIAN_POINT ( 'NONE',  ( 12.47602583993311498, -1.943637617989338651, 12.56471729223352085 ) ) ;
#15401=CARTESIAN_POINT ( 'NONE',  ( 18.05353730554815428, -1.987694103345771568, 13.85817950142401855 ) ) ;
#15412=CARTESIAN_POINT ( 'NONE',  ( 17.57898592363196855, -0.7189971323194248587, -12.57946912511937754 ) ) ;
#15413=CARTESIAN_POINT ( 'NONE',  ( 12.28979759248826298, 2.853877291412238559, -12.36206589979061832 ) ) ;
#15416=ORIENTED_EDGE ( 'NONE', *, *, #23182, .F. ) ;
#15423=CARTESIAN_POINT ( 'NONE',  ( 12.57019395242807036, 1.827067495629551841, 13.88026806835660842 ) ) ;
#15427=ORIENTED_EDGE ( 'NONE', *, *, #49837, .F. ) ;
#15428=CARTESIAN_POINT ( 'NONE',  ( 12.41909388474796216, -1.871095411850187018, 12.46029856231474930 ) ) ;
#15434=CARTESIAN_POINT ( 'NONE',  ( 12.10797143991212010, 0.1980440493285337555, 12.59844852634975787 ) ) ;
#15438=CARTESIAN_POINT ( 'NONE',  ( 12.12868457208159789, 2.220738826795316090, 12.40275942113247964 ) ) ;
#15445=CARTESIAN_POINT ( 'NONE',  ( 12.19222608798534502, 2.622765415552483770, 12.42211422047175517 ) ) ;
#15449=CARTESIAN_POINT ( 'NONE',  ( 12.64261153913240499, 0.6049396497608361400, 12.68060203380711570 ) ) ;
#15456=CARTESIAN_POINT ( 'NONE',  ( 12.27362767355647222, -2.829117748835542567, 13.59812893905842479 ) ) ;
#15457=CARTESIAN_POINT ( 'NONE',  ( 12.20843209895684645, 2.686266380639721785, 13.63213492624170264 ) ) ;
#15464=CARTESIAN_POINT ( 'NONE',  ( 17.98432920965424131, 2.954704375608638411, -12.33394473884602149 ) ) ;
#15466=CARTESIAN_POINT ( 'NONE',  ( 17.81530815051377203, 3.068584091763893795, 12.30073186569319610 ) ) ;
#15467=CARTESIAN_POINT ( 'NONE',  ( 17.65076761721691057, 3.243341803239792487, 13.61913462217096260 ) ) ;
#15476=ADVANCED_FACE ( 'NONE', ( #42501 ), #10331, .T. ) ;
#15489=CARTESIAN_POINT ( 'NONE',  ( 12.41737190959485382, 0.4903666734152603013, -13.88835870177955378 ) ) ;
#15490=CARTESIAN_POINT ( 'NONE',  ( 18.18005044388380043, 2.499999700417821380, 12.45156116530496604 ) ) ;
#15491=CIRCLE ( 'NONE', #54559, 2.200000000000001066 ) ;
#15500=CARTESIAN_POINT ( 'NONE',  ( 18.17921332558109881, -2.461874964459676907, -12.46038192087330820 ) ) ;
#15532=PLANE ( 'NONE',  #39193 ) ;
#15535=CARTESIAN_POINT ( 'NONE',  ( 18.14658900067671965, 2.701839613031566500, -12.40227423856772582 ) ) ;
#15542=CARTESIAN_POINT ( 'NONE',  ( 5.644459969794759502, 12.96885562310360029, -2.321858018549519453 ) ) ;
#15545=CARTESIAN_POINT ( 'NONE',  ( 12.19636936301369978, -0.1422617729927582730, -12.69893308522357422 ) ) ;
#15556=CARTESIAN_POINT ( 'NONE',  ( 17.55505043854144276, 0.6250000000000001110, -12.67928921589118474 ) ) ;
#15559=VERTEX_POINT ( 'NONE', #22755 ) ;
#15563=EDGE_LOOP ( 'NONE', ( #55049, #54617, #31300, #7131, #18405, #43010, #8824, #43981 ) ) ;
#15578=ORIENTED_EDGE ( 'NONE', *, *, #61407, .T. ) ;
#15593=CARTESIAN_POINT ( 'NONE',  ( 12.32580140628882681, 2.098690126660239130, -13.75042779764526735 ) ) ;
#15596=CARTESIAN_POINT ( 'NONE',  ( 18.14706097348721414, 0.2014071429975164695, 13.89805485625563541 ) ) ;
#15597=CARTESIAN_POINT ( 'NONE',  ( 18.17614081693745121, 0.08113699202310993563, 13.89976078941035631 ) ) ;
#15602=CARTESIAN_POINT ( 'NONE',  ( 7.100000000000000533, -13.17499999999999893, -1.613472157876637865E-15 ) ) ;
#15606=CARTESIAN_POINT ( 'NONE',  ( 12.56936319533972757, 3.210092459268786946, -13.62701963584631848 ) ) ;
#15611=EDGE_CURVE ( 'NONE', #47809, #16477, #16187, .T. ) ;
#15612=CARTESIAN_POINT ( 'NONE',  ( 18.27048529734872773, 0.1170514037749867675, 12.59946170170351643 ) ) ;
#15627=CARTESIAN_POINT ( 'NONE',  ( 17.65093748390281547, -3.195004315082954793, 12.18819265947264263 ) ) ;
#15632=CARTESIAN_POINT ( 'NONE',  ( 17.55505043854144276, -0.7192913403693006469, 12.57945229203838444 ) ) ;
#15642=CARTESIAN_POINT ( 'NONE',  ( 18.11581248800845145, 0.2761834754990897256, -13.89631168292871344 ) ) ;
#15653=DIRECTION ( 'NONE',  ( 0.000000000000000000, 0.000000000000000000, 1.000000000000000000 ) ) ;
#15656=ORIENTED_EDGE ( 'NONE', *, *, #36636, .F. ) ;
#15658=CARTESIAN_POINT ( 'NONE',  ( 12.18852176789205188, -2.603049415106243547, -12.42696357550859965 ) ) ;
#15663=CARTESIAN_POINT ( 'NONE',  ( 12.11707904423856164, -2.286486548259630158, -13.81204227851269195 ) ) ;
#15664=B_SPLINE_CURVE_WITH_KNOTS ( 'NONE', 3,
 ( #63562, #15676, #37005, #58321, #10423, #37687, #53082, #5181, #26516, #47846, #42592, #63900, #16015, #17753 ),
 .UNSPECIFIED., .F., .F.,
 ( 4, 2, 2, 2, 2, 2, 4 ),
 ( 0.000000000000000000, 0.2492980987600019183, 0.3739471481400044595, 0.4051094104850044286, 0.4362716728300042868, 0.4674339351750042004, 0.4985961975200040586 ),
 .UNSPECIFIED. ) ;
#15668=CARTESIAN_POINT ( 'NONE',  ( 18.23564136049840201, -2.231667926091398080, 12.40079771041856027 ) ) ;
#15676=CARTESIAN_POINT ( 'NONE',  ( 17.72043029662046010, 1.875000000000000444, -12.57545629021512212 ) ) ;
#15689=AXIS2_PLACEMENT_3D ( 'NONE', #5787, #54376, #27130 ) ;
#15690=CARTESIAN_POINT ( 'NONE',  ( 12.24208977126479070, -0.2715269968477702078, 12.69609476950840943 ) ) ;
#15691=CARTESIAN_POINT ( 'NONE',  ( 5.614176421966211805, -12.11993299477413366, -3.746642824815739292 ) ) ;
#15707=PRODUCT_DEFINITION_CONTEXT ( 'detailed design', #65019, 'design' ) ;
#15710=CARTESIAN_POINT ( 'NONE',  ( 18.18005044212796051, -2.500000099754955851, 13.67345740034994783 ) ) ;
#15713=CARTESIAN_POINT ( 'NONE',  ( 18.11617320663398445, -2.776000138870932776, -13.61099849375431958 ) ) ;
#15715=CARTESIAN_POINT ( 'NONE',  ( 4.599999999999999645, -0.7302158263239199032, -13.98094363220830871 ) ) ;
#15719=B_SPLINE_CURVE_WITH_KNOTS ( 'NONE', 1,
 ( #53604, #21778 ),
 .UNSPECIFIED., .F., .F.,
 ( 2, 2 ),
 ( 0.000000000000000000, 1.000000000000000000 ),
 .UNSPECIFIED. ) ;
#15734=AXIS2_PLACEMENT_3D ( 'NONE', #18377, #39699, #45972 ) ;
#15735=CARTESIAN_POINT ( 'NONE',  ( 12.19613275390595319, 2.089545048426563856, -12.42553124896410566 ) ) ;
#15738=CARTESIAN_POINT ( 'NONE',  ( 18.25313429507010099, -2.320711718358091424, 13.80631856085855169 ) ) ;
#15751=CARTESIAN_POINT ( 'NONE',  ( 17.72055336043788998, -0.7006927685645097936, -12.58050281163331796 ) ) ;
#15753=CARTESIAN_POINT ( 'NONE',  ( 12.76376210871183403, 3.124999999999998224, -12.28374662615010848 ) ) ;
#15764=CARTESIAN_POINT ( 'NONE',  ( 12.52212199933416237, -0.5573870965680521872, -12.68353347974201384 ) ) ;
#15767=CARTESIAN_POINT ( 'NONE',  ( 12.35083548769878625, -1.919332845685027822, 12.45296032288162813 ) ) ;
#15772=CARTESIAN_POINT ( 'NONE',  ( 12.12656756701886707, 0.2537702651956291744, 12.59744904646397679 ) ) ;
#15775=CARTESIAN_POINT ( 'NONE',  ( 12.09179812036142110, 2.610377073672085046, 12.32664058968472176 ) ) ;
#15783=CARTESIAN_POINT ( 'NONE',  ( 18.18005043824377154, 1.329526366183796371E-10, 12.70000000088145420 ) ) ;
#15786=CARTESIAN_POINT ( 'NONE',  ( 12.18827089114435758, 0.1029087316592282725, 12.69945830692958566 ) ) ;
#15791=CARTESIAN_POINT ( 'NONE',  ( 12.23000334607949036, -2.254948878044617633, 13.72238900567161402 ) ) ;
#15792=CARTESIAN_POINT ( 'NONE',  ( 12.22437278964929064, 2.731306219223309295, 13.62162349210572820 ) ) ;
#15802=CARTESIAN_POINT ( 'NONE',  ( 18.17519250343466908, 2.421563205337720959, -12.46952409297816544 ) ) ;
#15804=CARTESIAN_POINT ( 'NONE',  ( 18.12908148756949700, 2.747269642044513294, 12.39050915966048017 ) ) ;
#15807=CARTESIAN_POINT ( 'NONE',  ( 12.70654069052307555, 3.248070099070885064, 13.61800428248618466 ) ) ;
#15809=CARTESIAN_POINT ( 'NONE',  ( 4.599999999999999645, 1.760845406083394682, -12.47635457398814829 ) ) ;
#15823=FACE_OUTER_BOUND ( 'NONE', #22350, .T. ) ;
#15826=CARTESIAN_POINT ( 'NONE',  ( 17.55505043854147118, -3.125000000000000000, -25.00000000000000000 ) ) ;
#15834=CARTESIAN_POINT ( 'NONE',  ( 17.75808086271927522, -3.091459143609192495, -12.29388367502514612 ) ) ;
#15837=CARTESIAN_POINT ( 'NONE',  ( 12.23133660942382583, 0.2481576080865451894, 13.89702325994033671 ) ) ;
#15861=ORIENTED_EDGE ( 'NONE', *, *, #39805, .T. ) ;
#15867=CARTESIAN_POINT ( 'NONE',  ( 18.14127614488628382, 2.717147700443817815, -12.39835379074819954 ) ) ;
#15878=CARTESIAN_POINT ( 'NONE',  ( 12.18528753443599477, 0.08139242733401171048, -12.69965452654168026 ) ) ;
#15894=CARTESIAN_POINT ( 'NONE',  ( 17.89590342297354297, 3.023973030522680627, -13.54825986461598752 ) ) ;
#15895=ORIENTED_EDGE ( 'NONE', *, *, #38255, .T. ) ;
#15898=CARTESIAN_POINT ( 'NONE',  ( 17.67321579093595219, -0.7208442004938210301, -13.98143072948223953 ) ) ;
#15908=ORIENTED_EDGE ( 'NONE', *, *, #46883, .T. ) ;
#15912=CARTESIAN_POINT ( 'NONE',  ( 17.67442079356968065, -1.770331164897447573, -12.47501301698789611 ) ) ;
#15923=ORIENTED_EDGE ( 'NONE', *, *, #8369, .T. ) ;
#15933=CARTESIAN_POINT ( 'NONE',  ( 18.15872407313728587, 0.1621987986621301059, 13.89873133405097327 ) ) ;
#15938=CARTESIAN_POINT ( 'NONE',  ( 18.16002775367444144, -0.1622926916309997414, -13.89880504292134944 ) ) ;
#15949=CARTESIAN_POINT ( 'NONE',  ( 17.94753454920341440, -0.4864235087029702420, 12.68745975172790530 ) ) ;
#15960=LINE ( 'NONE', #5809, #8612 ) ;
#15966=CARTESIAN_POINT ( 'NONE',  ( 5.557969180997336167, 12.17302321295358603, 3.765215263421144432 ) ) ;
#15974=VERTEX_POINT ( 'NONE', #21215 ) ;
#15981=FACE_OUTER_BOUND ( 'NONE', #31904, .T. ) ;
#15986=CARTESIAN_POINT ( 'NONE',  ( 12.49878241383750321, 3.044913063694494770, -12.30777011605604798 ) ) ;
#15990=ORIENTED_EDGE ( 'NONE', *, *, #24138, .F. ) ;
#15994=ORIENTED_EDGE ( 'NONE', *, *, #30658, .F. ) ;
#16000=CARTESIAN_POINT ( 'NONE',  ( 12.10383213726159113, -2.332238815612519112, -13.80437617213671508 ) ) ;
#16005=CARTESIAN_POINT ( 'NONE',  ( 18.11163387652233681, -2.018964330316879607, 12.43719698804479101 ) ) ;
#16015=CARTESIAN_POINT ( 'NONE',  ( 18.18005043890188688, 2.480435639343892440, -12.45614914497210179 ) ) ;
#16020=CARTESIAN_POINT ( 'NONE',  ( 12.34709291757831195, -2.925445075551590612, 12.34221984780393733 ) ) ;
#16027=CARTESIAN_POINT ( 'NONE',  ( 12.76382339226414153, -0.6237239846186475312, 12.67937377942300614 ) ) ;
#16028=CARTESIAN_POINT ( 'NONE',  ( 5.584969860377806405, -12.14796130797234497, -3.754865623502119831 ) ) ;
#16034=CARTESIAN_POINT ( 'NONE',  ( 17.83329178774383550, 3.059742244759366514, 13.53861815793071877 ) ) ;
#16040=CARTESIAN_POINT ( 'NONE',  ( 5.657901059018296763, -12.07783836333845073, 3.734765664958815456 ) ) ;
#16046=VERTEX_POINT ( 'NONE', #14177 ) ;
#16048=CARTESIAN_POINT ( 'NONE',  ( 18.06381123663118871, -2.863168028152635713, -13.58964369048649523 ) ) ;
#16058=CARTESIAN_POINT ( 'NONE',  ( 17.94287402937880316, -0.4902502634346644905, 13.88836422974693718 ) ) ;
#16067=CARTESIAN_POINT ( 'NONE',  ( 12.53584957871190753, 1.812149883874475176, -12.46900695079346022 ) ) ;
#16085=CARTESIAN_POINT ( 'NONE',  ( 17.61479688768388741, -0.7169431667913691575, -12.57958639523259237 ) ) ;
#16088=ADVANCED_FACE ( 'NONE', ( #47366 ), #58193, .T. ) ;
#16091=ORIENTED_EDGE ( 'NONE', *, *, #28689, .T. ) ;
#16095=DIRECTION ( 'NONE',  ( 1.000000000000000000, 0.000000000000000000, 0.000000000000000000 ) ) ;
#16098=CARTESIAN_POINT ( 'NONE',  ( 18.25561427624396771, 2.667326636134571771, 12.31445830791193963 ) ) ;
#16102=CARTESIAN_POINT ( 'NONE',  ( 12.80505043854146940, -1.816877544077282636, 13.85235828181317252 ) ) ;
#16104=CARTESIAN_POINT ( 'NONE',  ( 12.27226887596755489, -1.991660198615909039, 12.44160671058019041 ) ) ;
#16112=CARTESIAN_POINT ( 'NONE',  ( 12.44248249217651647, 0.6233258800551656487, 12.58457734799055139 ) ) ;
#16116=CARTESIAN_POINT ( 'NONE',  ( 12.44904482565494419, 1.853472941501685289, 12.46293187093603194 ) ) ;
#16124=CARTESIAN_POINT ( 'NONE',  ( 12.20227052528876044, 2.665223631340718935, 12.41153314565065457 ) ) ;
#16135=CARTESIAN_POINT ( 'NONE',  ( 12.24735473125027774, -2.217676833728435604, 13.72929951782216484 ) ) ;
#16136=CARTESIAN_POINT ( 'NONE',  ( 12.18106278541542054, 2.459077072170055001, 13.68201856772054548 ) ) ;
#16138=ORIENTED_EDGE ( 'NONE', *, *, #26355, .T. ) ;
#16141=CARTESIAN_POINT ( 'NONE',  ( 18.17590806570262529, 2.418078130900048972, -13.69056546383534290 ) ) ;
#16143=CARTESIAN_POINT ( 'NONE',  ( 5.699999772733999492, -12.03770622561999915, -3.722046322334000124 ) ) ;
#16144=CARTESIAN_POINT ( 'NONE',  ( 18.14681149257596360, 2.701359571199342113, -12.40239981104076605 ) ) ;
#16146=CARTESIAN_POINT ( 'NONE',  ( 17.83361872141519910, 3.059864849503202588, 12.30332992014442439 ) ) ;
#16149=CARTESIAN_POINT ( 'NONE',  ( 12.75598089128350665, 1.787835849362446439, 13.88537514715543608 ) ) ;
#16154=EDGE_LOOP ( 'NONE', ( #16350, #55419, #27539, #6966 ) ) ;
#16157=ORIENTED_EDGE ( 'NONE', *, *, #52103, .T. ) ;
#16177=CARTESIAN_POINT ( 'NONE',  ( 18.16462229618758428, -2.361607881905639417, -12.48272818380096894 ) ) ;
#16182=CARTESIAN_POINT ( 'NONE',  ( 12.72272221947699045, 0.6198980793944576240, 13.88138779565240100 ) ) ;
#16187=B_SPLINE_CURVE_WITH_KNOTS ( 'NONE', 1,
 ( #12623, #33952 ),
 .UNSPECIFIED., .F., .F.,
 ( 2, 2 ),
 ( 0.000000000000000000, 1.000000000000000000 ),
 .UNSPECIFIED. ) ;
#16198=CARTESIAN_POINT ( 'NONE',  ( 18.27946005101761884, -2.709881966525854224, 13.73658560568321185 ) ) ;
#16200=CARTESIAN_POINT ( 'NONE',  ( 12.80505043854144276, 0.7192913403693015351, 12.57945229203838267 ) ) ;
#16205=CARTESIAN_POINT ( 'NONE',  ( 5.700000000000000178, 13.04986661130000059, 1.811520473896000016 ) ) ;
#16212=CARTESIAN_POINT ( 'NONE',  ( 18.09742839075014587, 2.810734143470918767, -12.37374591514403122 ) ) ;
#16222=CARTESIAN_POINT ( 'NONE',  ( 12.25134400021322456, 0.2899325138666232204, -12.69554708236672980 ) ) ;
#16237=CARTESIAN_POINT ( 'NONE',  ( 18.01279121882204137, 2.925678518064911859, -13.57390968381829310 ) ) ;
#16243=ORIENTED_EDGE ( 'NONE', *, *, #38938, .T. ) ;
#16245=CARTESIAN_POINT ( 'NONE',  ( 18.12841930325693696, 0.2489729014332486556, -12.69672092236991112 ) ) ;
#16254=VERTEX_POINT ( 'NONE', #31981 ) ;
#16259=CARTESIAN_POINT ( 'NONE',  ( 17.99974802964005605, -1.911958328522573414, -12.45409441785080773 ) ) ;
#16266=VERTEX_POINT ( 'NONE', #15199 ) ;
#16273=CARTESIAN_POINT ( 'NONE',  ( 12.39809172042338759, 2.025537470422473341, -13.76271392731541354 ) ) ;
#16277=CARTESIAN_POINT ( 'NONE',  ( 17.55505043854143921, -0.6250000000000001110, 13.88107975066923316 ) ) ;
#16283=CARTESIAN_POINT ( 'NONE',  ( 18.11245875480856071, -0.2828881521639263763, -13.89612849060967648 ) ) ;
#16292=CARTESIAN_POINT ( 'NONE',  ( 18.08578179881429548, -0.3302353423713645375, 12.69422546839060395 ) ) ;
#16309=CARTESIAN_POINT ( 'NONE',  ( 17.90971610687748594, 3.107943374821388272, -12.21068061720391995 ) ) ;
#16324=CARTESIAN_POINT ( 'NONE',  ( 17.55505043854147118, -3.199698446519375850, -12.18695736643652694 ) ) ;
#16339=CARTESIAN_POINT ( 'NONE',  ( 17.92027680868936201, 0.6284010951822294189, 12.58437167746827789 ) ) ;
#16346=CARTESIAN_POINT ( 'NONE',  ( 12.10457356466343626, -2.707610175640964734, -13.73569711802853277 ) ) ;
#16349=CARTESIAN_POINT ( 'NONE',  ( 18.28003019995800571, -2.460172313524578325, 12.35749544995779559 ) ) ;
#16350=ORIENTED_EDGE ( 'NONE', *, *, #64235, .F. ) ;
#16370=CARTESIAN_POINT ( 'NONE',  ( 12.39271969839518661, -0.4698014501121478559, 12.68830453558791405 ) ) ;
#16379=CARTESIAN_POINT ( 'NONE',  ( 18.15991033943441835, 2.341318227119850715, 13.70580147614463051 ) ) ;
#16389=ORIENTED_EDGE ( 'NONE', *, *, #15055, .F. ) ;
#16393=CARTESIAN_POINT ( 'NONE',  ( 17.67509761310387617, -1.797476384633009072, -13.88413128968476506 ) ) ;
#16410=CARTESIAN_POINT ( 'NONE',  ( 12.22684347114279824, 2.045928570575534788, -12.43279008976418787 ) ) ;
#16415=VECTOR ( 'NONE', #28779, 1000.000000000000000 ) ;
#16422=CARTESIAN_POINT ( 'NONE',  ( 12.32444827497858597, -3.019497106116459939, -12.23286052727262607 ) ) ;
#16428=CARTESIAN_POINT ( 'NONE',  ( 17.87637886473325466, -0.6448943924266655747, -12.58348668657565739 ) ) ;
#16429=CONICAL_SURFACE ( 'NONE', #13107, 12.69999976913000062, 0.7853981453603698926 ) ;
#16433=EDGE_LOOP ( 'NONE', ( #16758, #52289, #58773, #48819 ) ) ;
#16439=CARTESIAN_POINT ( 'NONE',  ( 18.21786174063354125, 2.187645605293237594, 12.40865382983254328 ) ) ;
#16443=CARTESIAN_POINT ( 'NONE',  ( 12.33074081237575648, -0.4072355409555394323, -12.69121720794965391 ) ) ;
#16446=CARTESIAN_POINT ( 'NONE',  ( 12.44969725703165864, -3.107561633766898535, 12.21077779329595181 ) ) ;
#16452=CARTESIAN_POINT ( 'NONE',  ( 12.57206729000417589, 0.6812425322175417186, 12.58157083403807164 ) ) ;
#16455=CARTESIAN_POINT ( 'NONE',  ( 12.41053097114615333, 2.984774150185583341, 12.32529705072536963 ) ) ;
#16456=DIRECTION ( 'NONE',  ( 1.000000000000000000, 0.000000000000000000, 0.000000000000000000 ) ) ;
#16462=CARTESIAN_POINT ( 'NONE',  ( 18.08719379937462435, -0.3285641700896766437, 12.69429818673183874 ) ) ;
#16466=CARTESIAN_POINT ( 'NONE',  ( 12.39297475233172641, 0.4699412921624549488, 12.68829632721468670 ) ) ;
#16467=DIRECTION ( 'NONE',  ( -1.000000000000000000, 0.000000000000000000, 0.000000000000000000 ) ) ;
#16469=CARTESIAN_POINT ( 'NONE',  ( 18.20120694895331681, 0.3761765225308036920, -12.59508068833545025 ) ) ;
#16474=CARTESIAN_POINT ( 'NONE',  ( 12.14279580514170220, -2.220721880347446220, 13.82275356517832243 ) ) ;
#16477=VERTEX_POINT ( 'NONE', #26303 ) ;
#16485=CARTESIAN_POINT ( 'NONE',  ( 18.12481736082884254, 2.757674955237351622, -12.38783183949681899 ) ) ;
#16491=CARTESIAN_POINT ( 'NONE',  ( 12.07956470885934586, 2.330212498102625762, 13.80606232674509215 ) ) ;
#16500=CARTESIAN_POINT ( 'NONE',  ( 17.59665311020859235, -3.123961325934789812, 13.52113166927136589 ) ) ;
#16502=VERTEX_POINT ( 'NONE', #4277 ) ;
#16507=DIRECTION ( 'NONE',  ( 1.000000000000000000, 0.000000000000000000, 0.000000000000000000 ) ) ;
#16508=CARTESIAN_POINT ( 'NONE',  ( 12.23478023516057611, 0.2564316838161031509, -13.89683092737869075 ) ) ;
#16518=CARTESIAN_POINT ( 'NONE',  ( 18.28072526159327893, -2.330763871328881187, -13.80597059071421562 ) ) ;
#16519=CARTESIAN_POINT ( 'NONE',  ( 18.06437450929129085, -2.862796250983955737, -12.35961424106608497 ) ) ;
#16528=CARTESIAN_POINT ( 'NONE',  ( 12.18028570900101215, 0.01996689158402554023, 13.89998575767904043 ) ) ;
#16550=ORIENTED_EDGE ( 'NONE', *, *, #53541, .T. ) ;
#16556=ADVANCED_FACE ( 'NONE', ( #65056 ), #22422, .F. ) ;
#16558=CARTESIAN_POINT ( 'NONE',  ( 18.10321044366099486, 2.800384071015809884, -12.37651499847982528 ) ) ;
#16577=CARTESIAN_POINT ( 'NONE',  ( 18.13610002192212534, 0.2304169715249079764, 12.69719098617350639 ) ) ;
#16581=VECTOR ( 'NONE', #430, 1000.000000000000114 ) ;
#16585=CARTESIAN_POINT ( 'NONE',  ( 18.16386294024314907, 2.642762625146028999, -13.64216358405141705 ) ) ;
#16586=ORIENTED_EDGE ( 'NONE', *, *, #20293, .F. ) ;
#16587=LINE ( 'NONE', #5745, #8319 ) ;
#16593=CARTESIAN_POINT ( 'NONE',  ( 18.12515139794686192, 0.2563289266177934400, -12.69652241465648679 ) ) ;
#16617=CARTESIAN_POINT ( 'NONE',  ( 12.66212950609378574, 3.108785237067038132, -13.52531707329825572 ) ) ;
#16621=CARTESIAN_POINT ( 'NONE',  ( 17.85613310415347144, 0.5477939754035893172, 13.88547043407462667 ) ) ;
#16625=CARTESIAN_POINT ( 'NONE',  ( 12.32624190542397002, 0.4017285589307815763, 13.89218662323935050 ) ) ;
#16626=CARTESIAN_POINT ( 'NONE',  ( 12.50370260275542478, -0.5476489827201047600, -13.88547809940108024 ) ) ;
#16628=CARTESIAN_POINT ( 'NONE',  ( 17.81146176621321331, -0.5702785222767412510, -13.88425216382592886 ) ) ;
#16635=CARTESIAN_POINT ( 'NONE',  ( 18.18003632999695895, -0.02081145935391651852, 12.69999906470293283 ) ) ;
#16639=ORIENTED_EDGE ( 'NONE', *, *, #51141, .T. ) ;
#16653=CARTESIAN_POINT ( 'NONE',  ( 5.518321182381299650, 12.20777697080807300, 3.787023466221932200 ) ) ;
#16668=CARTESIAN_POINT ( 'NONE',  ( 18.16600461949965961, -0.1321590433901045358, -13.89915950722680016 ) ) ;
#16671=CARTESIAN_POINT ( 'NONE',  ( 17.55505043854147118, -1.875000000000000000, 13.78631952119024895 ) ) ;
#16673=DIRECTION ( 'NONE',  ( -1.000000000000000000, 0.000000000000000000, 0.000000000000000000 ) ) ;
#16677=ORIENTED_EDGE ( 'NONE', *, *, #64209, .F. ) ;
#16682=CARTESIAN_POINT ( 'NONE',  ( 12.18180637322648430, -2.452078064253476519, -12.46259978693893267 ) ) ;
#16686=CARTESIAN_POINT ( 'NONE',  ( 12.23477282158795809, -2.066986176408053932, -13.84657559728969645 ) ) ;
#16688=CARTESIAN_POINT ( 'NONE',  ( 12.15578049617215939, -2.108731457858033842, 12.42302753736614562 ) ) ;
#16689=CARTESIAN_POINT ( 'NONE',  ( 18.27123885515672441, -2.366823750208070898, 12.37571350032474626 ) ) ;
#16700=CARTESIAN_POINT ( 'NONE',  ( 17.55505043854147118, -1.760910691117812954, -12.47634535983622861 ) ) ;
#16702=DIRECTION ( 'NONE',  ( -1.000000000000000000, 0.000000000000000000, 0.000000000000000000 ) ) ;
#16718=CARTESIAN_POINT ( 'NONE',  ( 18.15125141007961318, 2.312191647150520613, 13.71145324559127054 ) ) ;
#16728=ORIENTED_EDGE ( 'NONE', *, *, #49081, .F. ) ;
#16731=CARTESIAN_POINT ( 'NONE',  ( 18.23099845246962047, -2.253777188809249932, -13.81740256423587709 ) ) ;
#16751=CARTESIAN_POINT ( 'NONE',  ( 12.33239129661525268, 1.934538128658851885, -12.45060726317137778 ) ) ;
#16754=CARTESIAN_POINT ( 'NONE',  ( 18.16732611089587124, 2.625479215054820070, -13.64604457655927305 ) ) ;
#16758=ORIENTED_EDGE ( 'NONE', *, *, #15270, .F. ) ;
#16766=CARTESIAN_POINT ( 'NONE',  ( 17.81083341652436403, -0.6731412448965096162, -12.58200685883812753 ) ) ;
#16767=CARTESIAN_POINT ( 'NONE',  ( 12.18214412808134206, 2.552249690270588012, -12.43927262873618211 ) ) ;
#16776=CARTESIAN_POINT ( 'NONE',  ( 18.27918563591880385, 2.436421501371055065, 12.36221688302663146 ) ) ;
#16785=CARTESIAN_POINT ( 'NONE',  ( 12.25790434794253692, -2.952613167459266830, 12.24916959777017667 ) ) ;
#16793=CARTESIAN_POINT ( 'NONE',  ( 12.30913258640366870, -0.5248261352964553872, 12.58906749861124119 ) ) ;
#16796=CARTESIAN_POINT ( 'NONE',  ( 12.19425446308164140, 2.632875717725343012, 12.41961888770621592 ) ) ;
#16804=CARTESIAN_POINT ( 'NONE',  ( 18.06844660307579531, -0.3566172609784874492, 12.69326555881911034 ) ) ;
#16813=CARTESIAN_POINT ( 'NONE',  ( 12.41877979183516700, -1.899635599875575176, 13.87052873021461430 ) ) ;
#16825=CARTESIAN_POINT ( 'NONE',  ( 17.69913221809297710, 1.891485217175129963, -12.57274297139331587 ) ) ;
#16841=CARTESIAN_POINT ( 'NONE',  ( 17.99219435089542074, -2.053195051521780279, 13.75813171417237868 ) ) ;
#16850=CARTESIAN_POINT ( 'NONE',  ( 12.21982127437517285, 0.2196390009034050184, -13.89766917373429678 ) ) ;
#16860=CARTESIAN_POINT ( 'NONE',  ( 18.00599872992922457, -2.932869382066921826, -12.34010572687589757 ) ) ;
#16864=CARTESIAN_POINT ( 'NONE',  ( 12.54503913623221578, 3.068442045733652979, 13.53626685534802476 ) ) ;
#16866=CARTESIAN_POINT ( 'NONE',  ( 17.59669571873555682, -1.876302067258580619, 12.57524312254454202 ) ) ;
#16869=CIRCLE ( 'NONE', #55963, 12.60000000000000142 ) ;
#16870=CARTESIAN_POINT ( 'NONE',  ( 12.44045292577857786, 0.5080432161604395702, 13.88750743611952210 ) ) ;
#16871=ORIENTED_EDGE ( 'NONE', *, *, #1484, .F. ) ;
#16883=CARTESIAN_POINT ( 'NONE',  ( 12.80505043854143388, 1.787816316115912185, -13.88537766212463254 ) ) ;
#16913=CARTESIAN_POINT ( 'NONE',  ( 18.10291658807267368, 0.3009529451927861476, 12.69520353502463550 ) ) ;
#16919=CARTESIAN_POINT ( 'NONE',  ( 17.98387256218933672, 2.954798081836346402, -13.56641578797405323 ) ) ;
#16934=DIRECTION ( 'NONE',  ( 0.000000000000000000, 0.000000000000000000, -1.000000000000000000 ) ) ;
#16940=CARTESIAN_POINT ( 'NONE',  ( 17.65082925870469666, -1.766819657443025937, -12.47551016841904215 ) ) ;
#16954=CARTESIAN_POINT ( 'NONE',  ( 12.54721708147385506, 1.835134883933968064, -13.87920628830544878 ) ) ;
#16956=CARTESIAN_POINT ( 'NONE',  ( 18.17902784157848117, 0.04113803725885954027, 13.89993798560270832 ) ) ;
#16961=CARTESIAN_POINT ( 'NONE',  ( 12.18105065343300275, -0.04081304477956804178, 13.89993877190689453 ) ) ;
#16962=CARTESIAN_POINT ( 'NONE',  ( 12.54853131234585994, -0.5702303675871001065, -13.88425454623346944 ) ) ;
#16964=CARTESIAN_POINT ( 'NONE',  ( 18.18005043854833147, -0.04052532577797417906, -13.90000015527654931 ) ) ;
#16972=VECTOR ( 'NONE', #3948, 1000.000000000000000 ) ;
#16976=CARTESIAN_POINT ( 'NONE',  ( 18.17001854112162818, -0.1120021961262577387, 12.69934078656687682 ) ) ;
#16989=ORIENTED_EDGE ( 'NONE', *, *, #25252, .F. ) ;
#16990=B_SPLINE_CURVE_WITH_KNOTS ( 'NONE', 3,
 ( #3260, #57084, #36106, #24590, #56756, #45912, #46946, #8852, #67224, #19337, #30189, #61993, #62667, #24928, #14787, #57422, #9527, #30870, #68251, #12556 ),
 .UNSPECIFIED., .F., .F.,
 ( 4, 2, 2, 2, 2, 2, 2, 2, 2, 4 ),
 ( 0.5011597829075521426, 0.5050569721035867987, 0.5089541612996214548, 0.5167485396916908780, 0.5323372964758295023, 0.5635148100441073060, 0.5946923236123851098, 0.6258698371806629135, 0.7505798914537751276, 1.000000000000000000 ),
 .UNSPECIFIED. ) ;
#16992=CARTESIAN_POINT ( 'NONE',  ( 12.16000645811906544, 0.3284204639250600799, -12.59572022474404740 ) ) ;
#16994=CARTESIAN_POINT ( 'NONE',  ( 18.18412234634028479, 2.838955764657549175, -12.27602435542071824 ) ) ;
#16998=ORIENTED_EDGE ( 'NONE', *, *, #20827, .F. ) ;
#17008=CARTESIAN_POINT ( 'NONE',  ( 12.70915608521899465, 1.765590719831859223, -12.47568749010001632 ) ) ;
#17010=CARTESIAN_POINT ( 'NONE',  ( 18.17005425344203928, 0.1118032413084525528, -13.89939982891984904 ) ) ;
#17017=ORIENTED_EDGE ( 'NONE', *, *, #49352, .F. ) ;
#17026=CARTESIAN_POINT ( 'NONE',  ( 12.49819407809065908, -1.955416873541954592, -12.56189665940130062 ) ) ;
#17030=CARTESIAN_POINT ( 'NONE',  ( 12.43994760172713754, -1.886699913279273444, -13.87229234465171679 ) ) ;
#17033=CARTESIAN_POINT ( 'NONE',  ( 17.84655355976684632, -1.821424963963782506, 12.46765546240475508 ) ) ;
#17046=ORIENTED_EDGE ( 'NONE', *, *, #67881, .F. ) ;
#17063=CARTESIAN_POINT ( 'NONE',  ( 18.11274618065387898, 2.217676902473667333, 13.72925005197110870 ) ) ;
#17075=CARTESIAN_POINT ( 'NONE',  ( 18.24173484165870818, -2.753291453986189463, -13.72661349255300500 ) ) ;
#17094=ORIENTED_EDGE ( 'NONE', *, *, #45869, .F. ) ;
#17097=CARTESIAN_POINT ( 'NONE',  ( 12.22799143493887897, 2.916631933635859486, -12.25779765684317191 ) ) ;
#17114=CARTESIAN_POINT ( 'NONE',  ( 18.15872281507842700, 0.1622035078961276411, -12.69861136640060195 ) ) ;
#17115=CARTESIAN_POINT ( 'NONE',  ( 12.22440656764569056, 2.731388741921196850, -12.39466681324993225 ) ) ;
#17126=CARTESIAN_POINT ( 'NONE',  ( 18.05422494319413929, 1.958382419481330627, 12.44687927882536549 ) ) ;
#17127=DIRECTION ( 'NONE',  ( 1.000000000000000000, 0.000000000000000000, 0.000000000000000000 ) ) ;
#17133=CARTESIAN_POINT ( 'NONE',  ( 12.18817755169816053, -2.859236737590006516, 12.27131451573979248 ) ) ;
#17140=CARTESIAN_POINT ( 'NONE',  ( 12.38211335778635735, -0.5846869236304570450, 12.58643362292763612 ) ) ;
#17141=AXIS2_PLACEMENT_3D ( 'NONE', #35049, #35389, #3892 ) ;
#17144=CARTESIAN_POINT ( 'NONE',  ( 12.63203184702126691, 3.100663238843660352, 12.29110965694881941 ) ) ;
#17148=CARTESIAN_POINT ( 'NONE',  ( 17.82167905068868308, -0.6689867242971705430, 12.58222862546947241 ) ) ;
#17151=CARTESIAN_POINT ( 'NONE',  ( 17.82907313211138600, -0.5620966109762222107, 12.68325743355232582 ) ) ;
#17153=LINE ( 'NONE', #59808, #55361 ) ;
#17156=CARTESIAN_POINT ( 'NONE',  ( 7.100000000000000533, 0.000000000000000000, 0.000000000000000000 ) ) ;
#17157=CARTESIAN_POINT ( 'NONE',  ( 18.28019316479310774, -0.1878083608821064232, -12.60000737103649016 ) ) ;
#17158=CARTESIAN_POINT ( 'NONE',  ( 17.65323508308281930, 1.760912828005752884, -12.47634505842159847 ) ) ;
#17159=CARTESIAN_POINT ( 'NONE',  ( 12.22680470609052961, -2.076949241994384465, 13.84509419021260079 ) ) ;
#17177=DIRECTION ( 'NONE',  ( -0.000000000000000000, 0.7507612787780010288, 0.6605736161001442008 ) ) ;
#17179=CARTESIAN_POINT ( 'NONE',  ( 12.35751123582549127, 3.100314578113210207, 13.65257769756134820 ) ) ;
#17181=LINE ( 'NONE', #23472, #56711 ) ;
#17187=CARTESIAN_POINT ( 'NONE',  ( 18.15894044208802427, -2.662322226546016690, 13.63771003692132844 ) ) ;
#17193=LINE ( 'NONE', #42738, #16581 ) ;
#17197=CARTESIAN_POINT ( 'NONE',  ( 17.81057016328025000, 0.6732419856523146340, -12.58200148172923782 ) ) ;
#17198=B_SPLINE_CURVE_WITH_KNOTS ( 'NONE', 3,
 ( #9221, #57121, #39681, #35472, #30561, #55764, #56794, #34787, #7866, #50511, #51536, #2612, #23944, #45276 ),
 .UNSPECIFIED., .F., .F.,
 ( 4, 2, 2, 2, 2, 2, 4 ),
 ( 0.000000000000000000, 0.2492980987599822951, 0.3739471481399732067, 0.4051094104849721211, 0.4362716728299709801, 0.4674339351749699500, 0.4985961975199688090 ),
 .UNSPECIFIED. ) ;
#17200=AXIS2_PLACEMENT_3D ( 'NONE', #29596, #20109, #19768 ) ;
#17203=EDGE_CURVE ( 'NONE', #19729, #13791, #39346, .T. ) ;
#17220=CARTESIAN_POINT ( 'NONE',  ( 12.18004362304668575, 0.009762789003246823832, 13.90000041479089532 ) ) ;
#17249=CARTESIAN_POINT ( 'NONE',  ( 4.599999999999999645, -0.6250000000000001110, 13.88107975066923494 ) ) ;
#17261=CARTESIAN_POINT ( 'NONE',  ( 12.73299791870421060, 0.6209187240130102925, -12.67955909024710337 ) ) ;
#17263=CARTESIAN_POINT ( 'NONE',  ( 12.27225454754552558, 2.172654780177386780, -13.73747135094945371 ) ) ;
#17268=CARTESIAN_POINT ( 'NONE',  ( 12.15456646199063506, -0.3226776716457278593, -13.99628514671255886 ) ) ;
#17273=CARTESIAN_POINT ( 'NONE',  ( 5.619239821441324167, 12.11503533077830319, -3.745341923021909381 ) ) ;
#17277=CARTESIAN_POINT ( 'NONE',  ( 17.60330540716445213, 3.246896514464374661, -13.61828436941213205 ) ) ;
#17283=CARTESIAN_POINT ( 'NONE',  ( 17.55505043854143565, 1.787816316115924842, -13.88537766212463254 ) ) ;
#17290=CARTESIAN_POINT ( 'NONE',  ( 17.55505043854143565, 1.875000000000000000, -25.00000000000000000 ) ) ;
#17298=CARTESIAN_POINT ( 'NONE',  ( 17.99911394258101183, -3.049496102151224797, -12.22541657636149282 ) ) ;
#17303=DIRECTION ( 'NONE',  ( -1.000000000000000000, 0.000000000000000000, 0.000000000000000000 ) ) ;
#17310=CARTESIAN_POINT ( 'NONE',  ( 12.41877979183513148, 1.899635599875573178, -13.87052873021461785 ) ) ;
#17314=CARTESIAN_POINT ( 'NONE',  ( 18.23388030753891798, -0.2566959043864896484, 13.99765098363215188 ) ) ;
#17319=CARTESIAN_POINT ( 'NONE',  ( 12.39297058734143953, -0.4699376426033362031, 13.88930769708871971 ) ) ;
#17320=CARTESIAN_POINT ( 'NONE',  ( 12.26182380057219135, -0.3097576186077237170, -13.89536933048183975 ) ) ;
#17321=FACE_OUTER_BOUND ( 'NONE', #28095, .T. ) ;
#17331=CARTESIAN_POINT ( 'NONE',  ( 18.09636316215240015, -0.3125877143166536642, 12.69482668528968183 ) ) ;
#17333=CARTESIAN_POINT ( 'NONE',  ( 18.16637421207913761, -2.630058154436578643, -12.42030992558146707 ) ) ;
#17334=EDGE_LOOP ( 'NONE', ( #50558, #22930, #13644, #51158 ) ) ;
#17347=CARTESIAN_POINT ( 'NONE',  ( 12.08466115484542414, 0.08185661189466880705, -12.59973963693671983 ) ) ;
#17348=CARTESIAN_POINT ( 'NONE',  ( 17.55505043854144276, 0.6250000000000001110, 12.67928921589117586 ) ) ;
#17349=CARTESIAN_POINT ( 'NONE',  ( 17.92000013766227440, 3.102113379644126923, -12.21216327800867951 ) ) ;
#17366=CARTESIAN_POINT ( 'NONE',  ( 18.05092994784024540, -0.3809766167652369195, -13.89298487834588514 ) ) ;
#17373=ORIENTED_EDGE ( 'NONE', *, *, #18228, .T. ) ;
#17376=DIRECTION ( 'NONE',  ( 1.000000000000000000, 0.000000000000000000, 0.000000000000000000 ) ) ;
#17379=EDGE_LOOP ( 'NONE', ( #67227, #53157, #39898, #51424 ) ) ;
#17380=B_SPLINE_SURFACE_WITH_KNOTS ( 'NONE', 1, 3, ( 
 ( #2770, #2091, #1734, #12230, #60812, #34941, #54876, #34604, #18857, #33556, #23749, #55917, #44403, #38799, #12575, #8364, #34252, #6978, #33905, #12925, #45429, #40184, #49976, #55222, #29019, #13618, #23053, #29709, #65703, #51010, #50326, #24442, #55572, #28663, #23409, #44746, #66045, #18168, #45768, #17474, #60124, #39490, #45086, #13278, #66393, #18516, #39838, #61160, #30049, #20561, #56599, #63193, #41887, #51686, #24781, #51352, #57269, #68100, #25807, #20217, #57616, #62178, #14637, #46454, #31066, #15322, #62518, #19189, #9719, #3784, #3444, #61838, #41208, #36647, #35284, #14973, #68441, #13957, #57970, #40857, #47140, #30715, #10069, #35955, #56941, #9369, #52374, #19538, #25122, #52025 ),
 ( #67753, #19879, #67076, #4468, #14300, #31404, #41543, #30378, #35628, #4817, #52719, #4126, #26159, #40512, #8706, #25462, #62855, #46795, #36296, #9037, #46108, #67414, #59688, #21930, #53415, #32782, #43268, #11440, #47484, #63887, #27192, #68790, #54095, #11788, #5513, #58307, #54443, #16346, #48512, #38363, #20907, #33127, #42244, #48167, #26502, #6192, #6544, #26854, #22280, #16000, #27534, #15663, #42923, #5852, #620, #53070, #38014, #64575, #43622, #64916, #53755, #63550, #16686, #69142, #48860, #36994, #969, #37330, #271, #59339, #5169, #10410, #31752, #47832, #17030, #21250, #58654, #32439, #21586, #42578, #10755, #32099, #64229, #37673, #59002, #11104, #12145, #34167, #45000, #54790 ) ),
 .UNSPECIFIED., .F., .F., .F.,
 ( 2, 2 ),
 ( 4, 2, 2, 2, 2, 2, 2, 2, 2, 2, 2, 2, 2, 2, 2, 2, 2, 2, 2, 2, 2, 2, 2, 2, 2, 2, 2, 2, 2, 2, 2, 2, 2, 2, 2, 2, 2, 2, 2, 2, 2, 2, 2, 2, 4 ),
 ( 0.000000000000000000, 1.000000000000000000 ),
 ( 0.000000000000000000, 7.143002489358809843E-05, 0.0001428600497871761969, 0.0002142900746807642953, 0.0002857200995743523937, 0.0003214351120211464429, 0.0003571501244679404921, 0.0003928651369147345414, 0.0004285801493615285906, 0.0005000101742551166890, 0.0005357251867019107924, 0.0005714401991487047874, 0.0006071552115954987824, 0.0006428702240422928859, 0.0007143002489358809843, 0.0007857302738294690827, 0.0008214452862762631861, 0.0008571602987230571812, 0.0009285903236166452796, 0.001000020348510233378, 0.001071450373403821585, 0.001142880398297409575, 0.001214310423190997565, 0.001285740448084585772, 0.001321455460531379984, 0.001357170472978173979, 0.001428600497871761969, 0.001500030522765349959, 0.001535745535212143954, 0.001571460547658938165, 0.001607175560105732377, 0.001642890572552526372, 0.001714320597446114362, 0.001750035609892908357, 0.001785750622339702352, 0.001821465634786496347, 0.001857180647233290559, 0.001928610672126878766, 0.001964325684573672761, 0.002000040697020466756, 0.002035755709467261185, 0.002071470721914055180, 0.002142900746807643170, 0.002214330771701231160, 0.002285760796594819150 ),
 .UNSPECIFIED. ) ;
#17381=CARTESIAN_POINT ( 'NONE',  ( 12.70145053304005067, -1.883559157534606898, -12.57401126189225771 ) ) ;
#17387=CARTESIAN_POINT ( 'NONE',  ( 12.80505043854144098, -0.6250000000000006661, -13.88107975066922428 ) ) ;
#17388=CARTESIAN_POINT ( 'NONE',  ( 17.57591323121273064, -3.124999405572034927, 12.28374652565519831 ) ) ;
#17420=CARTESIAN_POINT ( 'NONE',  ( 17.98404385246622539, 2.954974373217227779, 13.56632247660221147 ) ) ;
#17432=CARTESIAN_POINT ( 'NONE',  ( 17.75741541229206177, -3.091422763980662403, -13.53001720626202520 ) ) ;
#17454=ORIENTED_EDGE ( 'NONE', *, *, #34669, .T. ) ;
#17457=CARTESIAN_POINT ( 'NONE',  ( 12.30724456330681349, 3.003488097433216097, -12.23679193692685097 ) ) ;
#17468=CARTESIAN_POINT ( 'NONE',  ( 12.53614341883834271, -3.148504814753052106, -12.20028441070642877 ) ) ;
#17474=CARTESIAN_POINT ( 'NONE',  ( 12.18828317886891455, -2.603111844536877495, -13.65101713889819557 ) ) ;
#17475=CARTESIAN_POINT ( 'NONE',  ( 18.16408092502819116, -0.1418569258565843816, -12.69895512164410079 ) ) ;
#17476=CARTESIAN_POINT ( 'NONE',  ( 12.47602583993394632, 1.943637617988461352, -12.56471729223955336 ) ) ;
#17480=( LENGTH_UNIT ( ) NAMED_UNIT ( * ) SI_UNIT ( .MILLI., .METRE. ) );
#17486=CARTESIAN_POINT ( 'NONE',  ( 18.24314268136835437, 2.253095180823019295, 12.39692251310592397 ) ) ;
#17493=CARTESIAN_POINT ( 'NONE',  ( 12.08596835297192307, -2.576236330983343148, 12.33383868535373118 ) ) ;
#17497=VECTOR ( 'NONE', #24318, 1000.000000000000000 ) ;
#17500=CARTESIAN_POINT ( 'NONE',  ( 12.08146954708835707, -0.04649795050485633352, 12.59991969135870171 ) ) ;
#17503=CARTESIAN_POINT ( 'NONE',  ( 12.41452611191162880, 2.987998126639116236, 12.32436705583800318 ) ) ;
#17509=CARTESIAN_POINT ( 'NONE',  ( 18.03350839596208033, -0.4021454014604768368, 12.69143011154429246 ) ) ;
#17519=CARTESIAN_POINT ( 'NONE',  ( 12.37945077454914156, -1.926407208811270033, 13.86683589633374503 ) ) ;
#17547=CARTESIAN_POINT ( 'NONE',  ( 18.16667230414096323, -2.370970514942110974, 13.69998174157045234 ) ) ;
#17550=ADVANCED_FACE ( 'NONE', ( #66123 ), #60543, .F. ) ;
#17560=DIRECTION ( 'NONE',  ( -0.000000000000000000, -0.000000000000000000, 1.000000000000000000 ) ) ;
#17563=ORIENTED_EDGE ( 'NONE', *, *, #43679, .T. ) ;
#17566=FACE_OUTER_BOUND ( 'NONE', #63069, .T. ) ;
#17570=CARTESIAN_POINT ( 'NONE',  ( 12.20320247475634545, 2.331154411892200962, 13.70777421733259516 ) ) ;
#17574=CARTESIAN_POINT ( 'NONE',  ( 12.32658172867158797, 0.5491314443420094449, 13.98923457196398168 ) ) ;
#17587=FACE_OUTER_BOUND ( 'NONE', #4673, .T. ) ;
#17589=CARTESIAN_POINT ( 'NONE',  ( 4.600000533658279878, -13.89999946622000060, -2.316960006352999632E-09 ) ) ;
#17592=CARTESIAN_POINT ( 'NONE',  ( 12.08019350287876925, 0.1887961028408512432, 12.59999260960569067 ) ) ;
#17609=EDGE_LOOP ( 'NONE', ( #46493, #20640, #8188, #13685 ) ) ;
#17622=DIRECTION ( 'NONE',  ( -1.000000000000000000, 6.086974017450490350E-15, -6.313390726317570167E-15 ) ) ;
#17626=CARTESIAN_POINT ( 'NONE',  ( 12.76393046405280174, 0.6239795106976173678, -13.88114172264460322 ) ) ;
#17631=CARTESIAN_POINT ( 'NONE',  ( 5.670648345173815663, 12.06568050912902734, -3.730933605404140430 ) ) ;
#17635=CARTESIAN_POINT ( 'NONE',  ( 17.77706283214423877, 1.915668542326107726, -13.78016448532188676 ) ) ;
#17643=CARTESIAN_POINT ( 'NONE',  ( 17.63846197675113103, 0.6206501420305031713, -12.67957965403867426 ) ) ;
#17644=PLANE ( 'NONE',  #20645 ) ;
#17645=ORIENTED_EDGE ( 'NONE', *, *, #58725, .F. ) ;
#17655=CARTESIAN_POINT ( 'NONE',  ( 17.91037351677410072, -3.107515944418828280, -12.21078942061118155 ) ) ;
#17665=CARTESIAN_POINT ( 'NONE',  ( 12.41482009541958931, 2.988314721215474368, -13.55768135971568178 ) ) ;
#17668=CARTESIAN_POINT ( 'NONE',  ( 17.67410956179875114, -0.7206971133477443336, 13.98143832535763131 ) ) ;
#17669=CARTESIAN_POINT ( 'NONE',  ( 17.88363324756175388, 0.5317637309505709453, 13.88630818040731718 ) ) ;
#17675=CARTESIAN_POINT ( 'NONE',  ( 12.39828470338709110, -0.4745495849572874958, 13.88909655037513602 ) ) ;
#17676=CARTESIAN_POINT ( 'NONE',  ( 12.24748039821077583, -0.2825697095353449928, -13.89613713856699029 ) ) ;
#17687=CARTESIAN_POINT ( 'NONE',  ( 17.71747088695468264, 0.6038699852804538803, 12.68066884516330362 ) ) ;
#17696=CARTESIAN_POINT ( 'NONE',  ( 12.58276127734165151, -1.915504326815320901, 13.78019217388816919 ) ) ;
#17706=CARTESIAN_POINT ( 'NONE',  ( 12.16008153508535194, -0.3287229608534210090, -12.59571550161850340 ) ) ;
#17722=CARTESIAN_POINT ( 'NONE',  ( 18.15872407313727876, -0.1621987986621310773, -13.89873133405096794 ) ) ;
#17734=CARTESIAN_POINT ( 'NONE',  ( 12.80505043854146940, -3.248109929747638347, 13.61799478206225444 ) ) ;
#17745=CARTESIAN_POINT ( 'NONE',  ( 17.83364017334651308, -3.059569048391924451, 12.30342972110860345 ) ) ;
#17753=CARTESIAN_POINT ( 'NONE',  ( 18.18005043799233178, 2.500000011518615395, -12.45159158845316405 ) ) ;
#17775=CARTESIAN_POINT ( 'NONE',  ( 18.25665235842813061, 2.332587565413955399, 13.80433135817204970 ) ) ;
#17787=CARTESIAN_POINT ( 'NONE',  ( 18.07920178076630435, -2.013390639430573170, -13.85446980737595979 ) ) ;
#17799=ORIENTED_EDGE ( 'NONE', *, *, #43986, .T. ) ;
#17802=ORIENTED_EDGE ( 'NONE', *, *, #6462, .T. ) ;
#17811=CARTESIAN_POINT ( 'NONE',  ( 12.09872039853181036, 2.644866564252636110, -12.31930286224045368 ) ) ;
#17819=B_SPLINE_SURFACE_WITH_KNOTS ( 'NONE', 1, 3, ( 
 ( #58403, #31847, #3539, #57712, #46206, #67513, #62278, #14396, #57032, #31168, #30470, #14733, #36049, #57366, #19980, #41302, #9820, #9470, #30812, #4227, #25564, #20314, #54543, #65007, #53848, #64318, #22024, #17126, #48954, #38809, #22717, #26603, #27288, #48257, #48608, #713, #26945, #365, #21679, #43372, #43014, #32875, #16439, #5945, #59092, #17486, #11533, #32195, #47924, #5599, #37768, #32533, #38461, #16776, #5263, #59433, #6286, #27981, #11195, #10851, #16098, #53163, #64671, #38107, #54187, #53510, #27633, #1063, #1400, #11884, #33221, #22374, #60134, #43713, #59780, #6640, #22, #12243, #49289, #44065, #65366, #21342, #42672, #58746, #63979, #37423, #29028, #39849, #51024, #34616, #3123, #49992, #55929, #23762, #49640, #18525, #33569, #2781, #61514, #8378, #7332, #6989, #40197, #2434 ),
 ( #40525, #56268, #45097, #34954, #8031, #45440, #66406, #29369, #12935, #7687, #50684, #24454, #1746, #23067, #66752, #44415, #2103, #55234, #18869, #54888, #23420, #13291, #28675, #13629, #45779, #61170, #65715, #19202, #29721, #44756, #39155, #24107, #67090, #61851, #28319, #17836, #60479, #12587, #33916, #66059, #18179, #39501, #60824, #34262, #55584, #50337, #51363, #20232, #52037, #31418, #20573, #52734, #30390, #15335, #25821, #14650, #25134, #4140, #47151, #9732, #68801, #4829, #56612, #57281, #9051, #9385, #30730, #56952, #46466, #51700, #31081, #67767, #4481, #30061, #8718, #19893, #3797, #20922, #36663, #25476, #57983, #36312, #68451, #46808, #14985, #62531, #68114, #57629, #26171, #3458, #24795, #41899, #46121, #41220, #35640, #63206, #13968, #35966, #62867, #41557, #10080, #47496, #52386, #67427 ) ),
 .UNSPECIFIED., .F., .F., .F.,
 ( 2, 2 ),
 ( 4, 2, 2, 2, 2, 2, 2, 2, 2, 2, 2, 2, 2, 2, 2, 2, 2, 2, 2, 2, 2, 2, 2, 2, 2, 2, 2, 2, 2, 2, 2, 2, 2, 2, 2, 2, 2, 2, 2, 2, 2, 2, 2, 2, 2, 2, 2, 2, 2, 2, 2, 4 ),
 ( 0.000000000000000000, 1.000000000000000000 ),
 ( 0.000000000000000000, 7.157017711320847928E-05, 0.0001431403542264169586, 0.0002147105313396254378, 0.0002326030756179275644, 0.0002504956198962296639, 0.0002862807084528339171, 0.0003220657970094381703, 0.0003578508855660424235, 0.0003936359741226466225, 0.0004294210626792508757, 0.0004652061512358551289, 0.0005009912397924593279, 0.0005367763283490635268, 0.0005725614169056678342, 0.0006441315940188763406, 0.0006799166825754805396, 0.0007157017711320848470, 0.0007335943154103870007, 0.0007514868596886890460, 0.0007872719482452932450, 0.0008588421253585017514, 0.0008946272139151059503, 0.0009304123024717102577, 0.0009661973910283144567, 0.001001982479584918656, 0.001073552656698127054, 0.001145122833811335668, 0.001216693010924544283, 0.001288263188037752681, 0.001359833365150961079, 0.001395618453707565387, 0.001431403542264169694, 0.001467188630820774001, 0.001502973719377378092, 0.001574543896490586490, 0.001646114073603795105, 0.001681899162160399412, 0.001717684250717003503, 0.001735576794995305656, 0.001753469339273607593, 0.001789254427830211901, 0.001860824604943420515, 0.001896609693500024823, 0.001932394782056628913, 0.001968179870613233004, 0.001986072414891535375, 0.002003964959169837311, 0.002075535136283045493, 0.002147105313396254107, 0.002218675490509462722, 0.002290245667622671337 ),
 .UNSPECIFIED. ) ;
#17820=CARTESIAN_POINT ( 'NONE',  ( 12.09902206169136818, -2.644659774828333365, -12.31933076163361029 ) ) ;
#17827=CARTESIAN_POINT ( 'NONE',  ( 18.06356912472852372, -0.3639343692979916667, -12.69299665021505419 ) ) ;
#17836=CARTESIAN_POINT ( 'NONE',  ( 18.07985789204853688, 2.160546346826199837, 12.52419258880425446 ) ) ;
#17845=CARTESIAN_POINT ( 'NONE',  ( 12.33364759508191355, -3.027124203391260870, 12.23096800428945841 ) ) ;
#17850=CARTESIAN_POINT ( 'NONE',  ( 12.57154173166082956, -0.6810629908226978335, 12.58158054216573518 ) ) ;
#17853=CARTESIAN_POINT ( 'NONE',  ( 12.78086743291007821, 1.761210985583066213, 12.47630298729255571 ) ) ;
#17870=CARTESIAN_POINT ( 'NONE',  ( 17.55505043854144276, -0.6250000000000001110, -12.67928921589118474 ) ) ;
#17871=CARTESIAN_POINT ( 'NONE',  ( 12.43914160838493821, -1.887194142572512945, 13.87222517180307690 ) ) ;
#17878=CARTESIAN_POINT ( 'NONE',  ( 18.15919096721171400, 2.338588349694056490, -13.70638546470270214 ) ) ;
#17883=CARTESIAN_POINT ( 'NONE',  ( 17.96249544862750369, 2.025954803622692868, -12.54949280001588896 ) ) ;
#17891=CARTESIAN_POINT ( 'NONE',  ( 17.92038287126899121, 0.6379138416578098436, -13.98550699733554303 ) ) ;
#17893=CARTESIAN_POINT ( 'NONE',  ( 12.24260341319699918, -2.772876882430816536, 12.38382274645855041 ) ) ;
#17894=ORIENTED_EDGE ( 'NONE', *, *, #36467, .T. ) ;
#17897=CARTESIAN_POINT ( 'NONE',  ( 17.86985707050058636, -3.040024008573237069, 13.54397559521889605 ) ) ;
#17902=CARTESIAN_POINT ( 'NONE',  ( 12.80505043854143388, 3.124999999999999556, -12.28374638332999602 ) ) ;
#17910=EDGE_LOOP ( 'NONE', ( #18101, #19663, #50793, #29860 ) ) ;
#17919=CARTESIAN_POINT ( 'NONE',  ( 12.27233953995986582, 2.172968329541575372, 13.73735571485410745 ) ) ;
#17924=CARTESIAN_POINT ( 'NONE',  ( 12.60420804235854675, -0.5919407257947376655, 13.88303015925714590 ) ) ;
#17946=ORIENTED_EDGE ( 'NONE', *, *, #15270, .T. ) ;
#17948=VECTOR ( 'NONE', #18275, 1000.000000000000114 ) ;
#17966=CARTESIAN_POINT ( 'NONE',  ( 12.23350478622814741, 2.246345293432832513, -13.72400836783244849 ) ) ;
#17971=CARTESIAN_POINT ( 'NONE',  ( 12.47502503668309615, 0.5311540453515636306, -13.88634387573209494 ) ) ;
#17974=DIRECTION ( 'NONE',  ( 1.000000000000000000, 0.000000000000000000, 0.000000000000000000 ) ) ;
#17979=CARTESIAN_POINT ( 'NONE',  ( 17.84567419427290602, 3.186977498899956185, -13.63243182350604243 ) ) ;
#17985=CARTESIAN_POINT ( 'NONE',  ( 18.18005043854144276, 0.000000000000000000, -25.00000000000000000 ) ) ;
#17986=CARTESIAN_POINT ( 'NONE',  ( 18.04535692659925417, 0.3877536850257900514, -12.69203640188974447 ) ) ;
#17987=AXIS2_PLACEMENT_3D ( 'NONE', #17249, #39615, #23875 ) ;
#17996=VERTEX_POINT ( 'NONE', #27266 ) ;
#17998=B_SPLINE_CURVE_WITH_KNOTS ( 'NONE', 1,
 ( #12833, #19099 ),
 .UNSPECIFIED., .F., .F.,
 ( 2, 2 ),
 ( 0.000000000000000000, 1.000000000000000000 ),
 .UNSPECIFIED. ) ;
#17999=CARTESIAN_POINT ( 'NONE',  ( 18.02766945781921137, -1.934589073148406779, -12.45059934707292548 ) ) ;
#18000=CIRCLE ( 'NONE', #34721, 12.84999890301999947 ) ;
#18010=CARTESIAN_POINT ( 'NONE',  ( 17.55505043854144276, 0.6250000000000001110, -25.00000000000000000 ) ) ;
#18013=CARTESIAN_POINT ( 'NONE',  ( 12.51770044094176981, 3.055120810438261891, -13.53992139506082104 ) ) ;
#18016=CARTESIAN_POINT ( 'NONE',  ( 17.57900095810616037, -0.7302151993337174796, 13.98094363222392467 ) ) ;
#18023=CARTESIAN_POINT ( 'NONE',  ( 12.31002172256219929, -0.3816054325215895160, 13.89295103372929496 ) ) ;
#18034=CARTESIAN_POINT ( 'NONE',  ( 12.61475641026223649, 0.7110419930738796079, 13.98197980709405108 ) ) ;
#18049=CARTESIAN_POINT ( 'NONE',  ( 12.11827192994440772, 0.2307628456012717488, -12.59789151516663175 ) ) ;
#18064=CARTESIAN_POINT ( 'NONE',  ( 17.98240304306455428, -0.4561791668615495787, -13.88992602861184089 ) ) ;
#18065=EDGE_CURVE ( 'NONE', #16046, #38239, #6281, .T. ) ;
#18072=CARTESIAN_POINT ( 'NONE',  ( 18.17608830303634093, -2.571081551981528879, 12.43475473546731891 ) ) ;
#18077=CARTESIAN_POINT ( 'NONE',  ( 12.61587921995040595, -3.224448188361915157, 13.62362021573694015 ) ) ;
#18085=CARTESIAN_POINT ( 'NONE',  ( 17.94956985871015931, -2.984774188598619649, 12.32531689504261685 ) ) ;
#18087=EDGE_CURVE ( 'NONE', #22430, #13791, #67068, .T. ) ;
#18091=CARTESIAN_POINT ( 'NONE',  ( 18.17891100653320891, 2.457162529407604712, 13.68241659864889748 ) ) ;
#18101=ORIENTED_EDGE ( 'NONE', *, *, #1880, .T. ) ;
#18111=AXIS2_PLACEMENT_3D ( 'NONE', #5188, #26525, #69161 ) ;
#18116=ORIENTED_EDGE ( 'NONE', *, *, #46844, .T. ) ;
#18118=CARTESIAN_POINT ( 'NONE',  ( 17.67509761310384064, 1.797476384633017066, 13.88413128968476684 ) ) ;
#18152=CARTESIAN_POINT ( 'NONE',  ( 12.10442723766653472, 2.667336250084659799, -12.31445622895738978 ) ) ;
#18162=CARTESIAN_POINT ( 'NONE',  ( 12.40831127361658837, -1.878029834076337723, -12.45925554172551308 ) ) ;
#18168=CARTESIAN_POINT ( 'NONE',  ( 12.20116045406121863, -2.662322297126388015, -13.63765712018376952 ) ) ;
#18169=CARTESIAN_POINT ( 'NONE',  ( 18.12436022580823902, 0.2580991232524043055, -12.69647497719791573 ) ) ;
#18179=CARTESIAN_POINT ( 'NONE',  ( 18.10356236467037050, 2.200227019994205779, 12.51636715934673205 ) ) ;
#18184=VERTEX_POINT ( 'NONE', #15316 ) ;
#18185=CARTESIAN_POINT ( 'NONE',  ( 12.21314472040068644, -2.700933736278045227, 12.40250870093142410 ) ) ;
#18192=CARTESIAN_POINT ( 'NONE',  ( 12.16275096843967951, -0.3336735144251360974, 12.59558214381612551 ) ) ;
#18196=ORIENTED_EDGE ( 'NONE', *, *, #32578, .F. ) ;
#18201=CARTESIAN_POINT ( 'NONE',  ( 17.88362877536322060, -0.5317665474973085615, 12.68501283761687226 ) ) ;
#18209=CARTESIAN_POINT ( 'NONE',  ( 18.11804139221521837, -2.771758052479264656, 13.61206300402962910 ) ) ;
#18224=DIRECTION ( 'NONE',  ( -1.000000000000000000, 0.000000000000000000, 0.000000000000000000 ) ) ;
#18228=EDGE_CURVE ( 'NONE', #44093, #46698, #9361, .T. ) ;
#18234=DIRECTION ( 'NONE',  ( 1.000000000000000000, 0.000000000000000000, 0.000000000000000000 ) ) ;
#18235=CARTESIAN_POINT ( 'NONE',  ( 12.22440656761272137, -2.731388741841335399, 12.39466681327069786 ) ) ;
#18239=CARTESIAN_POINT ( 'NONE',  ( 17.89590342297357495, -3.023973030522680627, 13.54825986461598397 ) ) ;
#18246=CARTESIAN_POINT ( 'NONE',  ( 17.55505043854147118, -3.125000000000000000, -25.00000000000000000 ) ) ;
#18262=CARTESIAN_POINT ( 'NONE',  ( 12.36790649065924086, 2.053195086250957591, 13.75808315936462378 ) ) ;
#18264=VERTEX_POINT ( 'NONE', #41879 ) ;
#18266=CARTESIAN_POINT ( 'NONE',  ( 12.09857429938281825, 0.1657344298535193272, 13.99903850390423088 ) ) ;
#18275=DIRECTION ( 'NONE',  ( -0.7071067939406878722, 0.000000000000000000, 0.7071067684324069402 ) ) ;
#18297=DIRECTION ( 'NONE',  ( 0.000000000000000000, -1.000000000000000000, 0.000000000000000000 ) ) ;
#18313=CARTESIAN_POINT ( 'NONE',  ( 12.09164601416805418, -0.1306247939804573710, -13.99939550958098344 ) ) ;
#18322=CARTESIAN_POINT ( 'NONE',  ( 17.98481728017920744, 2.046093834626821373, -13.75931539188737673 ) ) ;
#18331=ORIENTED_EDGE ( 'NONE', *, *, #33192, .T. ) ;
#18333=B_SPLINE_CURVE_WITH_KNOTS ( 'NONE', 3,
 ( #66494, #3218, #35046, #24885 ),
 .UNSPECIFIED., .F., .F.,
 ( 4, 4 ),
 ( 0.000000000000000000, 1.000000000000000000 ),
 .UNSPECIFIED. ) ;
#18335=CARTESIAN_POINT ( 'NONE',  ( 18.15125492452900957, -2.687770500432731691, -13.63179079422069861 ) ) ;
#18341=DIRECTION ( 'NONE',  ( 1.000000000000000000, 0.000000000000000000, 0.000000000000000000 ) ) ;
#18344=CARTESIAN_POINT ( 'NONE',  ( 18.16715147695115817, -2.094590662098729794, -12.42468172752983868 ) ) ;
#18354=CARTESIAN_POINT ( 'NONE',  ( 17.55505043854147118, -3.248147246781390329, -13.61798588129781074 ) ) ;
#18355=CARTESIAN_POINT ( 'NONE',  ( 12.25686392147156667, 2.040034559784659418, -13.85057184956195542 ) ) ;
#18358=CARTESIAN_POINT ( 'NONE',  ( 18.10142235202799199, 0.3036576181174170941, 13.89554011873103612 ) ) ;
#18366=CARTESIAN_POINT ( 'NONE',  ( 12.18002302684040572, 0.03981422818502264316, 13.90000146831297023 ) ) ;
#18367=CARTESIAN_POINT ( 'NONE',  ( 12.19576242957797518, -2.360357254127059434, 13.70208745183731835 ) ) ;
#18372=DIRECTION ( 'NONE',  ( -0.000000000000000000, -0.000000000000000000, 1.000000000000000000 ) ) ;
#18374=ORIENTED_EDGE ( 'NONE', *, *, #33192, .F. ) ;
#18375=CARTESIAN_POINT ( 'NONE',  ( 12.57118179866913366, -0.6928235585660844631, 13.98285841810620234 ) ) ;
#18377=CARTESIAN_POINT ( 'NONE',  ( 4.700001368028300597, 0.000000000000000000, 0.000000000000000000 ) ) ;
#18378=CARTESIAN_POINT ( 'NONE',  ( 12.20062903852581293, -0.1603600964026583309, 12.69865684038667908 ) ) ;
#18379=CARTESIAN_POINT ( 'NONE',  ( 18.13957898673052327, -2.721486385301765676, -12.39720401458348675 ) ) ;
#18384=CARTESIAN_POINT ( 'NONE',  ( 12.35317296531423104, -2.068098628661974914, 13.75563068618459184 ) ) ;
#18388=B_SPLINE_SURFACE_WITH_KNOTS ( 'NONE', 1, 3, ( 
 ( #64990, #33204, #54523, #6625, #22699, #44044, #65348, #27268, #49622, #1727, #345, #53829, #48591, #44397, #17468, #54870, #694, #11514, #6970, #21662, #32858, #32178, #54169, #53491, #5583, #22006, #42995, #64304, #37750, #16422, #11177, #43354, #65696, #34934, #24436, #40506, #39484, #39134, #3102, #34598, #55911, #12917, #29702, #33898, #61153, #17820, #60461, #18508, #13271, #24089, #61831, #13951, #2764, #30042, #12568, #23742, #55565, #45422, #66732, #8014, #29352, #18851, #45762, #67070, #7666, #51346, #3438, #7315, #34245, #29013, #24775, #13612, #19183, #50319, #50663, #35276, #2084, #40178, #55216, #45080, #56593, #39832, #2418, #61494, #8357, #18162, #56250, #28657, #51004, #49969, #8699, #23402, #44740, #60806, #66038, #66387, #14967, #36291, #62512, #10065, #14293, #41536, #46102, #40850, #68094, #62849, #4463, #42241 ),
 ( #67408, #56934, #58302, #52018, #14630, #68786, #46788, #31399, #19530, #35949, #25803, #47136, #4812, #57610, #4119, #62171, #25115, #20211, #5165, #36990, #35622, #10406, #9031, #30372, #51680, #67747, #41882, #19871, #3778, #30709, #68435, #57263, #9363, #25456, #41202, #9715, #31060, #52370, #52715, #26153, #63546, #20557, #47479, #57965, #63188, #15318, #36642, #20903, #15658, #31748, #53065, #46446, #37326, #48856, #33470, #38358, #16682, #69138, #59335, #964, #59684, #266, #22275, #27186, #32435, #60030, #54090, #43264, #53751, #48163, #6188, #27883, #11783, #48508, #37668, #64569, #64912, #38010, #22617, #43960, #11436, #58650, #43618, #54786, #33123, #32777, #21246, #27529, #17026, #54438, #21581, #6539, #614, #5848, #12139, #49194, #1302, #21926, #42918, #65267, #17381, #5509, #38710, #26498, #47828, #42573, #63883, #64225 ) ),
 .UNSPECIFIED., .F., .F., .F.,
 ( 2, 2 ),
 ( 4, 2, 2, 2, 2, 2, 2, 2, 2, 2, 2, 2, 2, 2, 2, 2, 2, 2, 2, 2, 2, 2, 2, 2, 2, 2, 2, 2, 2, 2, 2, 2, 2, 2, 2, 2, 2, 2, 2, 2, 2, 2, 2, 2, 2, 2, 2, 2, 2, 2, 2, 2, 2, 4 ),
 ( 0.000000000000000000, 1.000000000000000000 ),
 ( 0.000000000000000000, 7.156607294609339200E-05, 0.0001431321458921867840, 0.0001789151823652334597, 0.0002146982188382801624, 0.0002325897370748035138, 0.0002504812553113268652, 0.0002862642917843735680, 0.0003220473282574202708, 0.0003578303647304669193, 0.0003936134012035136221, 0.0004293964376765603249, 0.0004651794741496070276, 0.0004830709923861303519, 0.0005009625106226537304, 0.0005725285835687471360, 0.0006440946565148405415, 0.0007156607294609338386, 0.0007872268024070272442, 0.0008587928753531206497, 0.0008945759118261674067, 0.0009303589482992140553, 0.0009661419847722607038, 0.001001925021245307461, 0.001037708057718354218, 0.001073491094191400975, 0.001145057167137494272, 0.001180840203610541029, 0.001216623240083587569, 0.001252406276556634326, 0.001288189313029681083, 0.001359755385975774380, 0.001395538422448821137, 0.001431321458921867677, 0.001467104495394914434, 0.001502887531867961191, 0.001574453604814054488, 0.001646019677760147785, 0.001681802714233194542, 0.001717585750706241299, 0.001753368787179288056, 0.001789151823652334813, 0.001860717896598428111, 0.001896500933071474868, 0.001932283969544521408, 0.001968067006017567948, 0.002003850042490614922, 0.002039633078963661895, 0.002075416115436708436, 0.002146982188382801950, 0.002182765224855848490, 0.002218548261328895030, 0.002254331297801942004, 0.002290114334274988544 ),
 .UNSPECIFIED. ) ;
#18392=CARTESIAN_POINT ( 'NONE',  ( 12.25943167926922861, 0.4738025322793235627, -12.59109159930368449 ) ) ;
#18405=ORIENTED_EDGE ( 'NONE', *, *, #7360, .T. ) ;
#18411=CARTESIAN_POINT ( 'NONE',  ( 18.25531185377812449, -0.1895042076700518829, -13.99872220539657697 ) ) ;
#18415=DIRECTION ( 'NONE',  ( 1.000000000000000000, 0.000000000000000000, 0.000000000000000000 ) ) ;
#18417=CARTESIAN_POINT ( 'NONE',  ( 18.17920460084962286, -2.538974945121682758, 12.44245230910560451 ) ) ;
#18421=EDGE_CURVE ( 'NONE', #18264, #16254, #62505, .T. ) ;
#18432=CARTESIAN_POINT ( 'NONE',  ( 12.22351867101279232, -0.2292390942789200303, -13.89746050377129727 ) ) ;
#18433=CARTESIAN_POINT ( 'NONE',  ( 17.98432920965427328, -2.954704375608637967, 12.33394473884601794 ) ) ;
#18453=VECTOR ( 'NONE', #60169, 1000.000000000000000 ) ;
#18456=CARTESIAN_POINT ( 'NONE',  ( 18.24522866045826675, -0.2205548374446849313, 12.59807454672507632 ) ) ;
#18462=CARTESIAN_POINT ( 'NONE',  ( 17.92097207270825265, 1.887179018856774748, 13.87222722961341326 ) ) ;
#18476=ORIENTED_EDGE ( 'NONE', *, *, #37007, .T. ) ;
#18492=ORIENTED_EDGE ( 'NONE', *, *, #4738, .T. ) ;
#18498=CARTESIAN_POINT ( 'NONE',  ( 12.14412415394998668, 2.776584135961351674, -12.29026848248285830 ) ) ;
#18508=CARTESIAN_POINT ( 'NONE',  ( 12.09179812036145663, -2.610377073672084158, -12.32664058968471998 ) ) ;
#18516=CARTESIAN_POINT ( 'NONE',  ( 12.18472169747688660, -2.421093590824783703, -13.68984525495557314 ) ) ;
#18517=CARTESIAN_POINT ( 'NONE',  ( 18.02541143671232504, -0.4116921281473265304, -12.69102089861181248 ) ) ;
#18525=CARTESIAN_POINT ( 'NONE',  ( 17.81301359322643307, 3.153051599267165717, 12.19911286921121452 ) ) ;
#18526=CARTESIAN_POINT ( 'NONE',  ( 17.55505043854143921, -0.7302158263239086899, 13.98094363220831049 ) ) ;
#18529=CARTESIAN_POINT ( 'NONE',  ( 12.57114114721769838, -0.6824382160044792922, -12.58151825845880367 ) ) ;
#18531=CARTESIAN_POINT ( 'NONE',  ( 12.25653845796827035, -2.200227119461482861, 12.51640343681225787 ) ) ;
#18536=CARTESIAN_POINT ( 'NONE',  ( 12.31563516348837695, 0.3888461597108430756, 12.69199065798140680 ) ) ;
#18542=CARTESIAN_POINT ( 'NONE',  ( 12.64104727702813413, 1.896551500700491832, 12.57186431639862256 ) ) ;
#18554=CARTESIAN_POINT ( 'NONE',  ( 18.07980528509186868, -0.3396180385173929173, -12.69389128024175939 ) ) ;
#18557=CARTESIAN_POINT ( 'NONE',  ( 17.96849574077155154, -2.968826013449940238, 13.56277633467806787 ) ) ;
#18562=LINE ( 'NONE', #15715, #29921 ) ;
#18579=CARTESIAN_POINT ( 'NONE',  ( 18.20121223423996781, -0.3818843735617438173, -13.99543728850909297 ) ) ;
#18581=CARTESIAN_POINT ( 'NONE',  ( 12.23606560774678087, -2.758669204864329760, 12.38755309842819763 ) ) ;
#18585=CARTESIAN_POINT ( 'NONE',  ( 17.63746348810185793, -1.880115813469444230, 13.78555441649717928 ) ) ;
#18587=ORIENTED_EDGE ( 'NONE', *, *, #19573, .T. ) ;
#18608=CARTESIAN_POINT ( 'NONE',  ( 12.42225061842103173, 2.005837741177417310, 13.76588300560132261 ) ) ;
#18611=CARTESIAN_POINT ( 'NONE',  ( 12.34510720075386558, 0.4232991632631661894, -12.69050643261670430 ) ) ;
#18612=CARTESIAN_POINT ( 'NONE',  ( 12.58477985662609022, -0.5849891190461631307, 13.88342664904964430 ) ) ;
#18618=CARTESIAN_POINT ( 'NONE',  ( 17.55505043854143565, 3.125000000000000000, -25.00000000000000000 ) ) ;
#18623=DIRECTION ( 'NONE',  ( 1.000000000000000000, 0.000000000000000000, 0.000000000000000000 ) ) ;
#18624=CARTESIAN_POINT ( 'NONE',  ( 12.39015342239245854, 3.070413439580832016, 12.22017215029075388 ) ) ;
#18642=CARTESIAN_POINT ( 'NONE',  ( 12.30950027207670239, 2.881007065246251386, 13.58518188446331187 ) ) ;
#18646=CARTESIAN_POINT ( 'NONE',  ( 18.25703273071135158, 2.298329627318192792, -12.38863175403534989 ) ) ;
#18656=CARTESIAN_POINT ( 'NONE',  ( 12.18894359730773580, -0.3856318793704111569, -13.99470184309725873 ) ) ;
#18664=CARTESIAN_POINT ( 'NONE',  ( 18.17181771166723792, 2.603111764601558686, -13.65106951237197030 ) ) ;
#18672=CARTESIAN_POINT ( 'NONE',  ( 18.06407908477376623, 0.3627935496694635886, -12.69302875402908803 ) ) ;
#18679=ORIENTED_EDGE ( 'NONE', *, *, #66995, .T. ) ;
#18684=CARTESIAN_POINT ( 'NONE',  ( 18.22966818124863408, -2.744306698987320381, -12.29751612260396776 ) ) ;
#18688=B_SPLINE_CURVE_WITH_KNOTS ( 'NONE', 3,
 ( #59690, #48514, #21932, #11791, #43270, #64578, #59341, #16688, #38016, #54446, #32784, #49201, #54098, #43967, #6194, #1308 ),
 .UNSPECIFIED., .F., .F.,
 ( 4, 2, 2, 2, 2, 2, 2, 4 ),
 ( 0.000000000000000000, 0.06249999999999911182, 0.1249999999999982236, 0.2499999999999983347, 0.4999999999999987788, 0.7499999999999992228, 0.8749999999999996669, 1.000000000000000000 ),
 .UNSPECIFIED. ) ;
#18697=CARTESIAN_POINT ( 'NONE',  ( 12.21493840618615501, 2.942228658260936935, -13.68734401625692954 ) ) ;
#18700=CARTESIAN_POINT ( 'NONE',  ( 17.83170738868395588, 0.5608030988280853224, 13.88477341743901938 ) ) ;
#18702=EDGE_LOOP ( 'NONE', ( #43090, #36317, #50984, #45060 ) ) ;
#18708=CARTESIAN_POINT ( 'NONE',  ( 12.20205663652224892, -2.664445670458811755, 13.63720455645838214 ) ) ;
#18718=CARTESIAN_POINT ( 'NONE',  ( 17.60655599801541271, 0.6229596466635312080, 12.67942438339646571 ) ) ;
#18719=CARTESIAN_POINT ( 'NONE',  ( 12.23148815955828184, -0.2485241243391712040, 12.69673260777796209 ) ) ;
#18720=CARTESIAN_POINT ( 'NONE',  ( 17.76019544541307127, -3.091716410407808535, -12.29381940409253104 ) ) ;
#18723=CARTESIAN_POINT ( 'NONE',  ( 12.07911454974952115, -2.296549521770721913, -12.39040777274321670 ) ) ;
#18736=CARTESIAN_POINT ( 'NONE',  ( 12.27985646406008335, -0.3389720875425251689, -12.69391532355469110 ) ) ;
#18739=AXIS2_PLACEMENT_3D ( 'NONE', #40638, #40305, #3913 ) ;
#18747=PLANE ( 'NONE',  #17200 ) ;
#18754=CARTESIAN_POINT ( 'NONE',  ( 18.10028295948237798, -0.4818816852691614194, -13.99171642476389898 ) ) ;
#18765=CARTESIAN_POINT ( 'NONE',  ( 12.43967993051479759, -3.007449918965191760, -13.55258931251709242 ) ) ;
#18768=CARTESIAN_POINT ( 'NONE',  ( 12.08083412505908427, -2.710618184188187119, 13.73644169169829965 ) ) ;
#18776=CARTESIAN_POINT ( 'NONE',  ( 12.18028570900101215, -0.01996689158402697659, -13.89998575767903155 ) ) ;
#18777=CARTESIAN_POINT ( 'NONE',  ( 18.13637388831912745, -2.729759562904666037, 12.39509076542458921 ) ) ;
#18802=CARTESIAN_POINT ( 'NONE',  ( 17.67321935251239751, -0.7100593550699877410, 12.57997761080729759 ) ) ;
#18809=CARTESIAN_POINT ( 'NONE',  ( 18.06232794982559753, 1.996188719851612170, 13.85695876210811406 ) ) ;
#18813=ORIENTED_EDGE ( 'NONE', *, *, #19990, .T. ) ;
#18819=VERTEX_POINT ( 'NONE', #4502 ) ;
#18843=CARTESIAN_POINT ( 'NONE',  ( 12.21868246241196587, 2.283434118842407656, -12.49941978418538824 ) ) ;
#18846=VERTEX_POINT ( 'NONE', #19570 ) ;
#18851=CARTESIAN_POINT ( 'NONE',  ( 12.09756245983761147, -2.320968861236850422, -12.38441143973091840 ) ) ;
#18857=CARTESIAN_POINT ( 'NONE',  ( 12.58300520725476623, -3.084588251740257192, -13.53188417542246214 ) ) ;
#18858=CARTESIAN_POINT ( 'NONE',  ( 17.80401300531091024, -0.5733651658914323823, -12.68257300503909768 ) ) ;
#18861=CARTESIAN_POINT ( 'NONE',  ( 17.75579847504525333, -3.171737058802227338, 12.19426492080491542 ) ) ;
#18869=CARTESIAN_POINT ( 'NONE',  ( 17.87014202174171373, 1.960141137139741252, 12.56108054050352507 ) ) ;
#18875=CARTESIAN_POINT ( 'NONE',  ( 12.34586232581682808, -2.075512354070471854, 12.54043254740684077 ) ) ;
#18881=CARTESIAN_POINT ( 'NONE',  ( 12.55627843433555846, 0.5734477787136632587, 12.68256797703445038 ) ) ;
#18887=CARTESIAN_POINT ( 'NONE',  ( 12.58248715490565672, 1.915879699765342226, 12.56863216566090991 ) ) ;
#18903=CARTESIAN_POINT ( 'NONE',  ( 12.54773036592023949, -3.200672309338196797, 13.62922281487128906 ) ) ;
#18915=DIRECTION ( 'NONE',  ( -1.000000000000000000, 0.000000000000000000, 0.000000000000000000 ) ) ;
#18922=CARTESIAN_POINT ( 'NONE',  ( 12.26368341514495519, -2.812488373138167130, 12.37327521545045883 ) ) ;
#18925=CARTESIAN_POINT ( 'NONE',  ( 18.08598429698836085, -3.015255620044101192, 13.67144160714441981 ) ) ;
#18926=CARTESIAN_POINT ( 'NONE',  ( 17.55505043854143565, 3.125000000000000000, -13.52084414783465682 ) ) ;
#18938=CARTESIAN_POINT ( 'NONE',  ( 17.99623368854100747, 0.5708113556792957510, -12.58706429964239071 ) ) ;
#18939=DIRECTION ( 'NONE',  ( 0.000000000000000000, 0.7198977633594745296, 0.6940801180771756229 ) ) ;
#18947=CARTESIAN_POINT ( 'NONE',  ( 12.49029065891180146, 1.959656569402035142, 13.77327738386123102 ) ) ;
#18950=CARTESIAN_POINT ( 'NONE',  ( 12.18827089113675832, -0.1029087316210665626, -12.69945830692974553 ) ) ;
#18951=CARTESIAN_POINT ( 'NONE',  ( 12.78440349184324454, -0.6249994334955771835, 13.88107975403459626 ) ) ;
#18958=DIRECTION ( 'NONE',  ( -0.000000000000000000, -0.000000000000000000, 1.000000000000000000 ) ) ;
#18964=CARTESIAN_POINT ( 'NONE',  ( 12.58137933218754867, 3.164643396295684141, 12.19610741112356322 ) ) ;
#18985=CARTESIAN_POINT ( 'NONE',  ( 18.08807463888091860, 1.992345594299818501, -12.44148860874185125 ) ) ;
#19002=CARTESIAN_POINT ( 'NONE',  ( 18.10179698720198971, 2.997559868305863962, -13.67533242386441472 ) ) ;
#19007=EDGE_CURVE ( 'NONE', #34497, #38102, #32055, .T. ) ;
#19020=DIRECTION ( 'NONE',  ( 0.000000000000000000, 0.000000000000000000, 1.000000000000000000 ) ) ;
#19023=CARTESIAN_POINT ( 'NONE',  ( 17.87877696946770811, -3.124133162484060033, -12.20654824865395049 ) ) ;
#19031=CARTESIAN_POINT ( 'NONE',  ( 12.42020189403035779, 3.137187437229806086, -13.64398187047951971 ) ) ;
#19034=CARTESIAN_POINT ( 'NONE',  ( 17.78802761781599528, 0.6915911779535691695, 13.98290807251246548 ) ) ;
#19040=CARTESIAN_POINT ( 'NONE',  ( 12.27225454755311596, -2.172654780165926613, 13.73747135095148408 ) ) ;
#19053=CARTESIAN_POINT ( 'NONE',  ( 18.12461185120978868, 0.2575478136180248678, 12.69649014468028980 ) ) ;
#19054=CARTESIAN_POINT ( 'NONE',  ( 12.70148909159118844, -0.6166679310204360442, 12.67983904306179888 ) ) ;
#19064=CARTESIAN_POINT ( 'NONE',  ( 12.49249186488742680, -0.5416145769730054127, -12.68445494689095732 ) ) ;
#19069=ORIENTED_EDGE ( 'NONE', *, *, #68328, .T. ) ;
#19082=CARTESIAN_POINT ( 'NONE',  ( 18.25578913467704112, 0.1888260363403093667, -13.99874504378992413 ) ) ;
#19092=CARTESIAN_POINT ( 'NONE',  ( 17.96886609968857584, -2.968499926956239765, 12.32999726799531004 ) ) ;
#19099=CARTESIAN_POINT ( 'NONE',  ( 17.55505043854147118, -1.760845406083394682, 12.47635457398814829 ) ) ;
#19106=CARTESIAN_POINT ( 'NONE',  ( 12.47427908008581987, -0.5306878043354068542, -13.88636785578042421 ) ) ;
#19107=CARTESIAN_POINT ( 'NONE',  ( 18.16006747845244007, -2.341920795209953443, 12.48703680160762097 ) ) ;
#19130=FACE_OUTER_BOUND ( 'NONE', #8340, .T. ) ;
#19134=EDGE_CURVE ( 'NONE', #64166, #7303, #51241, .T. ) ;
#19136=ORIENTED_EDGE ( 'NONE', *, *, #3791, .T. ) ;
#19139=CARTESIAN_POINT ( 'NONE',  ( 17.99965052394114906, 1.940731178328044093, 13.86484045969604395 ) ) ;
#19141=DIRECTION ( 'NONE',  ( 1.000000000000000000, 0.000000000000000000, 0.000000000000000000 ) ) ;
#19146=CLOSED_SHELL ( 'NONE', ( #5869, #34070, #17550, #44949, #7055, #55904, #6373, #2873, #24871, #49985, #55116, #57093, #67961, #64711, #54632, #34419, #13849, #12959, #44013, #14847, #14132, #50541, #55316, #15476, #35796, #46655, #16088, #53616, #59120, #23837, #50527, #65419, #23915, #24001, #25393, #9335, #59657, #49003, #39479, #44140, #49794, #2627, #49474, #22436, #43536, #20704, #36520, #64004, #21686, #29814, #45369, #60362, #32280, #20207, #9208, #63064, #52725, #37009, #3022, #5346, #68025, #7797, #63421, #57916, #31283, #37355, #34152, #46013, #10175, #68806, #40443, #12228, #36409, #49051, #28845, #26861, #63430, #26401, #49577, #64453, #28407, #58478, #9074, #31535, #38030, #35638, #40272, #67382, #559, #645, #47066, #30398, #63822, #34851, #30722, #14990, #16556, #62809, #42079, #24419, #26524, #50519, #8490, #42002, #8214, #64685, #32316, #22040, #60635, #64762, #3988, #1756, #4471, #1569, #36519, #52662, #59597, #23238, #35753, #65022, #39756, #4164, #41433 ) ) ;
#19150=CARTESIAN_POINT ( 'NONE',  ( 18.03520353647602903, -3.065561386738608007, -13.66025540057654375 ) ) ;
#19161=ORIENTED_EDGE ( 'NONE', *, *, #40041, .T. ) ;
#19172=CARTESIAN_POINT ( 'NONE',  ( 12.39767999896653450, 2.025889534879409037, -12.54950459294603071 ) ) ;
#19178=B_SPLINE_CURVE_WITH_KNOTS ( 'NONE', 3,
 ( #55969, #66102, #40236, #13332, #8075, #12983, #55628, #29417, #50726, #45483, #61553, #13670, #34998, #56313, #57672, #47890, #16058, #3840, #36357, #10467, #9780, #58031, #46513, #63256, #58366, #42637, #30435, #20970, #31463, #51746, #62912, #31131, #56994, #63608, #9431, #47546, #52782, #20278, #52085, #63947, #31809, #25178, #52433, #4529, #15383, #53126 ),
 .UNSPECIFIED., .F., .F.,
 ( 4, 2, 2, 2, 2, 2, 2, 2, 2, 2, 2, 2, 2, 2, 1, 2, 2, 2, 2, 2, 1, 2, 2, 4 ),
 ( 0.000000000000000000, 0.06247329711231583427, 0.09370994566847631879, 0.1249465942246368033, 0.1405649185027146864, 0.1561832427807925694, 0.1874198913369436725, 0.2030382156150212780, 0.2186565398930988835, 0.2264657020321358682, 0.2342748641711728530, 0.2498931884492468225, 0.2811298370053947893, 0.2889389991444329397, 0.2967481612834710902, 0.3123664855615474467, 0.3279848098396238032, 0.3436031341177001597, 0.3748397826738527616, 0.3904581069519290071, 0.4060764312300053636, 0.4373130797861564112, 0.4685497283423075143, 0.4997863768984585620 ),
 .UNSPECIFIED. ) ;
#19182=ORIENTED_EDGE ( 'NONE', *, *, #65753, .F. ) ;
#19183=CARTESIAN_POINT ( 'NONE',  ( 12.18627227647246691, -2.104539383777993766, -12.42301525548629471 ) ) ;
#19189=CARTESIAN_POINT ( 'NONE',  ( 12.39041931600613466, -2.032227219086497616, -13.76156428297224998 ) ) ;
#19190=CARTESIAN_POINT ( 'NONE',  ( 17.62710295837868557, -0.6209187240130101815, -12.67955909024710337 ) ) ;
#19201=FACE_BOUND ( 'NONE', #63394, .T. ) ;
#19202=CARTESIAN_POINT ( 'NONE',  ( 17.98531014845338660, 2.046560857067137640, 12.54571659797612071 ) ) ;
#19207=CARTESIAN_POINT ( 'NONE',  ( 12.76350981947229890, -1.876041592482997400, 12.57528602315340294 ) ) ;
#19212=CARTESIAN_POINT ( 'NONE',  ( 12.30935811146625980, 0.3808128809978839624, 12.69231869260112155 ) ) ;
#19215=CARTESIAN_POINT ( 'NONE',  ( 12.24703709751428349, 2.218305284339069594, 12.51274264014588589 ) ) ;
#19228=CARTESIAN_POINT ( 'NONE',  ( 17.98740632602357792, -0.4515327042052340034, -12.68919950485279990 ) ) ;
#19235=CYLINDRICAL_SURFACE ( 'NONE', #23220, 0.6250000000000005551 ) ;
#19237=ORIENTED_EDGE ( 'NONE', *, *, #60776, .F. ) ;
#19242=DIRECTION ( 'NONE',  ( 1.000000000000000000, 0.000000000000000000, 0.000000000000000000 ) ) ;
#19253=CARTESIAN_POINT ( 'NONE',  ( 17.98272759268933285, 0.4562271229319662669, -13.88993195058941410 ) ) ;
#19256=CARTESIAN_POINT ( 'NONE',  ( 12.80505043854146940, -1.875000000000000444, 12.57545641911172396 ) ) ;
#19260=CARTESIAN_POINT ( 'NONE',  ( 17.84276413147956220, -1.945066902726407365, 13.77561296414734215 ) ) ;
#19261=CARTESIAN_POINT ( 'NONE',  ( 17.92097848889117273, 3.007049802571681862, -13.55275178749822018 ) ) ;
#19271=CARTESIAN_POINT ( 'NONE',  ( 18.10839966799242617, -0.4648927885597820553, -12.59142395508372836 ) ) ;
#19285=CARTESIAN_POINT ( 'NONE',  ( 12.17501771842803571, 2.156544773268126658, 13.83291087807201869 ) ) ;
#19288=CARTESIAN_POINT ( 'NONE',  ( 12.27345231320720842, -0.3288522286823944429, -12.69427358703204156 ) ) ;
#19289=CARTESIAN_POINT ( 'NONE',  ( 12.61757770595761663, -0.7057854747025462672, 13.98219993205038669 ) ) ;
#19299=CARTESIAN_POINT ( 'NONE',  ( 12.56425374667830397, 3.158898859712412577, 12.19759658245784628 ) ) ;
#19306=CARTESIAN_POINT ( 'NONE',  ( 12.21857308197417957, 2.283092344276015595, 12.49946922046772357 ) ) ;
#19317=VERTEX_POINT ( 'NONE', #41935 ) ;
#19323=PRODUCT_DEFINITION_SHAPE ( 'NONE', 'NONE',  #44514 ) ;
#19324=CARTESIAN_POINT ( 'NONE',  ( 17.55505043854143565, 3.125000000000000000, -12.28374638332999602 ) ) ;
#19327=CARTESIAN_POINT ( 'NONE',  ( 12.19673284866991914, 2.643529255688002788, -13.64196713149527618 ) ) ;
#19332=CARTESIAN_POINT ( 'NONE',  ( 12.09634358953518962, 0.1544074001204018831, -13.99915345895492003 ) ) ;
#19335=CARTESIAN_POINT ( 'NONE',  ( 18.18005043875544047, -2.480307847467646543, -13.67758270278766020 ) ) ;
#19337=CARTESIAN_POINT ( 'NONE',  ( 18.17512443068752148, 2.418970859032363308, 12.47009038073128551 ) ) ;
#19344=CARTESIAN_POINT ( 'NONE',  ( 18.10946311474933523, 2.988545908040622034, -13.67730534870324455 ) ) ;
#19357=CARTESIAN_POINT ( 'NONE',  ( 17.55505043854147118, -3.125000000000000000, -13.52078605991414761 ) ) ;
#19364=CARTESIAN_POINT ( 'NONE',  ( 17.93835418254527880, -2.006228213506225710, -12.55298903047910208 ) ) ;
#19370=CARTESIAN_POINT ( 'NONE',  ( -17.56123417799999942, -13.94845324556000143, -4.312847325879000770 ) ) ;
#19374=CARTESIAN_POINT ( 'NONE',  ( 12.17076609166787193, 2.871707895891075335, -13.70231394784453727 ) ) ;
#19377=CARTESIAN_POINT ( 'NONE',  ( 17.77667453761835503, 0.6953657024348723903, 13.98272072176121661 ) ) ;
#19384=CARTESIAN_POINT ( 'NONE',  ( 12.23350478621572357, -2.246345293463438697, 13.72400836782633959 ) ) ;
#19394=VECTOR ( 'NONE', #49291, 1000.000000000000000 ) ;
#19396=EDGE_CURVE ( 'NONE', #22430, #32483, #38405, .T. ) ;
#19401=LINE ( 'NONE', #35492, #39711 ) ;
#19409=ORIENTED_EDGE ( 'NONE', *, *, #19007, .T. ) ;
#19410=CARTESIAN_POINT ( 'NONE',  ( 12.70318068537856249, -0.6169782284476057477, -12.67981870385671428 ) ) ;
#19412=CARTESIAN_POINT ( 'NONE',  ( 12.21071179156234976, -2.693740719230159009, -12.40432020969549853 ) ) ;
#19424=AXIS2_PLACEMENT_3D ( 'NONE', #52306, #36230, #67008 ) ;
#19430=CARTESIAN_POINT ( 'NONE',  ( 18.03351914841130466, 0.5491314443420087787, -13.98923457196397635 ) ) ;
#19439=CARTESIAN_POINT ( 'NONE',  ( 12.18403211232070582, -2.428839562839110400, -13.68824371557135677 ) ) ;
#19445=CARTESIAN_POINT ( 'NONE',  ( 17.82923902985817222, 0.5617296175207505682, -13.88472048964184147 ) ) ;
#19452=CARTESIAN_POINT ( 'NONE',  ( 12.18407604397246580, 0.07155107330948899669, -13.89975717292030311 ) ) ;
#19453=CARTESIAN_POINT ( 'NONE',  ( 18.14163091156143892, -2.284010751868935429, 12.49929939428934311 ) ) ;
#19466=ORIENTED_EDGE ( 'NONE', *, *, #67374, .T. ) ;
#19472=DIRECTION ( 'NONE',  ( -0.000000000000000000, -0.000000000000000000, 1.000000000000000000 ) ) ;
#19480=CARTESIAN_POINT ( 'NONE',  ( 18.21574167892469731, 0.2964030593063826657, 12.59651778044212200 ) ) ;
#19481=DIRECTION ( 'NONE',  ( 1.000000000000000000, 0.000000000000000000, 0.000000000000000000 ) ) ;
#19488=CARTESIAN_POINT ( 'NONE',  ( 17.88835954937806605, 3.166508787604171982, 13.63720117115729558 ) ) ;
#19494=VECTOR ( 'NONE', #34409, 1000.000000000000000 ) ;
#19500=CARTESIAN_POINT ( 'NONE',  ( 17.85637496866994312, -3.182194879603819970, -13.63354919460145886 ) ) ;
#19506=CARTESIAN_POINT ( 'NONE',  ( 18.18005043824477696, 1.062919176435095297E-10, -13.90000000153291637 ) ) ;
#19520=CARTESIAN_POINT ( 'NONE',  ( 12.26933621011913722, 2.178034692540639750, -12.52080028461861616 ) ) ;
#19525=CIRCLE ( 'NONE', #63018, 13.17499999999999716 ) ;
#19530=CARTESIAN_POINT ( 'NONE',  ( 12.63203184702130244, -3.100663238843660352, -12.29110965694881408 ) ) ;
#19532=EDGE_CURVE ( 'NONE', #40405, #48911, #1694, .T. ) ;
#19537=DIRECTION ( 'NONE',  ( -0.000000000000000000, -0.000000000000000000, 1.000000000000000000 ) ) ;
#19538=CARTESIAN_POINT ( 'NONE',  ( 12.76358260308701986, -1.876037923228467186, -13.78611687077049197 ) ) ;
#19557=CARTESIAN_POINT ( 'NONE',  ( 12.38992078601024005, -2.032669449810693862, 12.54828005421690840 ) ) ;
#19563=CARTESIAN_POINT ( 'NONE',  ( 12.25868397512095243, 0.3036663359794751216, 12.69511825016612860 ) ) ;
#19567=CARTESIAN_POINT ( 'NONE',  ( 12.72194006826442347, 1.880463790526824441, 12.57452048663021849 ) ) ;
#19570=CARTESIAN_POINT ( 'NONE',  ( 12.80505043854143388, 1.875000000000000000, 13.78627172894481667 ) ) ;
#19573=EDGE_CURVE ( 'NONE', #7219, #27235, #32475, .T. ) ;
#19581=CARTESIAN_POINT ( 'NONE',  ( 18.02962380189445923, -0.4069377585276638398, -12.69123026938757981 ) ) ;
#19592=EDGE_CURVE ( 'NONE', #67932, #17996, #53684, .T. ) ;
#19607=CARTESIAN_POINT ( 'NONE',  ( 12.80505043854144276, 0.7302158263239216796, -13.98094363220830871 ) ) ;
#19611=CARTESIAN_POINT ( 'NONE',  ( 18.10179698720202879, -2.997559868305876840, 13.67533242386440939 ) ) ;
#19623=CARTESIAN_POINT ( 'NONE',  ( 18.22962529608893689, -0.2638285456865464007, -12.59724228039519822 ) ) ;
#19625=CARTESIAN_POINT ( 'NONE',  ( 5.500000000000000000, 11.06886219213000011, 1.536526853569999851 ) ) ;
#19636=CARTESIAN_POINT ( 'NONE',  ( 12.08109376178929217, 2.472831159707305826, 13.77990118939880482 ) ) ;
#19638=VERTEX_POINT ( 'NONE', #54228 ) ;
#19639=CARTESIAN_POINT ( 'NONE',  ( 12.31508698968652560, -0.3880315156974609159, -12.69202109203974338 ) ) ;
#19652=CARTESIAN_POINT ( 'NONE',  ( 12.38044747764041098, 3.063579277862370720, 12.22188755179955777 ) ) ;
#19663=ORIENTED_EDGE ( 'NONE', *, *, #21653, .F. ) ;
#19669=CARTESIAN_POINT ( 'NONE',  ( 12.80505043854143388, 3.124999999999999556, 13.52078605991414939 ) ) ;
#19677=CARTESIAN_POINT ( 'NONE',  ( 18.10394395700116021, 2.009981277211910111, -12.43865165640889892 ) ) ;
#19681=CARTESIAN_POINT ( 'NONE',  ( 12.19334556178055706, 2.628630841125718209, -13.64533835608825107 ) ) ;
#19696=CARTESIAN_POINT ( 'NONE',  ( 18.27991844657867659, 2.543687620403384031, -13.76699789025506071 ) ) ;
#19703=LINE ( 'NONE', #36462, #33713 ) ;
#19714=CARTESIAN_POINT ( 'NONE',  ( 18.08264632488623391, -2.164896798301380709, -12.52334278189865735 ) ) ;
#19723=CARTESIAN_POINT ( 'NONE',  ( 12.35242198444189299, 3.088429417998427962, -13.65509667848947473 ) ) ;
#19725=CARTESIAN_POINT ( 'NONE',  ( 17.64985702823327074, 0.7243378955761863303, 13.98124959093732400 ) ) ;
#19729=VERTEX_POINT ( 'NONE', #39197 ) ;
#19733=CARTESIAN_POINT ( 'NONE',  ( 12.21215155065115532, -2.301234877124808786, 13.71362569328431391 ) ) ;
#19746=DIRECTION ( 'NONE',  ( 1.000000000000000000, 0.000000000000000000, 0.000000000000000000 ) ) ;
#19748=CARTESIAN_POINT ( 'NONE',  ( 18.17043869202645112, -2.609785213645622992, -12.42531509792942934 ) ) ;
#19756=CARTESIAN_POINT ( 'NONE',  ( 5.700000000000000178, -11.06886219213000011, 1.536526853569999851 ) ) ;
#19758=CARTESIAN_POINT ( 'NONE',  ( 12.55627843433555491, -0.5734477787136643689, -12.68256797703446281 ) ) ;
#19759=CARTESIAN_POINT ( 'NONE',  ( 12.18199593247725865, -2.449686698172776289, -12.46314100319584384 ) ) ;
#19768=DIRECTION ( 'NONE',  ( 0.000000000000000000, -0.000000000000000000, 1.000000000000000000 ) ) ;
#19770=ORIENTED_EDGE ( 'NONE', *, *, #46838, .F. ) ;
#19776=CARTESIAN_POINT ( 'NONE',  ( 18.13027066859325487, -0.4451122480341416776, -13.99293440828418689 ) ) ;
#19784=VERTEX_POINT ( 'NONE', #20783 ) ;
#19786=CARTESIAN_POINT ( 'NONE',  ( 12.18947262544554100, -2.391368178663336952, -13.69585133610886452 ) ) ;
#19800=CARTESIAN_POINT ( 'NONE',  ( 12.26373570557222337, 0.3125842563278190545, -13.89527356689842996 ) ) ;
#19801=CARTESIAN_POINT ( 'NONE',  ( 18.15144633312242917, -2.312812061507715011, 12.49323956768624200 ) ) ;
#19810=DIRECTION ( 'NONE',  ( -1.000000000000000000, 0.000000000000000000, 0.000000000000000000 ) ) ;
#19812=ORIENTED_EDGE ( 'NONE', *, *, #23755, .F. ) ;
#19826=CARTESIAN_POINT ( 'NONE',  ( 17.60287381234529747, 0.7178228174669238904, 12.57953618971562548 ) ) ;
#19862=CARTESIAN_POINT ( 'NONE',  ( 12.18465059688361940, 2.421662038956231555, -12.46951891513069910 ) ) ;
#19871=CARTESIAN_POINT ( 'NONE',  ( 12.41452611191166255, -2.987998126639117125, -12.32436705583800673 ) ) ;
#19877=EDGE_CURVE ( 'NONE', #35474, #32730, #2819, .T. ) ;
#19879=CARTESIAN_POINT ( 'NONE',  ( 12.78089176142236383, -3.248146600645751114, -13.61798599873023718 ) ) ;
#19887=CARTESIAN_POINT ( 'NONE',  ( 12.15760927726063834, -0.3803681711079593963, -13.99548972734546126 ) ) ;
#19890=CARTESIAN_POINT ( 'NONE',  ( 4.700001368028300597, 14.00000000000000000, 0.000000000000000000 ) ) ;
#19893=CARTESIAN_POINT ( 'NONE',  ( 18.01300802853348415, 2.925445001331293149, 12.34219835790438680 ) ) ;
#19894=FACE_OUTER_BOUND ( 'NONE', #46813, .T. ) ;
#19908=CARTESIAN_POINT ( 'NONE',  ( 12.27985646406008335, 0.3389720875425228930, 12.69391532355468044 ) ) ;
#19921=CARTESIAN_POINT ( 'NONE',  ( 18.17906593022175343, -0.04061720356229615858, -12.69993396819151243 ) ) ;
#19922=EDGE_CURVE ( 'NONE', #11428, #32730, #66448, .T. ) ;
#19930=CARTESIAN_POINT ( 'NONE',  ( 18.14704975929777575, -2.701423609612692900, -13.62863833005038217 ) ) ;
#19949=CARTESIAN_POINT ( 'NONE',  ( 5.699999545467999695, -6.661338147750999827E-14, 12.60000000000318998 ) ) ;
#19950=CARTESIAN_POINT ( 'NONE',  ( 12.80505043854144276, 0.6951438842159466391, -13.94765567169527998 ) ) ;
#19955=CARTESIAN_POINT ( 'NONE',  ( 18.17294214856818968, -2.135913245783944259, 13.83611159055835316 ) ) ;
#19956=CARTESIAN_POINT ( 'NONE',  ( 17.86939907855665410, 3.040585884632406977, -13.54383026114252075 ) ) ;
#19957=ORIENTED_EDGE ( 'NONE', *, *, #5264, .F. ) ;
#19969=CARTESIAN_POINT ( 'NONE',  ( 18.01033200807251689, 0.5598083480993615302, -12.58755849294668394 ) ) ;
#19974=DIRECTION ( 'NONE',  ( 0.000000000000000000, -0.6194815870790952861, -0.7850111867164476509 ) ) ;
#19980=CARTESIAN_POINT ( 'NONE',  ( 17.85722199349616446, 1.826245811740494274, 12.46695042358089012 ) ) ;
#19981=CARTESIAN_POINT ( 'NONE',  ( 12.28223951138205550, 3.023960592195345853, 13.66951858831273370 ) ) ;
#19985=CARTESIAN_POINT ( 'NONE',  ( 12.18002295456110673, 0.03981407387464135084, -12.70000161046296938 ) ) ;
#19986=CARTESIAN_POINT ( 'NONE',  ( 12.21569938124766885, -0.4259565731506597674, 13.99353270933016979 ) ) ;
#19990=EDGE_CURVE ( 'NONE', #24800, #12380, #19178, .T. ) ;
#19996=CARTESIAN_POINT ( 'NONE',  ( 12.25620353052267042, 2.010025970016497521, 12.43864443381842833 ) ) ;
#20003=CARTESIAN_POINT ( 'NONE',  ( 12.18412391183566967, 2.571774448851283257, 12.43455553901978128 ) ) ;
#20013=CARTESIAN_POINT ( 'NONE',  ( 12.20879664878247972, 2.687389840184388756, 13.63187458905523286 ) ) ;
#20020=CARTESIAN_POINT ( 'NONE',  ( 17.89002091993512522, 1.842089822799531929, -12.46461944294985535 ) ) ;
#20022=CARTESIAN_POINT ( 'NONE',  ( 18.08677744227652795, 2.828625537428428149, 12.36890451985948758 ) ) ;
#20023=CARTESIAN_POINT ( 'NONE',  ( 12.30953092759153833, 2.881442378548828565, -13.58513712698574061 ) ) ;
#20027=CARTESIAN_POINT ( 'NONE',  ( 12.19581923677612778, 0.3960277493246568414, -13.99440111282555499 ) ) ;
#20035=CARTESIAN_POINT ( 'NONE',  ( 18.02697970389225546, 1.963589444787172233, -13.86161523094991210 ) ) ;
#20054=CARTESIAN_POINT ( 'NONE',  ( 17.78706641053896575, -1.919568985577241094, -12.56801103569108236 ) ) ;
#20058=B_SPLINE_CURVE_WITH_KNOTS ( 'NONE', 3,
 ( #34513, #60713, #55823, #66645, #1643, #65262, #28568, #49884, #12831, #18765, #7576, #22612, #44992, #40095, #61408, #56157, #28215, #33465, #1298, #29614, #12135, #54780, #6879, #30972, #68010, #35532, #46706, #20127, #41455, #14547, #24346, #24691, #62763, #63099, #25029, #40418, #14884, #67661, #36205, #9625, #3356, #46014, #46360, #57182, #68348, #51934, #20467, #67321, #4030, #41113, #66983, #35866, #50917, #57522, #52284, #25713, #19439, #45678, #4378, #19786, #62428, #14205, #40763, #57876, #47047, #9279, #41795, #25369, #15226 ),
 .UNSPECIFIED., .F., .F.,
 ( 4, 2, 2, 2, 2, 2, 2, 2, 2, 2, 2, 2, 2, 1, 2, 2, 2, 1, 2, 2, 2, 2, 1, 2, 2, 2, 2, 2, 2, 2, 2, 2, 2, 2, 2, 4 ),
 ( 0.000000000000000000, 0.06250000000004618528, 0.1250000000000923706, 0.1562500000001154632, 0.1875000000001385558, 0.2187500000001616485, 0.2343750000001731948, 0.2500000000001847411, 0.2812500000002073341, 0.2968750000002188805, 0.3125000000002304268, 0.3281250000002419731, 0.3437500000002535194, 0.3593750000002650657, 0.3671875000002713940, 0.3750000000002777223, 0.3906250000002883804, 0.3984375000002929879, 0.4023437500002955414, 0.4062500000002980949, 0.4218750000003073097, 0.4296875000003119172, 0.4335937500003141376, 0.4355468750003134160, 0.4375000000003126943, 0.4531250000003034795, 0.4687500000002942646, 0.4843750000002850498, 0.5000000000002757794, 0.5312500000002580158, 0.5468750000002491340, 0.5625000000002402523, 0.5937500000002230438, 0.6250000000002058353, 0.7500000000001374456, 1.000000000000000000 ),
 .UNSPECIFIED. ) ;
#20059=B_SPLINE_CURVE_WITH_KNOTS ( 'NONE', 1,
 ( #6403, #22833 ),
 .UNSPECIFIED., .F., .F.,
 ( 2, 2 ),
 ( 0.000000000000000000, 1.000000000000000000 ),
 .UNSPECIFIED. ) ;
#20061=FACE_OUTER_BOUND ( 'NONE', #14869, .T. ) ;
#20067=CARTESIAN_POINT ( 'NONE',  ( 18.20560607722001834, 0.3231860383015686677, 13.99628497142876249 ) ) ;
#20096=CARTESIAN_POINT ( 'NONE',  ( 17.79128410730675114, 1.798519029207210629, 12.47099317247404748 ) ) ;
#20099=CARTESIAN_POINT ( 'NONE',  ( 12.67437701660358584, 0.7076089047904963181, -12.58011506138061009 ) ) ;
#20100=CARTESIAN_POINT ( 'NONE',  ( 12.19562994360793873, -2.360937373121109850, -12.48287347411901571 ) ) ;
#20107=CARTESIAN_POINT ( 'NONE',  ( 17.80428133522791256, 0.5732558492893025104, 12.68257967785543627 ) ) ;
#20109=DIRECTION ( 'NONE',  ( 0.000000000000000000, 1.000000000000000000, 0.000000000000000000 ) ) ;
#20111=ORIENTED_EDGE ( 'NONE', *, *, #6255, .T. ) ;
#20125=EDGE_CURVE ( 'NONE', #32586, #12771, #7864, .T. ) ;
#20127=CARTESIAN_POINT ( 'NONE',  ( 12.23606299695368982, -2.758663578172445785, -13.61513466669021533 ) ) ;
#20138=CARTESIAN_POINT ( 'NONE',  ( 12.76344776297775674, 3.123961325724113891, 13.52107359494105765 ) ) ;
#20139=CARTESIAN_POINT ( 'NONE',  ( 18.06602350563010972, -2.139519659637397986, 12.52832261142687287 ) ) ;
#20140=VERTEX_POINT ( 'NONE', #27590 ) ;
#20157=DIRECTION ( 'NONE',  ( -1.000000000000000000, 0.000000000000000000, 0.000000000000000000 ) ) ;
#20159=CYLINDRICAL_SURFACE ( 'NONE', #22812, 0.6250000000000005551 ) ;
#20163=CARTESIAN_POINT ( 'NONE',  ( 18.27543972223745783, 0.08185661189466754417, 12.59973963693671806 ) ) ;
#20169=CARTESIAN_POINT ( 'NONE',  ( 17.93991242251030371, 3.137220474326295250, 13.64397427468587587 ) ) ;
#20179=CARTESIAN_POINT ( 'NONE',  ( 17.55505043854147118, -3.199751711897561801, 12.18694338143115452 ) ) ;
#20200=CARTESIAN_POINT ( 'NONE',  ( 12.51684016020880996, 3.054675744551020422, -12.30488183412682801 ) ) ;
#20204=EDGE_CURVE ( 'NONE', #48158, #26199, #65895, .T. ) ;
#20207=ADVANCED_FACE ( 'NONE', ( #17321 ), #32379, .F. ) ;
#20211=CARTESIAN_POINT ( 'NONE',  ( 12.52646068131089230, -3.059569037265597924, -12.30341205401442828 ) ) ;
#20217=CARTESIAN_POINT ( 'NONE',  ( 12.28917444793836466, -2.147008681356604498, -13.74197010666756746 ) ) ;
#20228=CARTESIAN_POINT ( 'NONE',  ( 18.14119057072321084, 2.717377330609857200, 13.62490400531196499 ) ) ;
#20231=CYLINDRICAL_SURFACE ( 'NONE', #33069, 12.59999999999999964 ) ;
#20232=CARTESIAN_POINT ( 'NONE',  ( 18.15708441975577259, 2.331821618626342296, 12.48915497634519411 ) ) ;
#20239=CARTESIAN_POINT ( 'NONE',  ( 12.36861073370957875, -2.947405515254782227, 12.33600917780096395 ) ) ;
#20263=CARTESIAN_POINT ( 'NONE',  ( 18.17219575274255305, -2.599291946992130953, 13.65190342897825815 ) ) ;
#20265=ORIENTED_EDGE ( 'NONE', *, *, #37553, .F. ) ;
#20268=CARTESIAN_POINT ( 'NONE',  ( 18.12600850643438477, -2.245563876552335802, -13.72409254399188150 ) ) ;
#20278=CARTESIAN_POINT ( 'NONE',  ( 18.14038165173055717, -0.2193642558659226471, 13.89767506191629387 ) ) ;
#20293=EDGE_CURVE ( 'NONE', #16266, #20309, #29227, .T. ) ;
#20295=CARTESIAN_POINT ( 'NONE',  ( 5.700000000000000178, -13.04986661130000059, -1.811520473896000016 ) ) ;
#20298=( NAMED_UNIT ( * ) SI_UNIT ( $, .STERADIAN. ) SOLID_ANGLE_UNIT ( ) );
#20300=CIRCLE ( 'NONE', #66060, 13.27499874714999883 ) ;
#20305=CARTESIAN_POINT ( 'NONE',  ( 18.26375634269467341, 0.1521017209118896429, -12.59908727444664045 ) ) ;
#20309=VERTEX_POINT ( 'NONE', #5367 ) ;
#20314=CARTESIAN_POINT ( 'NONE',  ( 17.97079960141759258, 1.890785106268465743, 12.45732622342820406 ) ) ;
#20315=CARTESIAN_POINT ( 'NONE',  ( 12.21441178144105422, 2.942030139115487941, 13.68739795509152657 ) ) ;
#20318=CARTESIAN_POINT ( 'NONE',  ( 12.17125901970653068, -0.3547769576528356783, 13.99550803169339730 ) ) ;
#20320=CARTESIAN_POINT ( 'NONE',  ( 12.58695046962341380, -1.794129438118917452, 12.47161187386927672 ) ) ;
#20321=CARTESIAN_POINT ( 'NONE',  ( 12.80505043854143388, 1.816877544077282636, -13.85235828181317252 ) ) ;
#20325=AXIS2_PLACEMENT_3D ( 'NONE', #50567, #55123, #18415 ) ;
#20326=CARTESIAN_POINT ( 'NONE',  ( 12.42221671361158286, 0.6112845611542794266, 12.58516990776527145 ) ) ;
#20330=CARTESIAN_POINT ( 'NONE',  ( 12.35979995375149265, 1.912019040637406020, 12.45409236230133843 ) ) ;
#20337=CARTESIAN_POINT ( 'NONE',  ( 12.20055951530072669, 2.340869620879587831, 12.48721223319318874 ) ) ;
#20350=CARTESIAN_POINT ( 'NONE',  ( 12.76358235960665333, -3.123961849445189731, 13.52113151862113938 ) ) ;
#20351=CARTESIAN_POINT ( 'NONE',  ( 12.30281274455054152, 2.118998859546890490, 13.74704000636842594 ) ) ;
#20358=CARTESIAN_POINT ( 'NONE',  ( 7.100000000000000533, -12.03770622561999915, -3.722046322334000124 ) ) ;
#20360=CARTESIAN_POINT ( 'NONE',  ( 18.14000279917953762, 2.720357798290597540, -12.39752072230842828 ) ) ;
#20362=CARTESIAN_POINT ( 'NONE',  ( 18.17998003037112653, 2.509683781191140994, 12.44929946636232998 ) ) ;
#20363=CARTESIAN_POINT ( 'NONE',  ( 12.20100803655143018, 2.660536037873024728, -13.63809770147455680 ) ) ;
#20367=CARTESIAN_POINT ( 'NONE',  ( 12.58342633946451983, 0.6953657024348841587, -13.98272072176121483 ) ) ;
#20378=CARTESIAN_POINT ( 'NONE',  ( 18.14566850323240033, 2.942004589604676923, -13.68740344564952593 ) ) ;
#20395=CARTESIAN_POINT ( 'NONE',  ( 17.81301359322647215, -3.153051599267181260, -12.19911286921121274 ) ) ;
#20397=CARTESIAN_POINT ( 'NONE',  ( 5.699999545467999695, 0.000000000000000000, 0.000000000000000000 ) ) ;
#20406=CARTESIAN_POINT ( 'NONE',  ( 18.05935379312178668, 0.5247499651446875246, 13.99016470477802443 ) ) ;
#20414=CARTESIAN_POINT ( 'NONE',  ( 12.33541982640536538, -2.912513636887091639, 13.57727066180282982 ) ) ;
#20427=CARTESIAN_POINT ( 'NONE',  ( 18.17813913392090797, -2.550022942166513040, -12.43977370302252439 ) ) ;
#20428=CARTESIAN_POINT ( 'NONE',  ( 4.600000127571202135, 13.89999852641999922, 0.000000000000000000 ) ) ;
#20434=AXIS2_PLACEMENT_3D ( 'NONE', #14541, #35858, #25362 ) ;
#20437=CARTESIAN_POINT ( 'NONE',  ( 17.74710428554446295, 3.180431966548184608, 12.19205794678931376 ) ) ;
#20440=CARTESIAN_POINT ( 'NONE',  ( 12.55608787177197172, 0.5733651658914313831, -12.68257300503909946 ) ) ;
#20441=CARTESIAN_POINT ( 'NONE',  ( 12.27404183469016274, -2.829784921991532087, -12.36859113742059080 ) ) ;
#20452=ORIENTED_EDGE ( 'NONE', *, *, #37553, .T. ) ;
#20467=CARTESIAN_POINT ( 'NONE',  ( 12.18999301580812222, -2.611634498318802677, -13.64910281353073707 ) ) ;
#20474=DIRECTION ( 'NONE',  ( 1.000000000000000000, 0.000000000000000000, 0.000000000000000000 ) ) ;
#20475=CARTESIAN_POINT ( 'NONE',  ( 17.80428097310739588, 0.5732560958663720507, -13.88408533439707071 ) ) ;
#20478=DIRECTION ( 'NONE',  ( 0.000000000000000000, 0.7914851585299630399, -0.6111883865280813843 ) ) ;
#20482=CARTESIAN_POINT ( 'NONE',  ( 12.42259655075931590, 2.994741173188553152, 13.55594337657171700 ) ) ;
#20486=EDGE_LOOP ( 'NONE', ( #28982, #56142, #66650, #9070 ) ) ;
#20497=CARTESIAN_POINT ( 'NONE',  ( 12.54853131227892327, 0.5702303675593314303, 13.88425454623471111 ) ) ;
#20507=CARTESIAN_POINT ( 'NONE',  ( 18.14493211602550460, 0.4188397444781293832, 12.59305179380755391 ) ) ;
#20535=EDGE_LOOP ( 'NONE', ( #16243, #36501, #65014, #63874 ) ) ;
#20539=EDGE_CURVE ( 'NONE', #16046, #62494, #64237, .T. ) ;
#20540=DIRECTION ( 'NONE',  ( -0.000000000000000000, -0.000000000000000000, 1.000000000000000000 ) ) ;
#20543=CARTESIAN_POINT ( 'NONE',  ( 18.12461517476719308, 0.2575405707509131892, -13.89679341043304106 ) ) ;
#20554=CARTESIAN_POINT ( 'NONE',  ( 17.78895972987641017, -0.6824382159985085128, 12.58151825845911453 ) ) ;
#20555=DIRECTION ( 'NONE',  ( -1.000000000000000000, 0.000000000000000000, 0.000000000000000000 ) ) ;
#20557=CARTESIAN_POINT ( 'NONE',  ( 12.21328932544282253, -2.701359397734038659, -12.40237271074984982 ) ) ;
#20561=CARTESIAN_POINT ( 'NONE',  ( 12.20052126010794780, -2.341019711503391942, -13.70584597024486939 ) ) ;
#20564=CARTESIAN_POINT ( 'NONE',  ( 18.21613312502040571, -2.776914653343700135, 12.29020858420810924 ) ) ;
#20573=CARTESIAN_POINT ( 'NONE',  ( 18.16680584898029593, 2.371606440122839832, 12.48054868302275722 ) ) ;
#20577=ORIENTED_EDGE ( 'NONE', *, *, #30982, .T. ) ;
#20580=CARTESIAN_POINT ( 'NONE',  ( 12.24413029362360561, -2.775858423521468943, 12.38303112237259640 ) ) ;
#20589=CARTESIAN_POINT ( 'NONE',  ( 12.80505043854144276, -0.6250000000000006661, 12.67928921589117586 ) ) ;
#20590=AXIS2_PLACEMENT_3D ( 'NONE', #510, #48751, #54332 ) ;
#20591=CARTESIAN_POINT ( 'NONE',  ( 5.699999772733999492, -12.03770622561999915, -3.722046322334000124 ) ) ;
#20600=CARTESIAN_POINT ( 'NONE',  ( 12.75601868327514410, -3.199663661910128187, -12.18696649917218977 ) ) ;
#20605=CARTESIAN_POINT ( 'NONE',  ( 5.602978689601446405, -12.13075210502338841, 3.749558893020384254 ) ) ;
#20611=ORIENTED_EDGE ( 'NONE', *, *, #39881, .T. ) ;
#20614=CARTESIAN_POINT ( 'NONE',  ( 18.17921951168942130, -2.461818733276639914, -13.68145094671735329 ) ) ;
#20616=DIRECTION ( 'NONE',  ( -1.000000000000000000, -0.000000000000000000, -0.000000000000000000 ) ) ;
#20628=EDGE_CURVE ( 'NONE', #11912, #1557, #38228, .T. ) ;
#20634=CARTESIAN_POINT ( 'NONE',  ( 12.09778329087091286, 2.320992115139772327, -12.38439064982923021 ) ) ;
#20637=CARTESIAN_POINT ( 'NONE',  ( 18.19085350568000337, -2.166991405623368561, 13.83127841112310819 ) ) ;
#20638=DIRECTION ( 'NONE',  ( 0.000000000000000000, -0.9553735099700839672, -0.2954005017724949389 ) ) ;
#20640=ORIENTED_EDGE ( 'NONE', *, *, #7360, .F. ) ;
#20645=AXIS2_PLACEMENT_3D ( 'NONE', #28128, #55736, #66555 ) ;
#20651=CARTESIAN_POINT ( 'NONE',  ( 17.74611058647003858, 0.5951698179256272869, -12.68122092285041624 ) ) ;
#20652=CARTESIAN_POINT ( 'NONE',  ( 12.39197104278336958, 2.969147788914954234, -12.32981191671632359 ) ) ;
#20662=CARTESIAN_POINT ( 'NONE',  ( 12.38995319333355916, 1.919216742092433314, 13.86782799095450258 ) ) ;
#20666=CARTESIAN_POINT ( 'NONE',  ( 12.08004253349365342, 0.01140630886273297576, 14.00000041621361291 ) ) ;
#20668=CARTESIAN_POINT ( 'NONE',  ( 12.54704051454020686, -1.807816716204558416, 12.46963574575698530 ) ) ;
#20670=CARTESIAN_POINT ( 'NONE',  ( 12.80505043854143388, 1.875000000000000000, -13.78631952119025428 ) ) ;
#20674=CARTESIAN_POINT ( 'NONE',  ( 12.36386718854188693, 0.5708113556792882015, 12.58706429964239071 ) ) ;
#20678=CARTESIAN_POINT ( 'NONE',  ( 12.47010838183367731, 1.842148406394422899, 12.46461078478868245 ) ) ;
#20690=CARTESIAN_POINT ( 'NONE',  ( 12.44873997947986055, 0.5136077743244018556, 12.68601957541667247 ) ) ;
#20695=CARTESIAN_POINT ( 'NONE',  ( 4.649999478197480052, 2.033928581112999763E-13, 13.22499948080971777 ) ) ;
#20696=CARTESIAN_POINT ( 'NONE',  ( 12.19422188688375641, -2.632730885462789328, 13.64441700900758114 ) ) ;
#20697=CARTESIAN_POINT ( 'NONE',  ( 12.19254401040021740, 2.624350118463367298, 13.64624664189957493 ) ) ;
#20704=ADVANCED_FACE ( 'NONE', ( #53591 ), #31933, .T. ) ;
#20705=CARTESIAN_POINT ( 'NONE',  ( 18.16486442019678904, 2.361571392960268856, -12.48278654574965785 ) ) ;
#20707=CARTESIAN_POINT ( 'NONE',  ( 18.16744427668637840, 2.624922642575843845, 12.42158156204347463 ) ) ;
#20729=CARTESIAN_POINT ( 'NONE',  ( 12.39297058755369463, 0.4699376427894553787, -13.88930769708015589 ) ) ;
#20736=VECTOR ( 'NONE', #62722, 1000.000000000000000 ) ;
#20774=CARTESIAN_POINT ( 'NONE',  ( 18.16257472042013532, 2.647071733601741084, -12.41611113201541450 ) ) ;
#20782=CARTESIAN_POINT ( 'NONE',  ( 17.55505043854143565, 1.760910691117812954, 12.47634535983622861 ) ) ;
#20783=CARTESIAN_POINT ( 'NONE',  ( 12.80505043854143388, 3.124999999999999556, -13.52084414783465505 ) ) ;
#20785=CARTESIAN_POINT ( 'NONE',  ( 12.32802524195760263, 0.4039503557775021014, -12.69135589213616377 ) ) ;
#20786=CARTESIAN_POINT ( 'NONE',  ( 12.22547077884265754, -2.733971791243574145, -12.39396907916229651 ) ) ;
#20792=DIRECTION ( 'NONE',  ( 0.000000000000000000, 1.000000000000000000, 0.000000000000000000 ) ) ;
#20793=SHAPE_DEFINITION_REPRESENTATION ( #19323, #8579 ) ;
#20812=CARTESIAN_POINT ( 'NONE',  ( 17.55505043854147118, -3.125000000000000000, -12.28373071562070074 ) ) ;
#20820=CARTESIAN_POINT ( 'NONE',  ( 17.69772537084632447, -0.6088395004560434032, -12.68034807294329980 ) ) ;
#20823=PLANE ( 'NONE',  #31929 ) ;
#20827=EDGE_CURVE ( 'NONE', #22839, #62111, #32565, .T. ) ;
#20837=CARTESIAN_POINT ( 'NONE',  ( 12.36772010770944696, 2.053374490018977205, -13.75810180220399026 ) ) ;
#20840=CARTESIAN_POINT ( 'NONE',  ( 17.69771933245237250, -0.6088408278571642018, 13.88204686096232621 ) ) ;
#20843=CARTESIAN_POINT ( 'NONE',  ( 12.39787770678336543, 0.4743614821706066409, 13.88910774393186998 ) ) ;
#20852=DIRECTION ( 'NONE',  ( 1.000000000000000000, -3.631529569662070274E-15, 1.174496025128702085E-14 ) ) ;
#20854=CARTESIAN_POINT ( 'NONE',  ( 17.88703114068441025, 0.6395598188657292127, 12.58375915074078577 ) ) ;
#20860=CARTESIAN_POINT ( 'NONE',  ( 18.05265757431621410, 3.049509720595960260, 13.66384965554843589 ) ) ;
#20872=CARTESIAN_POINT ( 'NONE',  ( 5.656849040862428346, 12.07883750122941002, 3.735095616318558687 ) ) ;
#20887=CARTESIAN_POINT ( 'NONE',  ( 17.96752346481819629, 0.4700078255514612557, -13.88931146942755390 ) ) ;
#20888=CARTESIAN_POINT ( 'NONE',  ( 5.499989001269300459, 12.65264518617999911, -3.063510750763999813 ) ) ;
#20893=CARTESIAN_POINT ( 'NONE',  ( 12.52601681438817138, 3.059349880828009738, -12.30349483713085235 ) ) ;
#20895=ORIENTED_EDGE ( 'NONE', *, *, #2019, .F. ) ;
#20903=CARTESIAN_POINT ( 'NONE',  ( 12.19026796737406748, -2.613005292445991223, -12.42452312575879425 ) ) ;
#20907=CARTESIAN_POINT ( 'NONE',  ( 12.08611717550378550, -2.614944066661595290, -13.75364144501312147 ) ) ;
#20909=DIRECTION ( 'NONE',  ( 1.000000000000000000, 0.000000000000000000, 0.000000000000000000 ) ) ;
#20911=CARTESIAN_POINT ( 'NONE',  ( 18.27818099403250329, -2.425134644239736126, 12.36441930324462213 ) ) ;
#20922=CARTESIAN_POINT ( 'NONE',  ( 17.99515569450505481, 2.943800350515566766, 12.33701119546411284 ) ) ;
#20932=EDGE_CURVE ( 'NONE', #1963, #11428, #37498, .T. ) ;
#20940=B_SPLINE_CURVE_WITH_KNOTS ( 'NONE', 3,
 ( #1927, #7860, #29194, #13459 ),
 .UNSPECIFIED., .F., .F.,
 ( 4, 4 ),
 ( 0.000000000000000000, 1.000000000000000000 ),
 .UNSPECIFIED. ) ;
#20952=CARTESIAN_POINT ( 'NONE',  ( 5.610802430940820429, -12.12319474034768341, 3.747515530461446254 ) ) ;
#20956=CARTESIAN_POINT ( 'NONE',  ( 18.17041169247335475, -2.609942250310885115, 13.64953311053600871 ) ) ;
#20959=CARTESIAN_POINT ( 'NONE',  ( 18.17186084707622484, -2.602861751209124552, -13.65107289232777177 ) ) ;
#20970=CARTESIAN_POINT ( 'NONE',  ( 18.05194036312017758, -0.3791492161817762163, 13.89304085482745421 ) ) ;
#20980=AXIS2_PLACEMENT_3D ( 'NONE', #62979, #36428, #10202 ) ;
#20981=CARTESIAN_POINT ( 'NONE',  ( 12.19289742234818696, 2.094552964378149973, -12.42468808284045245 ) ) ;
#20985=CARTESIAN_POINT ( 'NONE',  ( 18.27457017588621468, -2.425781798817269852, 13.78826143416240591 ) ) ;
#20992=CARTESIAN_POINT ( 'NONE',  ( 5.700000000000000178, -12.50865771883999855, 2.924687089724999911 ) ) ;
#20996=CARTESIAN_POINT ( 'NONE',  ( 17.78490268980527489, 0.5812897767837147400, -12.68208758371478595 ) ) ;
#21013=CARTESIAN_POINT ( 'NONE',  ( 12.61568544974634953, -1.785400273382258263, 12.47286636618916589 ) ) ;
#21020=CARTESIAN_POINT ( 'NONE',  ( 12.39267273778989420, 0.5917181940048591438, 12.58609996267493081 ) ) ;
#21024=CARTESIAN_POINT ( 'NONE',  ( 12.11481770488409282, 2.701029500518133286, 12.30709430042447394 ) ) ;
#21035=CARTESIAN_POINT ( 'NONE',  ( 12.29062685719103243, 0.3550721705843559173, 12.69332222955381972 ) ) ;
#21041=CARTESIAN_POINT ( 'NONE',  ( 12.29628962427838346, -2.863168005537272354, 13.58969864530831728 ) ) ;
#21042=CARTESIAN_POINT ( 'NONE',  ( 12.19259091224295233, 2.624575865621845860, 13.64619539111124347 ) ) ;
#21044=ORIENTED_EDGE ( 'NONE', *, *, #48613, .F. ) ;
#21049=CARTESIAN_POINT ( 'NONE',  ( 18.13637388831909192, 2.729759562904666037, -12.39509076542458743 ) ) ;
#21051=CARTESIAN_POINT ( 'NONE',  ( 18.09718405122000107, 2.811158313974275735, 12.37360767970025677 ) ) ;
#21074=CARTESIAN_POINT ( 'NONE',  ( 12.18827041298537495, 0.1029057169099007185, -13.89950510286185725 ) ) ;
#21078=ORIENTED_EDGE ( 'NONE', *, *, #36467, .F. ) ;
#21087=CARTESIAN_POINT ( 'NONE',  ( 17.99515569450509034, -2.943800350515567210, -12.33701119546411284 ) ) ;
#21092=CARTESIAN_POINT ( 'NONE',  ( 12.19636843800076953, -0.1422577892986798820, 13.89902525486551887 ) ) ;
#21103=ORIENTED_EDGE ( 'NONE', *, *, #1228, .F. ) ;
#21106=CARTESIAN_POINT ( 'NONE',  ( 12.29688428857270388, -2.864514977104569038, 13.58937626179410962 ) ) ;
#21121=CARTESIAN_POINT ( 'NONE',  ( 18.17055204341999897, 2.609142802180001830, -12.42550174407591079 ) ) ;
#21128=DIRECTION ( 'NONE',  ( -1.000000000000000000, 0.000000000000000000, 0.000000000000000000 ) ) ;
#21130=VERTEX_POINT ( 'NONE', #6643 ) ;
#21133=CARTESIAN_POINT ( 'NONE',  ( 12.27392562293325362, 0.3300695133819715466, -12.69424233780836531 ) ) ;
#21148=CARTESIAN_POINT ( 'NONE',  ( 17.80560960443411389, 3.072671113640228491, -13.53517819557379021 ) ) ;
#21149=VERTEX_POINT ( 'NONE', #55588 ) ;
#21156=CARTESIAN_POINT ( 'NONE',  ( 12.80505043854146940, -3.149899482173124987, -12.25147293255931125 ) ) ;
#21162=ORIENTED_EDGE ( 'NONE', *, *, #45342, .F. ) ;
#21166=CARTESIAN_POINT ( 'NONE',  ( 17.92061031166187846, -1.858910711595921583, -12.46212218156369111 ) ) ;
#21177=CARTESIAN_POINT ( 'NONE',  ( 12.21870270123686275, 2.283379404039359351, -13.71702370352176281 ) ) ;
#21181=CARTESIAN_POINT ( 'NONE',  ( 18.15028930682391106, -0.1908382484571597981, 13.89824168789395920 ) ) ;
#21186=CARTESIAN_POINT ( 'NONE',  ( 18.12842152809865937, -0.2489677813733684741, -13.89700419708378298 ) ) ;
#21195=CARTESIAN_POINT ( 'NONE',  ( 17.93128725136842760, -0.4990964484179727378, 12.68679736436866712 ) ) ;
#21202=DIRECTION ( 'NONE',  ( 0.000000000000000000, 0.000000000000000000, 1.000000000000000000 ) ) ;
#21211=CARTESIAN_POINT ( 'NONE',  ( 12.78109913421143418, -0.7192906882580946126, -12.57945229568000656 ) ) ;
#21213=CARTESIAN_POINT ( 'NONE',  ( 18.10200918459796426, 2.953257374879727948, -12.24902512628088402 ) ) ;
#21215=CARTESIAN_POINT ( 'NONE',  ( 12.80505043854143388, 3.124999999999999556, 13.52078605991414939 ) ) ;
#21216=ORIENTED_EDGE ( 'NONE', *, *, #558, .F. ) ;
#21227=CARTESIAN_POINT ( 'NONE',  ( 12.61539589080907042, 1.784264304835224690, -12.47303049908422778 ) ) ;
#21233=CARTESIAN_POINT ( 'NONE',  ( 12.80505043854143388, 3.124999999999999556, -12.28374638332999602 ) ) ;
#21243=CARTESIAN_POINT ( 'NONE',  ( 4.699998537092440642, 0.000000000000000000, 0.000000000000000000 ) ) ;
#21246=CARTESIAN_POINT ( 'NONE',  ( 12.47171258541606420, -1.971212359000197090, -12.55915788719762638 ) ) ;
#21248=DIRECTION ( 'NONE',  ( -1.000000000000000000, 0.000000000000000000, 0.000000000000000000 ) ) ;
#21250=CARTESIAN_POINT ( 'NONE',  ( 12.47131944427646388, -1.869655113073437347, -13.87459630548517886 ) ) ;
#21253=CARTESIAN_POINT ( 'NONE',  ( 18.14791645918234764, -2.065340611094598433, 12.42959220787597374 ) ) ;
#21258=DIRECTION ( 'NONE',  ( -1.000000000000000000, 5.085933197601780420E-15, -5.275114267344730344E-15 ) ) ;
#21265=CARTESIAN_POINT ( 'NONE',  ( 17.65333285645861139, -3.199628934752127840, -12.18697561682396646 ) ) ;
#21266=ORIENTED_EDGE ( 'NONE', *, *, #45869, .T. ) ;
#21276=CARTESIAN_POINT ( 'NONE',  ( 12.23133867660517282, -0.2481623978058218327, 12.69674179789668500 ) ) ;
#21283=CARTESIAN_POINT ( 'NONE',  ( 17.88684482918178986, 3.030051203688146622, 13.54658895838268684 ) ) ;
#21290=CARTESIAN_POINT ( 'NONE',  ( 18.18005043853712976, -0.02024571653066400273, -12.69999991888706958 ) ) ;
#21297=CARTESIAN_POINT ( 'NONE',  ( 18.17486206286454120, -2.582858869840499061, -13.65550477088448034 ) ) ;
#21310=ORIENTED_EDGE ( 'NONE', *, *, #32996, .T. ) ;
#21316=VECTOR ( 'NONE', #14505, 1000.000000000000114 ) ;
#21317=CARTESIAN_POINT ( 'NONE',  ( 12.78084734971786673, 1.760846085845573006, -12.47635444213890032 ) ) ;
#21331=DIRECTION ( 'NONE',  ( -1.000000000000000000, -0.000000000000000000, -0.000000000000000000 ) ) ;
#21333=CARTESIAN_POINT ( 'NONE',  ( 17.60287381234529036, -0.7178228174669354367, -12.57953618971562193 ) ) ;
#21338=VERTEX_POINT ( 'NONE', #31423 ) ;
#21341=CARTESIAN_POINT ( 'NONE',  ( 4.599999999999999645, 3.199751711897561357, -12.18694338143115452 ) ) ;
#21342=CARTESIAN_POINT ( 'NONE',  ( 18.03534466112214929, 3.019381283786335413, 12.23288205540259632 ) ) ;
#21348=CARTESIAN_POINT ( 'NONE',  ( 12.34378620361241374, -0.4226185364342202599, -12.69055435920471098 ) ) ;
#21351=CARTESIAN_POINT ( 'NONE',  ( 12.63888201721073834, -1.779588368642105012, 12.47369581775632952 ) ) ;
#21354=LINE ( 'NONE', #42682, #22015 ) ;
#21360=CARTESIAN_POINT ( 'NONE',  ( 12.18627227647243139, 2.104539383777987549, 12.42301525548629826 ) ) ;
#21373=CARTESIAN_POINT ( 'NONE',  ( 17.74278939939642186, 0.6963438834399311439, -12.58074676375273881 ) ) ;
#21375=VECTOR ( 'NONE', #43885, 1000.000000000000000 ) ;
#21376=CARTESIAN_POINT ( 'NONE',  ( 12.44779487374913529, -3.012931620461074989, 13.55119122998581283 ) ) ;
#21377=CARTESIAN_POINT ( 'NONE',  ( 12.18521525456554500, 2.580824917997073253, 13.65593716524227830 ) ) ;
#21386=CARTESIAN_POINT ( 'NONE',  ( 18.17899100331058548, 2.462234907104897008, -12.46031481527572637 ) ) ;
#21400=CYLINDRICAL_SURFACE ( 'NONE', #58561, 0.6250000000000005551 ) ;
#21408=CARTESIAN_POINT ( 'NONE',  ( 12.49507620391304030, 0.5430989695823158492, -13.88572189919474731 ) ) ;
#21420=CARTESIAN_POINT ( 'NONE',  ( 12.25867852505488820, -0.3036576181174179268, 13.89554011873103612 ) ) ;
#21421=ORIENTED_EDGE ( 'NONE', *, *, #4267, .F. ) ;
#21455=EDGE_CURVE ( 'NONE', #48720, #50331, #32464, .T. ) ;
#21465=CARTESIAN_POINT ( 'NONE',  ( 12.40045920100465260, 0.4764818960106717571, -12.68796903437993606 ) ) ;
#21468=CARTESIAN_POINT ( 'NONE',  ( 7.100000000000000533, 0.000000000000000000, 0.000000000000000000 ) ) ;
#21480=CARTESIAN_POINT ( 'NONE',  ( 17.86985707050055794, 3.040024008573237069, -13.54397559521889249 ) ) ;
#21496=EDGE_LOOP ( 'NONE', ( #38311, #36613, #15861, #34498 ) ) ;
#21502=CARTESIAN_POINT ( 'NONE',  ( 17.88934697238260796, -1.841816770035711981, -12.46465977041039963 ) ) ;
#21520=CARTESIAN_POINT ( 'NONE',  ( 18.17005425344203928, -0.1118032413084528998, 13.89939982891986148 ) ) ;
#21525=CARTESIAN_POINT ( 'NONE',  ( 12.44983642703673965, 0.5143249053291590878, 13.88719129590927892 ) ) ;
#21527=CARTESIAN_POINT ( 'NONE',  ( 17.92176811225533228, -0.5062908248731810001, -13.88759084003172717 ) ) ;
#21531=CIRCLE ( 'NONE', #4807, 1.799999999999999600 ) ;
#21535=CARTESIAN_POINT ( 'NONE',  ( 18.05074276561661861, -0.3808128809978877372, 12.69231869260112155 ) ) ;
#21545=LINE ( 'NONE', #22580, #53463 ) ;
#21564=CYLINDRICAL_SURFACE ( 'NONE', #36215, 0.6250000000000005551 ) ;
#21571=CARTESIAN_POINT ( 'NONE',  ( 12.70142344966302694, 3.116692473072851577, -12.28627407840914820 ) ) ;
#21575=EDGE_LOOP ( 'NONE', ( #8026, #25812, #6716, #11039, #2524 ) ) ;
#21581=CARTESIAN_POINT ( 'NONE',  ( 12.52557666887736509, -1.940868768839141500, -12.56439497327413335 ) ) ;
#21586=CARTESIAN_POINT ( 'NONE',  ( 12.51429325950075722, -1.848987300417688440, -13.87736530974562754 ) ) ;
#21589=CARTESIAN_POINT ( 'NONE',  ( 17.96998260175204010, -3.070456082915653528, 12.22016143605431004 ) ) ;
#21614=CARTESIAN_POINT ( 'NONE',  ( 12.64262999012820998, -0.6038699852804539914, 12.68066884516330717 ) ) ;
#21621=CARTESIAN_POINT ( 'NONE',  ( 17.69797138021023386, 3.108785234939712261, 13.52525919603468729 ) ) ;
#21626=CARTESIAN_POINT ( 'NONE',  ( 5.500000000000000000, -12.22293997673000021, 3.800173559041999827 ) ) ;
#21634=CARTESIAN_POINT ( 'NONE',  ( 17.63745110450242493, -3.119885622577724504, -13.52219988749414092 ) ) ;
#21653=EDGE_CURVE ( 'NONE', #26199, #16266, #6732, .T. ) ;
#21654=CARTESIAN_POINT ( 'NONE',  ( 12.44978597066678461, 1.852986171447649211, -12.46300423074626984 ) ) ;
#21657=CARTESIAN_POINT ( 'NONE',  ( 18.08654171823789980, 2.829006819463714795, -13.59815647008714556 ) ) ;
#21662=CARTESIAN_POINT ( 'NONE',  ( 12.45041481799821348, -3.107897655637140044, -12.21069225363714317 ) ) ;
#21668=CARTESIAN_POINT ( 'NONE',  ( 17.93128725136842760, 0.4990964484179722382, -12.68679736436867778 ) ) ;
#21669=CARTESIAN_POINT ( 'NONE',  ( 12.36790781773587788, 2.946786910900277334, -12.33618673617031014 ) ) ;
#21676=DIRECTION ( 'NONE',  ( 0.000000000000000000, 0.6556630511404241135, -0.7550536162215433222 ) ) ;
#21679=CARTESIAN_POINT ( 'NONE',  ( 18.17657007421211190, 2.109712673715142817, 12.42212297180517133 ) ) ;
#21686=ADVANCED_FACE ( 'NONE', ( #6383 ), #57017, .F. ) ;
#21688=CARTESIAN_POINT ( 'NONE',  ( 12.36094932703100469, -3.049537035394455309, 12.22540636754321497 ) ) ;
#21697=CARTESIAN_POINT ( 'NONE',  ( 12.22372692396748484, 2.729759399082355653, 12.39506432367437583 ) ) ;
#21703=EDGE_CURVE ( 'NONE', #29163, #40500, #49738, .T. ) ;
#21706=CARTESIAN_POINT ( 'NONE',  ( 12.64124574432521619, 3.108970204239923874, 12.28865804429016073 ) ) ;
#21710=CARTESIAN_POINT ( 'NONE',  ( 12.24298814200621521, 0.2740984087646521350, 12.69603503205126316 ) ) ;
#21713=CARTESIAN_POINT ( 'NONE',  ( 17.74460677677806686, 3.176355914710234707, -12.19306589750529035 ) ) ;
#21714=CARTESIAN_POINT ( 'NONE',  ( 12.18013031904085963, -2.522561724994069721, 13.66866813226131505 ) ) ;
#21716=CARTESIAN_POINT ( 'NONE',  ( 12.80505043854143388, 1.875000000000000000, 13.78627172894481667 ) ) ;
#21723=CARTESIAN_POINT ( 'NONE',  ( 17.86958940788776218, 3.040180081688693470, -12.30916660591379497 ) ) ;
#21729=CARTESIAN_POINT ( 'NONE',  ( 12.80505043854143388, 1.787797342887042840, 13.88538010501570774 ) ) ;
#21730=B_SPLINE_CURVE_WITH_KNOTS ( 'NONE', 3,
 ( #47860, #52750, #35981, #57643, #58680, #16028, #36679, #5539, #26878, #5194, #4845, #52053, #15691, #15003, #31778, #41234, #26532, #47512, #69166, #62545, #9402, #30744, #41916, #20591 ),
 .UNSPECIFIED., .F., .F.,
 ( 4, 2, 1, 1, 1, 2, 2, 1, 2, 2, 2, 2, 2, 4 ),
 ( 0.000000000000000000, 0.2499999999999459876, 0.3749999999999235056, 0.4374999999999063527, 0.4687499999999000244, 0.4843749999998934741, 0.4999999999998869238, 0.5624999999998998579, 0.5937499999999029665, 0.6249999999999059641, 0.6874999999999128475, 0.7499999999999197309, 0.8749999999999599209, 1.000000000000000000 ),
 .UNSPECIFIED. ) ;
#21734=APPLICATION_CONTEXT ( 'automotive_design' ) ;
#21740=CARTESIAN_POINT ( 'NONE',  ( 17.55505043854143921, 0.7302158263239199032, -13.98094363220830871 ) ) ;
#21748=CARTESIAN_POINT ( 'NONE',  ( 12.21931057679652177, -0.2190559830447486311, -13.89769592719591884 ) ) ;
#21754=ORIENTED_EDGE ( 'NONE', *, *, #59035, .T. ) ;
#21758=CARTESIAN_POINT ( 'NONE',  ( 17.65076761715808473, -3.243341803256440947, -13.61913462216701376 ) ) ;
#21759=CARTESIAN_POINT ( 'NONE',  ( 17.99149020822394363, -2.947405452019512317, -12.33598828993208230 ) ) ;
#21764=CARTESIAN_POINT ( 'NONE',  ( 18.17956732772856654, -2.474903466465859569, -12.45737214979850727 ) ) ;
#21766=CARTESIAN_POINT ( 'NONE',  ( 12.22351867101279588, 0.2292390942789186981, 13.89746050377130793 ) ) ;
#21777=EDGE_LOOP ( 'NONE', ( #66521, #15923, #34282, #34062 ) ) ;
#21778=CARTESIAN_POINT ( 'NONE',  ( 17.55505043854143921, 0.7302158263239199032, -13.98094363220830871 ) ) ;
#21780=CARTESIAN_POINT ( 'NONE',  ( 17.65075606735202740, -1.792616958753535439, 13.88476197432802373 ) ) ;
#21785=EDGE_CURVE ( 'NONE', #47809, #65244, #44512, .T. ) ;
#21791=B_SPLINE_CURVE_WITH_KNOTS ( 'NONE', 3,
 ( #36857, #32987, #6405, #27753, #32645, #5379, #49065, #1172, #53619 ),
 .UNSPECIFIED., .F., .F.,
 ( 4, 1, 2, 2, 4 ),
 ( 0.000000000000000000, 0.2499999999999998890, 0.3750000000000004996, 0.5000000000000011102, 1.000000000000000000 ),
 .UNSPECIFIED. ) ;
#21798=CARTESIAN_POINT ( 'NONE',  ( 18.17230637740977883, 2.598591657315551640, -12.42808133542726701 ) ) ;
#21804=CARTESIAN_POINT ( 'NONE',  ( 12.80505043854144098, 0.7302158263239095781, 13.98094363220830871 ) ) ;
#21808=CARTESIAN_POINT ( 'NONE',  ( 12.54669586862715036, 0.5691963043021760482, -12.68282590392938225 ) ) ;
#21813=EDGE_LOOP ( 'NONE', ( #40934, #59670, #738, #37773 ) ) ;
#21817=CARTESIAN_POINT ( 'NONE',  ( 18.18005043854147118, -2.500000000000000000, -25.00000000000000000 ) ) ;
#21823=CARTESIAN_POINT ( 'NONE',  ( 18.03303331148765665, 2.902815211882732616, -13.57973159350535397 ) ) ;
#21844=CARTESIAN_POINT ( 'NONE',  ( 18.17906596528623098, 0.04061643748080398519, -13.89993966956671834 ) ) ;
#21850=ORIENTED_EDGE ( 'NONE', *, *, #57925, .T. ) ;
#21859=CARTESIAN_POINT ( 'NONE',  ( 12.20019055993959078, 2.341318142288554061, -13.70585175580907666 ) ) ;
#21861=CARTESIAN_POINT ( 'NONE',  ( 18.11581248800844435, -0.2761834754990949992, 13.89631168292872587 ) ) ;
#21863=CARTESIAN_POINT ( 'NONE',  ( 17.63844293491913362, 0.6206536995415011804, 13.88134483103365824 ) ) ;
#21865=CARTESIAN_POINT ( 'NONE',  ( 12.30787805059924978, 0.3788776036388727952, 13.89305317344797253 ) ) ;
#21878=CARTESIAN_POINT ( 'NONE',  ( 18.08024441302280394, -0.3389720875425239477, 12.69391532355468044 ) ) ;
#21891=CARTESIAN_POINT ( 'NONE',  ( 12.58342066637852597, -0.6849607937330853824, -12.58136878870645070 ) ) ;
#21893=CARTESIAN_POINT ( 'NONE',  ( 17.97968936757969161, 3.063621360739230415, -12.22187700344946748 ) ) ;
#21894=CARTESIAN_POINT ( 'NONE',  ( 5.602673821508641794, 12.13104802960955197, 3.749633869517943197 ) ) ;
#21907=VECTOR ( 'NONE', #52873, 999.9999999999998863 ) ;
#21908=CARTESIAN_POINT ( 'NONE',  ( 18.02507847443574818, -0.4124479947379862121, -13.89177559470775236 ) ) ;
#21917=ORIENTED_EDGE ( 'NONE', *, *, #43679, .F. ) ;
#21926=CARTESIAN_POINT ( 'NONE',  ( 12.64104727702816433, -1.896551500700493165, -12.57186431639862256 ) ) ;
#21927=DIRECTION ( 'NONE',  ( -1.000000000000000000, 0.000000000000000000, 0.000000000000000000 ) ) ;
#21930=CARTESIAN_POINT ( 'NONE',  ( 12.28223951138208925, -3.023960592195344521, -13.66951858831273903 ) ) ;
#21932=CARTESIAN_POINT ( 'NONE',  ( 12.70915608519175954, -1.765590719838300959, 12.47568749009910505 ) ) ;
#21933=CARTESIAN_POINT ( 'NONE',  ( 18.26373780016888304, -2.633255345072546216, 12.32177353326231284 ) ) ;
#21945=B_SPLINE_CURVE_WITH_KNOTS ( 'NONE', 1,
 ( #5082, #29710 ),
 .UNSPECIFIED., .F., .F.,
 ( 2, 2 ),
 ( 0.000000000000000000, 1.000000000000000000 ),
 .UNSPECIFIED. ) ;
#21965=CARTESIAN_POINT ( 'NONE',  ( 17.99238080566774300, 2.053374525523682603, 13.75805324639251026 ) ) ;
#21973=LINE ( 'NONE', #314, #57752 ) ;
#21978=CARTESIAN_POINT ( 'NONE',  ( 17.94133460182555950, -1.899620958390729086, -13.87053073593715524 ) ) ;
#21998=CARTESIAN_POINT ( 'NONE',  ( 12.14218285455818602, 2.187615620731402810, -12.40865911928243470 ) ) ;
#22006=CARTESIAN_POINT ( 'NONE',  ( 12.36610530618396808, -3.052942130732431814, -12.22454734379039287 ) ) ;
#22014=CARTESIAN_POINT ( 'NONE',  ( 17.98979505986429572, 0.4491390935506892612, -12.68931154995402188 ) ) ;
#22015=VECTOR ( 'NONE', #63991, 1000.000000000000000 ) ;
#22024=CARTESIAN_POINT ( 'NONE',  ( 18.03667146358274920, 1.942392957153849409, 12.44938452643338955 ) ) ;
#22031=CARTESIAN_POINT ( 'NONE',  ( 12.68481529409928754, -3.190188709592561622, 12.18945115681611924 ) ) ;
#22037=CARTESIAN_POINT ( 'NONE',  ( 12.58275800453940363, -0.6847469513499573335, 12.58138041838080667 ) ) ;
#22039=CARTESIAN_POINT ( 'NONE',  ( 17.55505043854143565, 3.199751711897561801, -12.18694338143115452 ) ) ;
#22040=ADVANCED_FACE ( 'NONE', ( #57725 ), #12799, .T. ) ;
#22041=CARTESIAN_POINT ( 'NONE',  ( 12.20147980349668870, 2.662577969174664272, 12.41220455913371090 ) ) ;
#22047=CARTESIAN_POINT ( 'NONE',  ( 12.80505043854143388, 1.760910691117811844, 12.47634535983622861 ) ) ;
#22052=CARTESIAN_POINT ( 'NONE',  ( 12.21279950745852183, 0.1999332404310504574, 12.69788654131193795 ) ) ;
#22055=CARTESIAN_POINT ( 'NONE',  ( 17.60408629073138087, 3.199716927301896163, -12.18695251432576931 ) ) ;
#22058=CARTESIAN_POINT ( 'NONE',  ( 12.10810820711264846, -2.719264802799585823, 13.73338027651840321 ) ) ;
#22062=FACE_OUTER_BOUND ( 'NONE', #54905, .T. ) ;
#22086=CARTESIAN_POINT ( 'NONE',  ( 18.04669395734980597, -2.113974215446797089, 13.74779306078356278 ) ) ;
#22094=CARTESIAN_POINT ( 'NONE',  ( 12.19608251853991909, -0.1421750971574143596, -13.89904149565844627 ) ) ;
#22114=CARTESIAN_POINT ( 'NONE',  ( 12.76382393867145737, 0.6239806250735583371, 13.88114166035889241 ) ) ;
#22144=CARTESIAN_POINT ( 'NONE',  ( 5.619513196215851991, -12.94695275183270589, -2.446394349796571444 ) ) ;
#22153=CARTESIAN_POINT ( 'NONE',  ( 12.76382339226414864, 0.6237239846186464209, -12.67937377942301502 ) ) ;
#22176=EDGE_LOOP ( 'NONE', ( #39673, #41561, #36810, #10140 ) ) ;
#22192=ORIENTED_EDGE ( 'NONE', *, *, #26043, .T. ) ;
#22194=CARTESIAN_POINT ( 'NONE',  ( 18.18005043824477696, 1.062919176435095297E-10, -13.90000000153291637 ) ) ;
#22195=EDGE_CURVE ( 'NONE', #7548, #41308, #34726, .T. ) ;
#22201=ORIENTED_EDGE ( 'NONE', *, *, #40106, .F. ) ;
#22205=CARTESIAN_POINT ( 'NONE',  ( 12.24392764853879889, 2.776000094621842607, -13.61105252602849092 ) ) ;
#22208=CARTESIAN_POINT ( 'NONE',  ( 17.59627693841142460, -0.6239806250735587811, 13.88114166035889241 ) ) ;
#22212=CONICAL_SURFACE ( 'NONE', #54456, 1.899997304679999610, 0.7853981633972997312 ) ;
#22215=CARTESIAN_POINT ( 'NONE',  ( 12.18394749351799966, 0.08111026478887338464, 13.89976203980570979 ) ) ;
#22216=CARTESIAN_POINT ( 'NONE',  ( 12.29580333558936900, -0.3624858755954508682, -13.89364165472173873 ) ) ;
#22218=CARTESIAN_POINT ( 'NONE',  ( 17.90980351674997451, -0.5146449798727437130, -13.88717540043696808 ) ) ;
#22226=CARTESIAN_POINT ( 'NONE',  ( 18.12848705786300130, -0.2487950381773059993, 12.69672507751632118 ) ) ;
#22230=ORIENTED_EDGE ( 'NONE', *, *, #8235, .T. ) ;
#22235=B_SPLINE_CURVE_WITH_KNOTS ( 'NONE', 3,
 ( #21716, #43052, #11921, #65402 ),
 .UNSPECIFIED., .F., .F.,
 ( 4, 4 ),
 ( 0.000000000000000000, 1.000000000000000000 ),
 .UNSPECIFIED. ) ;
#22240=CARTESIAN_POINT ( 'NONE',  ( 12.19582542658656266, -0.3901114995139884911, -12.59396323349877989 ) ) ;
#22242=FACE_OUTER_BOUND ( 'NONE', #31471, .T. ) ;
#22254=CARTESIAN_POINT ( 'NONE',  ( 17.55505043854147118, -1.875000000000000000, -13.78627172894481667 ) ) ;
#22259=CARTESIAN_POINT ( 'NONE',  ( 18.17981516808187337, 0.01996689158402835743, -13.89998575767903155 ) ) ;
#22268=CARTESIAN_POINT ( 'NONE',  ( 17.67418791246062071, -1.797344534875189526, 13.88414834504120421 ) ) ;
#22275=CARTESIAN_POINT ( 'NONE',  ( 12.20003344249116317, -2.341920628070003563, -12.48700265052703884 ) ) ;
#22280=CARTESIAN_POINT ( 'NONE',  ( 12.09815554886061761, -2.355526959511359486, -13.80042145504354778 ) ) ;
#22284=CARTESIAN_POINT ( 'NONE',  ( 18.06303038656661286, -1.966720487694626041, 12.44556484937419150 ) ) ;
#22293=FACE_OUTER_BOUND ( 'NONE', #59345, .T. ) ;
#22295=CARTESIAN_POINT ( 'NONE',  ( 18.28081516007891949, -2.296096720418743242, -12.39048987308211203 ) ) ;
#22299=DIRECTION ( 'NONE',  ( -1.000000000000000000, 0.000000000000000000, 0.000000000000000000 ) ) ;
#22312=CARTESIAN_POINT ( 'NONE',  ( 18.14704975929774022, 2.701423609612693344, 13.62863833005038572 ) ) ;
#22323=CARTESIAN_POINT ( 'NONE',  ( 18.26096953105667353, -2.684662952176597006, -13.74018646639511765 ) ) ;
#22341=CARTESIAN_POINT ( 'NONE',  ( 17.65158693958703751, 1.792693047823491925, 13.88475221912152158 ) ) ;
#22343=ORIENTED_EDGE ( 'NONE', *, *, #37441, .T. ) ;
#22348=CARTESIAN_POINT ( 'NONE',  ( 12.29441019255333600, 2.991168332544433373, -12.23980925793768648 ) ) ;
#22350=EDGE_LOOP ( 'NONE', ( #17645, #37529, #541, #48088 ) ) ;
#22365=CARTESIAN_POINT ( 'NONE',  ( 17.89428234746476676, -0.5250240499537035532, -12.68539034781189301 ) ) ;
#22366=CARTESIAN_POINT ( 'NONE',  ( 12.18102902119794351, 2.459609776898156852, -12.46092926276592827 ) ) ;
#22374=CARTESIAN_POINT ( 'NONE',  ( 18.14595306053280410, 2.897894011715723472, 12.26224306838060407 ) ) ;
#22375=CARTESIAN_POINT ( 'NONE',  ( 17.55505043854144276, -0.6250000000000001110, 13.88107975066923316 ) ) ;
#22380=CARTESIAN_POINT ( 'NONE',  ( 12.25024874575448308, -2.943737818075154777, 12.25130580795035051 ) ) ;
#22384=DIRECTION ( 'NONE',  ( 0.000000000000000000, -0.6555644356537908557, -0.7551392392836745460 ) ) ;
#22387=CARTESIAN_POINT ( 'NONE',  ( 12.08466115484542946, -0.08185661189466741927, 12.59973963693671806 ) ) ;
#22392=CARTESIAN_POINT ( 'NONE',  ( 12.61477885367309604, 1.785717119372573825, 12.47282100101237212 ) ) ;
#22394=CARTESIAN_POINT ( 'NONE',  ( 4.599999999999999645, 0.000000000000000000, 0.000000000000000000 ) ) ;
#22396=CARTESIAN_POINT ( 'NONE',  ( 17.77668021070434889, -0.6849607937330753904, 12.58136878870645248 ) ) ;
#22406=CARTESIAN_POINT ( 'NONE',  ( 12.19498122944103713, -2.912558373969576397, 13.69368860183518599 ) ) ;
#22418=CARTESIAN_POINT ( 'NONE',  ( 17.88838831427747778, 1.971212373206994384, -12.55919681887186101 ) ) ;
#22422=PLANE ( 'NONE',  #23395 ) ;
#22430=VERTEX_POINT ( 'NONE', #14919 ) ;
#22431=CARTESIAN_POINT ( 'NONE',  ( 17.93750432894415070, -2.994741171281513736, 13.55599983589037372 ) ) ;
#22436=ADVANCED_FACE ( 'NONE', ( #68735 ), #47426, .T. ) ;
#22453=CARTESIAN_POINT ( 'NONE',  ( 12.46419745175922955, 3.023973028971910004, 13.54820305185629259 ) ) ;
#22454=CARTESIAN_POINT ( 'NONE',  ( 17.56547987801838318, -1.875000035136120458, 12.57545641098306000 ) ) ;
#22456=CARTESIAN_POINT ( 'NONE',  ( 12.24892445252029205, 0.2854033456632657506, 13.89606078824648172 ) ) ;
#22459=CARTESIAN_POINT ( 'NONE',  ( 5.500000000000000000, -13.94845324556000143, -4.312847325879000770 ) ) ;
#22472=CARTESIAN_POINT ( 'NONE',  ( 17.55505043854147118, -1.787816316115923954, 13.88537766212463254 ) ) ;
#22490=EDGE_CURVE ( 'NONE', #53037, #57647, #12762, .T. ) ;
#22498=CARTESIAN_POINT ( 'NONE',  ( 12.41737123625420125, 2.003119782516696645, -13.76653501054599893 ) ) ;
#22500=CARTESIAN_POINT ( 'NONE',  ( 5.500000000000000000, 12.87590651766999983, 2.791353855799999728 ) ) ;
#22508=CARTESIAN_POINT ( 'NONE',  ( 5.500000000000000000, 12.22293997673000021, -3.800173559029999648 ) ) ;
#22511=CARTESIAN_POINT ( 'NONE',  ( 18.14722095428668780, 2.700912180127440720, -13.62881044890620785 ) ) ;
#22513=PLANE ( 'NONE',  #20590 ) ;
#22527=CARTESIAN_POINT ( 'NONE',  ( 17.63827777595935231, -3.120766739611795071, -13.52195882727504106 ) ) ;
#22534=CARTESIAN_POINT ( 'NONE',  ( 17.82422846108294578, -1.812210939693179368, -12.46899807711483987 ) ) ;
#22536=AXIS2_PLACEMENT_3D ( 'NONE', #7235, #60717, #28928 ) ;
#22546=CARTESIAN_POINT ( 'NONE',  ( 12.63821499911163038, 1.807008444693749771, -13.88289391573714227 ) ) ;
#22550=CARTESIAN_POINT ( 'NONE',  ( 18.08498662421417791, -0.4989076128645613117, 13.99111800451625243 ) ) ;
#22552=ORIENTED_EDGE ( 'NONE', *, *, #21785, .F. ) ;
#22557=CARTESIAN_POINT ( 'NONE',  ( 12.27274360190958191, -0.3282986408113108268, -13.89479914614070211 ) ) ;
#22569=CARTESIAN_POINT ( 'NONE',  ( 18.17177216100527914, -0.1019009512359500130, 12.69945530929771493 ) ) ;
#22571=CARTESIAN_POINT ( 'NONE',  ( 18.14655301452571834, -2.701944876743755053, -12.40222020716218410 ) ) ;
#22580=CARTESIAN_POINT ( 'NONE',  ( 17.55505043854143565, 3.125000000000000000, -13.52084414783465682 ) ) ;
#22585=CARTESIAN_POINT ( 'NONE',  ( 12.08006680260081467, -0.02395120399004109155, -12.59999907117299855 ) ) ;
#22587=CARTESIAN_POINT ( 'NONE',  ( 17.65081963855157099, 3.193844305817326479, -12.18849311783432654 ) ) ;
#22596=ORIENTED_EDGE ( 'NONE', *, *, #20628, .T. ) ;
#22602=CARTESIAN_POINT ( 'NONE',  ( 18.01141113125041571, -0.4275223103465174423, -13.89116040406442032 ) ) ;
#22612=CARTESIAN_POINT ( 'NONE',  ( 12.40004937879933067, -2.976133613074172679, -13.56081502232354907 ) ) ;
#22616=ORIENTED_EDGE ( 'NONE', *, *, #23183, .F. ) ;
#22617=CARTESIAN_POINT ( 'NONE',  ( 12.35269809054582701, -2.068595867586759951, -12.54166796000261108 ) ) ;
#22620=DIRECTION ( 'NONE',  ( -0.000000000000000000, -0.000000000000000000, 1.000000000000000000 ) ) ;
#22621=DIRECTION ( 'NONE',  ( -1.000000000000000000, 0.000000000000000000, 0.000000000000000000 ) ) ;
#22624=CARTESIAN_POINT ( 'NONE',  ( 17.86072591669553944, -3.045244688009580702, 12.30767216807748987 ) ) ;
#22641=EDGE_CURVE ( 'NONE', #21130, #44214, #27747, .T. ) ;
#22653=CARTESIAN_POINT ( 'NONE',  ( 17.93716281226432230, 2.994693044426598671, 13.55594923565224974 ) ) ;
#22668=CARTESIAN_POINT ( 'NONE',  ( 17.74755423490966066, -3.094705742910454305, -13.52911976267489713 ) ) ;
#22678=STYLED_ITEM ( 'NONE', ( #42655 ), #30272 ) ;
#22691=CARTESIAN_POINT ( 'NONE',  ( 12.44969725703162311, 3.107561633766895426, -12.21077779329595359 ) ) ;
#22699=CARTESIAN_POINT ( 'NONE',  ( 12.68571266918098317, -3.190282694684599907, -12.18942654693561067 ) ) ;
#22707=CARTESIAN_POINT ( 'NONE',  ( 18.08578179881429193, 0.3302353423713645375, -12.69422546839061461 ) ) ;
#22708=CARTESIAN_POINT ( 'NONE',  ( 12.18136627099982405, 2.541785745017987264, -12.44176459540348922 ) ) ;
#22711=ORIENTED_EDGE ( 'NONE', *, *, #19573, .F. ) ;
#22714=FILL_AREA_STYLE ('',( #7682 ) ) ;
#22717=CARTESIAN_POINT ( 'NONE',  ( 18.10358258445729973, 2.009225442943100681, 12.43878435193939858 ) ) ;
#22721=CARTESIAN_POINT ( 'NONE',  ( 12.08019350287876037, -0.1887961028407837971, -12.59999260960569245 ) ) ;
#22723=VERTEX_POINT ( 'NONE', #44950 ) ;
#22724=CARTESIAN_POINT ( 'NONE',  ( 12.40918755490010739, -3.083210392534605937, 12.21694967330944692 ) ) ;
#22730=CARTESIAN_POINT ( 'NONE',  ( 12.21516876105738802, -0.4188397444781318257, 12.59305179380755213 ) ) ;
#22734=CARTESIAN_POINT ( 'NONE',  ( 12.61225881068683918, 3.094544630460535739, 12.29295341835051047 ) ) ;
#22752=CARTESIAN_POINT ( 'NONE',  ( 12.12912605232854801, -2.253778109953310516, 13.81740241363613642 ) ) ;
#22755=CARTESIAN_POINT ( 'NONE',  ( 12.80505043854146940, -1.875000000000000444, -12.57541666120756396 ) ) ;
#22771=DIRECTION ( 'NONE',  ( 0.000000000000000000, -0.7914851585299630399, 0.6111883865280813843 ) ) ;
#22777=CARTESIAN_POINT ( 'NONE',  ( 18.17537916830627864, -2.421093501972792605, 13.68989611939600159 ) ) ;
#22788=CARTESIAN_POINT ( 'NONE',  ( 17.71955056974170617, 0.7009231686363512903, -12.58048995873114073 ) ) ;
#22797=CARTESIAN_POINT ( 'NONE',  ( 17.74540238971360750, -1.811773551562723350, -13.88227535917553546 ) ) ;
#22800=CARTESIAN_POINT ( 'NONE',  ( 12.80505043854144276, -0.6600719421079697113, 13.91436771118226012 ) ) ;
#22801=CARTESIAN_POINT ( 'NONE',  ( 12.64211699103822539, 1.896258653787259885, 13.78307619201600431 ) ) ;
#22805=CARTESIAN_POINT ( 'NONE',  ( 12.38211732427673972, 0.5935699150349409425, 13.98741755999924763 ) ) ;
#22806=ORIENTED_EDGE ( 'NONE', *, *, #47320, .T. ) ;
#22812=AXIS2_PLACEMENT_3D ( 'NONE', #51289, #19472, #31347 ) ;
#22833=CARTESIAN_POINT ( 'NONE',  ( 17.55505043854143565, 3.125000000000000000, -12.28374638332999602 ) ) ;
#22839=VERTEX_POINT ( 'NONE', #5026 ) ;
#22850=CARTESIAN_POINT ( 'NONE',  ( 5.699999999999998401, 13.03908314205310681, 1.889202640492164242 ) ) ;
#22853=CARTESIAN_POINT ( 'NONE',  ( 12.08612513405891953, -0.09509187666555325713, -13.99968209810982067 ) ) ;
#22856=LINE ( 'NONE', #65851, #28792 ) ;
#22859=ORIENTED_EDGE ( 'NONE', *, *, #28984, .T. ) ;
#22861=CARTESIAN_POINT ( 'NONE',  ( 17.96968152693878551, 2.032227188856707389, -13.76161273592455103 ) ) ;
#22872=CARTESIAN_POINT ( 'NONE',  ( 18.08719379937744165, 0.3285641700854472491, -12.69429818673162202 ) ) ;
#22877=CARTESIAN_POINT ( 'NONE',  ( 18.17052368435256682, -2.609308838451334100, -13.64962199044944491 ) ) ;
#22884=CARTESIAN_POINT ( 'NONE',  ( 17.94092590763760242, -3.089486433945226374, -12.21536380989863524 ) ) ;
#22885=CARTESIAN_POINT ( 'NONE',  ( 17.55505043854144631, 0.7192913403693005359, 12.57945229203838267 ) ) ;
#22891=FACE_OUTER_BOUND ( 'NONE', #13875, .T. ) ;
#22894=CARTESIAN_POINT ( 'NONE',  ( 12.42293806700074832, 2.994693046128884539, -13.55600569395198995 ) ) ;
#22897=CARTESIAN_POINT ( 'NONE',  ( 17.95947766544255586, 0.4766231184928877984, 13.88900205690512735 ) ) ;
#22902=CARTESIAN_POINT ( 'NONE',  ( 12.33073330760568176, -0.4072264708333818151, 13.89197624347111848 ) ) ;
#22903=CARTESIAN_POINT ( 'NONE',  ( 12.43800705101901372, -0.5060514260813850917, -13.88760251447818206 ) ) ;
#22915=CARTESIAN_POINT ( 'NONE',  ( 17.77555300520474546, 0.5848996845204763595, 12.68186405703078989 ) ) ;
#22924=CARTESIAN_POINT ( 'NONE',  ( 12.66121447289699553, -1.891428313113427961, 13.78385349382386060 ) ) ;
#22928=DIRECTION ( 'NONE',  ( -1.000000000000000000, 0.000000000000000000, 0.000000000000000000 ) ) ;
#22930=ORIENTED_EDGE ( 'NONE', *, *, #65099, .F. ) ;
#22931=CARTESIAN_POINT ( 'NONE',  ( 12.11457469949690591, 0.2196334679052245331, -12.59809060309703277 ) ) ;
#22947=CARTESIAN_POINT ( 'NONE',  ( 18.18005725403618911, 0.009762789003249052952, -13.90000041479088289 ) ) ;
#22957=CARTESIAN_POINT ( 'NONE',  ( 12.80505043854146940, -1.760910691117821614, -12.47634535983622683 ) ) ;
#22968=DIRECTION ( 'NONE',  ( 1.000000000000000000, 0.000000000000000000, 0.000000000000000000 ) ) ;
#22972=CARTESIAN_POINT ( 'NONE',  ( 17.94181191902913852, -1.871597878487309297, 12.46022310877027195 ) ) ;
#23003=CARTESIAN_POINT ( 'NONE',  ( 18.20194470744735327, 2.188139888162242475, 13.82794850388582653 ) ) ;
#23014=ORIENTED_EDGE ( 'NONE', *, *, #45342, .T. ) ;
#23017=CARTESIAN_POINT ( 'NONE',  ( 17.78650313621487200, -3.080655036186602747, -13.53295239609827050 ) ) ;
#23038=CARTESIAN_POINT ( 'NONE',  ( 12.70216005901004586, 1.883184384472671891, -12.57411343304723594 ) ) ;
#23039=EDGE_CURVE ( 'NONE', #62256, #4104, #30002, .T. ) ;
#23053=CARTESIAN_POINT ( 'NONE',  ( 12.32706758141029368, -2.902815230603663643, -13.57967619870183640 ) ) ;
#23054=CARTESIAN_POINT ( 'NONE',  ( 18.15598060823833038, 0.1720826094844778720, -12.69843621396829292 ) ) ;
#23067=CARTESIAN_POINT ( 'NONE',  ( 17.80610932905893407, 1.927548246225502471, 12.56666212246289582 ) ) ;
#23074=CARTESIAN_POINT ( 'NONE',  ( 12.15423239032309866, -2.797846099084075000, 12.28544569950199516 ) ) ;
#23082=CARTESIAN_POINT ( 'NONE',  ( 12.41154142318501385, -0.6042324041877022989, 12.58550538354983672 ) ) ;
#23085=CARTESIAN_POINT ( 'NONE',  ( 12.47303194318975450, 3.029615900428510145, 12.31225512782603282 ) ) ;
#23096=LINE ( 'NONE', #27663, #13258 ) ;
#23098=CARTESIAN_POINT ( 'NONE',  ( 18.20569531736705216, 2.110314541875505157, -12.42277286985108731 ) ) ;
#23100=CARTESIAN_POINT ( 'NONE',  ( 12.48119050255588292, -1.864280969780530928, 13.87532308892432553 ) ) ;
#23110=LINE ( 'NONE', #44463, #37681 ) ;
#23120=CARTESIAN_POINT ( 'NONE',  ( 18.27990784067586105, -0.1916560647366354619, -13.99999316327169829 ) ) ;
#23123=CARTESIAN_POINT ( 'NONE',  ( 12.24916108028120831, -2.785825388767152688, 12.38039059669299569 ) ) ;
#23129=CARTESIAN_POINT ( 'NONE',  ( 18.11595230660373090, -2.775896237034515490, 13.61106543307220207 ) ) ;
#23151=CARTESIAN_POINT ( 'NONE',  ( 12.27782020686940534, 2.164202955609506152, 13.73892120162924968 ) ) ;
#23155=CARTESIAN_POINT ( 'NONE',  ( 12.15994429558105949, 0.3334496638227513188, 13.99603244703262739 ) ) ;
#23159=CARTESIAN_POINT ( 'NONE',  ( 21.49999863197000138, -14.00000000000000000, 0.000000000000000000 ) ) ;
#23164=CARTESIAN_POINT ( 'NONE',  ( 4.649999478197380576, 0.000000000000000000, -9.325873406851000657E-14 ) ) ;
#23167=CARTESIAN_POINT ( 'NONE',  ( 17.55505043854143565, 3.125000000000000000, -25.00000000000000000 ) ) ;
#23182=EDGE_CURVE ( 'NONE', #13672, #15974, #11271, .T. ) ;
#23183=EDGE_CURVE ( 'NONE', #10762, #40405, #31092, .T. ) ;
#23204=CIRCLE ( 'NONE', #68967, 13.17499999999999538 ) ;
#23205=CARTESIAN_POINT ( 'NONE',  ( 12.08032335320030093, -0.02332822437944849850, -13.99998565365491388 ) ) ;
#23216=CARTESIAN_POINT ( 'NONE',  ( 17.81260085050721287, 3.200899519495046697, -13.62917211583035026 ) ) ;
#23220=AXIS2_PLACEMENT_3D ( 'NONE', #40230, #34991, #7370 ) ;
#23224=CARTESIAN_POINT ( 'NONE',  ( 17.92176999529980819, 0.5062894560746492578, -12.68641719396730316 ) ) ;
#23229=CARTESIAN_POINT ( 'NONE',  ( 18.18005044575085449, -2.500000006795658702, -13.67340643792831401 ) ) ;
#23237=CARTESIAN_POINT ( 'NONE',  ( 18.03667146358278117, -1.942392957153856514, -12.44938452643338955 ) ) ;
#23238=ADVANCED_FACE ( 'NONE', ( #17566 ), #54621, .T. ) ;
#23246=LINE ( 'NONE', #12412, #50387 ) ;
#23249=CARTESIAN_POINT ( 'NONE',  ( 12.37605701841384409, 2.954974367521622458, -13.56637846613975462 ) ) ;
#23253=CARTESIAN_POINT ( 'NONE',  ( 17.78490373093669774, 0.5812901181791684246, 13.88363587338390559 ) ) ;
#23259=CARTESIAN_POINT ( 'NONE',  ( 12.64394750692856917, -0.6042238833877793258, -13.88232004407405462 ) ) ;
#23273=CIRCLE ( 'NONE', #32213, 14.00000000000000000 ) ;
#23274=CARTESIAN_POINT ( 'NONE',  ( 18.12908148756441307, -2.747269642056539229, -12.39050915965749766 ) ) ;
#23289=CARTESIAN_POINT ( 'NONE',  ( 12.08617037725597143, -0.09400131084488008715, -12.59965472429369093 ) ) ;
#23290=CARTESIAN_POINT ( 'NONE',  ( 12.48752230513397343, -1.955425561953247682, -12.56195022951900775 ) ) ;
#23306=CARTESIAN_POINT ( 'NONE',  ( 17.93540541742265049, -0.4960449563116382521, -13.88808666890936827 ) ) ;
#23312=CARTESIAN_POINT ( 'NONE',  ( 18.15933590972274558, -2.660621711755056573, 12.41273490637200894 ) ) ;
#23327=CARTESIAN_POINT ( 'NONE',  ( 18.00033872679592051, -1.911966235111655310, 12.45410047071287529 ) ) ;
#23331=CARTESIAN_POINT ( 'NONE',  ( 18.18005043875541560, 2.480307850574838380, 13.67758270212689276 ) ) ;
#23358=CARTESIAN_POINT ( 'NONE',  ( 17.63745110450239295, 3.119885622577724504, 13.52219988749413737 ) ) ;
#23369=CARTESIAN_POINT ( 'NONE',  ( 18.10159474502875554, -2.998280829653927615, -13.67518427740799325 ) ) ;
#23375=EDGE_CURVE ( 'NONE', #31711, #53691, #11290, .T. ) ;
#23391=CARTESIAN_POINT ( 'NONE',  ( 12.60227161487510195, 1.908786995848723134, -12.56986146204938493 ) ) ;
#23395=AXIS2_PLACEMENT_3D ( 'NONE', #5649, #17177, #7041 ) ;
#23399=CARTESIAN_POINT ( 'NONE',  ( 18.00096209673668213, 0.5835546240207898361, 13.98799446466929197 ) ) ;
#23402=CARTESIAN_POINT ( 'NONE',  ( 12.50259176966692110, -1.826373719304919208, -12.46693171540044531 ) ) ;
#23409=CARTESIAN_POINT ( 'NONE',  ( 12.23130451870208013, -2.748081639521273267, -13.61765624098743466 ) ) ;
#23410=CARTESIAN_POINT ( 'NONE',  ( 18.11105811251409037, 0.2856309244984027718, -12.69568149856438311 ) ) ;
#23412=CARTESIAN_POINT ( 'NONE',  ( 12.18936456685720771, 2.391983199617983225, -12.47610573829950553 ) ) ;
#23420=CARTESIAN_POINT ( 'NONE',  ( 17.89634705932796166, 1.976313534945128847, 12.55826774113814892 ) ) ;
#23425=CARTESIAN_POINT ( 'NONE',  ( 12.35913603394561733, -0.5748214923286987244, -12.58705572532422856 ) ) ;
#23427=CARTESIAN_POINT ( 'NONE',  ( 12.18751053307003929, -2.401600969044472844, 12.47399295505823069 ) ) ;
#23430=DIRECTION ( 'NONE',  ( 0.000000000000000000, 0.000000000000000000, 1.000000000000000000 ) ) ;
#23432=CARTESIAN_POINT ( 'NONE',  ( 12.18894565086185189, -0.3798658283128588664, 12.59428767283704964 ) ) ;
#23435=CARTESIAN_POINT ( 'NONE',  ( 12.21176631991875894, 2.303170217796229213, 12.49524360984840321 ) ) ;
#23443=CARTESIAN_POINT ( 'NONE',  ( 17.55505043854144276, -0.6250000000000001110, 12.67928921589117586 ) ) ;
#23451=CARTESIAN_POINT ( 'NONE',  ( 18.11145169124086962, -2.784830482494844439, 13.60891328693116442 ) ) ;
#23454=FACE_BOUND ( 'NONE', #33378, .T. ) ;
#23462=DIRECTION ( 'NONE',  ( -0.000000000000000000, -0.000000000000000000, 1.000000000000000000 ) ) ;
#23472=CARTESIAN_POINT ( 'NONE',  ( 4.599999999999999645, 1.760910691117812954, 12.47634535983622861 ) ) ;
#23473=CARTESIAN_POINT ( 'NONE',  ( 12.19259201841644646, -2.624586292374573748, 12.42169361726068821 ) ) ;
#23477=CARTESIAN_POINT ( 'NONE',  ( 17.65850582825309090, -3.116720375661584441, 13.52313201004804810 ) ) ;
#23491=ORIENTED_EDGE ( 'NONE', *, *, #24138, .T. ) ;
#23497=CARTESIAN_POINT ( 'NONE',  ( 12.19623795424363344, 2.642762699020543504, 13.64211084970869514 ) ) ;
#23501=CARTESIAN_POINT ( 'NONE',  ( 12.27511425286870406, 0.4989076128645561492, 13.99111800451625243 ) ) ;
#23539=EDGE_CURVE ( 'NONE', #64966, #34497, #47581, .T. ) ;
#23546=EDGE_LOOP ( 'NONE', ( #169, #12073, #56895, #4037 ) ) ;
#23548=CARTESIAN_POINT ( 'NONE',  ( 12.32658172867158441, -0.5491314443420151070, -13.98923457196397635 ) ) ;
#23553=CARTESIAN_POINT ( 'NONE',  ( 5.629847151467805233, 12.10477468259546896, -3.742618271631844351 ) ) ;
#23554=ORIENTED_EDGE ( 'NONE', *, *, #60554, .F. ) ;
#23556=CARTESIAN_POINT ( 'NONE',  ( 17.91291100103719458, 1.987489628841895062, -13.76889314140747800 ) ) ;
#23557=ORIENTED_EDGE ( 'NONE', *, *, #22490, .F. ) ;
#23558=DIRECTION ( 'NONE',  ( -0.000000000000000000, -0.000000000000000000, 1.000000000000000000 ) ) ;
#23563=CARTESIAN_POINT ( 'NONE',  ( 17.82907313225565105, 0.5620966109058860294, -12.68325743355609347 ) ) ;
#23569=CARTESIAN_POINT ( 'NONE',  ( 17.55505043854147118, -1.875000000000000000, 13.78631952119024895 ) ) ;
#23574=CARTESIAN_POINT ( 'NONE',  ( 18.23388167758336920, -2.733449996235739032, -12.29993400349665045 ) ) ;
#23581=VECTOR ( 'NONE', #9130, 1000.000000000000000 ) ;
#23588=CARTESIAN_POINT ( 'NONE',  ( 12.08553199184720128, 2.425689856710291803, -13.78827816593211786 ) ) ;
#23591=CARTESIAN_POINT ( 'NONE',  ( 17.55505043854143921, -0.7302158263239079128, 13.98094363220831227 ) ) ;
#23596=CARTESIAN_POINT ( 'NONE',  ( 12.80505043854144276, -0.6250000000000001110, 13.88107975066923316 ) ) ;
#23597=CARTESIAN_POINT ( 'NONE',  ( 12.18203530713735816, -2.449198598491955536, 13.68410320369877731 ) ) ;
#23610=CARTESIAN_POINT ( 'NONE',  ( 18.14710087547454975, 0.2005123242923287363, 12.69787478206144016 ) ) ;
#23618=CARTESIAN_POINT ( 'NONE',  ( 12.37517135966890258, -2.046199321548340500, 13.75929785978298270 ) ) ;
#23626=CARTESIAN_POINT ( 'NONE',  ( 12.08004251007353957, 0.01123479547582826449, -12.60000044989513590 ) ) ;
#23644=CARTESIAN_POINT ( 'NONE',  ( 17.91845017417216113, 0.6323113780857140265, -13.98571806661953154 ) ) ;
#23650=CARTESIAN_POINT ( 'NONE',  ( 18.14127614474869787, -2.717147700817308831, 12.39835379065202225 ) ) ;
#23661=CARTESIAN_POINT ( 'NONE',  ( 5.500000000000000000, -12.87590651766999983, -2.791353855799999728 ) ) ;
#23664=CARTESIAN_POINT ( 'NONE',  ( 12.23548570231569066, -0.2575405707509104136, -13.89679341043304106 ) ) ;
#23665=CARTESIAN_POINT ( 'NONE',  ( 17.78683280784129650, -3.080523647204256754, 12.29718062304645620 ) ) ;
#23673=AXIS2_PLACEMENT_3D ( 'NONE', #50651, #56582, #60793 ) ;
#23685=CARTESIAN_POINT ( 'NONE',  ( 12.80505043854144276, -0.6250000000000001110, -12.67928921589118652 ) ) ;
#23693=CARTESIAN_POINT ( 'NONE',  ( 17.96742813929298421, -0.5917181940048611422, 12.58609996267493081 ) ) ;
#23699=CARTESIAN_POINT ( 'NONE',  ( 17.65134488495969123, 1.793858269351531254, 13.88459860980089644 ) ) ;
#23710=CARTESIAN_POINT ( 'NONE',  ( 17.82352195865856714, -3.196339915866920123, -13.63023968027430755 ) ) ;
#23732=CARTESIAN_POINT ( 'NONE',  ( 12.52605318029421078, 1.940633248599431537, -12.56447441435821943 ) ) ;
#23742=CARTESIAN_POINT ( 'NONE',  ( 12.08117318674012708, -2.436835578774661837, -12.36211850556986214 ) ) ;
#23749=CARTESIAN_POINT ( 'NONE',  ( 12.54503913623225131, -3.068442045733653867, -13.53626685534801588 ) ) ;
#23750=EDGE_CURVE ( 'NONE', #42176, #57880, #12065, .T. ) ;
#23751=CARTESIAN_POINT ( 'NONE',  ( 18.08617525414963723, -0.3300695133819651073, -12.69424233780836531 ) ) ;
#23755=EDGE_CURVE ( 'NONE', #51860, #7219, #23246, .T. ) ;
#23762=CARTESIAN_POINT ( 'NONE',  ( 17.84610786052055076, 3.139226446220193978, 12.20267444563224579 ) ) ;
#23767=ORIENTED_EDGE ( 'NONE', *, *, #42317, .F. ) ;
#23768=CARTESIAN_POINT ( 'NONE',  ( 12.27745450063685162, -2.164896879444428546, 12.52337953207688237 ) ) ;
#23775=CARTESIAN_POINT ( 'NONE',  ( 12.52850951125299872, 0.5605836838512540110, 12.68334204399184273 ) ) ;
#23778=CARTESIAN_POINT ( 'NONE',  ( 12.36723811880910340, 2.053846804184053632, 12.54438404081591862 ) ) ;
#23790=CARTESIAN_POINT ( 'NONE',  ( 17.83819980924002024, -0.5572757172051777674, -12.68354006032887327 ) ) ;
#23793=CARTESIAN_POINT ( 'NONE',  ( 17.71839800377770047, -3.104623491297848314, 13.52646211264960563 ) ) ;
#23796=CARTESIAN_POINT ( 'NONE',  ( 17.63806710036372749, -1.880187906035670764, -13.78549581173514937 ) ) ;
#23797=DIRECTION ( 'NONE',  ( -0.000000000000000000, -0.000000000000000000, 1.000000000000000000 ) ) ;
#23802=B_SPLINE_CURVE_WITH_KNOTS ( 'NONE', 3,
 ( #34401, #29156, #50126, #8504, #29851, #34740, #66881, #60610, #24585, #56402, #7124, #13421, #51159, #40320, #45229, #1887 ),
 .UNSPECIFIED., .F., .F.,
 ( 4, 2, 2, 2, 2, 2, 2, 4 ),
 ( 0.000000000000000000, 0.06250000000000098532, 0.1250000000000019706, 0.2499999999999998890, 0.4999999999999988898, 0.7499999999999977796, 0.8749999999999988898, 1.000000000000000000 ),
 .UNSPECIFIED. ) ;
#23816=CARTESIAN_POINT ( 'NONE',  ( 12.17997668546738410, -2.480562828864417924, 12.45612489593431249 ) ) ;
#23820=CARTESIAN_POINT ( 'NONE',  ( 18.27043923978330753, -2.638421884002154716, 13.74915584829237858 ) ) ;
#23823=ORIENTED_EDGE ( 'NONE', *, *, #39063, .T. ) ;
#23837=ADVANCED_FACE ( 'NONE', ( #22891 ), #1271, .F. ) ;
#23842=AXIS2_PLACEMENT_3D ( 'NONE', #55230, #44753, #49989 ) ;
#23844=CARTESIAN_POINT ( 'NONE',  ( 12.80505043854144276, -0.7302158263239078018, 13.98094363220830871 ) ) ;
#23845=CARTESIAN_POINT ( 'NONE',  ( 12.29504137777687056, 2.138585174375768450, 13.74345269122308721 ) ) ;
#23848=CARTESIAN_POINT ( 'NONE',  ( 12.30788008554897672, 0.3788802689573961824, -12.69239629739823449 ) ) ;
#23849=CARTESIAN_POINT ( 'NONE',  ( 12.50529577747504639, 0.6653129401483712790, 13.98418548573915743 ) ) ;
#23852=CARTESIAN_POINT ( 'NONE',  ( 5.700000000000000178, 13.94845324556000143, 4.312847325879000770 ) ) ;
#23871=VECTOR ( 'NONE', #19810, 1000.000000000000000 ) ;
#23875=DIRECTION ( 'NONE',  ( 1.000000000000000000, 0.000000000000000000, 0.000000000000000000 ) ) ;
#23880=ORIENTED_EDGE ( 'NONE', *, *, #21455, .F. ) ;
#23885=CARTESIAN_POINT ( 'NONE',  ( 17.61541550669253198, 1.763241988052385745, -12.47601615708916434 ) ) ;
#23887=AXIS2_PLACEMENT_3D ( 'NONE', #12679, #61947, #40285 ) ;
#23896=CARTESIAN_POINT ( 'NONE',  ( 12.27511425286869695, -0.4989076128645703045, -13.99111800451625065 ) ) ;
#23902=EDGE_LOOP ( 'NONE', ( #61338, #44865, #51049, #11825 ) ) ;
#23904=CARTESIAN_POINT ( 'NONE',  ( 17.83362577474377986, 1.940423258991959443, -13.77633750067930229 ) ) ;
#23911=CARTESIAN_POINT ( 'NONE',  ( 17.59542495529381512, 0.6250000000000000000, -12.67928922306854211 ) ) ;
#23915=ADVANCED_FACE ( 'NONE', ( #54362 ), #67139, .T. ) ;
#23925=CARTESIAN_POINT ( 'NONE',  ( 18.14725124545929091, -2.065010783240470271, -12.42963489304855251 ) ) ;
#23926=DIRECTION ( 'NONE',  ( -1.000000000000000000, 0.000000000000000000, 0.000000000000000000 ) ) ;
#23933=B_SPLINE_CURVE_WITH_KNOTS ( 'NONE', 1,
 ( #15632, #31718 ),
 .UNSPECIFIED., .F., .F.,
 ( 2, 2 ),
 ( 0.000000000000000000, 1.000000000000000000 ),
 .UNSPECIFIED. ) ;
#23938=CARTESIAN_POINT ( 'NONE',  ( 12.20814394425992866, 2.932476687367332691, -13.68943695263252103 ) ) ;
#23942=CARTESIAN_POINT ( 'NONE',  ( 18.08024975107899124, 0.3389646381316565038, 13.89444110642641661 ) ) ;
#23944=CARTESIAN_POINT ( 'NONE',  ( 18.18005043890192596, -2.480435635901940383, 12.45614914577398835 ) ) ;
#23945=ORIENTED_EDGE ( 'NONE', *, *, #22641, .T. ) ;
#23949=CARTESIAN_POINT ( 'NONE',  ( 12.18135539520747201, -2.541609601506828131, 13.66455050636339230 ) ) ;
#23957=CARTESIAN_POINT ( 'NONE',  ( 12.35923975622791993, 0.5837697427126086192, 13.98798827748084683 ) ) ;
#23959=CARTESIAN_POINT ( 'NONE',  ( 18.12876220047771270, 0.2481623978058146718, 12.69674179789668678 ) ) ;
#23964=CARTESIAN_POINT ( 'NONE',  ( 12.35662541763808697, -3.053258836671836729, -12.22465729756448205 ) ) ;
#23974=CARTESIAN_POINT ( 'NONE',  ( 12.31563516348837872, -0.3888461597108449630, -12.69199065798141568 ) ) ;
#23991=CARTESIAN_POINT ( 'NONE',  ( 17.87656099625190365, 0.6549277419692614011, -13.98467727287827067 ) ) ;
#23992=VERTEX_POINT ( 'NONE', #45268 ) ;
#23997=CARTESIAN_POINT ( 'NONE',  ( 18.16648463839231198, -2.629536980443115013, 12.42046771388698723 ) ) ;
#23999=CARTESIAN_POINT ( 'NONE',  ( 12.80505043854146940, -1.798940460745208636, -12.50936912696000469 ) ) ;
#24000=EDGE_CURVE ( 'NONE', #16502, #12996, #58211, .T. ) ;
#24001=ADVANCED_FACE ( 'NONE', ( #20061 ), #50503, .T. ) ;
#24005=CIRCLE ( 'NONE', #63047, 13.27499874714999883 ) ;
#24013=CARTESIAN_POINT ( 'NONE',  ( 12.30917092924264722, 0.3809766167652363644, -13.89298487834588514 ) ) ;
#24014=CARTESIAN_POINT ( 'NONE',  ( 17.93883077754968625, -2.006280984399066103, 12.55302554764000789 ) ) ;
#24026=ORIENTED_EDGE ( 'NONE', *, *, #23755, .T. ) ;
#24037=CARTESIAN_POINT ( 'NONE',  ( 18.05935420056438190, -0.5168989769797245337, 12.58939571008426839 ) ) ;
#24038=PLANE ( 'NONE',  #48367 ) ;
#24043=CARTESIAN_POINT ( 'NONE',  ( 17.55505043854143565, 1.787797342887043284, 13.88538010501571129 ) ) ;
#24054=FACE_OUTER_BOUND ( 'NONE', #46281, .T. ) ;
#24077=CARTESIAN_POINT ( 'NONE',  ( 12.34709291757827820, 2.925445075551588836, -12.34221984780394088 ) ) ;
#24081=ORIENTED_EDGE ( 'NONE', *, *, #67374, .F. ) ;
#24089=CARTESIAN_POINT ( 'NONE',  ( 12.08628615590300015, -2.575951425301590714, -12.33388065128748146 ) ) ;
#24097=CARTESIAN_POINT ( 'NONE',  ( 17.71747088695469330, -0.6038699852804519930, -12.68066884516331783 ) ) ;
#24102=ORIENTED_EDGE ( 'NONE', *, *, #19396, .F. ) ;
#24104=CARTESIAN_POINT ( 'NONE',  ( 17.63827777591714252, 3.120766739620285612, 13.52195882727199994 ) ) ;
#24107=CARTESIAN_POINT ( 'NONE',  ( 18.04714676118036110, 2.114551447792224703, 12.53305202231724635 ) ) ;
#24112=CARTESIAN_POINT ( 'NONE',  ( 12.55399154093078806, -1.927548249315101492, 12.56670145065455024 ) ) ;
#24118=CARTESIAN_POINT ( 'NONE',  ( 12.18006454708593544, 0.02081145935391313928, 12.69999906470293283 ) ) ;
#24122=CARTESIAN_POINT ( 'NONE',  ( 12.46308409927488903, 1.976751580904479555, 12.55819113744975191 ) ) ;
#24123=VERTEX_POINT ( 'NONE', #48006 ) ;
#24134=CARTESIAN_POINT ( 'NONE',  ( 18.15698397287705035, -0.1703900907606387127, -12.69849596185835239 ) ) ;
#24137=CARTESIAN_POINT ( 'NONE',  ( 18.12893921138742570, -2.747599606323546606, 13.61782120253034023 ) ) ;
#24138=EDGE_CURVE ( 'NONE', #12771, #25486, #30900, .T. ) ;
#24142=LINE ( 'NONE', #50371, #25277 ) ;
#24159=CARTESIAN_POINT ( 'NONE',  ( 17.92010247872368822, -0.6380582629978912568, -13.98550026811524738 ) ) ;
#24161=CARTESIAN_POINT ( 'NONE',  ( 12.20163823188996055, -2.663908709744649883, 12.41191052568941267 ) ) ;
#24165=CARTESIAN_POINT ( 'NONE',  ( 18.07784313215200456, -3.023931901684169699, 13.66952493495815624 ) ) ;
#24168=CARTESIAN_POINT ( 'NONE',  ( 17.55505043854144276, -0.7192913403693006469, 12.57945229203838444 ) ) ;
#24173=B_SPLINE_CURVE_WITH_KNOTS ( 'NONE', 3,
 ( #45652, #40392, #1967, #23290, #44631, #7544, #2307, #47018, #41084, #51907, #24661, #52948, #67636, #3661, #25686, #20100, #26035, #30260, #41426, #19759, #62735, #9599, #40736, #46679, #36522, #31628, #35837, #46334, #52597, #14520, #45983, #62061, #57155, #62401, #41768, #63071, #67295, #30941, #57845, #9251, #30593, #14857, #19412, #14175, #67983, #36179, #52257, #20786, #42117, #4353, #35502, #56823, #68320, #63423, #20441, #9952, #15197, #8923, #31289, #51565, #25001, #4692, #4004, #25341, #47364, #57491, #68669 ),
 .UNSPECIFIED., .F., .F.,
 ( 4, 2, 2, 2, 2, 2, 2, 2, 2, 2, 2, 2, 2, 2, 1, 1, 1, 2, 2, 2, 2, 2, 2, 2, 2, 2, 2, 2, 2, 2, 2, 2, 2, 2, 4 ),
 ( 0.000000000000000000, 0.1250000000000327793, 0.2500000000000655587, 0.3125000000000821010, 0.3437500000000908718, 0.3750000000000996425, 0.4062500000001083578, 0.4218750000001123546, 0.4375000000001163514, 0.4687500000001243450, 0.4843750000001280642, 0.5000000000001317835, 0.5156250000001355582, 0.5312500000001393330, 0.5468750000001431077, 0.5546875000001444400, 0.5585937500001448841, 0.5605468750001451061, 0.5625000000001453282, 0.5781250000001366685, 0.5859375000001322276, 0.5898437500001300071, 0.5937500000001277867, 0.6093750000001217915, 0.6171875000001194600, 0.6250000000001170175, 0.6406250000001136868, 0.6562500000001103562, 0.6718750000001070255, 0.6875000000001036948, 0.7187500000000964784, 0.7343750000000918154, 0.7500000000000870415, 0.8750000000000436318, 1.000000000000000000 ),
 .UNSPECIFIED. ) ;
#24188=CARTESIAN_POINT ( 'NONE',  ( 12.47274432058961047, 1.970265487500628465, 13.77159998682696340 ) ) ;
#24192=CARTESIAN_POINT ( 'NONE',  ( 12.72336162088762457, 0.6199801057749227962, -12.67962184309742923 ) ) ;
#24193=CARTESIAN_POINT ( 'NONE',  ( 12.33502240264713379, -0.4124479947379854905, 13.89177559470776302 ) ) ;
#24202=CARTESIAN_POINT ( 'NONE',  ( 12.32444827497856110, 3.019497106116454610, 12.23286052727262607 ) ) ;
#24220=DIRECTION ( 'NONE',  ( 0.000000000000000000, 0.000000000000000000, 1.000000000000000000 ) ) ;
#24229=CARTESIAN_POINT ( 'NONE',  ( 18.24341944916325886, 2.253723043306036455, -12.39680838072757751 ) ) ;
#24232=CARTESIAN_POINT ( 'NONE',  ( 12.80505043854143388, 3.124999999999999556, -13.52084414783465505 ) ) ;
#24238=CARTESIAN_POINT ( 'NONE',  ( 12.21516724099298834, -0.4251989115648944773, -13.99355557726514476 ) ) ;
#24240=CARTESIAN_POINT ( 'NONE',  ( 18.17227403027940724, -2.399493853283785949, -13.69423063306952670 ) ) ;
#24244=CYLINDRICAL_SURFACE ( 'NONE', #58567, 1.999999999999999556 ) ;
#24247=CARTESIAN_POINT ( 'NONE',  ( 17.55505043854143565, 3.248109929747637015, -13.61799478206225444 ) ) ;
#24254=CARTESIAN_POINT ( 'NONE',  ( 17.75497146383150948, 0.5922552425849882951, -12.68140545289945642 ) ) ;
#24259=CARTESIAN_POINT ( 'NONE',  ( 18.11654246900412701, -2.224740281559051791, 13.72801203774633549 ) ) ;
#24267=CARTESIAN_POINT ( 'NONE',  ( 18.20050923854816816, -2.808308534135717682, -12.28305809155435746 ) ) ;
#24271=CARTESIAN_POINT ( 'NONE',  ( 17.55505043854144276, 0.6250000000000001110, -25.00000000000000000 ) ) ;
#24281=CARTESIAN_POINT ( 'NONE',  ( 12.08020514495812847, 2.544320517268823245, -13.76688091865072749 ) ) ;
#24284=CARTESIAN_POINT ( 'NONE',  ( 18.25531185377811383, 0.1895042076700463041, 13.99872220539657164 ) ) ;
#24290=CARTESIAN_POINT ( 'NONE',  ( 12.63945631780195988, -1.891770379292689874, 13.78384844198601122 ) ) ;
#24297=ORIENTED_EDGE ( 'NONE', *, *, #64210, .F. ) ;
#24311=CONICAL_SURFACE ( 'NONE', #33252, 13.94999927503000059, 0.7853981058017837080 ) ;
#24317=CARTESIAN_POINT ( 'NONE',  ( 12.57154173166082778, 0.6810629908227098239, -12.58158054216573518 ) ) ;
#24318=DIRECTION ( 'NONE',  ( -1.000000000000000000, 0.000000000000000000, -3.663735981262999544E-14 ) ) ;
#24336=CARTESIAN_POINT ( 'NONE',  ( 17.97713831050997513, -0.5938246120522460147, -13.98740230410798091 ) ) ;
#24346=CARTESIAN_POINT ( 'NONE',  ( 12.22437278969013263, -2.731306219322056528, -13.62162349208237089 ) ) ;
#24347=CARTESIAN_POINT ( 'NONE',  ( 5.500000000000000000, -13.17499999999999893, 0.000000000000000000 ) ) ;
#24349=VERTEX_POINT ( 'NONE', #57039 ) ;
#24354=CARTESIAN_POINT ( 'NONE',  ( 18.18005044575085449, -2.500000006795658702, -13.67340643792831401 ) ) ;
#24355=CARTESIAN_POINT ( 'NONE',  ( 12.80505043854144276, 0.7192913403693015351, 12.57945229203838267 ) ) ;
#24357=CARTESIAN_POINT ( 'NONE',  ( 12.19636843800076775, 0.1422577892986776338, -13.89902525486550466 ) ) ;
#24358=CARTESIAN_POINT ( 'NONE',  ( 17.84375123822105991, -1.945578272181329504, 12.56362807389522018 ) ) ;
#24368=FACE_OUTER_BOUND ( 'NONE', #29797, .T. ) ;
#24371=ORIENTED_EDGE ( 'NONE', *, *, #37441, .F. ) ;
#24382=CARTESIAN_POINT ( 'NONE',  ( 17.60275121352128025, -0.7181168112306479667, 12.57951960855070261 ) ) ;
#24384=CARTESIAN_POINT ( 'NONE',  ( 12.80505043854146940, -3.199751711897561801, 12.18694338143115452 ) ) ;
#24390=CARTESIAN_POINT ( 'NONE',  ( 18.24173484165867976, 2.753291453986174808, 13.72661349255300856 ) ) ;
#24399=ORIENTED_EDGE ( 'NONE', *, *, #50518, .F. ) ;
#24401=CARTESIAN_POINT ( 'NONE',  ( 17.65063036598055390, -3.242172222319712471, -13.61940987276824799 ) ) ;
#24419=ADVANCED_FACE ( 'NONE', ( #29 ), #40177, .T. ) ;
#24428=CARTESIAN_POINT ( 'NONE',  ( 12.18529561036834608, 2.583342615503332773, -12.43180850209203392 ) ) ;
#24434=CARTESIAN_POINT ( 'NONE',  ( 17.55505043854143921, -0.7302158263239086899, 13.98094363220831049 ) ) ;
#24436=CARTESIAN_POINT ( 'NONE',  ( 12.21438802940097901, -2.898246740288921153, -12.26216014320957015 ) ) ;
#24442=CARTESIAN_POINT ( 'NONE',  ( 12.24873136391195416, -2.785023419893231988, -13.60881341097601371 ) ) ;
#24443=B_SPLINE_CURVE_WITH_KNOTS ( 'NONE', 3,
 ( #32003, #54690, #64469, #26405, #69046, #16245, #16593, #862, #7481, #60975, #22872, #28834, #18672, #13773, #17986, #28479, #34759, #65863, #35106, #44221, #39305, #49796, #29173, #60628, #45592, #50145, #23224, #40004, #65515, #2250, #6788, #1550, #23563, #44904, #34421, #2926, #24254, #13088, #55735, #17643, #23911, #38967 ),
 .UNSPECIFIED., .F., .F.,
 ( 4, 2, 2, 2, 2, 2, 2, 2, 2, 2, 2, 2, 2, 1, 2, 2, 2, 2, 2, 1, 2, 4 ),
 ( 0.4997863768847486954, 0.5623130797741535680, 0.6248397826635585517, 0.6404714583859092425, 0.6561031341082600443, 0.6873664855529640905, 0.7029981612753175568, 0.7186298369976709122, 0.7264456748588475898, 0.7342615127200242675, 0.7498931884423775118, 0.7811565398870811139, 0.7889723777482554601, 0.7967882156094298063, 0.8124198913317783877, 0.8280515670541268580, 0.8436832427764753284, 0.8749465942211771541, 0.8905782699435280669, 0.9062099456658790908, 0.9374732971105860235, 1.000000000000000000 ),
 .UNSPECIFIED. ) ;
#24446=LINE ( 'NONE', #41548, #43403 ) ;
#24454=CARTESIAN_POINT ( 'NONE',  ( 17.77742128654737286, 1.915804696728241163, 12.56864479336925200 ) ) ;
#24456=DIRECTION ( 'NONE',  ( -1.000000000000000000, 0.000000000000000000, 0.000000000000000000 ) ) ;
#24461=CARTESIAN_POINT ( 'NONE',  ( 12.39767999896657003, -2.025889534879409037, 12.54950459294602894 ) ) ;
#24466=CARTESIAN_POINT ( 'NONE',  ( 12.80505043854144276, 0.6249999999999995559, 12.67928921589117586 ) ) ;
#24470=CARTESIAN_POINT ( 'NONE',  ( 12.80505043854143388, 1.874999999999998890, 12.57541666120756041 ) ) ;
#24478=DIRECTION ( 'NONE',  ( 0.000000000000000000, 0.7270098363383213913, -0.6866270442294909460 ) ) ;
#24481=ORIENTED_EDGE ( 'NONE', *, *, #46838, .T. ) ;
#24489=CARTESIAN_POINT ( 'NONE',  ( 12.80505043854146940, -3.248109929747638347, 13.61799478206225444 ) ) ;
#24490=DIRECTION ( 'NONE',  ( 1.000000000000000000, 0.000000000000000000, 0.000000000000000000 ) ) ;
#24498=CARTESIAN_POINT ( 'NONE',  ( 17.55505043854144276, -0.6250000000000001110, -12.67928921589118474 ) ) ;
#24502=CARTESIAN_POINT ( 'NONE',  ( 12.80505043854144276, 0.6249999999999995559, -12.67928921589118652 ) ) ;
#24504=DIRECTION ( 'NONE',  ( -1.000000000000000000, -0.000000000000000000, -0.000000000000000000 ) ) ;
#24511=CARTESIAN_POINT ( 'NONE',  ( 12.18798377888046502, -2.400256349692730495, 12.47427327512308359 ) ) ;
#24514=CARTESIAN_POINT ( 'NONE',  ( 17.99865897956992811, -3.095937021190230620, 13.65340307249647545 ) ) ;
#24515=CARTESIAN_POINT ( 'NONE',  ( 5.700000000000000178, -12.50865771883999855, 2.924687089724999911 ) ) ;
#24525=CARTESIAN_POINT ( 'NONE',  ( 18.05078025084783278, 0.5250004125410518974, -12.58906021966016020 ) ) ;
#24536=CARTESIAN_POINT ( 'NONE',  ( 12.09815554886058386, 2.355526959511344387, 13.80042145504355311 ) ) ;
#24540=CARTESIAN_POINT ( 'NONE',  ( 12.57406965109622909, 0.5808252089534533535, -12.68211610571899861 ) ) ;
#24541=CARTESIAN_POINT ( 'NONE',  ( 12.08472014176158282, -0.08359636179364632325, 13.99975542440154186 ) ) ;
#24549=B_SPLINE_SURFACE_WITH_KNOTS ( 'NONE', 1, 3, ( 
 ( #48319, #424, #16500, #37827, #23477, #6004, #59839, #44127, #27344, #11946, #1809, #66119, #1118, #11590, #17897, #49011, #18239, #48666, #22431, #54245, #7050, #43773, #49700, #771, #32590, #65067, #6347, #59148, #12646, #49347, #60540, #12300, #23129, #28039, #60196, #38518, #33284, #17187, #27695, #54948, #33633, #54600, #6698, #33976, #1462, #22777, #65425, #17547, #32934, #28386, #38874, #39214, #11252, #65771, #7392, #44479, #55297, #28738, #50054, #2161, #44816, #53904, #22086, #43431, #64725, #16841, #38163, #59493, #45157, #35016, #13347, #55986, #34672, #29781, #8091, #19260, #29435, #40250, #45501, #3857, #67147, #56330, #66814, #61231, #40588, #46183, #18585, #14375, #61913, #40932 ),
 ( #35355, #56677, #8777, #3186, #13000, #50741, #30119, #51761, #13686, #29085, #51422, #8434, #3517, #67492, #2838, #25192, #55645, #61571, #24514, #7745, #51084, #24855, #46526, #24165, #18925, #19611, #45835, #67834, #50395, #14029, #62254, #35694, #57010, #9110, #2495, #34326, #30448, #39560, #60884, #23820, #66463, #39913, #42321, #31823, #58045, #20985, #68516, #63271, #25883, #36372, #15738, #63622, #47212, #57687, #43609, #20637, #54084, #19955, #9797, #68864, #47562, #48850, #10147, #41963, #41279, #68174, #15401, #49187, #11776, #62587, #33118, #14709, #37066, #957, #31477, #52799, #41618, #36026, #4543, #58378, #31147, #52448, #62926, #10485, #36726, #22268, #27879, #27522, #38351, #4892 ) ),
 .UNSPECIFIED., .F., .F., .F.,
 ( 2, 2 ),
 ( 4, 2, 2, 2, 2, 2, 2, 2, 2, 2, 2, 2, 2, 2, 2, 2, 2, 2, 2, 2, 2, 2, 2, 2, 2, 2, 2, 2, 2, 2, 2, 2, 2, 2, 2, 2, 2, 2, 2, 2, 2, 2, 2, 2, 4 ),
 ( 0.000000000000000000, 1.000000000000000000 ),
 ( 0.000000000000000000, 7.142752612018008851E-05, 0.0001428550522403601770, 0.0002142825783605402791, 0.0002857101044807203540, 0.0003214238675408103915, 0.0003571376306009004832, 0.0003928513936609905207, 0.0004285651567210805582, 0.0004999926828412606331, 0.0005357064459013507248, 0.0005714202089614407081, 0.0006071339720215306913, 0.0006428477350816207830, 0.0007142752612018009664, 0.0007857027873219810414, 0.0008214165503820710246, 0.0008571303134421611163, 0.0009285578395623411913, 0.0009999853656825212662, 0.001071412891802701450, 0.001142840417922881416, 0.001214267944043061383, 0.001285695470163241566, 0.001321409233223331658, 0.001357122996283421749, 0.001428550522403601933, 0.001499978048523782116, 0.001535691811583872208, 0.001571405574643962083, 0.001607119337704051958, 0.001642833100764142049, 0.001714260626884322233, 0.001749974389944412324, 0.001785688153004502416, 0.001821401916064592508, 0.001857115679124682383, 0.001928543205244862349, 0.001964256968304952441, 0.001999970731365042532, 0.002035684494425132624, 0.002071398257485222716, 0.002142825783605402899, 0.002214253309725583083, 0.002285680835845762832 ),
 .UNSPECIFIED. ) ;
#24555=DIRECTION ( 'NONE',  ( 0.000000000000000000, -1.000000000000000000, 0.000000000000000000 ) ) ;
#24569=B_SPLINE_CURVE_WITH_KNOTS ( 'NONE', 3,
 ( #5718, #42106, #63411, #58866, #9586, #21798, #21121, #26370, #68656, #138, #63755, #20774, #9938, #37535, #48374, #15535, #15867, #57830, #64097, #36509, #32311, #31615, #16558, #16212, #31275, #10972, #53621, #36859, #43132, #37199, #58518, #27061, #25675, #30931, #52586, #4680, #10621, #5031, #31964, #58179, #64436, #53280, #10281, #26021, #483, #52241, #47697 ),
 .UNSPECIFIED., .F., .F.,
 ( 4, 2, 2, 2, 2, 2, 2, 2, 1, 2, 2, 2, 2, 2, 2, 1, 2, 2, 1, 2, 2, 2, 2, 2, 4 ),
 ( 0.4985961975200040586, 0.5299339351750088634, 0.5456028040025113768, 0.5612716728300137792, 0.5691061072437652024, 0.5769405416575167367, 0.5926094104850196942, 0.6004438448987712285, 0.6082782793125226517, 0.6239471481400227226, 0.6396160169675227936, 0.6552848857950228645, 0.6709537546225230464, 0.6866226234500231174, 0.7022914922775231883, 0.7179603611050232592, 0.7492980987600234011, 0.7649669675875218067, 0.7806358364150202123, 0.8119735740700166904, 0.8433113117250129465, 0.8746490493800094246, 0.9059867870350057917, 0.9373245246900021588, 1.000000000000000000 ),
 .UNSPECIFIED. ) ;
#24571=FACE_OUTER_BOUND ( 'NONE', #26464, .T. ) ;
#24573=VERTEX_POINT ( 'NONE', #14232 ) ;
#24578=CARTESIAN_POINT ( 'NONE',  ( 18.27887336143457375, 2.529852868668377663, -12.34343546511471246 ) ) ;
#24581=CARTESIAN_POINT ( 'NONE',  ( 12.18033707851134650, 2.521449564491300421, -13.66889060753329055 ) ) ;
#24585=CARTESIAN_POINT ( 'NONE',  ( 18.28051081950323820, 2.330210462401051785, -13.80606256597729775 ) ) ;
#24586=CARTESIAN_POINT ( 'NONE',  ( 12.30074708396108285, 0.5247499651446917435, -13.99016470477802443 ) ) ;
#24589=CARTESIAN_POINT ( 'NONE',  ( 18.14737500097629663, -2.299536442346259424, -13.71390152310622845 ) ) ;
#24590=CARTESIAN_POINT ( 'NONE',  ( 18.18000379063191474, 2.491959044446622862, 12.45343158198893008 ) ) ;
#24597=CARTESIAN_POINT ( 'NONE',  ( 18.08598429698832888, 3.015255620044098084, -13.67144160714441803 ) ) ;
#24608=CARTESIAN_POINT ( 'NONE',  ( 5.699999545467999695, 12.03770622561999915, -3.722046322334000124 ) ) ;
#24615=CARTESIAN_POINT ( 'NONE',  ( 17.76275439675993084, -1.910499210220269362, -12.56953514877129763 ) ) ;
#24628=CARTESIAN_POINT ( 'NONE',  ( 12.47175297079831147, 3.166474622353412816, -13.63720910406327036 ) ) ;
#24631=CARTESIAN_POINT ( 'NONE',  ( 18.16428164030674708, 0.3960277493246572855, 13.99440111282555499 ) ) ;
#24647=CARTESIAN_POINT ( 'NONE',  ( 12.08019303639033737, -0.1916560649207423583, 13.99999316327168941 ) ) ;
#24660=CARTESIAN_POINT ( 'NONE',  ( 12.30913258640365804, 0.5248261352964559423, -12.58906749861124119 ) ) ;
#24661=CARTESIAN_POINT ( 'NONE',  ( 12.23322259331983197, -2.246983130391676298, -12.50693187469075163 ) ) ;
#24662=EDGE_CURVE ( 'NONE', #62522, #67932, #39598, .T. ) ;
#24670=CARTESIAN_POINT ( 'NONE',  ( 17.93438960674995997, 0.4968201168833306092, 12.68691926186746599 ) ) ;
#24681=CARTESIAN_POINT ( 'NONE',  ( 18.20553441509224868, 0.3226776716457254168, -13.99628514671255886 ) ) ;
#24682=ORIENTED_EDGE ( 'NONE', *, *, #50915, .T. ) ;
#24686=FACE_OUTER_BOUND ( 'NONE', #29548, .T. ) ;
#24688=CARTESIAN_POINT ( 'NONE',  ( 18.03251246676483888, -2.904216811341680415, 12.34819510225881523 ) ) ;
#24691=CARTESIAN_POINT ( 'NONE',  ( 12.22105292107917762, -2.722876829297403489, -13.62360956001007573 ) ) ;
#24696=CARTESIAN_POINT ( 'NONE',  ( 17.93438719463079423, 0.4968219663173571443, -13.88804946349586977 ) ) ;
#24701=CARTESIAN_POINT ( 'NONE',  ( 12.18127378141864980, -0.04040202251154306756, -13.89992604541789589 ) ) ;
#24703=CARTESIAN_POINT ( 'NONE',  ( 18.12629019086307025, -2.246197018143532009, 12.50711533121134522 ) ) ;
#24713=LINE ( 'NONE', #46037, #13846 ) ;
#24722=CARTESIAN_POINT ( 'NONE',  ( 12.80505043854143388, 3.248109929747637015, -13.61799478206225444 ) ) ;
#24724=CARTESIAN_POINT ( 'NONE',  ( 5.500000000000000000, 0.000000000000000000, 0.000000000000000000 ) ) ;
#24726=CARTESIAN_POINT ( 'NONE',  ( 17.97714073376501531, -0.5849390254007678092, 12.58641711472857594 ) ) ;
#24744=CARTESIAN_POINT ( 'NONE',  ( 17.57920672810400831, -3.248146558128260697, -13.61798601073640747 ) ) ;
#24766=CARTESIAN_POINT ( 'NONE',  ( 12.33348197901552901, 2.910306952023486549, -12.34646687328217141 ) ) ;
#24771=AXIS2_PLACEMENT_3D ( 'NONE', #12376, #33362, #34405 ) ;
#24775=CARTESIAN_POINT ( 'NONE',  ( 12.15765997487498140, -2.156065442695497048, -12.41416509552196956 ) ) ;
#24781=CARTESIAN_POINT ( 'NONE',  ( 12.24262961005306849, -2.226644062380152445, -13.72761226533214618 ) ) ;
#24792=CARTESIAN_POINT ( 'NONE',  ( 17.55505043854143565, 3.125000000000000000, 13.52078605991414939 ) ) ;
#24795=CARTESIAN_POINT ( 'NONE',  ( 17.83408408707288473, 3.059349868707512687, 12.30347716376230416 ) ) ;
#24800=VERTEX_POINT ( 'NONE', #44166 ) ;
#24801=CARTESIAN_POINT ( 'NONE',  ( 12.28874679351410215, -2.147634260983757315, 12.52674262693622609 ) ) ;
#24810=CARTESIAN_POINT ( 'NONE',  ( 12.66323998097240278, 0.6090396975623076914, 12.68033511803395363 ) ) ;
#24813=CARTESIAN_POINT ( 'NONE',  ( 12.57288091590946166, 1.919630123611446360, 12.56800073041603483 ) ) ;
#24814=ORIENTED_EDGE ( 'NONE', *, *, #36528, .F. ) ;
#24823=AXIS2_PLACEMENT_3D ( 'NONE', #38856, #64706, #27674 ) ;
#24831=CYLINDRICAL_SURFACE ( 'NONE', #67680, 12.59999999999999964 ) ;
#24838=CARTESIAN_POINT ( 'NONE',  ( 18.12577783848187352, 2.244501219363363997, -13.72435250368102366 ) ) ;
#24852=CARTESIAN_POINT ( 'NONE',  ( 12.30233513030085035, -2.119611855452840032, 12.53231127769699782 ) ) ;
#24855=CARTESIAN_POINT ( 'NONE',  ( 18.05244152647599165, -3.049274110449837760, 13.66389386579125897 ) ) ;
#24866=CARTESIAN_POINT ( 'NONE',  ( 18.10028187597348293, 0.4746736627229694583, -12.59106879393900513 ) ) ;
#24871=ADVANCED_FACE ( 'NONE', ( #62623 ), #67873, .F. ) ;
#24872=ORIENTED_EDGE ( 'NONE', *, *, #56578, .T. ) ;
#24878=CARTESIAN_POINT ( 'NONE',  ( 12.27297424062789588, 2.021448577728815366, 13.85330429709570943 ) ) ;
#24881=CARTESIAN_POINT ( 'NONE',  ( 12.18504239630149577, -0.08143391448655303011, -12.69966978411006053 ) ) ;
#24882=CARTESIAN_POINT ( 'NONE',  ( 12.80505043854144276, -0.7302158263239079128, 13.98094363220831049 ) ) ;
#24883=ORIENTED_EDGE ( 'NONE', *, *, #62314, .T. ) ;
#24885=CARTESIAN_POINT ( 'NONE',  ( 12.80505043854144276, -0.6250000000000001110, 12.67928921589117586 ) ) ;
#24896=LINE ( 'NONE', #4246, #9040 ) ;
#24900=CARTESIAN_POINT ( 'NONE',  ( 12.19038559396453003, 2.613250548423018405, 12.42445786899044791 ) ) ;
#24903=DIRECTION ( 'NONE',  ( 0.000000000000000000, -0.7198977633595244896, -0.6940801180771238865 ) ) ;
#24907=LINE ( 'NONE', #40989, #41037 ) ;
#24908=FACE_OUTER_BOUND ( 'NONE', #37571, .T. ) ;
#24916=CARTESIAN_POINT ( 'NONE',  ( 17.98134286629677092, 1.897806848213327457, -12.45626380386397791 ) ) ;
#24921=CARTESIAN_POINT ( 'NONE',  ( 12.19034750719933236, 2.613044105544683582, -13.64883414298571296 ) ) ;
#24925=CARTESIAN_POINT ( 'NONE',  ( 12.11831821888144844, 0.2353130933619010101, -13.99804086085458898 ) ) ;
#24927=CARTESIAN_POINT ( 'NONE',  ( 12.80505043854144276, -0.6250000000000001110, -25.00000000000000000 ) ) ;
#24928=CARTESIAN_POINT ( 'NONE',  ( 18.14750831224828431, 2.299919532987898751, 12.49594326304257486 ) ) ;
#24934=CARTESIAN_POINT ( 'NONE',  ( 18.14661026972999736, 2.095745652224534794, -13.84225217829565580 ) ) ;
#24954=CARTESIAN_POINT ( 'NONE',  ( 17.74302412089502567, -1.903914349118853488, -12.57063651914289792 ) ) ;
#24964=CARTESIAN_POINT ( 'NONE',  ( 12.17655141950252329, 2.882034090924098457, -13.70014555608276119 ) ) ;
#24967=CARTESIAN_POINT ( 'NONE',  ( 18.27863135987957222, -0.04720351400548002813, 13.99992551180917388 ) ) ;
#24973=DIRECTION ( 'NONE',  ( 0.000000000000000000, 0.000000000000000000, 1.000000000000000000 ) ) ;
#24974=CARTESIAN_POINT ( 'NONE',  ( 12.18026105735682663, -2.480641341388361454, 13.67754910898214149 ) ) ;
#25000=CARTESIAN_POINT ( 'NONE',  ( 12.72331806630340978, -0.6199686954221036439, -12.67962180225518942 ) ) ;
#25001=CARTESIAN_POINT ( 'NONE',  ( 12.34829947333263256, -2.926730327383867181, -12.34183739588157458 ) ) ;
#25019=CARTESIAN_POINT ( 'NONE',  ( 18.24178265820144773, -0.2353130933619061449, -13.99804086085459254 ) ) ;
#25029=CARTESIAN_POINT ( 'NONE',  ( 12.21057441424792422, -2.692955410772802871, -13.63058632108330137 ) ) ;
#25040=CARTESIAN_POINT ( 'NONE',  ( 12.29698918160474186, 0.3645810575750328963, -13.89357890581303501 ) ) ;
#25041=CARTESIAN_POINT ( 'NONE',  ( 18.14999129509867259, -2.691763112583330564, 12.40484894414121975 ) ) ;
#25051=CARTESIAN_POINT ( 'NONE',  ( 17.55505043854147118, -3.125000000000000000, 12.28374638332999780 ) ) ;
#25064=CARTESIAN_POINT ( 'NONE',  ( 17.94855945389787166, 0.6042324041877016327, 12.58550538354983672 ) ) ;
#25076=AXIS2_PLACEMENT_3D ( 'NONE', #50146, #60629, #12044 ) ;
#25080=EDGE_CURVE ( 'NONE', #48333, #12771, #21730, .T. ) ;
#25082=DIRECTION ( 'NONE',  ( 0.000000000000000000, 1.000000000000000000, 0.000000000000000000 ) ) ;
#25098=ORIENTED_EDGE ( 'NONE', *, *, #67246, .F. ) ;
#25105=CARTESIAN_POINT ( 'NONE',  ( 12.29572644340311349, 2.862796356722883573, -12.35963739789472804 ) ) ;
#25110=DIRECTION ( 'NONE',  ( 0.000000000000000000, 1.000000000000000000, 2.114232622412000242E-14 ) ) ;
#25115=CARTESIAN_POINT ( 'NONE',  ( 12.54493252275451454, -3.068391087487185587, -12.30078773432380324 ) ) ;
#25122=CARTESIAN_POINT ( 'NONE',  ( 12.78422741110794192, -1.875000586273901870, -13.78627160872173185 ) ) ;
#25130=CARTESIAN_POINT ( 'NONE',  ( 18.15005478418062523, 2.691381137403321855, 13.63095209219456905 ) ) ;
#25134=CARTESIAN_POINT ( 'NONE',  ( 18.17892392841393345, 2.542707335428990412, 12.44153274845740142 ) ) ;
#25147=CARTESIAN_POINT ( 'NONE',  ( 12.18107318252211435, 0.04114048977874578544, 12.69993211551498469 ) ) ;
#25156=CARTESIAN_POINT ( 'NONE',  ( 17.87051611373833637, 1.960066664249855206, 13.77321273358846021 ) ) ;
#25161=B_SPLINE_CURVE_WITH_KNOTS ( 'NONE', 3,
 ( #26935, #15753, #48248, #46881, #68188, #36385, #4560, #25898, #37080, #5256, #47227, #57355, #20652, #354, #21669, #42664, #41978, #64311, #47915, #36039, #15413, #36739, #9459, #12, #10162, #26248, #47575, #58393, #25555, #43363, #17115, #5935, #38449, #6633, #49980, #6277, #28308, #33213, #64663, #48600, #60470, #59772, #33558, #54879, #32866, #1392, #60126, #54533, #43705, #44406, #16767, #22708, #2093, #27971, #49282, #22366, #38099, #44052, #59424, #23412, #49631, #6981, #11522, #65357, #65000, #44748, #17476, #59084, #27278 ),
 .UNSPECIFIED., .F., .F.,
 ( 4, 2, 2, 2, 2, 2, 2, 2, 2, 2, 2, 2, 2, 1, 2, 2, 2, 1, 2, 2, 2, 2, 1, 2, 2, 2, 2, 2, 2, 2, 2, 2, 2, 2, 2, 4 ),
 ( 0.000000000000000000, 0.06249999999997735145, 0.1249999999999547029, 0.1562499999999433786, 0.1874999999999320544, 0.2187499999999207301, 0.2343749999999142908, 0.2499999999999078515, 0.2812499999998929745, 0.2968749999998860356, 0.3124999999998790967, 0.3281249999998721578, 0.3437499999998652189, 0.3593749999998582800, 0.3671874999998542277, 0.3749999999998501754, 0.3906249999998412936, 0.3984374999998368527, 0.4023437499998346878, 0.4062499999998324673, 0.4218749999998229749, 0.4296874999998182010, 0.4335937499998163136, 0.4355468749998162026, 0.4374999999998160916, 0.4531249999998210876, 0.4687499999998260836, 0.4843749999998310796, 0.4999999999998361311, 0.5312499999998461231, 0.5468749999998507860, 0.5624999999998554490, 0.5937499999998658851, 0.6249999999998763212, 0.7499999999999168443, 1.000000000000000000 ),
 .UNSPECIFIED. ) ;
#25163=CARTESIAN_POINT ( 'NONE',  ( 17.71610594244102188, -0.6042361944557627096, -12.68064620454363478 ) ) ;
#25168=CARTESIAN_POINT ( 'NONE',  ( 17.81540764135920440, -1.931433452195108869, -13.77768866547343407 ) ) ;
#25178=CARTESIAN_POINT ( 'NONE',  ( 18.17180742357672685, -0.1030366931642786449, 13.89950396794448473 ) ) ;
#25189=CARTESIAN_POINT ( 'NONE',  ( 12.19537138483621064, -2.360847786584734820, 12.48294616049498629 ) ) ;
#25192=CARTESIAN_POINT ( 'NONE',  ( 17.94045008455787382, -3.136494811772694735, 13.64413575143460911 ) ) ;
#25193=CARTESIAN_POINT ( 'NONE',  ( 17.63932472559542930, 3.120604413325762216, -13.52206336586467295 ) ) ;
#25198=ORIENTED_EDGE ( 'NONE', *, *, #36528, .T. ) ;
#25199=SURFACE_STYLE_USAGE ( .BOTH. , #30794 ) ;
#25205=CARTESIAN_POINT ( 'NONE',  ( 18.13005353941771958, 0.4382646521645942594, -12.59237917444261434 ) ) ;
#25216=CARTESIAN_POINT ( 'NONE',  ( 12.32410271629023057, 1.971482746313077516, 13.86049503924169279 ) ) ;
#25218=ORIENTED_EDGE ( 'NONE', *, *, #9133, .F. ) ;
#25220=CARTESIAN_POINT ( 'NONE',  ( 12.50368198879321824, 0.5476376383131742465, -12.68410501634012988 ) ) ;
#25221=B_SPLINE_CURVE_WITH_KNOTS ( 'NONE', 3,
 ( #58213, #21156, #58551, #5418 ),
 .UNSPECIFIED., .F., .F.,
 ( 4, 4 ),
 ( 0.000000000000000000, 1.000000000000000000 ),
 .UNSPECIFIED. ) ;
#25222=CARTESIAN_POINT ( 'NONE',  ( 12.57207325926688846, -0.6915911779535657278, 13.98290807251246726 ) ) ;
#25226=CARTESIAN_POINT ( 'NONE',  ( 12.80505043854143388, 3.248109929747637015, -13.61799478206225444 ) ) ;
#25233=CARTESIAN_POINT ( 'NONE',  ( 12.14231515301101005, 2.188169521966901954, 12.40854677421460472 ) ) ;
#25237=CARTESIAN_POINT ( 'NONE',  ( 12.80505043854144276, 0.6564304467897706941, -12.64601024127358286 ) ) ;
#25240=CARTESIAN_POINT ( 'NONE',  ( 12.20324964191634898, 2.330992520694229686, 12.48933099340106700 ) ) ;
#25248=CARTESIAN_POINT ( 'NONE',  ( 12.72203378256782358, -1.880187905311242691, 13.78554362285501789 ) ) ;
#25252=EDGE_CURVE ( 'NONE', #64156, #21338, #10668, .T. ) ;
#25259=CARTESIAN_POINT ( 'NONE',  ( 17.82442946238793624, 1.812220263014552746, -12.46899672597967346 ) ) ;
#25262=CARTESIAN_POINT ( 'NONE',  ( 18.08152692720025101, 2.836954189442855601, 12.36664858736386741 ) ) ;
#25263=CARTESIAN_POINT ( 'NONE',  ( 12.18233509006103610, 2.554099910133862394, -13.66183974826738279 ) ) ;
#25267=CARTESIAN_POINT ( 'NONE',  ( 12.64055492385137391, 0.7115697451012049646, -13.98190580764195978 ) ) ;
#25271=B_SPLINE_CURVE_WITH_KNOTS ( 'NONE', 3,
 ( #44309, #34154, #18417, #18072, #39389, #65605, #55125, #13523, #28565, #23997, #49880, #1990, #23312, #12828, #28922, #50227, #23650, #39742, #35186, #62760, #56499, #25710, #61738, #31310, #40415, #47042, #9622, #13858, #57179, #24688, #66980, #67658, #52622, #19092, #63096, #8604, #51931, #4715, #45675, #35863, #29953, #3686, #30968, #41110, #51257, #8946, #9274 ),
 .UNSPECIFIED., .F., .F.,
 ( 4, 2, 2, 2, 2, 2, 2, 2, 1, 2, 2, 2, 2, 2, 2, 1, 2, 2, 1, 2, 2, 2, 2, 2, 4 ),
 ( 0.4985961975199688090, 0.5299339351749688953, 0.5456028040024686332, 0.5612716728299683711, 0.5691061072437181290, 0.5769405416574677758, 0.5926094104849677358, 0.6004438448987177157, 0.6082782793124676957, 0.6239471481399688768, 0.6396160169674700580, 0.6552848857949711281, 0.6709537546224723092, 0.6866226234499734904, 0.7022914922774745605, 0.7179603611049757417, 0.7492980987599813236, 0.7649669675874821717, 0.7806358364149829088, 0.8119735740699847160, 0.8433113117249863011, 0.8746490493799881083, 0.9059867870349896934, 0.9373245246899915006, 1.000000000000000000 ),
 .UNSPECIFIED. ) ;
#25277=VECTOR ( 'NONE', #24490, 1000.000000000000000 ) ;
#25279=CARTESIAN_POINT ( 'NONE',  ( 18.05353730554811520, 1.987694103345767127, -13.85817950142402033 ) ) ;
#25297=CARTESIAN_POINT ( 'NONE',  ( 17.60340893540761797, -3.198498114537105419, -12.18727270072288604 ) ) ;
#25305=CARTESIAN_POINT ( 'NONE',  ( 12.70947385406807406, 3.242135136469467049, -13.61941870117945541 ) ) ;
#25306=FACE_OUTER_BOUND ( 'NONE', #30142, .T. ) ;
#25340=CARTESIAN_POINT ( 'NONE',  ( 12.34869027095183469, -0.4275228316712924581, -12.69032453495386648 ) ) ;
#25341=CARTESIAN_POINT ( 'NONE',  ( 12.48631554272197874, -3.044136704961547757, -12.30804282041571085 ) ) ;
#25345=EDGE_LOOP ( 'NONE', ( #15416, #22343, #44528, #27084 ) ) ;
#25359=CARTESIAN_POINT ( 'NONE',  ( 17.55505043854144276, -0.7302158263239267866, -13.98094363220830871 ) ) ;
#25362=DIRECTION ( 'NONE',  ( 0.000000000000000000, 0.000000000000000000, 1.000000000000000000 ) ) ;
#25369=CARTESIAN_POINT ( 'NONE',  ( 12.63953418767025205, -1.875000000000001110, -13.78627077332612316 ) ) ;
#25381=CARTESIAN_POINT ( 'NONE',  ( 12.35432851685904332, 2.933105360581561349, 13.57195094675647873 ) ) ;
#25382=CARTESIAN_POINT ( 'NONE',  ( 17.80628805164909423, -1.927626392034356595, 12.56668820897845507 ) ) ;
#25383=ORIENTED_EDGE ( 'NONE', *, *, #13666, .F. ) ;
#25393=ADVANCED_FACE ( 'NONE', ( #55013 ), #24311, .T. ) ;
#25400=CARTESIAN_POINT ( 'NONE',  ( 17.55505043854143565, 1.875000000000000000, -25.00000000000000000 ) ) ;
#25402=CARTESIAN_POINT ( 'NONE',  ( 12.15512143692708946, 2.141660958113119850, -13.83591020988682807 ) ) ;
#25404=VECTOR ( 'NONE', #26390, 1000.000000000000000 ) ;
#25409=CARTESIAN_POINT ( 'NONE',  ( 17.77734287254348189, 0.6847469513499552241, 12.58138041838080667 ) ) ;
#25416=CARTESIAN_POINT ( 'NONE',  ( 17.91962727382262344, 3.149549635603924091, 13.64113161598088197 ) ) ;
#25447=CARTESIAN_POINT ( 'NONE',  ( 12.18088753964548410, 2.461875156572521650, -12.46041398465086480 ) ) ;
#25451=ORIENTED_EDGE ( 'NONE', *, *, #14154, .T. ) ;
#25453=CARTESIAN_POINT ( 'NONE',  ( 17.92003806251651099, -0.6285461057673430441, 12.58436427553280268 ) ) ;
#25456=CARTESIAN_POINT ( 'NONE',  ( 12.30801118402051841, -2.879457308712141117, -12.35502813289141599 ) ) ;
#25462=CARTESIAN_POINT ( 'NONE',  ( 12.41963733656425006, -3.136527823945748583, -13.64412816271520157 ) ) ;
#25473=CARTESIAN_POINT ( 'NONE',  ( 18.13614788748274620, 2.730255577391087929, 13.62187136670912047 ) ) ;
#25476=CARTESIAN_POINT ( 'NONE',  ( 17.98409414022578545, 2.954502725563342480, 12.33397020297173441 ) ) ;
#25486=VERTEX_POINT ( 'NONE', #20358 ) ;
#25487=CARTESIAN_POINT ( 'NONE',  ( 12.64121575286209698, -3.103492734220866023, 12.29027329182862616 ) ) ;
#25494=CARTESIAN_POINT ( 'NONE',  ( 12.29653175235435825, -0.3639343692979916112, 12.69299665021503998 ) ) ;
#25513=CARTESIAN_POINT ( 'NONE',  ( 18.16777246618443442, -2.623276685093039795, 13.64654026452092062 ) ) ;
#25517=CARTESIAN_POINT ( 'NONE',  ( 17.83329178774387813, -3.059742244759365182, -13.53861815793072054 ) ) ;
#25554=CARTESIAN_POINT ( 'NONE',  ( 18.15103067362390377, 0.4097539338085404714, -12.59333942654355809 ) ) ;
#25555=CARTESIAN_POINT ( 'NONE',  ( 12.23173037681283759, 2.748912840245765654, -12.39010626689092831 ) ) ;
#25564=CARTESIAN_POINT ( 'NONE',  ( 17.95101261602633613, 1.877525629946211971, 12.45933154191684444 ) ) ;
#25565=CARTESIAN_POINT ( 'NONE',  ( 12.27409806343526100, 3.015283977741789023, 13.67143535301651447 ) ) ;
#25569=CARTESIAN_POINT ( 'NONE',  ( 12.60523857536293413, -0.5937411427281895637, -12.68132466675194436 ) ) ;
#25571=CARTESIAN_POINT ( 'NONE',  ( 12.10797096423121566, -0.2010519787742775510, 13.99856097495847607 ) ) ;
#25582=CARTESIAN_POINT ( 'NONE',  ( 12.13758509790269535, 2.198972988417282615, 12.40663693328272466 ) ) ;
#25585=DIRECTION ( 'NONE',  ( -0.000000000000000000, -0.000000000000000000, 1.000000000000000000 ) ) ;
#25592=ORIENTED_EDGE ( 'NONE', *, *, #37783, .T. ) ;
#25594=CARTESIAN_POINT ( 'NONE',  ( 12.54851516855890381, -0.5702235047293728876, 12.68276536598237136 ) ) ;
#25600=CARTESIAN_POINT ( 'NONE',  ( 12.34612353109750771, -2.075598726024750817, 13.75436385846647624 ) ) ;
#25601=CARTESIAN_POINT ( 'NONE',  ( 12.19790361218675123, 2.648659041011996784, 13.64075350830020561 ) ) ;
#25608=CARTESIAN_POINT ( 'NONE',  ( 18.17062868725393088, 2.391413364859044322, -12.47623124499065383 ) ) ;
#25610=CARTESIAN_POINT ( 'NONE',  ( 18.12474152634368707, 2.757110843030302849, 12.38793583425497147 ) ) ;
#25611=CARTESIAN_POINT ( 'NONE',  ( 12.34854013679137275, 2.926988005533238013, -13.57357535316153019 ) ) ;
#25625=CARTESIAN_POINT ( 'NONE',  ( 17.99906018690869658, 1.940665501735318932, -13.86484298168864093 ) ) ;
#25633=CARTESIAN_POINT ( 'NONE',  ( 21.59999953993000332, -1.509903313490000218E-14, 12.84999890301438796 ) ) ;
#25642=CARTESIAN_POINT ( 'NONE',  ( 17.57925770490775008, -3.199697828486423479, -12.18695748817155078 ) ) ;
#25648=ORIENTED_EDGE ( 'NONE', *, *, #7227, .T. ) ;
#25651=DIRECTION ( 'NONE',  ( 1.000000000000000000, 0.000000000000000000, 0.000000000000000000 ) ) ;
#25652=CARTESIAN_POINT ( 'NONE',  ( 12.78089499409913721, 3.248109241121360125, -13.61799491149521302 ) ) ;
#25653=CARTESIAN_POINT ( 'NONE',  ( 18.13027066859324421, 0.4451122480341191956, 13.99293440828418866 ) ) ;
#25675=CARTESIAN_POINT ( 'NONE',  ( 17.98439275848187435, 2.954313498893424317, -12.33404747595914053 ) ) ;
#25681=CARTESIAN_POINT ( 'NONE',  ( 17.65333285638452310, 3.199628934752181131, 12.18697561682395936 ) ) ;
#25684=CARTESIAN_POINT ( 'NONE',  ( 12.46581852961811521, 0.5250240499537035532, -12.68539034781189301 ) ) ;
#25686=CARTESIAN_POINT ( 'NONE',  ( 12.20055951530588345, -2.340869620859903577, -12.48721223319660290 ) ) ;
#25698=EDGE_LOOP ( 'NONE', ( #41281, #51637, #21310, #36627, #62907, #3117, #17454, #28511, #20265, #16728 ) ) ;
#25701=CARTESIAN_POINT ( 'NONE',  ( 17.55505043854147118, -1.760845406083394682, 12.47635457398814829 ) ) ;
#25710=CARTESIAN_POINT ( 'NONE',  ( 18.11183118189959274, -2.784086580389351973, 12.38085211673737085 ) ) ;
#25713=CARTESIAN_POINT ( 'NONE',  ( 12.18106278541768894, -2.459077072136087505, -13.68201856772773972 ) ) ;
#25743=CARTESIAN_POINT ( 'NONE',  ( 18.03457755489743519, 0.4008875276915725983, 13.89221989487217002 ) ) ;
#25752=CARTESIAN_POINT ( 'NONE',  ( 12.61470515272479531, 1.811791595463774662, -13.88227300399932673 ) ) ;
#25755=CARTESIAN_POINT ( 'NONE',  ( 12.80505043854146940, -3.125000000000000000, 12.28374638332999780 ) ) ;
#25757=CARTESIAN_POINT ( 'NONE',  ( 17.61479688768388741, 0.7169431667913548356, 12.57958639523259414 ) ) ;
#25772=CARTESIAN_POINT ( 'NONE',  ( 18.20569531734444269, -2.110314541856637582, 12.42277286985408224 ) ) ;
#25779=LINE ( 'NONE', #58278, #51857 ) ;
#25799=CARTESIAN_POINT ( 'NONE',  ( 4.600000207916445483, 2.033928581112999763E-13, -2.806643806251999915E-13 ) ) ;
#25803=CARTESIAN_POINT ( 'NONE',  ( 12.61225881068687471, -3.094544630460537515, -12.29295341835050870 ) ) ;
#25807=CARTESIAN_POINT ( 'NONE',  ( 12.27782020686944264, -2.164202955609507040, -13.73892120162925146 ) ) ;
#25811=CARTESIAN_POINT ( 'NONE',  ( 18.25219266138124752, -2.678721125794444546, 12.31196912072773308 ) ) ;
#25812=ORIENTED_EDGE ( 'NONE', *, *, #57509, .F. ) ;
#25814=VERTEX_POINT ( 'NONE', #38500 ) ;
#25816=CARTESIAN_POINT ( 'NONE',  ( 7.100000000000000533, 11.06886219213000011, 1.536526853569999851 ) ) ;
#25818=EDGE_CURVE ( 'NONE', #39916, #6106, #23110, .T. ) ;
#25821=CARTESIAN_POINT ( 'NONE',  ( 18.18011893007460600, 2.482032845566129797, 12.45575022786950825 ) ) ;
#25828=CARTESIAN_POINT ( 'NONE',  ( 12.54473519888579247, -3.068232154748443463, 12.30085162971233181 ) ) ;
#25840=DIRECTION ( 'NONE',  ( 0.000000000000000000, -1.000000000000000000, -0.000000000000000000 ) ) ;
#25845=CARTESIAN_POINT ( 'NONE',  ( 12.61551017421867371, -3.176304576338894403, -12.19307927066143549 ) ) ;
#25853=CARTESIAN_POINT ( 'NONE',  ( 18.16264250297551541, -2.646798802813860263, 13.64122832078476222 ) ) ;
#25856=CARTESIAN_POINT ( 'NONE',  ( 18.05171780850500340, -2.879539315883433481, -13.58554773987827780 ) ) ;
#25879=CARTESIAN_POINT ( 'NONE',  ( 12.30583355256787925, 1.958333444515651278, -12.44688698484233846 ) ) ;
#25883=CARTESIAN_POINT ( 'NONE',  ( 18.26192063240349839, -2.355523948311723625, 13.80042196861912984 ) ) ;
#25884=CARTESIAN_POINT ( 'NONE',  ( 18.18005044212792143, 2.500000099754956739, -13.67345740034994250 ) ) ;
#25897=CARTESIAN_POINT ( 'NONE',  ( 18.19734990864321134, -0.3336735144251442020, -12.59558214381612551 ) ) ;
#25898=CARTESIAN_POINT ( 'NONE',  ( 12.49090498480046030, 3.040702594601116360, -12.30901830445451317 ) ) ;
#25906=CARTESIAN_POINT ( 'NONE',  ( 12.54749102628328394, 3.200935012631479726, 13.62916378024774566 ) ) ;
#25909=CARTESIAN_POINT ( 'NONE',  ( 12.72380912727782665, -0.6210782762608558771, -12.67955178808352201 ) ) ;
#25910=CARTESIAN_POINT ( 'NONE',  ( 12.48412837678613663, -0.6552116771452474175, 13.98466387211990636 ) ) ;
#25919=CARTESIAN_POINT ( 'NONE',  ( 12.20907020345898708, 0.4097539338085392502, 12.59333942654355631 ) ) ;
#25923=CARTESIAN_POINT ( 'NONE',  ( 12.15236716622352553, 2.166683524422403639, 12.41231652552486686 ) ) ;
#25930=CARTESIAN_POINT ( 'NONE',  ( 12.24474413020373120, 2.777098231215099577, 12.38267839998011333 ) ) ;
#25934=CARTESIAN_POINT ( 'NONE',  ( 12.57406965100004115, -0.5808252089135508278, 12.68211610572158676 ) ) ;
#25940=CARTESIAN_POINT ( 'NONE',  ( 12.24392764853882909, -2.776000094621844383, 13.61105252602849269 ) ) ;
#25948=CARTESIAN_POINT ( 'NONE',  ( 18.17231130205936651, 2.401422691383823249, -12.47401593597049363 ) ) ;
#25950=CARTESIAN_POINT ( 'NONE',  ( 18.16560600475770570, 2.633677672902523970, 12.41941284449930549 ) ) ;
#25952=CARTESIAN_POINT ( 'NONE',  ( 7.100000000000000533, 0.000000000000000000, 0.000000000000000000 ) ) ;
#25970=CARTESIAN_POINT ( 'NONE',  ( 18.20032535889732728, 2.850937372247256629, -13.70665064220730578 ) ) ;
#25976=CARTESIAN_POINT ( 'NONE',  ( 12.31002172224689417, 0.3816054321151358120, -13.89295103374429452 ) ) ;
#25988=CARTESIAN_POINT ( 'NONE',  ( 18.07985789204857241, -2.160546346826200281, -12.52419258880425446 ) ) ;
#25989=B_SPLINE_CURVE_WITH_KNOTS ( 'NONE', 3,
 ( #8135, #40627, #25237, #67880 ),
 .UNSPECIFIED., .F., .F.,
 ( 4, 4 ),
 ( 0.000000000000000000, 1.000000000000000000 ),
 .UNSPECIFIED. ) ;
#25991=CARTESIAN_POINT ( 'NONE',  ( 18.18004831022864920, -2.496998393457253052, -12.45226267666597764 ) ) ;
#26013=CARTESIAN_POINT ( 'NONE',  ( 17.55505043854143565, 3.125000000000000000, 12.28373071562070074 ) ) ;
#26015=ORIENTED_EDGE ( 'NONE', *, *, #64655, .F. ) ;
#26021=CARTESIAN_POINT ( 'NONE',  ( 17.69835410961234601, 3.108690103397766080, -12.28870081725901464 ) ) ;
#26030=CARTESIAN_POINT ( 'NONE',  ( 5.613892321701079879, 12.94560306677573003, -2.448221637638912540 ) ) ;
#26034=CARTESIAN_POINT ( 'NONE',  ( 12.18402519556254582, 0.07112609253419313604, -12.69973757146476778 ) ) ;
#26035=CARTESIAN_POINT ( 'NONE',  ( 12.19317846011760231, -2.372225799441026961, -12.48041235929229131 ) ) ;
#26043=EDGE_CURVE ( 'NONE', #18846, #31306, #43847, .T. ) ;
#26045=CARTESIAN_POINT ( 'NONE',  ( 17.96717518398639157, 0.4698982333288769242, 12.68829846774584702 ) ) ;
#26049=EDGE_LOOP ( 'NONE', ( #44379, #40705, #24297, #8605 ) ) ;
#26072=EDGE_CURVE ( 'NONE', #27235, #41308, #29158, .T. ) ;
#26076=CARTESIAN_POINT ( 'NONE',  ( 12.24873136391192041, 2.785023419893231544, 13.60881341097601549 ) ) ;
#26084=CARTESIAN_POINT ( 'NONE',  ( 12.58276127734161420, 1.915504326815320013, -13.78019217388817275 ) ) ;
#26087=CARTESIAN_POINT ( 'NONE',  ( 18.15598102061104768, 0.1720826668005503712, 13.89857125525885095 ) ) ;
#26089=CARTESIAN_POINT ( 'NONE',  ( 18.11689869022392330, 0.2739455836253519294, 13.89636968673578288 ) ) ;
#26091=CARTESIAN_POINT ( 'NONE',  ( 12.70148458879910258, 0.6166668696481631962, 13.88158203759213549 ) ) ;
#26098=CARTESIAN_POINT ( 'NONE',  ( 12.70851731079302738, 1.792711832343931277, -13.88474979353736316 ) ) ;
#26102=CARTESIAN_POINT ( 'NONE',  ( 18.27863132999452134, 0.04649795050485548698, 12.59991969135870349 ) ) ;
#26117=CARTESIAN_POINT ( 'NONE',  ( 12.36861573454710417, -0.5743932053698046492, -12.58690132123599348 ) ) ;
#26138=CARTESIAN_POINT ( 'NONE',  ( 17.88582179699705677, 0.5306878043354081864, -13.88636785578042421 ) ) ;
#26153=CARTESIAN_POINT ( 'NONE',  ( 12.22372692396752214, -2.729759399082356097, -12.39506432367437228 ) ) ;
#26159=CARTESIAN_POINT ( 'NONE',  ( 12.47114117431411628, -3.166196762519386088, -13.63727363649663360 ) ) ;
#26162=CARTESIAN_POINT ( 'NONE',  ( 18.28010889142763418, -2.506697083851611385, 12.34815906022512877 ) ) ;
#26171=CARTESIAN_POINT ( 'NONE',  ( 17.86131849338080713, 3.044913046804099466, 12.30775201372484062 ) ) ;
#26185=CARTESIAN_POINT ( 'NONE',  ( 12.73299791870420528, -0.6209187240130109586, 12.67955909024709094 ) ) ;
#26199=VERTEX_POINT ( 'NONE', #12375 ) ;
#26200=CARTESIAN_POINT ( 'NONE',  ( 5.602426839032973227, -12.13128594426829743, 3.749700506050578142 ) ) ;
#26208=CARTESIAN_POINT ( 'NONE',  ( 17.87051611373836835, -1.960066664249855428, -13.77321273358845843 ) ) ;
#26229=CARTESIAN_POINT ( 'NONE',  ( 12.43945954148914801, 1.858853511423154137, -12.46213071393704830 ) ) ;
#26231=CYLINDRICAL_SURFACE ( 'NONE', #42958, 0.6250000000000005551 ) ;
#26233=CARTESIAN_POINT ( 'NONE',  ( 18.17041169247255183, 2.609942250314817525, -13.64953311053513296 ) ) ;
#26246=CARTESIAN_POINT ( 'NONE',  ( 18.03335409833309910, -0.5406785836137845136, -12.58839662496522749 ) ) ;
#26248=CARTESIAN_POINT ( 'NONE',  ( 12.24916108029646544, 2.785825388795849289, -12.38039059668517794 ) ) ;
#26256=CARTESIAN_POINT ( 'NONE',  ( 12.47131944427643013, 1.869655113073432684, 13.87459630548518064 ) ) ;
#26261=CARTESIAN_POINT ( 'NONE',  ( 12.40905465428149057, -1.877469967418637919, 12.45933993000109119 ) ) ;
#26267=CARTESIAN_POINT ( 'NONE',  ( 12.33591545429645464, 0.5485298171726803451, 12.58805670501782181 ) ) ;
#26273=CARTESIAN_POINT ( 'NONE',  ( 12.22616922475384094, 2.046442494456562677, 12.43271557125384597 ) ) ;
#26281=CARTESIAN_POINT ( 'NONE',  ( 12.23610050212269584, 2.758887154479852111, 12.38747357478535704 ) ) ;
#26284=CARTESIAN_POINT ( 'NONE',  ( 12.33074081236783037, 0.4072355409458908171, 12.69121720795053676 ) ) ;
#26290=CARTESIAN_POINT ( 'NONE',  ( 12.30838305349012352, -2.879539296179474572, 13.58560287457177829 ) ) ;
#26291=CARTESIAN_POINT ( 'NONE',  ( 12.21057441422015089, 2.692955410687026596, 13.63058632110301360 ) ) ;
#26298=CARTESIAN_POINT ( 'NONE',  ( 18.17889124921891053, 2.543048589645668489, -12.44148151073661701 ) ) ;
#26300=DIRECTION ( 'NONE',  ( -1.000000000000000000, 0.000000000000000000, 0.000000000000000000 ) ) ;
#26302=CARTESIAN_POINT ( 'NONE',  ( 17.79094441636205914, 1.825864066358003468, 13.88043842654293769 ) ) ;
#26303=CARTESIAN_POINT ( 'NONE',  ( 17.55505043854143565, 3.248109929747637903, -13.61799478206225444 ) ) ;
#26336=CARTESIAN_POINT ( 'NONE',  ( 17.89623257347368934, -3.023758741516315407, -12.31397229722846731 ) ) ;
#26339=CARTESIAN_POINT ( 'NONE',  ( 18.17974523562955369, -2.479825770562639864, -12.45623811636028044 ) ) ;
#26344=CARTESIAN_POINT ( 'NONE',  ( 17.55505043854147118, -2.500000000000000000, -25.00000000000000000 ) ) ;
#26345=CARTESIAN_POINT ( 'NONE',  ( 12.58176516051270255, 3.212719125873748194, -13.62638797003614144 ) ) ;
#26355=EDGE_CURVE ( 'NONE', #67648, #5374, #4887, .T. ) ;
#26370=CARTESIAN_POINT ( 'NONE',  ( 18.16726790532411329, 2.625885335067867921, -12.42137433334332464 ) ) ;
#26382=CARTESIAN_POINT ( 'NONE',  ( 12.22381919988786692, -0.2299973361971402452, -12.69720198919504739 ) ) ;
#26390=DIRECTION ( 'NONE',  ( 1.000000000000000000, 0.000000000000000000, 0.000000000000000000 ) ) ;
#26401=ADVANCED_FACE ( 'NONE', ( #68946 ), #59142, .T. ) ;
#26405=CARTESIAN_POINT ( 'NONE',  ( 18.16002653635654696, 0.1622975231916133354, -12.69869204565246612 ) ) ;
#26406=EDGE_CURVE ( 'NONE', #38239, #21130, #11246, .T. ) ;
#26418=CARTESIAN_POINT ( 'NONE',  ( 18.05194036310204098, 0.3791492162054622139, -13.89304085482682360 ) ) ;
#26419=CARTESIAN_POINT ( 'NONE',  ( 17.77555300520474191, -0.5848996845204773587, -12.68186405703079167 ) ) ;
#26434=CARTESIAN_POINT ( 'NONE',  ( 18.14024860221783442, -0.2197089332467998812, 13.89766776387047642 ) ) ;
#26442=CARTESIAN_POINT ( 'NONE',  ( 18.02801947738339194, -0.4085868565494372717, -13.89191718360344119 ) ) ;
#26449=CARTESIAN_POINT ( 'NONE',  ( 17.75589797987077745, -0.5919389804100247954, 12.68142457171642157 ) ) ;
#26464=EDGE_LOOP ( 'NONE', ( #49420, #25451, #58843, #4300 ) ) ;
#26465=FACE_OUTER_BOUND ( 'NONE', #10238, .T. ) ;
#26480=CARTESIAN_POINT ( 'NONE',  ( 12.08055032392396555, 2.669683454821158097, -12.31540075205778528 ) ) ;
#26488=DIRECTION ( 'NONE',  ( -0.000000000000000000, -0.000000000000000000, 1.000000000000000000 ) ) ;
#26498=CARTESIAN_POINT ( 'NONE',  ( 12.75302363333809019, -1.877081947669210660, -12.57507557223851080 ) ) ;
#26501=CARTESIAN_POINT ( 'NONE',  ( 12.80505043854146940, -3.199698446519381179, -12.18695736643652516 ) ) ;
#26502=CARTESIAN_POINT ( 'NONE',  ( 12.08109376178932948, -2.472831159707302273, -13.77990118939880126 ) ) ;
#26505=CARTESIAN_POINT ( 'NONE',  ( 17.90971610687751792, -3.107943374821394045, 12.21068061720392173 ) ) ;
#26516=CARTESIAN_POINT ( 'NONE',  ( 18.16418420726525795, 2.358504521564765533, -12.48345420460929134 ) ) ;
#26518=CARTESIAN_POINT ( 'NONE',  ( 17.74468889437873997, -1.784327658740600508, -12.47302143557414134 ) ) ;
#26524=ADVANCED_FACE ( 'NONE', ( #60190 ), #28034, .F. ) ;
#26525=DIRECTION ( 'NONE',  ( 1.000000000000000000, 0.000000000000000000, 0.000000000000000000 ) ) ;
#26531=CARTESIAN_POINT ( 'NONE',  ( 12.24897804304629467, -0.2853680816562785827, 12.69568625917503013 ) ) ;
#26532=CARTESIAN_POINT ( 'NONE',  ( 5.634466645576519106, -12.10031501007063603, -3.741403512701606537 ) ) ;
#26540=CARTESIAN_POINT ( 'NONE',  ( 5.500000000000000000, -13.04986661130000059, 1.811520473896000016 ) ) ;
#26554=CARTESIAN_POINT ( 'NONE',  ( 18.17246482408074471, -2.400822122662769065, -13.69396077230720721 ) ) ;
#26577=B_SPLINE_CURVE_WITH_KNOTS ( 'NONE', 3,
 ( #40581, #67485, #19950, #19607 ),
 .UNSPECIFIED., .F., .F.,
 ( 4, 4 ),
 ( 0.000000000000000000, 1.000000000000000000 ),
 .UNSPECIFIED. ) ;
#26578=CARTESIAN_POINT ( 'NONE',  ( 12.11326330726100586, 2.264210275637937642, -12.39489744172470509 ) ) ;
#26581=CARTESIAN_POINT ( 'NONE',  ( 18.12893921139219344, 2.747599606312327136, -13.61782120253283956 ) ) ;
#26593=CARTESIAN_POINT ( 'NONE',  ( 17.68572386047929967, -0.7076089047904995377, -12.58011506138061009 ) ) ;
#26603=CARTESIAN_POINT ( 'NONE',  ( 18.12596594012297757, 2.036641643015555836, 12.43431447687783020 ) ) ;
#26606=CARTESIAN_POINT ( 'NONE',  ( 12.32101752300973629, -0.3953985757065832107, -12.69171505958691704 ) ) ;
#26608=EDGE_CURVE ( 'NONE', #41143, #2693, #17181, .T. ) ;
#26610=CARTESIAN_POINT ( 'NONE',  ( 12.29727795756348918, -1.966522083383877462, 12.44559612467660337 ) ) ;
#26617=CARTESIAN_POINT ( 'NONE',  ( 12.48426296206727670, 0.6451567829544476718, 12.58347320810647929 ) ) ;
#26621=CARTESIAN_POINT ( 'NONE',  ( 12.08558010717399256, 2.390021230702581434, 12.37125449870879024 ) ) ;
#26630=CARTESIAN_POINT ( 'NONE',  ( 12.21429833799748188, 2.704300905804447819, 12.40162098798462331 ) ) ;
#26640=CARTESIAN_POINT ( 'NONE',  ( 12.18472282150165320, -2.421014800242780929, 13.68991273180144574 ) ) ;
#26643=ORIENTED_EDGE ( 'NONE', *, *, #54008, .T. ) ;
#26649=CARTESIAN_POINT ( 'NONE',  ( 17.74290558058741496, 3.096122732672591749, -12.29249473893052347 ) ) ;
#26651=CARTESIAN_POINT ( 'NONE',  ( 18.18005043873315785, 2.501166356630923016, 12.45128845099852199 ) ) ;
#26670=VECTOR ( 'NONE', #26488, 1000.000000000000000 ) ;
#26675=CARTESIAN_POINT ( 'NONE',  ( 12.34379246210524173, 0.4226248002247757207, -13.89137006864033985 ) ) ;
#26685=CARTESIAN_POINT ( 'NONE',  ( 17.83408408707291670, -3.059349868707512687, -12.30347716376230238 ) ) ;
#26686=CARTESIAN_POINT ( 'NONE',  ( 7.100000000000000533, 0.000000000000000000, 0.000000000000000000 ) ) ;
#26689=CARTESIAN_POINT ( 'NONE',  ( 12.20411985647183251, -0.1720826668005533966, 13.89857125525885095 ) ) ;
#26700=ORIENTED_EDGE ( 'NONE', *, *, #65253, .F. ) ;
#26729=CARTESIAN_POINT ( 'NONE',  ( 12.39271969839518839, 0.4698014501121452469, -12.68830453558792826 ) ) ;
#26738=CARTESIAN_POINT ( 'NONE',  ( 18.01651533407960670, 0.4224082573471430457, 12.69056396414930887 ) ) ;
#26745=CARTESIAN_POINT ( 'NONE',  ( 18.11136953712599862, 2.785023373216928277, -13.60886753798840587 ) ) ;
#26746=EDGE_LOOP ( 'NONE', ( #61384, #60685, #21044, #56563, #45610 ) ) ;
#26750=EDGE_CURVE ( 'NONE', #34701, #6933, #26577, .T. ) ;
#26768=ORIENTED_EDGE ( 'NONE', *, *, #18065, .F. ) ;
#26770=CARTESIAN_POINT ( 'NONE',  ( 17.57925147499693352, -1.760911370824147504, -12.47634522799707746 ) ) ;
#26785=CARTESIAN_POINT ( 'NONE',  ( 18.17481363285255469, -0.08139021474669956568, 13.89968437038781524 ) ) ;
#26786=CARTESIAN_POINT ( 'NONE',  ( 17.97806348702467005, 0.4608880372546551030, 13.88973238275223387 ) ) ;
#26787=B_SPLINE_CURVE_WITH_KNOTS ( 'NONE', 1,
 ( #48632, #734 ),
 .UNSPECIFIED., .F., .F.,
 ( 2, 2 ),
 ( 0.000000000000000000, 1.000000000000000000 ),
 .UNSPECIFIED. ) ;
#26789=CARTESIAN_POINT ( 'NONE',  ( 12.49453886772563038, 0.5425156946249201084, 13.88574935929170806 ) ) ;
#26791=CARTESIAN_POINT ( 'NONE',  ( 18.17614081687046124, -0.08113699236157925765, -13.89976078940779480 ) ) ;
#26800=CARTESIAN_POINT ( 'NONE',  ( 18.18005727183074782, 0.009762034906138391047, 12.70000045436730751 ) ) ;
#26804=ORIENTED_EDGE ( 'NONE', *, *, #37871, .T. ) ;
#26816=CARTESIAN_POINT ( 'NONE',  ( 17.99403275303994576, 3.052983340820297542, -12.22453705205519014 ) ) ;
#26817=CARTESIAN_POINT ( 'NONE',  ( 5.687176560458846453, 12.04993902413980678, 3.725892264571312396 ) ) ;
#26830=CARTESIAN_POINT ( 'NONE',  ( 17.65768761389442432, 0.6168528257048864205, -13.88157091029610157 ) ) ;
#26831=ORIENTED_EDGE ( 'NONE', *, *, #12060, .T. ) ;
#26836=CARTESIAN_POINT ( 'NONE',  ( 17.55505043854143565, 1.787797342887044394, 13.88538010501570952 ) ) ;
#26854=CARTESIAN_POINT ( 'NONE',  ( 12.09560501594675230, -2.367229839359598298, -13.79841893036761036 ) ) ;
#26857=CARTESIAN_POINT ( 'NONE',  ( 18.14576286523421800, -2.898275280820969524, 12.26215340014708310 ) ) ;
#26861=ADVANCED_FACE ( 'NONE', ( #58375 ), #29581, .T. ) ;
#26878=CARTESIAN_POINT ( 'NONE',  ( 5.598857209341685071, -12.13471601160040514, -3.750691118698022741 ) ) ;
#26885=CARTESIAN_POINT ( 'NONE',  ( 17.74755423490962158, 3.094705742910453861, 13.52911976267489891 ) ) ;
#26889=B_SPLINE_CURVE_WITH_KNOTS ( 'NONE', 3,
 ( #3315, #14165, #4677, #52238 ),
 .UNSPECIFIED., .F., .F.,
 ( 4, 4 ),
 ( 0.000000000000000000, 1.000000000000000000 ),
 .UNSPECIFIED. ) ;
#26899=CARTESIAN_POINT ( 'NONE',  ( 18.13331639930713735, -2.076941473624323020, -13.84509535655099199 ) ) ;
#26914=VERTEX_POINT ( 'NONE', #26836 ) ;
#26916=CARTESIAN_POINT ( 'NONE',  ( 12.36031510016526092, 1.911905511008637149, -12.45410252665035600 ) ) ;
#26917=EDGE_CURVE ( 'NONE', #54460, #49162, #68775, .T. ) ;
#26921=CARTESIAN_POINT ( 'NONE',  ( 18.15932194351565698, 2.660757700747661936, -13.63806486294889098 ) ) ;
#26926=ORIENTED_EDGE ( 'NONE', *, *, #23375, .F. ) ;
#26933=CARTESIAN_POINT ( 'NONE',  ( 18.05096829067923281, -0.5248261352964527227, -12.58906749861124119 ) ) ;
#26935=CARTESIAN_POINT ( 'NONE',  ( 12.80505043854143388, 3.124999999999999556, -12.28374638332999602 ) ) ;
#26942=PLANE ( 'NONE',  #36116 ) ;
#26945=CARTESIAN_POINT ( 'NONE',  ( 18.16715147695112620, 2.094590662098726241, 12.42468172752983868 ) ) ;
#26947=CARTESIAN_POINT ( 'NONE',  ( 4.599999999999999645, 3.248109929747638347, -13.61799478206225622 ) ) ;
#26952=CARTESIAN_POINT ( 'NONE',  ( 12.19613275390598695, -2.089545048426566964, 12.42553124896410566 ) ) ;
#26955=DIRECTION ( 'NONE',  ( 0.000000000000000000, 0.000000000000000000, 1.000000000000000000 ) ) ;
#26958=CARTESIAN_POINT ( 'NONE',  ( 12.25981900110941503, 0.4746736627229529160, 12.59106879393900513 ) ) ;
#26961=CARTESIAN_POINT ( 'NONE',  ( 12.79295051314559650, 1.760910731560546116, 12.47634535177225068 ) ) ;
#26974=CARTESIAN_POINT ( 'NONE',  ( 17.64998052285767471, 0.7146386402664155479, -12.57972080578569063 ) ) ;
#26976=B_SPLINE_CURVE_WITH_KNOTS ( 'NONE', 1,
 ( #48067, #53313 ),
 .UNSPECIFIED., .F., .F.,
 ( 2, 2 ),
 ( 0.000000000000000000, 1.000000000000000000 ),
 .UNSPECIFIED. ) ;
#26977=VECTOR ( 'NONE', #63384, 1000.000000000000000 ) ;
#26978=CARTESIAN_POINT ( 'NONE',  ( 12.19536857401210384, -2.360987227094835106, 13.70197821715308528 ) ) ;
#26979=CARTESIAN_POINT ( 'NONE',  ( 12.20052776708265974, 2.340020608672652269, 13.70605490524154746 ) ) ;
#26986=CARTESIAN_POINT ( 'NONE',  ( 18.15144633312240074, 2.312812061507714567, -12.49323956768624377 ) ) ;
#27002=FACE_OUTER_BOUND ( 'NONE', #1811, .T. ) ;
#27010=CARTESIAN_POINT ( 'NONE',  ( 12.21236231059852706, -0.1994024998447188335, -13.89809293279807534 ) ) ;
#27012=DIRECTION ( 'NONE',  ( -0.7071067792008891573, -0.5090928532370920800, -0.4907386978739921579 ) ) ;
#27022=DIRECTION ( 'NONE',  ( -0.000000000000000000, -0.000000000000000000, 1.000000000000000000 ) ) ;
#27024=CARTESIAN_POINT ( 'NONE',  ( 18.13653212795703595, -2.729361600744797833, -12.39516738912175242 ) ) ;
#27030=CARTESIAN_POINT ( 'NONE',  ( 12.27392385059252788, 0.3300666952397307008, 13.89473968862478870 ) ) ;
#27031=ORIENTED_EDGE ( 'NONE', *, *, #50189, .F. ) ;
#27045=CARTESIAN_POINT ( 'NONE',  ( 17.60411830284109058, -1.787854822559178825, 13.88537270421500658 ) ) ;
#27061=CARTESIAN_POINT ( 'NONE',  ( 17.99289217962403242, 2.946103266174030288, -12.33638055411239698 ) ) ;
#27068=ORIENTED_EDGE ( 'NONE', *, *, #53256, .F. ) ;
#27069=CARTESIAN_POINT ( 'NONE',  ( 12.23133867660517282, 0.2481623978058206392, -12.69674179789669211 ) ) ;
#27073=CARTESIAN_POINT ( 'NONE',  ( 12.80505043854143388, 3.199698446519374517, 12.18695736643652694 ) ) ;
#27074=ORIENTED_EDGE ( 'NONE', *, *, #50711, .T. ) ;
#27084=ORIENTED_EDGE ( 'NONE', *, *, #30811, .T. ) ;
#27085=EDGE_CURVE ( 'NONE', #47262, #48720, #32011, .T. ) ;
#27107=CARTESIAN_POINT ( 'NONE',  ( 18.17180742357641421, 0.1030366931658452667, -13.89950396794446874 ) ) ;
#27115=EDGE_LOOP ( 'NONE', ( #20611, #32014, #64037, #40327 ) ) ;
#27117=ORIENTED_EDGE ( 'NONE', *, *, #50668, .T. ) ;
#27121=CARTESIAN_POINT ( 'NONE',  ( 12.33386765766680071, 2.911124516513513782, -13.57763168322026637 ) ) ;
#27125=CARTESIAN_POINT ( 'NONE',  ( 17.86832607310548937, -0.5412024733746028105, 13.88582008197803042 ) ) ;
#27128=CARTESIAN_POINT ( 'NONE',  ( 12.32512809855874636, 0.4004137791749501352, 13.89223825656494249 ) ) ;
#27130=DIRECTION ( 'NONE',  ( 0.000000000000000000, 0.000000000000000000, -1.000000000000000000 ) ) ;
#27131=CARTESIAN_POINT ( 'NONE',  ( 17.55505043854144276, -0.6250000000000001110, -13.88107975066922428 ) ) ;
#27140=CARTESIAN_POINT ( 'NONE',  ( 17.91892138177005123, -0.5082598251325827210, 12.68630931495243352 ) ) ;
#27148=CARTESIAN_POINT ( 'NONE',  ( 5.599997304680200294, -13.94845324556000143, 4.312847325879000770 ) ) ;
#27156=CARTESIAN_POINT ( 'NONE',  ( 17.88886072129108840, 3.119102935781167041, -12.20783478086261020 ) ) ;
#27167=ORIENTED_EDGE ( 'NONE', *, *, #32444, .F. ) ;
#27171=CARTESIAN_POINT ( 'NONE',  ( 17.65691712177036976, -0.6169787192598745751, -13.88156336867696616 ) ) ;
#27176=CARTESIAN_POINT ( 'NONE',  ( 12.60202002655570652, 3.091459147703855770, -12.29390037902081545 ) ) ;
#27183=CARTESIAN_POINT ( 'NONE',  ( 18.28019316479975132, 0.1878083608816567551, 12.60000737103649016 ) ) ;
#27186=CARTESIAN_POINT ( 'NONE',  ( 12.20865459317947632, -2.312811904845647248, -12.49320495213145676 ) ) ;
#27192=CARTESIAN_POINT ( 'NONE',  ( 12.17639632831540020, -2.882401473261796632, -13.70008095139100313 ) ) ;
#27196=CARTESIAN_POINT ( 'NONE',  ( 17.99403275303998129, -3.052983340820298874, 12.22453705205519192 ) ) ;
#27199=EDGE_LOOP ( 'NONE', ( #17802, #41025, #51788, #10291 ) ) ;
#27204=CARTESIAN_POINT ( 'NONE',  ( 12.80505043854144276, -0.6250000000000001110, 13.88107975066923316 ) ) ;
#27225=CARTESIAN_POINT ( 'NONE',  ( 18.17486206286450923, 2.582858869840499061, 13.65550477088448034 ) ) ;
#27234=CARTESIAN_POINT ( 'NONE',  ( 17.55505043854147118, -3.125000000000000000, -25.00000000000000000 ) ) ;
#27235=VERTEX_POINT ( 'NONE', #56498 ) ;
#27238=CARTESIAN_POINT ( 'NONE',  ( 18.23517937092941921, -2.264898893658558787, -13.81558401759068744 ) ) ;
#27258=CARTESIAN_POINT ( 'NONE',  ( 12.16862919417105537, 2.135222488495307935, -12.41776696322756912 ) ) ;
#27263=CARTESIAN_POINT ( 'NONE',  ( 18.18005043852537383, 2.520325007585968002, -13.66916896904722734 ) ) ;
#27266=CARTESIAN_POINT ( 'NONE',  ( 21.35000154058000277, -12.59999999999999964, 0.000000000000000000 ) ) ;
#27268=CARTESIAN_POINT ( 'NONE',  ( 12.61585440497584187, -3.174879747171414746, -12.19344691178323181 ) ) ;
#27276=CARTESIAN_POINT ( 'NONE',  ( 17.96724410757352786, 0.4699213205053987541, -12.68829855189362732 ) ) ;
#27278=CARTESIAN_POINT ( 'NONE',  ( 12.80505043854143388, 1.875000000000000000, -12.57545641911172751 ) ) ;
#27282=B_SPLINE_CURVE_WITH_KNOTS ( 'NONE', 1,
 ( #10991, #15556 ),
 .UNSPECIFIED., .F., .F.,
 ( 2, 2 ),
 ( 0.000000000000000000, 1.000000000000000000 ),
 .UNSPECIFIED. ) ;
#27288=CARTESIAN_POINT ( 'NONE',  ( 18.13320831056631732, 2.045970293963734310, 12.43278322311361883 ) ) ;
#27292=CARTESIAN_POINT ( 'NONE',  ( 12.80505043854143388, 3.124999999999999556, -12.28374638332999602 ) ) ;
#27294=CARTESIAN_POINT ( 'NONE',  ( 12.56948062052972936, -3.161141996800568066, 12.19701735778311580 ) ) ;
#27299=CARTESIAN_POINT ( 'NONE',  ( 12.58342066637853129, 0.6849607937330760565, 12.58136878870645248 ) ) ;
#27302=CARTESIAN_POINT ( 'NONE',  ( 12.23528344688399017, 2.757674802278836879, 12.38780605717373184 ) ) ;
#27303=FACE_BOUND ( 'NONE', #66259, .T. ) ;
#27310=CARTESIAN_POINT ( 'NONE',  ( 12.21071179159800124, 2.693740719347354151, 12.40432020966558113 ) ) ;
#27314=CARTESIAN_POINT ( 'NONE',  ( 12.44244977486500048, 0.5091670850904397305, 12.68626057781341210 ) ) ;
#27318=CARTESIAN_POINT ( 'NONE',  ( 12.08020514495816400, -2.544320517268841453, 13.76688091865072572 ) ) ;
#27328=CARTESIAN_POINT ( 'NONE',  ( 17.62782920531150310, 1.879164230502278210, -12.57477362212319250 ) ) ;
#27334=CARTESIAN_POINT ( 'NONE',  ( 12.08061556837357386, 2.709898641938862429, 13.73658242091902615 ) ) ;
#27335=LINE ( 'NONE', #416, #21907 ) ;
#27344=CARTESIAN_POINT ( 'NONE',  ( 17.77709566067065339, -3.084588255221574649, 13.53194174261899541 ) ) ;
#27351=CARTESIAN_POINT ( 'NONE',  ( 12.43745875772600584, -1.881346041095415478, -13.87306493546281239 ) ) ;
#27352=CARTESIAN_POINT ( 'NONE',  ( 12.54858531451517223, 0.5700392133823489749, -13.88426419246400378 ) ) ;
#27359=ORIENTED_EDGE ( 'NONE', *, *, #40389, .T. ) ;
#27364=CARTESIAN_POINT ( 'NONE',  ( 17.71888513161123413, -3.103492732303466450, -12.29025695670424945 ) ) ;
#27368=CARTESIAN_POINT ( 'NONE',  ( 17.74851076052204490, -1.905606517475760597, 12.57039381402181455 ) ) ;
#27370=CARTESIAN_POINT ( 'NONE',  ( 12.27985112600388717, -0.3389646381316569479, 13.89444110642641661 ) ) ;
#27408=CARTESIAN_POINT ( 'NONE',  ( 12.17440657078182475, 2.124933824806637173, -12.41953149444585947 ) ) ;
#27414=CARTESIAN_POINT ( 'NONE',  ( 5.667284894747531609, 12.98956018755431785, 2.203076747946188352 ) ) ;
#27415=EDGE_LOOP ( 'NONE', ( #66800, #4500, #16157 ) ) ;
#27426=CARTESIAN_POINT ( 'NONE',  ( 17.96876343269822129, 2.968584057511098884, -13.56283743052908619 ) ) ;
#27447=CARTESIAN_POINT ( 'NONE',  ( 18.02961597915983205, 0.4069473558587370920, -13.89198745890301723 ) ) ;
#27458=CARTESIAN_POINT ( 'NONE',  ( 12.68500746440619764, 1.797494983113959277, -13.88412888179957605 ) ) ;
#27462=CARTESIAN_POINT ( 'NONE',  ( 18.02561562912593018, -0.4118363585311525799, 13.89180007025485786 ) ) ;
#27466=CARTESIAN_POINT ( 'NONE',  ( 12.49507620378167871, -0.5430989695073406009, 13.88572189919897326 ) ) ;
#27467=CARTESIAN_POINT ( 'NONE',  ( 12.38194801265181333, -0.4608083867824254720, -13.88973595540270800 ) ) ;
#27469=CARTESIAN_POINT ( 'NONE',  ( 18.04535492079093828, -0.3877560771919992266, -13.89272419024339733 ) ) ;
#27478=EDGE_CURVE ( 'NONE', #22723, #62822, #25221, .T. ) ;
#27481=CARTESIAN_POINT ( 'NONE',  ( 18.04446571359450147, -0.3888461597108445189, 12.69199065798140680 ) ) ;
#27495=CARTESIAN_POINT ( 'NONE',  ( 12.35444711458464973, -0.5635217852607019573, -12.58739276154098086 ) ) ;
#27497=CARTESIAN_POINT ( 'NONE',  ( 17.84599613952810415, 3.139413506986218128, -12.20262697555083342 ) ) ;
#27498=CARTESIAN_POINT ( 'NONE',  ( 5.619729929256978451, 12.11456185543956288, 3.745214083257081938 ) ) ;
#27513=CARTESIAN_POINT ( 'NONE',  ( 17.57900095810616392, 0.7302151993337242519, -13.98094363222392111 ) ) ;
#27515=DIRECTION ( 'NONE',  ( 1.000000000000000000, 0.000000000000000000, 0.000000000000000000 ) ) ;
#27522=CARTESIAN_POINT ( 'NONE',  ( 17.60314900679416183, -1.789028854058319684, 13.88522169503354142 ) ) ;
#27529=CARTESIAN_POINT ( 'NONE',  ( 12.48926758269845827, -1.960545016317334355, -12.56101064709213766 ) ) ;
#27534=CARTESIAN_POINT ( 'NONE',  ( 12.10694218860116855, -2.320713384140930202, -13.80631828123456728 ) ) ;
#27538=CARTESIAN_POINT ( 'NONE',  ( 17.74290558058745049, -3.096122732672591749, 12.29249473893052524 ) ) ;
#27539=ORIENTED_EDGE ( 'NONE', *, *, #26750, .F. ) ;
#27559=AXIS2_PLACEMENT_3D ( 'NONE', #18246, #6704, #7752 ) ;
#27567=CARTESIAN_POINT ( 'NONE',  ( 18.08101717074206150, 2.837770499550323233, 13.59594328884928593 ) ) ;
#27581=CARTESIAN_POINT ( 'NONE',  ( 17.74496479089906487, -1.812889415971018048, -13.88212816151363782 ) ) ;
#27590=CARTESIAN_POINT ( 'NONE',  ( 17.55505043854147118, -1.875000000000000000, -13.78627172894481667 ) ) ;
#27595=CARTESIAN_POINT ( 'NONE',  ( 17.60412247570698341, 3.248108758003381613, 13.61799506159946382 ) ) ;
#27597=ORIENTED_EDGE ( 'NONE', *, *, #4078, .F. ) ;
#27599=CARTESIAN_POINT ( 'NONE',  ( 12.68481529409925379, 3.190188709592562066, -12.18945115681612101 ) ) ;
#27619=CARTESIAN_POINT ( 'NONE',  ( 18.12461185120978868, -0.2575478136180262556, -12.69649014468030757 ) ) ;
#27633=CARTESIAN_POINT ( 'NONE',  ( 18.21592075161430557, 2.776565552903136336, 12.29027267990593764 ) ) ;
#27634=CARTESIAN_POINT ( 'NONE',  ( 12.80505043854143388, 1.787797342887043062, 13.88538010501570952 ) ) ;
#27640=CARTESIAN_POINT ( 'NONE',  ( 12.08853825830071038, -2.367028970089855466, 12.37569070051500653 ) ) ;
#27644=DIRECTION ( 'NONE',  ( 1.000000000000000000, 0.000000000000000000, 0.000000000000000000 ) ) ;
#27646=CARTESIAN_POINT ( 'NONE',  ( 12.13047558099396284, -0.2638285456865435696, 12.59724228039519645 ) ) ;
#27650=CARTESIAN_POINT ( 'NONE',  ( 12.37577160951050814, 2.954704321271699019, 12.33392404961603894 ) ) ;
#27654=CARTESIAN_POINT ( 'NONE',  ( 18.22023691865391015, -0.2863297863804597498, 12.59675086341328409 ) ) ;
#27658=CARTESIAN_POINT ( 'NONE',  ( 17.75497146387445468, -0.5922552425703458967, 12.68140545290050802 ) ) ;
#27662=CARTESIAN_POINT ( 'NONE',  ( 12.19590851926989927, 0.1412562895068591451, 12.69896251113184427 ) ) ;
#27663=CARTESIAN_POINT ( 'NONE',  ( 12.80505043854144276, 0.6250000000000001110, 13.88107975066923494 ) ) ;
#27666=CARTESIAN_POINT ( 'NONE',  ( 21.60000021221999944, 12.84999978760999895, 2.874107720315999839E-09 ) ) ;
#27670=CARTESIAN_POINT ( 'NONE',  ( 12.18865279333487095, -2.902449960337692314, 13.69583488376822622 ) ) ;
#27674=DIRECTION ( 'NONE',  ( 1.000000000000000000, 0.000000000000000000, 0.000000000000000000 ) ) ;
#27680=CARTESIAN_POINT ( 'NONE',  ( 17.59669571873551774, 1.876302067258580619, -12.57524312254454379 ) ) ;
#27695=CARTESIAN_POINT ( 'NONE',  ( 18.16386294024318460, -2.642762625146028110, 13.64216358405140994 ) ) ;
#27702=CARTESIAN_POINT ( 'NONE',  ( 4.650000881942760067, -3.073097332162000125E-13, -5.595524044110998485E-14 ) ) ;
#27720=CARTESIAN_POINT ( 'NONE',  ( 12.49024380163858439, 3.040024005673538809, 13.54391858567110241 ) ) ;
#27724=CARTESIAN_POINT ( 'NONE',  ( 12.20981157025896913, 0.1908382484571561621, 13.89824168789395920 ) ) ;
#27747=B_SPLINE_CURVE_WITH_KNOTS ( 'NONE', 3,
 ( #44611, #40377, #65906, #61699, #18375, #2970, #60670, #29571, #24647, #50873, #61019, #23957, #35487, #18034, #7880, #50528 ),
 .UNSPECIFIED., .F., .F.,
 ( 4, 2, 2, 2, 2, 2, 2, 4 ),
 ( 0.000000000000000000, 0.06249999999999941713, 0.1249999999999988343, 0.2499999999999997224, 0.4999999999999998890, 0.7500000000000000000, 0.8749999999999998890, 1.000000000000000000 ),
 .UNSPECIFIED. ) ;
#27753=CARTESIAN_POINT ( 'NONE',  ( 5.613892323500530246, -12.94560306806822503, 2.448221630819331640 ) ) ;
#27786=CARTESIAN_POINT ( 'NONE',  ( 17.55505043854143565, 1.875000000000000000, -12.57545641911172751 ) ) ;
#27796=CARTESIAN_POINT ( 'NONE',  ( 17.81484293439625688, -3.068795199404298124, -13.53617370485920013 ) ) ;
#27804=CARTESIAN_POINT ( 'NONE',  ( 17.81303847540711516, -1.807878129530196221, -12.46962684194071791 ) ) ;
#27812=CARTESIAN_POINT ( 'NONE',  ( 5.600023899775999681, -13.94845324556000143, -4.312847325879000770 ) ) ;
#27816=CARTESIAN_POINT ( 'NONE',  ( 12.50306195774379958, 1.853743832531304481, -13.87673314481786591 ) ) ;
#27820=CARTESIAN_POINT ( 'NONE',  ( 18.06311169547814899, 0.3645810575750376703, 13.89357890581305099 ) ) ;
#27826=CARTESIAN_POINT ( 'NONE',  ( 12.52211160811865120, -0.5573818237641869899, 13.88495700090146734 ) ) ;
#27827=CARTESIAN_POINT ( 'NONE',  ( 12.42340929148597617, -0.4950008743047930593, -13.88813607082249035 ) ) ;
#27829=CARTESIAN_POINT ( 'NONE',  ( 18.06407613793124511, -0.3627976900031492646, -13.89363072198946547 ) ) ;
#27837=CARTESIAN_POINT ( 'NONE',  ( 17.63678281077947574, -0.6199686954221033108, 12.67962180225517876 ) ) ;
#27840=CARTESIAN_POINT ( 'NONE',  ( 17.55505043854147118, -3.125000000000000000, -12.28373071562070074 ) ) ;
#27843=DIRECTION ( 'NONE',  ( 1.000000000000000000, 0.000000000000000000, 0.000000000000000000 ) ) ;
#27850=CARTESIAN_POINT ( 'NONE',  ( 12.08472055051100824, -0.08234928811777623980, -12.59973629603894274 ) ) ;
#27868=CARTESIAN_POINT ( 'NONE',  ( 17.63678025734560251, -0.6199690124688013171, -13.88138352397877462 ) ) ;
#27879=CARTESIAN_POINT ( 'NONE',  ( 17.65064139367258988, -1.793792787906298036, 13.88460705996369349 ) ) ;
#27883=CARTESIAN_POINT ( 'NONE',  ( 12.26133075698776942, -2.191112520879996861, -12.51819442860477416 ) ) ;
#27890=CARTESIAN_POINT ( 'NONE',  ( 18.07990072965513662, -1.983698511703248180, 12.44287000959587175 ) ) ;
#27901=DIRECTION ( 'NONE',  ( 0.000000000000000000, 0.000000000000000000, 1.000000000000000000 ) ) ;
#27919=CARTESIAN_POINT ( 'NONE',  ( 18.14022514731436431, 2.720460039646585670, 13.62418930002215589 ) ) ;
#27932=CARTESIAN_POINT ( 'NONE',  ( 17.99965052394119169, -1.940731178328038098, -13.86484045969604395 ) ) ;
#27952=CARTESIAN_POINT ( 'NONE',  ( 12.47064909367909280, 3.118799700203781722, -12.20791227269315549 ) ) ;
#27970=CARTESIAN_POINT ( 'NONE',  ( 17.84124069827833736, -0.5557204214162416722, -12.68363025601217053 ) ) ;
#27971=CARTESIAN_POINT ( 'NONE',  ( 12.18009334795431187, 2.513081858645665356, -12.44854102044448929 ) ) ;
#27975=SURFACE_SIDE_STYLE ('',( #49987 ) ) ;
#27979=EDGE_CURVE ( 'NONE', #38102, #18184, #10840, .T. ) ;
#27981=CARTESIAN_POINT ( 'NONE',  ( 18.27407156835991131, 2.576234207239477492, 12.33383912514346470 ) ) ;
#27985=CARTESIAN_POINT ( 'NONE',  ( 12.80505043854144276, -0.7192913403693169672, -12.57945229203838267 ) ) ;
#27987=CARTESIAN_POINT ( 'NONE',  ( 12.10343314470982179, -2.298052811141204188, 12.38866778002552849 ) ) ;
#27995=CARTESIAN_POINT ( 'NONE',  ( 12.08123681970977259, 0.04734719685816674017, 12.59993264914401045 ) ) ;
#27998=CARTESIAN_POINT ( 'NONE',  ( 12.49937493268693878, 3.045244672522429141, 12.30765407517399446 ) ) ;
#28015=CARTESIAN_POINT ( 'NONE',  ( 12.56965099582940049, -1.826966356815477255, 13.88028256676999384 ) ) ;
#28028=CARTESIAN_POINT ( 'NONE',  ( 17.66882634972349209, 1.885356762137523345, -12.57375482825836777 ) ) ;
#28034=PLANE ( 'NONE',  #29919 ) ;
#28039=CARTESIAN_POINT ( 'NONE',  ( 18.12467946932838814, -2.757395321821673129, 13.61549383066600782 ) ) ;
#28046=CARTESIAN_POINT ( 'NONE',  ( 12.61577834527631303, -1.811481987162395724, -13.88231333970466608 ) ) ;
#28048=CARTESIAN_POINT ( 'NONE',  ( 17.87583791501561237, 0.6451567829544448962, -12.58347320810647929 ) ) ;
#28050=DIRECTION ( 'NONE',  ( 1.000000000000000000, 0.000000000000000000, 0.000000000000000000 ) ) ;
#28051=ORIENTED_EDGE ( 'NONE', *, *, #26072, .T. ) ;
#28061=CARTESIAN_POINT ( 'NONE',  ( 12.21287994455106229, 2.700912243963291992, 13.62875716402589532 ) ) ;
#28062=CARTESIAN_POINT ( 'NONE',  ( 17.69913221809301263, -1.891485217175129963, 12.57274297139331587 ) ) ;
#28065=CARTESIAN_POINT ( 'NONE',  ( 12.23548570231569066, 0.2575405707509094144, 13.89679341043304994 ) ) ;
#28078=CARTESIAN_POINT ( 'NONE',  ( 18.20318779774994056, -2.896782429227412692, 13.69773569391997547 ) ) ;
#28080=CARTESIAN_POINT ( 'NONE',  ( 12.61731147765582328, 0.6963438834333895988, 12.58074676375310474 ) ) ;
#28095=EDGE_LOOP ( 'NONE', ( #35413, #47145, #61489, #3367 ) ) ;
#28105=CARTESIAN_POINT ( 'NONE',  ( 12.21215155063535640, 2.301234877171830284, -13.71362569327517100 ) ) ;
#28110=CARTESIAN_POINT ( 'NONE',  ( 12.41655229043184860, 0.4896942981276207196, -13.88839019180475809 ) ) ;
#28113=EDGE_CURVE ( 'NONE', #1557, #15559, #66736, .T. ) ;
#28119=CARTESIAN_POINT ( 'NONE',  ( 17.71798387292786003, 1.896258650311507310, -13.78312406285443004 ) ) ;
#28121=LINE ( 'NONE', #45242, #4917 ) ;
#28125=CARTESIAN_POINT ( 'NONE',  ( 17.65064139367255436, 1.793792787906293595, -13.88460705996369704 ) ) ;
#28128=CARTESIAN_POINT ( 'NONE',  ( 4.599999999999999645, 1.760910691117812954, 12.47634535983622861 ) ) ;
#28131=CARTESIAN_POINT ( 'NONE',  ( 18.14649830798774843, -2.702104747124480344, -13.62846271472191262 ) ) ;
#28139=CARTESIAN_POINT ( 'NONE',  ( 18.24176189833876194, -2.711585165818146681, -12.30477270241628496 ) ) ;
#28151=CARTESIAN_POINT ( 'NONE',  ( 12.30838305349008444, 2.879539296179473684, -13.58560287457177473 ) ) ;
#28154=CARTESIAN_POINT ( 'NONE',  ( 17.98240304306455428, 0.4561791668615490236, 13.88992602861185155 ) ) ;
#28159=CARTESIAN_POINT ( 'NONE',  ( 12.28049946560828865, -0.3399327000516478847, 13.89440849577454351 ) ) ;
#28168=CIRCLE ( 'NONE', #3553, 13.17499999999999716 ) ;
#28171=CARTESIAN_POINT ( 'NONE',  ( 17.78508576848220812, 0.5812174491462176462, 12.68209204657792810 ) ) ;
#28174=CARTESIAN_POINT ( 'NONE',  ( 17.71871529295699332, -3.104542143066329363, -12.28994062198766457 ) ) ;
#28188=CARTESIAN_POINT ( 'NONE',  ( 12.18894565086184478, 0.3798658283128608093, -12.59428767283705497 ) ) ;
#28202=ORIENTED_EDGE ( 'NONE', *, *, #3173, .T. ) ;
#28206=CARTESIAN_POINT ( 'NONE',  ( 18.08024975107899479, -0.3389646381316551715, -13.89444110642640773 ) ) ;
#28215=CARTESIAN_POINT ( 'NONE',  ( 12.33523313523883580, -2.912685155760744049, -13.57718188376844282 ) ) ;
#28220=EDGE_LOOP ( 'NONE', ( #25098, #41263, #53099, #52000 ) ) ;
#28225=CARTESIAN_POINT ( 'NONE',  ( 12.80505043854143388, 1.875000000000000000, -12.57545641911172751 ) ) ;
#28228=CARTESIAN_POINT ( 'NONE',  ( 17.56715138999752313, -1.760845446529460512, 12.47635456592353620 ) ) ;
#28258=CARTESIAN_POINT ( 'NONE',  ( 18.01266241223991216, 2.926178784092880569, 13.57373383468747363 ) ) ;
#28270=CARTESIAN_POINT ( 'NONE',  ( 18.28009623694103070, -2.497067955185374277, -13.77553007214568481 ) ) ;
#28292=CARTESIAN_POINT ( 'NONE',  ( 12.11461379017076112, 2.700589376673574016, -12.30719081517758084 ) ) ;
#28294=EDGE_LOOP ( 'NONE', ( #52117, #25198, #24102, #60984 ) ) ;
#28307=CARTESIAN_POINT ( 'NONE',  ( 18.18003632999695895, 0.02081145935391477686, -12.69999906470294526 ) ) ;
#28308=CARTESIAN_POINT ( 'NONE',  ( 12.20841262068627842, 2.686198883114174762, -12.40625987438722788 ) ) ;
#28314=( NAMED_UNIT ( * ) PLANE_ANGLE_UNIT ( ) SI_UNIT ( $, .RADIAN. ) );
#28319=CARTESIAN_POINT ( 'NONE',  ( 18.07135403277170127, 2.147634186626015573, 12.52670565379012579 ) ) ;
#28327=CARTESIAN_POINT ( 'NONE',  ( 12.31158149911131794, -3.007516552431697132, 12.23580242208396562 ) ) ;
#28335=CARTESIAN_POINT ( 'NONE',  ( 12.08612546794236486, -0.09367178904474190992, 12.59965724591066483 ) ) ;
#28339=CARTESIAN_POINT ( 'NONE',  ( 12.70862826151950919, 1.767199679044270333, 12.47545624547677434 ) ) ;
#28357=CARTESIAN_POINT ( 'NONE',  ( 17.79118476696435280, 3.162166141421089094, -12.19676423671823962 ) ) ;
#28359=CARTESIAN_POINT ( 'NONE',  ( 12.11351653522384098, -2.298558756435003403, 13.81002389223456106 ) ) ;
#28365=B_SPLINE_CURVE_WITH_KNOTS ( 'NONE', 3,
 ( #22472, #27045, #21780, #54644, #37522, #59191, #10956, #53606, #64079, #16198, #28078, #11293, #43115, #5704, #6738, #814 ),
 .UNSPECIFIED., .F., .F.,
 ( 4, 2, 2, 2, 2, 2, 2, 4 ),
 ( 0.000000000000000000, 0.06250000000000162370, 0.1250000000000032474, 0.2500000000000022760, 0.5000000000000005551, 0.7499999999999987788, 0.8749999999999994449, 1.000000000000000000 ),
 .UNSPECIFIED. ) ;
#28378=CARTESIAN_POINT ( 'NONE',  ( 17.74534446683495048, 0.7110419930699937163, -13.98197980709423582 ) ) ;
#28379=DIRECTION ( 'NONE',  ( 1.000000000000000000, 0.000000000000000000, 0.000000000000000000 ) ) ;
#28380=CARTESIAN_POINT ( 'NONE',  ( 12.23173037680160569, -2.748912840219636333, 12.39010626689776196 ) ) ;
#28386=CARTESIAN_POINT ( 'NONE',  ( 18.15957959476903838, -2.341019627110876744, 13.70589624875886514 ) ) ;
#28394=CARTESIAN_POINT ( 'NONE',  ( 12.80505043854146940, -1.787797342887047947, -13.88538010501570774 ) ) ;
#28407=ADVANCED_FACE ( 'NONE', ( #44663 ), #44318, .F. ) ;
#28408=CARTESIAN_POINT ( 'NONE',  ( 12.19562740135367918, 2.360953413553768421, 13.70191948036521268 ) ) ;
#28415=CARTESIAN_POINT ( 'NONE',  ( 12.10431174240586216, 0.1888260363403126418, 13.99874504378992413 ) ) ;
#28416=VERTEX_POINT ( 'NONE', #2341 ) ;
#28421=VECTOR ( 'NONE', #54997, 1000.000000000000000 ) ;
#28448=CONICAL_SURFACE ( 'NONE', #52997, 13.22499948080999843, 0.7853981240402999608 ) ;
#28453=EDGE_CURVE ( 'NONE', #58820, #66385, #51628, .T. ) ;
#28458=CARTESIAN_POINT ( 'NONE',  ( 12.18791262560835342, 2.399397798254620628, -13.69429647071889811 ) ) ;
#28460=CARTESIAN_POINT ( 'NONE',  ( 12.56893612372510205, 3.162115968191201443, 12.19677724224926685 ) ) ;
#28463=CARTESIAN_POINT ( 'NONE',  ( 12.08466087602982597, -0.08309727575450116810, -13.99975851644561686 ) ) ;
#28468=CARTESIAN_POINT ( 'NONE',  ( 5.601974509047820128, 12.13172069192291680, -3.749825701181556781 ) ) ;
#28471=CARTESIAN_POINT ( 'NONE',  ( 17.72176632460244861, 3.228945123492080516, -13.62255252064306177 ) ) ;
#28478=CARTESIAN_POINT ( 'NONE',  ( 17.84579744522521239, 1.849003904486290484, -13.87736309738764540 ) ) ;
#28479=CARTESIAN_POINT ( 'NONE',  ( 18.03457482787555577, 0.4008908244826864808, -12.69148415474307789 ) ) ;
#28481=EDGE_LOOP ( 'NONE', ( #5338, #24481, #5173, #63250 ) ) ;
#28483=CARTESIAN_POINT ( 'NONE',  ( 18.08141525686298579, -2.837131573376346694, -13.59610056796362088 ) ) ;
#28489=CARTESIAN_POINT ( 'NONE',  ( 18.20581337561481305, -2.797825772877925221, -12.28545032770987255 ) ) ;
#28504=CARTESIAN_POINT ( 'NONE',  ( 12.70235978774137919, 3.116847232384802435, -13.52309701207074433 ) ) ;
#28507=CARTESIAN_POINT ( 'NONE',  ( 18.05092994784023830, 0.3809766167652354207, 13.89298487834589402 ) ) ;
#28509=B_SPLINE_CURVE_WITH_KNOTS ( 'NONE', 1,
 ( #18354, #33747 ),
 .UNSPECIFIED., .F., .F.,
 ( 2, 2 ),
 ( 0.000000000000000000, 1.000000000000000000 ),
 .UNSPECIFIED. ) ;
#28511=ORIENTED_EDGE ( 'NONE', *, *, #24662, .T. ) ;
#28513=CARTESIAN_POINT ( 'NONE',  ( 12.40587428659213387, -0.4809231526391881117, 13.88880064789875668 ) ) ;
#28514=CARTESIAN_POINT ( 'NONE',  ( 12.34511315269137199, -0.4233056299066826345, -13.89132630015665448 ) ) ;
#28516=CARTESIAN_POINT ( 'NONE',  ( 17.55505043854147118, -1.875000000000000000, -25.00000000000000000 ) ) ;
#28526=B_SPLINE_CURVE_WITH_KNOTS ( 'NONE', 1,
 ( #43218, #40060 ),
 .UNSPECIFIED., .F., .F.,
 ( 2, 2 ),
 ( 0.000000000000000000, 1.000000000000000000 ),
 .UNSPECIFIED. ) ;
#28527=CARTESIAN_POINT ( 'NONE',  ( 18.01167108103433279, 0.4268810874232056851, 12.69034564040269331 ) ) ;
#28529=CARTESIAN_POINT ( 'NONE',  ( 18.10295792975328411, -2.800845226996505399, -12.37636719702903676 ) ) ;
#28543=CARTESIAN_POINT ( 'NONE',  ( 12.28357442006479872, 0.4998493492227008006, -12.59008424712974872 ) ) ;
#28552=CYLINDRICAL_SURFACE ( 'NONE', #874, 0.6250000000000005551 ) ;
#28559=CARTESIAN_POINT ( 'NONE',  ( 18.15913552218862037, 0.1616183441363971129, -13.89875400931294180 ) ) ;
#28565=CARTESIAN_POINT ( 'NONE',  ( 18.16752965499882677, -2.624502286956208685, 12.42171427751213919 ) ) ;
#28568=CARTESIAN_POINT ( 'NONE',  ( 12.52739587006843358, -3.060316261558335693, -13.53846823646701125 ) ) ;
#28581=CARTESIAN_POINT ( 'NONE',  ( 17.71812653075902944, -3.103437839927554176, 12.29028812931824000 ) ) ;
#28613=CARTESIAN_POINT ( 'NONE',  ( 18.27051424461482654, 2.638143613628436412, 13.74920933505747556 ) ) ;
#28625=CARTESIAN_POINT ( 'NONE',  ( 17.72083032727078233, -3.229203862303416717, -13.62249117442682333 ) ) ;
#28643=ORIENTED_EDGE ( 'NONE', *, *, #10664, .F. ) ;
#28649=CARTESIAN_POINT ( 'NONE',  ( 12.72249460523637410, 1.880133632676046718, -12.57461455596142841 ) ) ;
#28657=CARTESIAN_POINT ( 'NONE',  ( 12.43868857148329177, -1.859375588728228390, -12.46205283878465053 ) ) ;
#28663=CARTESIAN_POINT ( 'NONE',  ( 12.23542143184363695, -2.757395375068925958, -13.61543998564092028 ) ) ;
#28664=CARTESIAN_POINT ( 'NONE',  ( 18.06882650195508333, 0.3560396104572006726, -12.69328656575056691 ) ) ;
#28667=EDGE_CURVE ( 'NONE', #24349, #41143, #5152, .T. ) ;
#28669=EDGE_CURVE ( 'NONE', #55276, #56202, #5732, .T. ) ;
#28675=CARTESIAN_POINT ( 'NONE',  ( 17.92180752009628009, 1.993817408553323789, 12.55519104945816977 ) ) ;
#28682=CARTESIAN_POINT ( 'NONE',  ( 12.26933621011917275, -2.178034692540640638, 12.52080028461861794 ) ) ;
#28686=LINE ( 'NONE', #7696, #30966 ) ;
#28689=EDGE_CURVE ( 'NONE', #66385, #57125, #38465, .T. ) ;
#28691=CARTESIAN_POINT ( 'NONE',  ( 12.67437701660358762, -0.7076089047904881024, 12.58011506138061009 ) ) ;
#28694=CARTESIAN_POINT ( 'NONE',  ( 12.37468788209170611, 2.046657606614539215, 12.54569895759544984 ) ) ;
#28700=CARTESIAN_POINT ( 'NONE',  ( 17.93439305966544950, -0.4967428619541083279, 12.68692192486686743 ) ) ;
#28707=CARTESIAN_POINT ( 'NONE',  ( 17.81487012555341209, -3.068783844980979669, 13.53623303301404590 ) ) ;
#28709=CARTESIAN_POINT ( 'NONE',  ( 12.09654996457813603, -2.673023974430121630, 13.74245554503370492 ) ) ;
#28716=CARTESIAN_POINT ( 'NONE',  ( 17.72013721789504714, 1.891648809754047367, -13.78386988243240907 ) ) ;
#28722=CARTESIAN_POINT ( 'NONE',  ( 18.11306383842991252, 2.218305400803588512, -12.51277866499342650 ) ) ;
#28733=CARTESIAN_POINT ( 'NONE',  ( 12.19311196923565710, -2.627115700264358367, 12.42106741838665585 ) ) ;
#28738=CARTESIAN_POINT ( 'NONE',  ( 18.08776130068898524, -2.172968270232229493, 13.73740491327006197 ) ) ;
#28751=CARTESIAN_POINT ( 'NONE',  ( 17.55505043854147118, -3.125000000000000000, 13.52084414783465682 ) ) ;
#28754=EDGE_CURVE ( 'NONE', #21149, #45407, #41604, .T. ) ;
#28763=CARTESIAN_POINT ( 'NONE',  ( 12.18472169747684575, 2.421093590824782815, 13.68984525495557314 ) ) ;
#28767=CARTESIAN_POINT ( 'NONE',  ( 12.52839348839893674, -0.5608030988280898743, 13.88477341743901938 ) ) ;
#28779=DIRECTION ( 'NONE',  ( 1.000000000000000000, 0.000000000000000000, 0.000000000000000000 ) ) ;
#28780=DIRECTION ( 'NONE',  ( 0.000000000000000000, 1.000000000000000000, 0.000000000000000000 ) ) ;
#28781=VECTOR ( 'NONE', #8299, 1000.000000000000000 ) ;
#28785=CARTESIAN_POINT ( 'NONE',  ( 12.15889392806725056, 0.3761765224702128263, 12.59508068833789451 ) ) ;
#28792=VECTOR ( 'NONE', #17974, 1000.000000000000000 ) ;
#28797=B_SPLINE_CURVE_WITH_KNOTS ( 'NONE', 3,
 ( #15783, #48284, #37113, #390, #63317, #58427, #42700, #32223, #64695, #11221, #16462, #16804, #37794, #9846, #7013, #39177, #17509, #12264, #12609, #55609, #54212, #60500, #2124, #7355, #45120, #28700, #43738, #6312, #59458, #18201, #33940, #49664, #17151, #7710, #29049, #55261, #27658, #50015, #1084, #38483, #33593, #23443 ),
 .UNSPECIFIED., .F., .F.,
 ( 4, 2, 2, 2, 2, 2, 2, 2, 2, 2, 2, 2, 2, 1, 2, 2, 2, 2, 2, 1, 2, 4 ),
 ( 0.4997863768847483068, 0.5623130797741622278, 0.6248397826635760932, 0.6404714583859291155, 0.6561031341082821378, 0.6873664855529879603, 0.7029981612753410936, 0.7186298369976940048, 0.7264456748588704604, 0.7342615127200470271, 0.7498931884424000494, 0.7811565398871087584, 0.7889723777482845479, 0.7967882156094603374, 0.8124198913318116944, 0.8280515670541630513, 0.8436832427765145193, 0.8749465942212126812, 0.8905782699435618177, 0.9062099456659109542, 0.9374732971106091162, 1.000000000000000000 ),
 .UNSPECIFIED. ) ;
#28818=CARTESIAN_POINT ( 'NONE',  ( 12.70954970454857502, -0.7242550212506043694, -13.98125389334239443 ) ) ;
#28823=LINE ( 'NONE', #2572, #19494 ) ;
#28826=CARTESIAN_POINT ( 'NONE',  ( 17.88894803995536975, 3.166162608671027723, -13.63728156593011498 ) ) ;
#28827=EDGE_LOOP ( 'NONE', ( #14518, #44334, #17894, #29880 ) ) ;
#28834=CARTESIAN_POINT ( 'NONE',  ( 18.06844660307443817, 0.3566172609805220994, -12.69326555881922047 ) ) ;
#28839=CARTESIAN_POINT ( 'NONE',  ( 18.09719409069527885, -2.811143122832467700, -13.60247644589073879 ) ) ;
#28845=ADVANCED_FACE ( 'NONE', ( #3586 ), #13070, .F. ) ;
#28848=CARTESIAN_POINT ( 'NONE',  ( 18.06139486453147569, -2.995281757671043987, -12.23880324656448870 ) ) ;
#28859=CARTESIAN_POINT ( 'NONE',  ( 12.15817878876224434, 2.188143349582272634, -13.82794795582454483 ) ) ;
#28864=CARTESIAN_POINT ( 'NONE',  ( 18.05115593671926533, -0.5330308249010320409, 13.98985951701901520 ) ) ;
#28865=CARTESIAN_POINT ( 'NONE',  ( 17.94293712292327925, 0.4901002083121274722, 13.88836944287485586 ) ) ;
#28869=CARTESIAN_POINT ( 'NONE',  ( 12.53102142821679976, -0.5618070541888602332, 13.88471645277480171 ) ) ;
#28870=CARTESIAN_POINT ( 'NONE',  ( 12.21880568483910245, -2.282463263798835129, 13.71720984526819009 ) ) ;
#28882=CARTESIAN_POINT ( 'NONE',  ( 12.27274573047528072, -0.3283020094990616311, 12.69430739907260630 ) ) ;
#28884=CARTESIAN_POINT ( 'NONE',  ( 17.93744643711337972, -2.994789699036757735, -12.32241545780482816 ) ) ;
#28889=CARTESIAN_POINT ( 'NONE',  ( 12.39809172042342311, -2.025537470422473785, 13.76271392731540821 ) ) ;
#28898=CARTESIAN_POINT ( 'NONE',  ( 12.12656756701885641, -0.2537702651956292854, -12.59744904646397679 ) ) ;
#28911=ORIENTED_EDGE ( 'NONE', *, *, #23539, .T. ) ;
#28916=CARTESIAN_POINT ( 'NONE',  ( 18.21574553171934596, 0.3008963210924943121, -13.99677033988233354 ) ) ;
#28917=EDGE_LOOP ( 'NONE', ( #6700, #3096, #20577, #31578 ) ) ;
#28922=CARTESIAN_POINT ( 'NONE',  ( 18.15015087270999672, -2.691082634310324462, 12.40501869838522708 ) ) ;
#28923=ORIENTED_EDGE ( 'NONE', *, *, #52011, .T. ) ;
#28928=DIRECTION ( 'NONE',  ( 1.000000000000000000, 0.000000000000000000, 0.000000000000000000 ) ) ;
#28937=CARTESIAN_POINT ( 'NONE',  ( 12.37737328439355089, -0.4562271229319654342, -13.88993195058941410 ) ) ;
#28938=CARTESIAN_POINT ( 'NONE',  ( 17.77951638133176360, -1.796077334879284892, 12.47133186514445491 ) ) ;
#28961=CARTESIAN_POINT ( 'NONE',  ( 17.74252821691605320, -0.6952251598378670350, 12.58080715426405938 ) ) ;
#28967=CARTESIAN_POINT ( 'NONE',  ( 18.25201697486997432, 2.719281809836141317, 13.73337690942506129 ) ) ;
#28970=VERTEX_POINT ( 'NONE', #14443 ) ;
#28982=ORIENTED_EDGE ( 'NONE', *, *, #13827, .F. ) ;
#28984=EDGE_CURVE ( 'NONE', #59995, #17996, #60531, .T. ) ;
#29001=CARTESIAN_POINT ( 'NONE',  ( 12.54459593125679362, 1.931762302728656788, -12.56598641381995307 ) ) ;
#29013=CARTESIAN_POINT ( 'NONE',  ( 12.15236716622355750, -2.166683524422402751, -12.41231652552486864 ) ) ;
#29018=LINE ( 'NONE', #50325, #66550 ) ;
#29019=CARTESIAN_POINT ( 'NONE',  ( 12.34730967147305591, -2.925678532231709816, -13.57385403034849425 ) ) ;
#29020=CARTESIAN_POINT ( 'NONE',  ( 18.12876220047771270, -0.2481623978058161428, -12.69674179789669211 ) ) ;
#29028=CARTESIAN_POINT ( 'NONE',  ( 17.94092590763757755, 3.089486433945234811, 12.21536380989863702 ) ) ;
#29035=CARTESIAN_POINT ( 'NONE',  ( 12.46375379917807713, -1.976313547018314631, 12.55830662486076932 ) ) ;
#29038=DIRECTION ( 'NONE',  ( -1.000000000000000000, 0.000000000000000000, 0.000000000000000000 ) ) ;
#29040=CARTESIAN_POINT ( 'NONE',  ( 12.74530398939900167, -0.7169431667913570561, 12.57958639523259414 ) ) ;
#29048=CARTESIAN_POINT ( 'NONE',  ( 5.500000000000000000, -12.22296174243999900, -3.800101973039000214 ) ) ;
#29049=CARTESIAN_POINT ( 'NONE',  ( 17.78594645489210890, -0.5808586469551295650, 12.68211397078189862 ) ) ;
#29055=CARTESIAN_POINT ( 'NONE',  ( 17.96717518460240726, -0.4698982327886221944, -12.68829846777228632 ) ) ;
#29060=CARTESIAN_POINT ( 'NONE',  ( 17.55505043854147118, -1.874999999999999556, -13.78627172894481845 ) ) ;
#29069=CARTESIAN_POINT ( 'NONE',  ( 18.09739622855035890, 2.188708726545602001, -13.73458559204160423 ) ) ;
#29072=ORIENTED_EDGE ( 'NONE', *, *, #36220, .T. ) ;
#29081=CARTESIAN_POINT ( 'NONE',  ( 12.27407495020797334, -2.829836729544706664, 12.36860105340724658 ) ) ;
#29085=CARTESIAN_POINT ( 'NONE',  ( 17.84567419427294155, -3.186977498899958849, 13.63243182350604243 ) ) ;
#29097=FACE_OUTER_BOUND ( 'NONE', #35097, .T. ) ;
#29104=DIRECTION ( 'NONE',  ( 0.000000000000000000, -1.000000000000000000, 0.000000000000000000 ) ) ;
#29109=CARTESIAN_POINT ( 'NONE',  ( 12.80505043854143210, 3.248147246781388109, 13.61798588129781074 ) ) ;
#29111=ORIENTED_EDGE ( 'NONE', *, *, #3016, .F. ) ;
#29112=CARTESIAN_POINT ( 'NONE',  ( 12.35320888716225518, 0.4320279635882856573, -12.69011309768868934 ) ) ;
#29113=CARTESIAN_POINT ( 'NONE',  ( 12.64343601369307279, -0.6040897852209341501, 13.88232707694115398 ) ) ;
#29156=CARTESIAN_POINT ( 'NONE',  ( 17.60411830284828483, 1.787854822559049595, -13.88537270421502612 ) ) ;
#29157=CARTESIAN_POINT ( 'NONE',  ( 12.42135566322309081, -0.6200266137005091549, -13.98626978124057629 ) ) ;
#29158=LINE ( 'NONE', #7465, #42185 ) ;
#29162=CARTESIAN_POINT ( 'NONE',  ( 5.610802430945667219, 12.12319474034293521, -3.747515530460208133 ) ) ;
#29163=VERTEX_POINT ( 'NONE', #19949 ) ;
#29165=CARTESIAN_POINT ( 'NONE',  ( 17.75752317324808160, 1.908613644657472408, -13.78124409819558949 ) ) ;
#29173=CARTESIAN_POINT ( 'NONE',  ( 17.96217742567913334, 0.4744044024703746310, -12.68807559258215711 ) ) ;
#29178=CARTESIAN_POINT ( 'NONE',  ( 18.15005478421819518, -2.691381137285254965, -13.63095209222209903 ) ) ;
#29179=ORIENTED_EDGE ( 'NONE', *, *, #55982, .F. ) ;
#29184=CARTESIAN_POINT ( 'NONE',  ( 18.27150181675466811, -2.367044107065576775, -12.37568780170008509 ) ) ;
#29194=CARTESIAN_POINT ( 'NONE',  ( 12.80505043854143388, 3.207073286498425269, -13.58561123731972131 ) ) ;
#29195=CARTESIAN_POINT ( 'NONE',  ( 12.48231810865423874, 3.171873548221313843, -13.63595416837495300 ) ) ;
#29198=CARTESIAN_POINT ( 'NONE',  ( 17.65691712177036621, 0.6169787192598746861, 13.88156336867697149 ) ) ;
#29207=CARTESIAN_POINT ( 'NONE',  ( 12.80505043854146940, -1.875000000000000444, 13.78631952119025605 ) ) ;
#29218=CARTESIAN_POINT ( 'NONE',  ( 17.99001832964330916, 0.4489258298041814421, 12.68932177688764362 ) ) ;
#29219=CARTESIAN_POINT ( 'NONE',  ( 12.53084373025215648, -0.5620101268951274154, 12.68326259363504960 ) ) ;
#29227=B_SPLINE_CURVE_WITH_KNOTS ( 'NONE', 3,
 ( #29207, #29903, #24290, #61352, #8212, #66588, #13127, #19040, #61010, #46307, #19384, #28870, #19733, #50516, #66245, #18367, #2281, #13472, #45627, #23597, #61690, #24974, #60661, #34455, #7871, #23949, #35137, #2617, #34792, #12776, #34105, #7515, #56103, #14151, #29561, #45283, #66930, #35479, #55769, #18708, #40369, #56800, #56450, #55422, #8555, #51208, #50178, #8897, #30236, #44940, #39689, #4325, #36152, #48019, #31948, #120, #21106, #31260, #53265, #20414, #52922, #41742, #57815, #46993, #62709, #68642, #41403 ),
 .UNSPECIFIED., .F., .F.,
 ( 4, 2, 2, 2, 2, 2, 2, 2, 2, 2, 2, 2, 2, 2, 1, 1, 1, 2, 2, 2, 2, 2, 2, 2, 2, 2, 2, 2, 2, 2, 2, 2, 2, 2, 4 ),
 ( 0.000000000000000000, 0.1250000000000047740, 0.2500000000000094369, 0.3125000000000108247, 0.3437500000000110467, 0.3750000000000113243, 0.4062500000000115463, 0.4218750000000118239, 0.4375000000000121014, 0.4687500000000127121, 0.4843750000000134892, 0.5000000000000142109, 0.5156250000000149880, 0.5312500000000157652, 0.5468750000000164313, 0.5546875000000169864, 0.5585937500000174305, 0.5605468750000180966, 0.5625000000000186517, 0.5781250000000179856, 0.5859375000000167644, 0.5898437500000160982, 0.5937500000000154321, 0.6093750000000172085, 0.6171875000000173195, 0.6250000000000175415, 0.6406250000000172085, 0.6562500000000169864, 0.6718750000000166533, 0.6875000000000163203, 0.7187500000000149880, 0.7343750000000135447, 0.7500000000000119904, 0.8750000000000059952, 1.000000000000000000 ),
 .UNSPECIFIED. ) ;
#29231=DIRECTION ( 'NONE',  ( -0.000000000000000000, -0.000000000000000000, 1.000000000000000000 ) ) ;
#29234=CARTESIAN_POINT ( 'NONE',  ( 12.66323998097239922, -0.6090396975623090237, -12.68033511803396252 ) ) ;
#29248=ORIENTED_EDGE ( 'NONE', *, *, #36220, .F. ) ;
#29254=CARTESIAN_POINT ( 'NONE',  ( 18.20015658150182958, 0.3334496638227510412, -13.99603244703262739 ) ) ;
#29266=CARTESIAN_POINT ( 'NONE',  ( 12.75534451565735417, -1.787855198891555641, 13.88537265576021262 ) ) ;
#29273=CARTESIAN_POINT ( 'NONE',  ( 12.18201982513761550, -0.05063168410658510504, -13.89988098555964946 ) ) ;
#29274=CARTESIAN_POINT ( 'NONE',  ( 18.17988829291491371, -2.482516021556980590, 12.45565317647434611 ) ) ;
#29275=ORIENTED_EDGE ( 'NONE', *, *, #8235, .F. ) ;
#29297=DIRECTION ( 'NONE',  ( -1.000000000000000000, 0.000000000000000000, 0.000000000000000000 ) ) ;
#29300=CARTESIAN_POINT ( 'NONE',  ( 18.26112048795754106, -0.1637242582067935659, 12.59894148523291157 ) ) ;
#29302=CARTESIAN_POINT ( 'NONE',  ( 5.500000000000000000, -12.22293997673000021, 3.800173559041999827 ) ) ;
#29306=CARTESIAN_POINT ( 'NONE',  ( 17.94133460182552753, 1.899620958390740855, 13.87053073593715169 ) ) ;
#29321=CARTESIAN_POINT ( 'NONE',  ( 12.80505043854143210, 3.248147246781388553, 13.61798588129781251 ) ) ;
#29341=CARTESIAN_POINT ( 'NONE',  ( 12.20998423544383904, 2.691370015539682026, -12.40494896326797303 ) ) ;
#29352=CARTESIAN_POINT ( 'NONE',  ( 12.09087492024913679, -2.355317862440514887, -12.37790828721919212 ) ) ;
#29365=( LENGTH_UNIT ( ) NAMED_UNIT ( * ) SI_UNIT ( .MILLI., .METRE. ) );
#29367=CARTESIAN_POINT ( 'NONE',  ( 18.08671416524397912, 2.828730077974936030, 13.59817001273920489 ) ) ;
#29369=CARTESIAN_POINT ( 'NONE',  ( 17.74302412089499015, 1.903914349118853488, 12.57063651914289437 ) ) ;
#29377=CARTESIAN_POINT ( 'NONE',  ( 12.19547854351947080, -2.361608046327441812, 12.48276200957626081 ) ) ;
#29385=CARTESIAN_POINT ( 'NONE',  ( 12.19008233596125379, 0.1120021961262550880, 12.69934078656687682 ) ) ;
#29389=CARTESIAN_POINT ( 'NONE',  ( 12.18490839767382816, 2.421563015655831652, 12.46949130182971821 ) ) ;
#29393=EDGE_CURVE ( 'NONE', #23992, #26199, #49546, .T. ) ;
#29405=CARTESIAN_POINT ( 'NONE',  ( 18.01231764196698748, -2.926478478965309105, 13.57371117741642408 ) ) ;
#29409=CARTESIAN_POINT ( 'NONE',  ( 12.48231810865427249, -3.171873548221312067, 13.63595416837495122 ) ) ;
#29417=CARTESIAN_POINT ( 'NONE',  ( 17.80428097309404833, -0.5732560958719012945, 13.88408533439657511 ) ) ;
#29430=CARTESIAN_POINT ( 'NONE',  ( 12.18396690407210770, -2.429413046053483960, 12.46775848779559759 ) ) ;
#29435=CARTESIAN_POINT ( 'NONE',  ( 17.83362577474381183, -1.940423258991959665, 13.77633750067930407 ) ) ;
#29446=CARTESIAN_POINT ( 'NONE',  ( 17.74252821691605675, 0.6952251598378719200, -12.58080715426406293 ) ) ;
#29458=CARTESIAN_POINT ( 'NONE',  ( 12.51733672169663869, 1.945066915100360116, 13.77556489992940847 ) ) ;
#29460=ORIENTED_EDGE ( 'NONE', *, *, #14445, .F. ) ;
#29461=CARTESIAN_POINT ( 'NONE',  ( 12.44983299083951600, 0.5143225249093883455, -12.68597987476780276 ) ) ;
#29464=CARTESIAN_POINT ( 'NONE',  ( 12.47502503668309615, -0.5311540453515625204, 13.88634387573209139 ) ) ;
#29465=EDGE_CURVE ( 'NONE', #51860, #46362, #49483, .T. ) ;
#29476=CARTESIAN_POINT ( 'NONE',  ( 21.59999953993000332, -1.509903313490000218E-14, 4.329869796037999436E-14 ) ) ;
#29479=VECTOR ( 'NONE', #2618, 1000.000000000000227 ) ;
#29484=CARTESIAN_POINT ( 'NONE',  ( 12.18782402014237753, 2.399945986244715446, 12.47432385254658804 ) ) ;
#29487=VECTOR ( 'NONE', #35130, 1000.000000000000000 ) ;
#29500=CARTESIAN_POINT ( 'NONE',  ( 18.23564136049837003, 2.231667926091399412, -12.40079771041855849 ) ) ;
#29504=CARTESIAN_POINT ( 'NONE',  ( 12.22445506991028807, 2.731418686063790791, -13.62164890390593008 ) ) ;
#29511=CARTESIAN_POINT ( 'NONE',  ( 12.22921562908470072, -0.4443071882833348196, -13.99296005428181466 ) ) ;
#29521=CARTESIAN_POINT ( 'NONE',  ( 17.59651827076216080, 1.876037923068245794, -13.78616466676677632 ) ) ;
#29530=EDGE_LOOP ( 'NONE', ( #66596, #64945, #14028, #46113 ) ) ;
#29534=ORIENTED_EDGE ( 'NONE', *, *, #20628, .F. ) ;
#29540=CARTESIAN_POINT ( 'NONE',  ( 18.25660817874747721, -2.298073654326284299, -12.38866391276717316 ) ) ;
#29541=DIRECTION ( 'NONE',  ( 0.000000000000000000, -0.9586353287323918781, 0.2846371488511973413 ) ) ;
#29548=EDGE_LOOP ( 'NONE', ( #52627, #46515, #67520, #12269 ) ) ;
#29549=DIRECTION ( 'NONE',  ( 1.000000000000000000, 0.000000000000000000, 0.000000000000000000 ) ) ;
#29552=CARTESIAN_POINT ( 'NONE',  ( 12.14421144042236378, 2.819066901275890213, -13.71325475029871299 ) ) ;
#29555=PLANE ( 'NONE',  #52913 ) ;
#29561=CARTESIAN_POINT ( 'NONE',  ( 12.19234151475259864, -2.623341432797029693, 13.64652576243516968 ) ) ;
#29571=CARTESIAN_POINT ( 'NONE',  ( 12.15888864290852389, -0.3818843736424570312, 13.99543728850611046 ) ) ;
#29573=CARTESIAN_POINT ( 'NONE',  ( 17.93599305328152482, 0.4959072410923922036, 12.68697406334525368 ) ) ;
#29574=CARTESIAN_POINT ( 'NONE',  ( 12.42340696056926852, -0.4949990737637007254, 12.68701406539598331 ) ) ;
#29575=CARTESIAN_POINT ( 'NONE',  ( 18.17603698667415202, -2.571536872247066174, -12.43461505417294077 ) ) ;
#29581=B_SPLINE_SURFACE_WITH_KNOTS ( 'NONE', 1, 3, ( 
 ( #10481, #21317, #41960, #68859, #53482, #32169, #31474, #31819, #48582, #42646, #63266, #36722, #16067, #4888, #337, #48231, #52445, #21654, #26229, #5575, #68511, #37400, #32504, #26916, #53138, #16751, #58042, #25879, #42316, #47558, #42987, #64296, #16410, #37741, #59068, #15735, #20981, #38079, #5916, #27408, #27258, #686, #21998, #47900, #43341, #5238, #26578, #63957, #31143, #20634, #64645, #58721, #9792, #4539, #47209, #10143, #52796, #6614, #39127, #17811, #18152, #28292, #65338, #59405, #38429, #12213, #18498, #50310, #11504, #2409, #32849, #55207, #17097, #64982, #34236, #44035, #59753, #22348, #54161, #17457, #49263, #60453, #49959, #54513, #6961, #38782, #60795, #49612, #22691, #27952, #11855, #6261, #12908, #12558, #33194, #1373, #60109, #33890, #33543, #27599, #65688, #1719, #48929, #54859 ),
 ( #1035, #7307, #55555, #28649, #23038, #66374, #43686, #44388, #2073, #23391, #44731, #66028, #39473, #7654, #29001, #23732, #45070, #46780, #62499, #30034, #41194, #62163, #51671, #8686, #40840, #19172, #13941, #56241, #61143, #50653, #52008, #45752, #8347, #14622, #40496, #3767, #39823, #29693, #19520, #67399, #67739, #51336, #67062, #13261, #18843, #61823, #68084, #30698, #34585, #4111, #55901, #35611, #19862, #25447, #14284, #61484, #8005, #24428, #56924, #66723, #35941, #29341, #2753, #3430, #30363, #13603, #9023, #46437, #57254, #50994, #9355, #25105, #35267, #3092, #24766, #24077, #46091, #45414, #40169, #34924, #56584, #256, #58636, #37317, #10740, #36633, #5154, #58989, #15986, #20200, #20893, #47469, #14959, #32086, #52706, #15308, #27176, #42909, #10397, #21571, #42564, #53402, #58292, #21233 ) ),
 .UNSPECIFIED., .F., .F., .F.,
 ( 2, 2 ),
 ( 4, 2, 2, 2, 2, 2, 2, 2, 2, 2, 2, 2, 2, 2, 2, 2, 2, 2, 2, 2, 2, 2, 2, 2, 2, 2, 2, 2, 2, 2, 2, 2, 2, 2, 2, 2, 2, 2, 2, 2, 2, 2, 2, 2, 2, 2, 2, 2, 2, 2, 2, 4 ),
 ( 0.000000000000000000, 1.000000000000000000 ),
 ( 0.000000000000000000, 7.157624699936004573E-05, 0.0001431524939987200915, 0.0002147287409980801372, 0.0002326228027479201486, 0.0002505168644977601600, 0.0002863049879974401829, 0.0003220931114971202058, 0.0003578812349968002286, 0.0003936693584964802515, 0.0004294574819961602744, 0.0004652456054958402972, 0.0005010337289955203201, 0.0005368218524952003429, 0.0005726099759948803658, 0.0006441862229942404115, 0.0006799743464939204344, 0.0007157624699936004573, 0.0007336565317434404687, 0.0007515505934932804801, 0.0007873387169929605030, 0.0008589149639923205487, 0.0008947030874920005716, 0.0009304912109916805944, 0.0009662793344913606173, 0.001002067457991040640, 0.001073643704990400686, 0.001145219951989760732, 0.001216796198989120777, 0.001288372445988480823, 0.001359948692987840869, 0.001395736816487520892, 0.001431524939987200915, 0.001467313063486880937, 0.001503101186986560960, 0.001574677433985921006, 0.001646253680985281052, 0.001682041804484961075, 0.001717829927984641097, 0.001735723989734481217, 0.001753618051484321120, 0.001789406174984001143, 0.001860982421983361189, 0.001896770545483041212, 0.001932558668982721235, 0.001968346792482401041, 0.001986240854232241160, 0.002004134915982081280, 0.002075711162981441326, 0.002147287409980801372, 0.002218863656980161417, 0.002290439903979521463 ),
 .UNSPECIFIED. ) ;
#29586=CARTESIAN_POINT ( 'NONE',  ( 12.48372201234962731, 0.6448943924266595795, -12.58348668657565739 ) ) ;
#29596=CARTESIAN_POINT ( 'NONE',  ( 17.55505043854143565, 3.125000000000000000, -25.00000000000000000 ) ) ;
#29604=CARTESIAN_POINT ( 'NONE',  ( 18.27044831935229752, -0.1190513140356078692, -13.99949878896183719 ) ) ;
#29614=CARTESIAN_POINT ( 'NONE',  ( 12.29692076505851972, -2.864061239596868536, -13.58942221846003484 ) ) ;
#29624=CARTESIAN_POINT ( 'NONE',  ( 12.18829585510503399, -0.1017048024283968843, -13.89950429703523938 ) ) ;
#29625=CARTESIAN_POINT ( 'NONE',  ( 18.01444767332564112, -2.076107767824256989, 12.54031350746514129 ) ) ;
#29632=CARTESIAN_POINT ( 'NONE',  ( 18.17227403027676758, 2.399493853270739496, 13.69423063307216282 ) ) ;
#29650=CIRCLE ( 'NONE', #49690, 13.17499999999999538 ) ;
#29658=CARTESIAN_POINT ( 'NONE',  ( 17.59651852071652556, 3.123961849275329161, 13.52107344427228952 ) ) ;
#29693=CARTESIAN_POINT ( 'NONE',  ( 12.27200335545529519, 2.173637791136409092, -12.52166559990193839 ) ) ;
#29702=CARTESIAN_POINT ( 'NONE',  ( 12.11481770488412657, -2.701029500518122184, -12.30709430042447750 ) ) ;
#29709=CARTESIAN_POINT ( 'NONE',  ( 12.30785086506347525, -2.879247442421006387, -13.58563033715519452 ) ) ;
#29710=CARTESIAN_POINT ( 'NONE',  ( 17.55505043854147118, -3.199698446519375850, -12.18695736643652694 ) ) ;
#29713=DIRECTION ( 'NONE',  ( -0.7071068219128313626, 0.000000000000000000, 0.7071067404602613404 ) ) ;
#29714=ORIENTED_EDGE ( 'NONE', *, *, #20932, .F. ) ;
#29717=CARTESIAN_POINT ( 'NONE',  ( 18.17920330502308701, 2.539026862123676231, 13.66507545609737662 ) ) ;
#29721=CARTESIAN_POINT ( 'NONE',  ( 17.99268395210757632, 2.053674450599853873, 12.54441556206896990 ) ) ;
#29722=DIRECTION ( 'NONE',  ( 0.000000000000000000, 0.000000000000000000, 1.000000000000000000 ) ) ;
#29726=CARTESIAN_POINT ( 'NONE',  ( 12.18088753964551429, -2.461875156572522094, 12.46041398465085948 ) ) ;
#29732=CARTESIAN_POINT ( 'NONE',  ( 12.44955242156041919, 0.5141503178158078891, 12.68598964581896738 ) ) ;
#29737=CARTESIAN_POINT ( 'NONE',  ( 12.70145053304001515, 1.883559157534606232, 12.57401126189226304 ) ) ;
#29749=CARTESIAN_POINT ( 'NONE',  ( 18.14037995566704708, -0.2193687868931910034, -12.69745523514908925 ) ) ;
#29753=CARTESIAN_POINT ( 'NONE',  ( 12.42020189403039154, -3.137187437229797649, 13.64398187047951794 ) ) ;
#29773=CARTESIAN_POINT ( 'NONE',  ( 17.83221471278436354, 0.5605600754933557361, -13.88478672247768664 ) ) ;
#29777=CARTESIAN_POINT ( 'NONE',  ( 12.47149800526937646, -3.028907606606671354, 12.31248708664185543 ) ) ;
#29781=CARTESIAN_POINT ( 'NONE',  ( 17.88735652878719051, -1.970265470216408410, 13.77164815731349989 ) ) ;
#29784=ORIENTED_EDGE ( 'NONE', *, *, #68328, .F. ) ;
#29787=DIRECTION ( 'NONE',  ( 1.000000000000000000, 0.000000000000000000, 0.000000000000000000 ) ) ;
#29793=CARTESIAN_POINT ( 'NONE',  ( 18.05935420056438900, 0.5168989769797246447, -12.58939571008426839 ) ) ;
#29797=EDGE_LOOP ( 'NONE', ( #59775, #29072, #2701, #55202 ) ) ;
#29803=CARTESIAN_POINT ( 'NONE',  ( 12.36142641661517239, 3.095968474608999710, 13.65339594101960863 ) ) ;
#29807=CARTESIAN_POINT ( 'NONE',  ( 12.58522439486011812, 0.5851582065079803385, -12.68184838022456340 ) ) ;
#29808=CARTESIAN_POINT ( 'NONE',  ( 12.49249577546344447, -0.5416168188285658269, 13.88579828294358798 ) ) ;
#29814=ADVANCED_FACE ( 'NONE', ( #61057 ), #68431, .F. ) ;
#29835=LINE ( 'NONE', #13738, #47783 ) ;
#29844=CARTESIAN_POINT ( 'NONE',  ( 17.84655355976681790, 1.821424963963778954, -12.46765546240475686 ) ) ;
#29851=CARTESIAN_POINT ( 'NONE',  ( 17.79083366723151727, 1.825854556024153474, -13.88043960113665953 ) ) ;
#29856=CARTESIAN_POINT ( 'NONE',  ( 17.72017830064981325, -1.875000000000000666, -13.78627079974488900 ) ) ;
#29860=ORIENTED_EDGE ( 'NONE', *, *, #47586, .F. ) ;
#29862=CARTESIAN_POINT ( 'NONE',  ( 17.99865897956989613, 3.095937021190220850, -13.65340307249647900 ) ) ;
#29869=DIRECTION ( 'NONE',  ( -1.000000000000000000, -0.000000000000000000, -0.000000000000000000 ) ) ;
#29880=ORIENTED_EDGE ( 'NONE', *, *, #11348, .T. ) ;
#29882=CARTESIAN_POINT ( 'NONE',  ( 17.84319482158669246, -1.945290144093657192, -12.56363827966045044 ) ) ;
#29893=CARTESIAN_POINT ( 'NONE',  ( 12.22896558337868989, 2.961354171198296914, -13.68321881638708604 ) ) ;
#29895=CARTESIAN_POINT ( 'NONE',  ( 18.27397574302396066, -0.09509187666555490859, 13.99968209810982600 ) ) ;
#29898=ORIENTED_EDGE ( 'NONE', *, *, #26917, .T. ) ;
#29903=CARTESIAN_POINT ( 'NONE',  ( 12.72228957555996942, -1.875000000000000666, 13.78631905550009407 ) ) ;
#29919=AXIS2_PLACEMENT_3D ( 'NONE', #49342, #22771, #28379 ) ;
#29921=VECTOR ( 'NONE', #3496, 1000.000000000000000 ) ;
#29925=CARTESIAN_POINT ( 'NONE',  ( 12.58477481432937672, -0.5849872192492366896, -12.68185863724643170 ) ) ;
#29934=EDGE_CURVE ( 'NONE', #57425, #7219, #63946, .T. ) ;
#29947=CARTESIAN_POINT ( 'NONE',  ( 17.81092223849609724, 0.6836428945794175149, -13.98330131869062321 ) ) ;
#29953=CARTESIAN_POINT ( 'NONE',  ( 17.77858768906186882, -3.083996659902246140, 12.29614209097516841 ) ) ;
#29963=CARTESIAN_POINT ( 'NONE',  ( 17.59562484679850058, 0.6250000000000004441, -13.88107975066922783 ) ) ;
#29968=CARTESIAN_POINT ( 'NONE',  ( 12.76382393867146092, -0.6239806250735595583, -13.88114166035887997 ) ) ;
#29969=CARTESIAN_POINT ( 'NONE',  ( 18.17584245753829464, -2.573100139072833414, 12.43426722069302315 ) ) ;
#29981=ORIENTED_EDGE ( 'NONE', *, *, #19396, .T. ) ;
#29989=CARTESIAN_POINT ( 'NONE',  ( 12.75598008710589326, 3.248071441111126667, -13.61800396221869214 ) ) ;
#29994=CARTESIAN_POINT ( 'NONE',  ( 18.14418133822493928, -0.4193891200559137222, 12.59302195412780456 ) ) ;
#30000=CARTESIAN_POINT ( 'NONE',  ( 18.13331639930710537, 2.076941473624324797, 13.84509535655099199 ) ) ;
#30002=LINE ( 'NONE', #67030, #3510 ) ;
#30034=CARTESIAN_POINT ( 'NONE',  ( 12.47240630447277709, 1.970775872724741973, -12.55927287175691198 ) ) ;
#30042=CARTESIAN_POINT ( 'NONE',  ( 12.07989974639902542, -2.471827770301485039, -12.35516928474874554 ) ) ;
#30049=CARTESIAN_POINT ( 'NONE',  ( 12.19562740135371470, -2.360953413553769309, -13.70191948036522156 ) ) ;
#30058=LINE ( 'NONE', #45436, #2629 ) ;
#30060=DIRECTION ( 'NONE',  ( 1.000000000000000000, 0.000000000000000000, 0.000000000000000000 ) ) ;
#30061=CARTESIAN_POINT ( 'NONE',  ( 18.03321709926671801, 2.902596714178123261, 12.34859794581418768 ) ) ;
#30066=CARTESIAN_POINT ( 'NONE',  ( 12.20882029558155502, -2.312280790556522359, 12.49335225873939059 ) ) ;
#30072=CARTESIAN_POINT ( 'NONE',  ( 12.54694134722857513, 0.5693054069933383143, 12.68281928773556366 ) ) ;
#30078=CARTESIAN_POINT ( 'NONE',  ( 12.42127013197880281, 2.006280959398175856, 12.55298695860708946 ) ) ;
#30089=CARTESIAN_POINT ( 'NONE',  ( 5.700000000000000178, 13.04986661130000059, -1.811520473896000016 ) ) ;
#30092=CARTESIAN_POINT ( 'NONE',  ( 17.83317199298538824, -3.060086213985775405, 13.53858764060002962 ) ) ;
#30103=CARTESIAN_POINT ( 'NONE',  ( 17.55505043854144276, -0.6250000000000001110, -25.00000000000000000 ) ) ;
#30119=CARTESIAN_POINT ( 'NONE',  ( 17.74479774746059846, -3.223061189501819523, 13.62394687717146802 ) ) ;
#30131=CARTESIAN_POINT ( 'NONE',  ( 18.25531039711340497, 0.1866745257715810569, -12.59862229962904401 ) ) ;
#30132=DIRECTION ( 'NONE',  ( -1.000000000000000000, 0.000000000000000000, 0.000000000000000000 ) ) ;
#30140=CARTESIAN_POINT ( 'NONE',  ( 12.14271297744733680, 2.220151667091618819, 13.82285866607422520 ) ) ;
#30142=EDGE_LOOP ( 'NONE', ( #5926, #36577, #30962, #11112, #14288, #16998, #62008 ) ) ;
#30143=CARTESIAN_POINT ( 'NONE',  ( 12.21931228143050774, 0.2190605494068694759, -12.69747807323824951 ) ) ;
#30165=CARTESIAN_POINT ( 'NONE',  ( 12.18035041863818790, 2.521826826515520370, 12.44645458618487588 ) ) ;
#30179=CARTESIAN_POINT ( 'NONE',  ( 18.27123885515668889, 2.366823750208064681, -12.37571350032474982 ) ) ;
#30182=CARTESIAN_POINT ( 'NONE',  ( 12.18135539521807509, 2.541609601666299678, -13.66455050632895585 ) ) ;
#30189=CARTESIAN_POINT ( 'NONE',  ( 18.17241432538235202, 2.400344151293695827, 12.47423995685674392 ) ) ;
#30195=CARTESIAN_POINT ( 'NONE',  ( 18.22053876895016344, 2.807780685761759987, -13.71555663160087235 ) ) ;
#30203=CARTESIAN_POINT ( 'NONE',  ( 21.35000154058000277, -1.509903258602878808E-14, 12.59999999999999964 ) ) ;
#30204=EDGE_CURVE ( 'NONE', #53074, #51860, #21531, .T. ) ;
#30214=CARTESIAN_POINT ( 'NONE',  ( 17.91340230256481547, -1.987833194700776795, -12.55624649895498024 ) ) ;
#30224=CARTESIAN_POINT ( 'NONE',  ( 12.30746066369761138, 3.049480053538142776, -13.66385627579028572 ) ) ;
#30226=LINE ( 'NONE', #13800, #29487 ) ;
#30236=CARTESIAN_POINT ( 'NONE',  ( 12.23181585140601868, -2.749296767780423867, 13.61742212735507351 ) ) ;
#30242=DIRECTION ( 'NONE',  ( -1.000000000000000000, 0.000000000000000000, 0.000000000000000000 ) ) ;
#30259=CARTESIAN_POINT ( 'NONE',  ( 12.53820945512841156, 0.6689034848678672152, -12.58223305319197749 ) ) ;
#30260=CARTESIAN_POINT ( 'NONE',  ( 12.18782402015739130, -2.399945986167177914, -12.47432385256424858 ) ) ;
#30263=LINE ( 'NONE', #7901, #58462 ) ;
#30272=MANIFOLD_SOLID_BREP ( 'Stock-MAS-678-1', #19146 ) ;
#30279=CARTESIAN_POINT ( 'NONE',  ( 18.17115727977514439, 0.3856318793703991665, -13.99470184309726051 ) ) ;
#30299=CARTESIAN_POINT ( 'NONE',  ( 12.27431752107753837, 0.3302328523437060848, -13.89472426752320899 ) ) ;
#30300=CARTESIAN_POINT ( 'NONE',  ( 18.17639191339637250, -2.431702999347771676, 12.46724561074273652 ) ) ;
#30323=CARTESIAN_POINT ( 'NONE',  ( 18.20009441896381119, 0.3284204639250540847, 12.59572022474404562 ) ) ;
#30363=CARTESIAN_POINT ( 'NONE',  ( 12.22356881520513561, 2.729361768173758751, -12.39519383931446228 ) ) ;
#30366=EDGE_LOOP ( 'NONE', ( #24883, #49375, #58483 ) ) ;
#30372=CARTESIAN_POINT ( 'NONE',  ( 12.44743307598047899, -3.012678875451597627, -12.31720924913609139 ) ) ;
#30378=CARTESIAN_POINT ( 'NONE',  ( 12.56988000877540301, -3.209076157321562484, -13.62724777954567124 ) ) ;
#30381=CARTESIAN_POINT ( 'NONE',  ( 17.60324894539392560, -3.198552395131814663, 12.18725844837784855 ) ) ;
#30384=CARTESIAN_POINT ( 'NONE',  ( 12.57118179864146157, 0.6928235585492461546, -13.98285841810701413 ) ) ;
#30387=CARTESIAN_POINT ( 'NONE',  ( 18.14649830791793406, 2.702104747329968859, 13.62846271467367920 ) ) ;
#30390=CARTESIAN_POINT ( 'NONE',  ( 18.17545025690710148, 2.421661855460688795, 12.46948612151124181 ) ) ;
#30398=ADVANCED_FACE ( 'NONE', ( #10834 ), #18388, .T. ) ;
#30404=CARTESIAN_POINT ( 'NONE',  ( 12.37030581721858269, 0.4491390935506875404, 12.68931154995401123 ) ) ;
#30426=CARTESIAN_POINT ( 'NONE',  ( 12.27426597077013604, -3.015840035300837663, 13.67132055224443654 ) ) ;
#30435=CARTESIAN_POINT ( 'NONE',  ( 18.04536508903462888, -0.3876148459371224764, 13.89272660623140787 ) ) ;
#30447=EDGE_LOOP ( 'NONE', ( #42232, #63783, #5856, #34119, #19161, #56946, #64202, #66637, #29898, #15228, #8036, #13634 ) ) ;
#30448=CARTESIAN_POINT ( 'NONE',  ( 18.24190944330475617, -2.752675741764516903, 13.72673684790926352 ) ) ;
#30461=CARTESIAN_POINT ( 'NONE',  ( 17.99148514253577602, 0.5743932053697992091, -12.58690132123599525 ) ) ;
#30470=CARTESIAN_POINT ( 'NONE',  ( 17.79602238657562907, 1.801771354310892859, 12.47051018296934011 ) ) ;
#30471=CARTESIAN_POINT ( 'NONE',  ( 12.41963733656421098, 3.136527823945737925, 13.64412816271520335 ) ) ;
#30473=ORIENTED_EDGE ( 'NONE', *, *, #4804, .F. ) ;
#30474=CARTESIAN_POINT ( 'NONE',  ( 12.19590851927750386, -0.1412562895450219513, -12.69896251113170749 ) ) ;
#30475=CARTESIAN_POINT ( 'NONE',  ( 12.54953656384602922, -0.6834693007276645416, 13.98330741474946137 ) ) ;
#30482=COLOUR_RGB ( '', 0.09019608, 0.27058824, 0.51372549) ;
#30494=CARTESIAN_POINT ( 'NONE',  ( 12.18137864099478129, 2.541952522782075174, 12.44169427841725017 ) ) ;
#30501=B_SPLINE_CURVE_WITH_KNOTS ( 'NONE', 3,
 ( #8088, #12296, #51080, #12640, #49696, #1805, #50047, #44474, #29777, #7739, #66460, #50737, #44812, #35011, #3183, #7045, #66114, #45153, #8431, #55293, #44123, #2835, #29081, #18922, #39556, #23123, #17893, #18581, #28380, #12995, #18235, #56327, #61228, #65420, #34668, #55641, #39210, #24161, #38870, #2156, #40247, #28733, #33970, #60191, #61567, #23473, #33628, #45497, #13682, #34319, #39909, #60880, #50392, #2492, #23816, #13344, #29430, #61909, #24511, #40928, #25189, #30785, #41616, #51418, #45832, #24852, #15397, #41277, #19256 ),
 .UNSPECIFIED., .F., .F.,
 ( 4, 2, 2, 2, 2, 2, 2, 2, 2, 2, 2, 2, 2, 1, 2, 2, 2, 1, 2, 2, 2, 2, 1, 2, 2, 2, 2, 2, 2, 2, 2, 2, 2, 2, 2, 4 ),
 ( 0.000000000000000000, 0.06249999999998720468, 0.1249999999999744094, 0.1562499999999680256, 0.1874999999999616140, 0.2187499999999552025, 0.2343749999999517886, 0.2499999999999483746, 0.2812499999999429900, 0.2968749999999389377, 0.3124999999999349409, 0.3281249999999308886, 0.3437499999999268363, 0.3593749999999228395, 0.3671874999999213407, 0.3749999999999198419, 0.3906249999999188427, 0.3984374999999183986, 0.4023437499999183986, 0.4062499999999184541, 0.4218749999999176215, 0.4296874999999177880, 0.4335937499999183431, 0.4355468749999186207, 0.4374999999999188427, 0.4531249999999202305, 0.4687499999999215627, 0.4843749999999229505, 0.4999999999999242828, 0.5312499999999269473, 0.5468749999999288347, 0.5624999999999306111, 0.5937499999999351630, 0.6249999999999397149, 0.7499999999999591438, 1.000000000000000000 ),
 .UNSPECIFIED. ) ;
#30505=DIRECTION ( 'NONE',  ( 1.000000000000000000, 0.000000000000000000, 0.000000000000000000 ) ) ;
#30512=CARTESIAN_POINT ( 'NONE',  ( 18.27818099403247132, 2.425134644239746340, -12.36441930324461858 ) ) ;
#30514=CARTESIAN_POINT ( 'NONE',  ( 18.16712151969790412, 2.626596269802297989, 12.42116978061485710 ) ) ;
#30517=CARTESIAN_POINT ( 'NONE',  ( 12.35418469965838995, 2.932966736137118335, -13.57204261866905526 ) ) ;
#30521=CARTESIAN_POINT ( 'NONE',  ( 12.35439258730998446, 0.5721320424853930664, -13.98830666644471421 ) ) ;
#30530=CARTESIAN_POINT ( 'NONE',  ( 18.27898184041757901, 2.472823623527002912, -13.77990254017907112 ) ) ;
#30548=CARTESIAN_POINT ( 'NONE',  ( 17.71825832218067731, -1.896331189961580455, -12.57190091395960252 ) ) ;
#30561=CARTESIAN_POINT ( 'NONE',  ( 18.10184288975604616, -2.186031417450792880, 12.51954808658139839 ) ) ;
#30580=CARTESIAN_POINT ( 'NONE',  ( 17.55505043854147118, -3.248109929747637903, 13.61799478206225444 ) ) ;
#30592=CARTESIAN_POINT ( 'NONE',  ( 12.80505043854144276, 0.7192913403693124152, -12.57945229203838267 ) ) ;
#30593=CARTESIAN_POINT ( 'NONE',  ( 12.20453436417063386, -2.673271222646852241, -12.40950569886774879 ) ) ;
#30597=EDGE_LOOP ( 'NONE', ( #21917, #17373, #46615, #41801 ) ) ;
#30600=CARTESIAN_POINT ( 'NONE',  ( 17.88388243132641975, 0.5319787655177421470, 12.68500714331677770 ) ) ;
#30610=CARTESIAN_POINT ( 'NONE',  ( 17.78802761781599884, -0.6915911779535856008, -13.98290807251246726 ) ) ;
#30619=CARTESIAN_POINT ( 'NONE',  ( 12.80505043854146940, -3.166036643249212634, 13.55322769257718996 ) ) ;
#30636=CARTESIAN_POINT ( 'NONE',  ( 18.09722825099193599, -2.811571021179180896, 12.37353494292366030 ) ) ;
#30637=EDGE_LOOP ( 'NONE', ( #45585, #34072, #61996, #68667 ) ) ;
#30654=CARTESIAN_POINT ( 'NONE',  ( 12.56916471290115922, 1.825881566112697696, -13.88043612360007550 ) ) ;
#30657=CARTESIAN_POINT ( 'NONE',  ( 12.80505043854146940, -3.199751711897561801, 12.18694338143115452 ) ) ;
#30658=EDGE_CURVE ( 'NONE', #42176, #38787, #11027, .T. ) ;
#30660=CARTESIAN_POINT ( 'NONE',  ( 18.05096829067922215, 0.5248261352964532778, 12.58906749861124119 ) ) ;
#30668=CARTESIAN_POINT ( 'NONE',  ( 18.00769469217370400, 3.088460579138320394, 13.65508963078420379 ) ) ;
#30671=VECTOR ( 'NONE', #58151, 1000.000000000000000 ) ;
#30684=DIRECTION ( 'NONE',  ( 0.9999999998140244317, 1.053700670848026541E-05, -1.615309289866040602E-05 ) ) ;
#30698=CARTESIAN_POINT ( 'NONE',  ( 12.20301641406251747, 2.331821773330017944, -12.48918929053769844 ) ) ;
#30705=CARTESIAN_POINT ( 'NONE',  ( 17.60358162559704454, -0.7192569394297189111, 12.57945425907933945 ) ) ;
#30709=CARTESIAN_POINT ( 'NONE',  ( 12.39079901834620223, -2.968443430305767627, -12.32999838110541191 ) ) ;
#30715=CARTESIAN_POINT ( 'NONE',  ( 12.60257768741567119, -1.908613650260962080, -13.78119617999061219 ) ) ;
#30721=LINE ( 'NONE', #57275, #7111 ) ;
#30722=ADVANCED_FACE ( 'NONE', ( #59249 ), #61375, .T. ) ;
#30725=CARTESIAN_POINT ( 'NONE',  ( 18.15949994872952900, 2.660112427294489379, 13.63815955491932641 ) ) ;
#30730=CARTESIAN_POINT ( 'NONE',  ( 18.12468263438040239, 2.757387671472310675, 12.38786642819432515 ) ) ;
#30736=CARTESIAN_POINT ( 'NONE',  ( 12.37600679962892158, -2.954502784796254833, 12.33399089453511621 ) ) ;
#30740=CARTESIAN_POINT ( 'NONE',  ( 4.599999999999999645, -1.760845406083394460, 12.47635457398814651 ) ) ;
#30743=CARTESIAN_POINT ( 'NONE',  ( 12.25134400021322456, -0.2899325138666248303, 12.69554708236671914 ) ) ;
#30744=CARTESIAN_POINT ( 'NONE',  ( 5.687176560462543939, -12.04993902413650453, -3.725892264570328738 ) ) ;
#30748=ORIENTED_EDGE ( 'NONE', *, *, #68903, .T. ) ;
#30758=CARTESIAN_POINT ( 'NONE',  ( 12.80505043854144276, 0.6249999999999994449, 12.67928921589117586 ) ) ;
#30764=CARTESIAN_POINT ( 'NONE',  ( 17.93834580300584847, -2.005905130196156350, -13.76587868752633170 ) ) ;
#30785=CARTESIAN_POINT ( 'NONE',  ( 12.20035750765565474, -2.340667166417027989, 12.48730567878010156 ) ) ;
#30794=SURFACE_SIDE_STYLE ('',( #68871 ) ) ;
#30800=CARTESIAN_POINT ( 'NONE',  ( 17.97714073376502242, 0.5849390254007825751, -12.58641711472857594 ) ) ;
#30803=FACE_OUTER_BOUND ( 'NONE', #23546, .T. ) ;
#30811=EDGE_CURVE ( 'NONE', #31059, #15974, #30721, .T. ) ;
#30812=CARTESIAN_POINT ( 'NONE',  ( 17.92061031166184293, 1.858910711595916920, 12.46212218156369111 ) ) ;
#30813=CARTESIAN_POINT ( 'NONE',  ( 12.35155033006829584, 1.948172666216917648, 13.86379038907994854 ) ) ;
#30830=CARTESIAN_POINT ( 'NONE',  ( 12.11312973616745303, 2.264845417406522898, 12.39478132878350358 ) ) ;
#30841=CARTESIAN_POINT ( 'NONE',  ( 12.32512882946257626, -0.4004146477438858542, 12.69150435581809688 ) ) ;
#30844=EDGE_CURVE ( 'NONE', #6933, #68711, #59440, .T. ) ;
#30848=CARTESIAN_POINT ( 'NONE',  ( 12.61254665343902026, -3.094705746550273862, 13.52917745889216761 ) ) ;
#30849=CARTESIAN_POINT ( 'NONE',  ( 12.27415370857974253, 2.829964016144990158, 13.59786649615043430 ) ) ;
#30856=CARTESIAN_POINT ( 'NONE',  ( 17.81516833538380951, 3.068391096118999517, -12.30080513712136003 ) ) ;
#30859=CARTESIAN_POINT ( 'NONE',  ( 17.96892410184997857, 2.968447989616221694, 12.32999203180360581 ) ) ;
#30861=CARTESIAN_POINT ( 'NONE',  ( 12.18865263575256641, 2.603587051988978995, -13.65094575294710211 ) ) ;
#30870=CARTESIAN_POINT ( 'NONE',  ( 17.88333207277291592, 1.943312949629576458, 12.56472734206311692 ) ) ;
#30875=EDGE_CURVE ( 'NONE', #35032, #53691, #30263, .T. ) ;
#30877=CARTESIAN_POINT ( 'NONE',  ( 18.24299778933909622, 2.286486205740245303, -13.81204233372297985 ) ) ;
#30883=DIRECTION ( 'NONE',  ( -0.000000000000000000, -0.000000000000000000, 1.000000000000000000 ) ) ;
#30884=DIRECTION ( 'NONE',  ( 1.000000000000000000, 0.000000000000000000, 0.000000000000000000 ) ) ;
#30894=CARTESIAN_POINT ( 'NONE',  ( 17.74512657133773175, -3.174942931788179212, -12.19343219266723466 ) ) ;
#30900=LINE ( 'NONE', #10942, #26977 ) ;
#30905=CARTESIAN_POINT ( 'NONE',  ( 17.87597250029675067, 0.6552116771452413113, 13.98466387211990458 ) ) ;
#30908=ORIENTED_EDGE ( 'NONE', *, *, #43836, .T. ) ;
#30911=CIRCLE ( 'NONE', #55471, 13.17499999999999538 ) ;
#30929=CONICAL_SURFACE ( 'NONE', #15305, 2.100041432634999428, 0.7853981633972997312 ) ;
#30931=CARTESIAN_POINT ( 'NONE',  ( 17.96886609968823834, 2.968499926956509327, -12.32999726799525142 ) ) ;
#30937=CARTESIAN_POINT ( 'NONE',  ( 18.20346453088224692, 2.853274009421435498, 12.27345743254588228 ) ) ;
#30940=CARTESIAN_POINT ( 'NONE',  ( 12.23548902587310039, 0.2575478136180237021, -12.69649014468030757 ) ) ;
#30941=CARTESIAN_POINT ( 'NONE',  ( 12.19849796477692649, -2.650903665370842432, -12.41512439159400216 ) ) ;
#30949=CARTESIAN_POINT ( 'NONE',  ( 17.96364285780273207, 0.4729642818460892961, 12.68814481171623321 ) ) ;
#30962=ORIENTED_EDGE ( 'NONE', *, *, #29465, .T. ) ;
#30966=VECTOR ( 'NONE', #54898, 1000.000000000000114 ) ;
#30968=CARTESIAN_POINT ( 'NONE',  ( 17.71828964457739986, -3.103661179288114802, 12.29022416951141139 ) ) ;
#30972=CARTESIAN_POINT ( 'NONE',  ( 12.26374059925572446, -2.812587983977303363, -13.60212386632697346 ) ) ;
#30980=CARTESIAN_POINT ( 'NONE',  ( 17.63676827340842479, 0.6210358159842679360, -13.88132258802015251 ) ) ;
#30982=EDGE_CURVE ( 'NONE', #19317, #64156, #57311, .T. ) ;
#30994=CARTESIAN_POINT ( 'NONE',  ( 12.48958479105534458, 1.960066648180104565, -13.77326086059893839 ) ) ;
#31006=CARTESIAN_POINT ( 'NONE',  ( 12.08083412505891907, 2.710618184153621435, -13.73644169170462703 ) ) ;
#31014=CARTESIAN_POINT ( 'NONE',  ( 17.93858415168864440, 0.6105138165311991827, 12.58520200551375545 ) ) ;
#31017=AXIS2_PLACEMENT_3D ( 'NONE', #58950, #11057, #64520 ) ;
#31032=DIRECTION ( 'NONE',  ( -0.000000000000000000, -0.000000000000000000, 1.000000000000000000 ) ) ;
#31047=ORIENTED_EDGE ( 'NONE', *, *, #65040, .T. ) ;
#31059=VERTEX_POINT ( 'NONE', #2988 ) ;
#31060=CARTESIAN_POINT ( 'NONE',  ( 12.26287255281689248, -2.811570894161415257, -12.37351047967075779 ) ) ;
#31066=CARTESIAN_POINT ( 'NONE',  ( 12.34634080959765079, -2.074995934380768681, -13.75442486551247789 ) ) ;
#31071=CARTESIAN_POINT ( 'NONE',  ( 18.24702988622819788, -2.264821834935305311, 12.39478563874201633 ) ) ;
#31074=CARTESIAN_POINT ( 'NONE',  ( 12.80505043854144098, -0.7302158263239267866, -13.98094363220830871 ) ) ;
#31081=CARTESIAN_POINT ( 'NONE',  ( 18.08671436482205763, 2.829189290800525391, 12.36876367364217089 ) ) ;
#31084=CIRCLE ( 'NONE', #34438, 14.00000000000000000 ) ;
#31088=CARTESIAN_POINT ( 'NONE',  ( 12.23131043852900035, -2.748092942712452746, 12.39032383288960126 ) ) ;
#31092=B_SPLINE_CURVE_WITH_KNOTS ( 'NONE', 3,
 ( #65087, #65445, #21758, #7066, #1480, #11966, #32612, #64397, #48685, #16518, #65789, #33302, #6717, #32952, #22797, #54966, #64745, #33995 ),
 .UNSPECIFIED., .F., .F.,
 ( 4, 2, 2, 2, 2, 2, 2, 2, 4 ),
 ( 0.000000000000000000, 0.06250000000000212330, 0.1250000000000042466, 0.2500000000000045519, 0.5000000000000019984, 0.7499999999999994449, 0.8749999999999998890, 0.9375000000000000000, 1.000000000000000000 ),
 .UNSPECIFIED. ) ;
#31093=LINE ( 'NONE', #30740, #39496 ) ;
#31096=CARTESIAN_POINT ( 'NONE',  ( 12.37753504985973763, -0.4560270868711872594, 12.68898073362800005 ) ) ;
#31106=CARTESIAN_POINT ( 'NONE',  ( 17.77733961940312213, 1.915504334253006036, 13.78014422891542345 ) ) ;
#31116=UNCERTAINTY_MEASURE_WITH_UNIT (LENGTH_MEASURE( 1.000000000000000082E-05 ), #41969, 'distance_accuracy_value', 'NONE');
#31120=CARTESIAN_POINT ( 'NONE',  ( 17.98492955360213230, -2.046199355803459241, -13.75924933913552550 ) ) ;
#31130=VECTOR ( 'NONE', #29787, 1000.000000000000000 ) ;
#31131=CARTESIAN_POINT ( 'NONE',  ( 18.08681467610534810, -0.3285836819713975343, 13.89477675118381406 ) ) ;
#31143=CARTESIAN_POINT ( 'NONE',  ( 12.10343314470978804, 2.298052811141196194, -12.38866778002552849 ) ) ;
#31147=CARTESIAN_POINT ( 'NONE',  ( 17.81256277267588217, -1.835326726223547089, 13.87917840078988263 ) ) ;
#31148=CARTESIAN_POINT ( 'NONE',  ( 18.12459608109056575, 2.757432806191179253, -13.61548201701641858 ) ) ;
#31159=CARTESIAN_POINT ( 'NONE',  ( 18.20534100106117847, 0.3182341284860654151, -12.59598505207571328 ) ) ;
#31168=CARTESIAN_POINT ( 'NONE',  ( 17.79030838958606964, 1.799800542995206643, 12.47079474911150143 ) ) ;
#31169=CARTESIAN_POINT ( 'NONE',  ( 12.51441652845167596, 3.187012454917759641, 13.63242365153888791 ) ) ;
#31172=CARTESIAN_POINT ( 'NONE',  ( 12.49508659849326264, -0.5431048944669121248, -12.68437082641160529 ) ) ;
#31173=CARTESIAN_POINT ( 'NONE',  ( 12.10478902330476991, -0.1895042076700523548, 13.99872220539657164 ) ) ;
#31175=CARTESIAN_POINT ( 'NONE',  ( 12.78084734971790581, -1.760846085845585218, 12.47635444213890743 ) ) ;
#31181=CARTESIAN_POINT ( 'NONE',  ( 12.23732871802943656, 0.4475098806653827199, 12.59205372277267898 ) ) ;
#31184=CARTESIAN_POINT ( 'NONE',  ( 12.54683914358772867, 1.807964460291305642, 12.46961431371563478 ) ) ;
#31191=CARTESIAN_POINT ( 'NONE',  ( 17.55505043854147118, -1.875000000000000000, 12.57545641911172396 ) ) ;
#31192=CARTESIAN_POINT ( 'NONE',  ( 12.19254223316779218, 2.624341221351141229, 12.42172529681850435 ) ) ;
#31196=CARTESIAN_POINT ( 'NONE',  ( 12.61465226496487979, -0.5953800884222990586, 12.68120857324682937 ) ) ;
#31201=CARTESIAN_POINT ( 'NONE',  ( 12.24277986057918888, -2.226901448799674998, 13.72760233995392731 ) ) ;
#31202=CARTESIAN_POINT ( 'NONE',  ( 12.19240574131726618, 2.623658934113291874, 13.64640170894116267 ) ) ;
#31211=CARTESIAN_POINT ( 'NONE',  ( 17.93748940951487114, 2.994360127459124943, -12.32254798267195994 ) ) ;
#31218=CARTESIAN_POINT ( 'NONE',  ( 12.10797096423120678, 0.2010519787742809927, -13.99856097495847607 ) ) ;
#31222=ORIENTED_EDGE ( 'NONE', *, *, #49083, .T. ) ;
#31227=CARTESIAN_POINT ( 'NONE',  ( 18.10291081608025010, 2.039210736883923403, -13.85070288166277841 ) ) ;
#31233=CARTESIAN_POINT ( 'NONE',  ( 12.19590749974583943, 0.1412517844600120476, -13.89905214520220333 ) ) ;
#31239=ORIENTED_EDGE ( 'NONE', *, *, #46884, .T. ) ;
#31244=CARTESIAN_POINT ( 'NONE',  ( 18.02785359611327465, -2.090732611440656807, -12.53755739145392845 ) ) ;
#31260=CARTESIAN_POINT ( 'NONE',  ( 12.30953092759835243, -2.881442378557633077, 13.58513712698411524 ) ) ;
#31275=CARTESIAN_POINT ( 'NONE',  ( 18.08697361606112253, 2.828309738171238319, -12.36901404291605289 ) ) ;
#31283=ADVANCED_FACE ( 'NONE', ( #24054 ), #54838, .F. ) ;
#31284=CARTESIAN_POINT ( 'NONE',  ( 17.55505043854144276, -0.6250000000000001110, 12.67928921589117586 ) ) ;
#31285=CARTESIAN_POINT ( 'NONE',  ( 5.579147251786431561, 12.92151814336059168, -2.574492155646014968 ) ) ;
#31288=CARTESIAN_POINT ( 'NONE',  ( 12.24445512745668374, -0.2765170649790825719, -12.69595318831094666 ) ) ;
#31289=CARTESIAN_POINT ( 'NONE',  ( 12.32868821303769735, -2.904730879140380750, -12.34800599561816092 ) ) ;
#31296=CARTESIAN_POINT ( 'NONE',  ( 17.77478288641002635, 0.5854877332479576646, 12.68183053513773473 ) ) ;
#31300=ORIENTED_EDGE ( 'NONE', *, *, #69048, .F. ) ;
#31306=VERTEX_POINT ( 'NONE', #14936 ) ;
#31310=CARTESIAN_POINT ( 'NONE',  ( 18.09742839077966892, -2.810734143419357345, 12.37374591515774291 ) ) ;
#31323=CARTESIAN_POINT ( 'NONE',  ( 4.599999999999999645, 3.199751711897561801, -12.18694338143115452 ) ) ;
#31326=CARTESIAN_POINT ( 'NONE',  ( 12.60230703261658114, 3.091556739796027742, 13.52998185037902701 ) ) ;
#31330=ORIENTED_EDGE ( 'NONE', *, *, #19592, .F. ) ;
#31338=CARTESIAN_POINT ( 'NONE',  ( 18.12842152808600460, 0.2489677814039778780, 13.89700419708307066 ) ) ;
#31347=DIRECTION ( 'NONE',  ( 1.000000000000000000, 0.000000000000000000, 0.000000000000000000 ) ) ;
#31352=CARTESIAN_POINT ( 'NONE',  ( 18.27886405737312003, -0.04734719685816868306, 12.59993264914401045 ) ) ;
#31369=CARTESIAN_POINT ( 'NONE',  ( 12.71024088650322348, -0.7135009822675040247, -12.57978225961209162 ) ) ;
#31386=CARTESIAN_POINT ( 'NONE',  ( 18.01189197849805623, 0.4270206790917140394, -13.89118144889037509 ) ) ;
#31399=CARTESIAN_POINT ( 'NONE',  ( 12.64197434038402790, -3.103437838334064836, -12.29027179270079273 ) ) ;
#31404=CARTESIAN_POINT ( 'NONE',  ( 12.63832872341681757, -3.228981699441164199, -13.62254385108541754 ) ) ;
#31409=CARTESIAN_POINT ( 'NONE',  ( 18.27533594408738438, -2.564445959844779743, 12.33627802783496286 ) ) ;
#31418=CARTESIAN_POINT ( 'NONE',  ( 18.16462229618754520, 2.361607881905639417, 12.48272818380096716 ) ) ;
#31423=CARTESIAN_POINT ( 'NONE',  ( 21.49999863197000138, 14.00000000000000000, 0.000000000000000000 ) ) ;
#31432=CARTESIAN_POINT ( 'NONE',  ( 12.26342954938196961, -0.3125562302819448468, 12.69484091569602668 ) ) ;
#31440=CARTESIAN_POINT ( 'NONE',  ( 17.65854462812407988, 1.883284865257428775, 13.78503182716601394 ) ) ;
#31450=CARTESIAN_POINT ( 'NONE',  ( 18.17918907329226741, -2.539311109799761379, 13.66506621000925037 ) ) ;
#31454=CARTESIAN_POINT ( 'NONE',  ( 18.00692794902808558, -2.068098667605225316, -13.75558205683924484 ) ) ;
#31463=CARTESIAN_POINT ( 'NONE',  ( 18.06139357115090860, -0.3666408745423706539, 13.89349736880855524 ) ) ;
#31471=EDGE_LOOP ( 'NONE', ( #46402, #6265, #4822, #7564, #41398 ) ) ;
#31472=VECTOR ( 'NONE', #11720, 1000.000000000000000 ) ;
#31474=CARTESIAN_POINT ( 'NONE',  ( 12.61568544974630690, 1.785400273382270919, -12.47286636618916589 ) ) ;
#31477=CARTESIAN_POINT ( 'NONE',  ( 17.92014050163765049, -1.886715056483322384, 13.87229028472749981 ) ) ;
#31478=CARTESIAN_POINT ( 'NONE',  ( 18.13950502221108252, 2.721680755780143013, -13.62394404490971489 ) ) ;
#31484=CARTESIAN_POINT ( 'NONE',  ( 7.100000000000000533, -11.06886219213000011, -1.536526853569999851 ) ) ;
#31490=CARTESIAN_POINT ( 'NONE',  ( 18.04446571359449791, 0.3888461597108446854, -12.69199065798141568 ) ) ;
#31501=CARTESIAN_POINT ( 'NONE',  ( 12.68590879673670102, 1.797325930449587661, 13.88415075348993533 ) ) ;
#31506=CARTESIAN_POINT ( 'NONE',  ( 12.50285324413425947, -1.826185914346432071, 12.46695919779662454 ) ) ;
#31513=CARTESIAN_POINT ( 'NONE',  ( 12.21591953885794624, 0.4193891200559139998, 12.59302195412780456 ) ) ;
#31517=CARTESIAN_POINT ( 'NONE',  ( 12.12640605329506016, 2.733942857944761773, 12.29982446443561805 ) ) ;
#31524=CARTESIAN_POINT ( 'NONE',  ( 12.21947784598696352, 2.718529666067204253, 12.39796232694461331 ) ) ;
#31535=ADVANCED_FACE ( 'NONE', ( #26465 ), #35157, .T. ) ;
#31536=CARTESIAN_POINT ( 'NONE',  ( 12.18523880347864718, -2.582858790010648331, 13.65555696386475404 ) ) ;
#31537=CARTESIAN_POINT ( 'NONE',  ( 12.23172337865302062, 2.748896841597663787, 13.61745941693664186 ) ) ;
#31545=CARTESIAN_POINT ( 'NONE',  ( 18.14999129509864417, 2.691763112583329676, -12.40484894414121975 ) ) ;
#31548=CARTESIAN_POINT ( 'NONE',  ( 18.00364620834145768, 1.936356668727586827, 13.86561588860068461 ) ) ;
#31551=FACE_OUTER_BOUND ( 'NONE', #30637, .T. ) ;
#31554=CARTESIAN_POINT ( 'NONE',  ( 12.80505043854146940, -3.125000000000000000, -13.52078605991414761 ) ) ;
#31565=EDGE_LOOP ( 'NONE', ( #1098, #1560, #67688, #15195 ) ) ;
#31578=ORIENTED_EDGE ( 'NONE', *, *, #50711, .F. ) ;
#31583=CARTESIAN_POINT ( 'NONE',  ( 17.63823367518483565, -3.119790641614041959, -12.28531617466518000 ) ) ;
#31592=CARTESIAN_POINT ( 'NONE',  ( 12.57032717430620927, 3.208883835765880654, -13.62729181966624203 ) ) ;
#31596=VERTEX_POINT ( 'NONE', #35601 ) ;
#31615=CARTESIAN_POINT ( 'NONE',  ( 18.11183118192862906, 2.784086580334055316, -12.38085211675188013 ) ) ;
#31619=MECHANICAL_DESIGN_GEOMETRIC_PRESENTATION_REPRESENTATION('',(#22678),#2624);
#31624=CARTESIAN_POINT ( 'NONE',  ( 18.00454058111931488, 1.908039605461288035, 12.45487753842856726 ) ) ;
#31627=CARTESIAN_POINT ( 'NONE',  ( 12.21985383964851479, 0.2197131112048736901, -12.69744725510432914 ) ) ;
#31628=CARTESIAN_POINT ( 'NONE',  ( 12.18137864098527068, -2.541952522640275713, -12.44169427845088194 ) ) ;
#31635=LINE ( 'NONE', #21817, #9430 ) ;
#31652=VERTEX_POINT ( 'NONE', #51663 ) ;
#31664=CARTESIAN_POINT ( 'NONE',  ( 18.12548987803202394, 0.2560590259361279486, -13.89684012171647787 ) ) ;
#31665=CARTESIAN_POINT ( 'NONE',  ( 17.56537431432192520, -0.6249999662751110074, -12.67928921590352154 ) ) ;
#31667=FACE_OUTER_BOUND ( 'NONE', #68456, .T. ) ;
#31682=CARTESIAN_POINT ( 'NONE',  ( 18.02496672415909629, 0.4121037244271885669, 13.89177745834280842 ) ) ;
#31687=CARTESIAN_POINT ( 'NONE',  ( 17.94896392901328142, -0.4852513397796477945, -13.88859817538105013 ) ) ;
#31694=CARTESIAN_POINT ( 'NONE',  ( 17.91829918956259604, 0.6226057762474783708, 12.58460959628226483 ) ) ;
#31704=DIRECTION ( 'NONE',  ( 1.000000000000000000, 0.000000000000000000, 0.000000000000000000 ) ) ;
#31711=VERTEX_POINT ( 'NONE', #63168 ) ;
#31718=CARTESIAN_POINT ( 'NONE',  ( 17.55505043854144276, -0.6250000000000001110, 12.67928921589117586 ) ) ;
#31731=DIRECTION ( 'NONE',  ( 0.7071067784121117805, -0.5090965378051087731, 0.4907348766070088186 ) ) ;
#31748=CARTESIAN_POINT ( 'NONE',  ( 12.18551697106549447, -2.583096739011645937, -12.43182067874258756 ) ) ;
#31752=CARTESIAN_POINT ( 'NONE',  ( 12.38995319333359646, -1.919216742092435757, -13.86782799095450258 ) ) ;
#31755=CARTESIAN_POINT ( 'NONE',  ( 18.21784200350680294, -2.188139590168308501, 12.40855205325248534 ) ) ;
#31758=AXIS2_PLACEMENT_3D ( 'NONE', #1946, #18372, #50183 ) ;
#31767=CARTESIAN_POINT ( 'NONE',  ( 18.00302879683550117, -3.053770323303487189, -12.22453350000937888 ) ) ;
#31770=CARTESIAN_POINT ( 'NONE',  ( 12.22356881520516758, -2.729361768173760083, 12.39519383931446228 ) ) ;
#31777=CARTESIAN_POINT ( 'NONE',  ( 12.55608787177197172, -0.5733651658914331595, 12.68257300503909235 ) ) ;
#31778=CARTESIAN_POINT ( 'NONE',  ( 5.624287198480453220, -12.11015306275925951, -3.744045437480271410 ) ) ;
#31779=DIRECTION ( 'NONE',  ( 1.000000000000000000, 0.000000000000000000, 0.000000000000000000 ) ) ;
#31784=CARTESIAN_POINT ( 'NONE',  ( 17.63806710036368841, 1.880187906035670764, 13.78549581173515115 ) ) ;
#31790=CARTESIAN_POINT ( 'NONE',  ( 5.666085114158424751, -12.07002994274972885, 3.732314430518076875 ) ) ;
#31800=CARTESIAN_POINT ( 'NONE',  ( 18.02766551172502574, -2.090896903265579088, -13.75171326662667504 ) ) ;
#31809=CARTESIAN_POINT ( 'NONE',  ( 18.16417894366952979, -0.1413088920361047773, 13.89905105385967410 ) ) ;
#31819=CARTESIAN_POINT ( 'NONE',  ( 12.58695046962338182, 1.794129438118912345, -12.47161187386927672 ) ) ;
#31823=CARTESIAN_POINT ( 'NONE',  ( 18.28005242394221241, -2.496404808517243890, 13.77565028140659287 ) ) ;
#31824=CARTESIAN_POINT ( 'NONE',  ( 18.15114771542447158, 2.688105180712813347, -13.63176637566754934 ) ) ;
#31837=CARTESIAN_POINT ( 'NONE',  ( 17.80382244274732173, 0.5734477787136645910, -12.68256797703446281 ) ) ;
#31847=CARTESIAN_POINT ( 'NONE',  ( 17.57925147499690155, 1.760911370824148392, 12.47634522799707568 ) ) ;
#31864=CARTESIAN_POINT ( 'NONE',  ( 12.08418858410074748, 2.401692437127234125, 12.36899414651120566 ) ) ;
#31872=CARTESIAN_POINT ( 'NONE',  ( 12.27404183471215937, 2.829784922027013483, 12.36859113741106420 ) ) ;
#31876=CARTESIAN_POINT ( 'NONE',  ( 12.80505043854144276, 0.6249999999999994449, 12.67928921589117586 ) ) ;
#31884=CARTESIAN_POINT ( 'NONE',  ( 12.19646863228101452, -2.642680340209514256, 13.64216715890481524 ) ) ;
#31885=CARTESIAN_POINT ( 'NONE',  ( 12.21224535002822442, 2.300944246528859871, 13.71363154654899041 ) ) ;
#31894=CARTESIAN_POINT ( 'NONE',  ( 18.14163091156140695, 2.284010751868936762, -12.49929939428933601 ) ) ;
#31896=CARTESIAN_POINT ( 'NONE',  ( 18.17508965102116036, 2.579233224688229242, 12.43275545429011686 ) ) ;
#31901=DIRECTION ( 'NONE',  ( -1.000000000000000000, -0.000000000000000000, -0.000000000000000000 ) ) ;
#31904=EDGE_LOOP ( 'NONE', ( #4397, #19770, #3942, #29111, #15994 ) ) ;
#31911=ORIENTED_EDGE ( 'NONE', *, *, #61407, .F. ) ;
#31917=CARTESIAN_POINT ( 'NONE',  ( 12.37275480865975830, 0.4515881962949890860, -13.89013012614793041 ) ) ;
#31928=CARTESIAN_POINT ( 'NONE',  ( 17.98035626696893985, -2.958002308262751789, -12.33297292539930368 ) ) ;
#31929=AXIS2_PLACEMENT_3D ( 'NONE', #31323, #20478, #14557 ) ;
#31931=DIRECTION ( 'NONE',  ( -1.000000000000000000, 0.000000000000000000, 0.000000000000000000 ) ) ;
#31933=PLANE ( 'NONE',  #54767 ) ;
#31934=CARTESIAN_POINT ( 'NONE',  ( 12.18107303550439902, -0.04113803725886359952, 13.89993798560270832 ) ) ;
#31948=CARTESIAN_POINT ( 'NONE',  ( 12.27416439418442096, -2.829982835910819006, 13.59791655269246924 ) ) ;
#31964=CARTESIAN_POINT ( 'NONE',  ( 17.83355475039667226, 3.059894173695237640, -12.30333952404643227 ) ) ;
#31978=CARTESIAN_POINT ( 'NONE',  ( 12.18532624936142206, -0.08167875237853008952, -12.69965198491187230 ) ) ;
#31981=CARTESIAN_POINT ( 'NONE',  ( 4.699998537092440642, -13.17499999999999893, 0.000000000000000000 ) ) ;
#32003=CARTESIAN_POINT ( 'NONE',  ( 18.18005043824376443, -1.329523415562850021E-10, -12.70000000088146486 ) ) ;
#32006=EDGE_LOOP ( 'NONE', ( #57069, #37855, #748, #54602 ) ) ;
#32011=CIRCLE ( 'NONE', #44297, 13.89999852641999922 ) ;
#32014=ORIENTED_EDGE ( 'NONE', *, *, #28113, .T. ) ;
#32033=CARTESIAN_POINT ( 'NONE',  ( 18.17981516808187337, -0.01996689158402818742, 13.89998575767904043 ) ) ;
#32034=CARTESIAN_POINT ( 'NONE',  ( 18.05194946931286282, 0.3792369704146499876, 13.89303997536584667 ) ) ;
#32036=DIRECTION ( 'NONE',  ( -1.000000000000000000, -0.000000000000000000, -0.000000000000000000 ) ) ;
#32045=CARTESIAN_POINT ( 'NONE',  ( 18.16373151406918396, -0.1422617729927601882, 12.69893308522357245 ) ) ;
#32055=B_SPLINE_CURVE_WITH_KNOTS ( 'NONE', 3,
 ( #11228, #22055, #48984, #21713, #28357, #43048, #49320, #1091, #64351, #33601, #23098, #49673, #1782, #32564, #17158, #5977 ),
 .UNSPECIFIED., .F., .F.,
 ( 4, 2, 2, 2, 2, 2, 2, 4 ),
 ( 0.000000000000000000, 0.06250000000000084655, 0.1250000000000016931, 0.2500000000000031641, 0.5000000000000033307, 0.7500000000000034417, 0.8750000000000017764, 1.000000000000000000 ),
 .UNSPECIFIED. ) ;
#32061=CARTESIAN_POINT ( 'NONE',  ( 12.54953071380263019, -0.6732419856523256252, -12.58200148172923605 ) ) ;
#32063=CARTESIAN_POINT ( 'NONE',  ( 17.82398025068293990, 3.148553868299631908, -12.20027175159510335 ) ) ;
#32065=AXIS2_PLACEMENT_3D ( 'NONE', #66762, #50002, #40206 ) ;
#32079=CARTESIAN_POINT ( 'NONE',  ( 12.43681290820071794, 1.853313662622533053, -12.46300903943780725 ) ) ;
#32086=CARTESIAN_POINT ( 'NONE',  ( 12.55417570215094614, 3.072462724870959505, -12.29958987976101703 ) ) ;
#32093=DIRECTION ( 'NONE',  ( 1.000000000000000000, 0.000000000000000000, 0.000000000000000000 ) ) ;
#32099=CARTESIAN_POINT ( 'NONE',  ( 12.57019395242810589, -1.827067495629554728, -13.88026806835660842 ) ) ;
#32102=CARTESIAN_POINT ( 'NONE',  ( 17.97968936757972713, -3.063621360739239297, 12.22187700344946037 ) ) ;
#32125=CARTESIAN_POINT ( 'NONE',  ( 12.21300000160833399, -0.2005123242923285698, 12.69787478206144016 ) ) ;
#32129=CIRCLE ( 'NONE', #41053, 13.17499999999999538 ) ;
#32137=CARTESIAN_POINT ( 'NONE',  ( 18.00692794902805005, 2.068098667605222207, 13.75558205683924484 ) ) ;
#32148=CARTESIAN_POINT ( 'NONE',  ( 18.14139820495729438, -2.283379482803411076, -13.71697381851088160 ) ) ;
#32168=CIRCLE ( 'NONE', #863, 2.000000000000000444 ) ;
#32169=CARTESIAN_POINT ( 'NONE',  ( 12.63888201721070637, 1.779588368642098573, -12.47369581775632952 ) ) ;
#32172=AXIS2_PLACEMENT_3D ( 'NONE', #40245, #66458, #2490 ) ;
#32173=CARTESIAN_POINT ( 'NONE',  ( 18.01231764194518092, 2.926478478987347032, -13.57371117741004340 ) ) ;
#32174=VERTEX_POINT ( 'NONE', #21740 ) ;
#32178=CARTESIAN_POINT ( 'NONE',  ( 12.41985246593411141, -3.089908466900599393, -12.21525705840281972 ) ) ;
#32184=CARTESIAN_POINT ( 'NONE',  ( 17.91054845552246277, 0.5141503178158084442, -12.68598964581897626 ) ) ;
#32195=CARTESIAN_POINT ( 'NONE',  ( 18.25351233825839259, 2.286726172143656477, 12.39076325940497902 ) ) ;
#32204=CARTESIAN_POINT ( 'NONE',  ( 12.22684347114283199, -2.045928570575545891, 12.43279008976418964 ) ) ;
#32213=AXIS2_PLACEMENT_3D ( 'NONE', #47514, #46483, #3812 ) ;
#32214=CARTESIAN_POINT ( 'NONE',  ( 12.15765997487494587, 2.156065442695494383, 12.41416509552197134 ) ) ;
#32216=DIRECTION ( 'NONE',  ( 0.000000000000000000, -1.000000000000000000, 0.000000000000000000 ) ) ;
#32223=CARTESIAN_POINT ( 'NONE',  ( 18.11689826751005938, -0.2739464174237275507, 12.69602652205148985 ) ) ;
#32225=ORIENTED_EDGE ( 'NONE', *, *, #22195, .F. ) ;
#32228=CARTESIAN_POINT ( 'NONE',  ( 12.39828795399329664, 0.4745523466136125079, 12.68806523617751125 ) ) ;
#32232=CARTESIAN_POINT ( 'NONE',  ( 12.29449213756047676, -2.138932443162072872, 13.74345175514785033 ) ) ;
#32233=CARTESIAN_POINT ( 'NONE',  ( 12.18403211231679606, 2.428839562872916691, 13.68824371556415720 ) ) ;
#32235=ORIENTED_EDGE ( 'NONE', *, *, #51062, .T. ) ;
#32244=CARTESIAN_POINT ( 'NONE',  ( 18.11762593468200322, 2.227530255644427637, -12.51091528569613764 ) ) ;
#32249=DIRECTION ( 'NONE',  ( 0.000000000000000000, -0.9905022095861402143, -0.1374968101629056305 ) ) ;
#32265=CARTESIAN_POINT ( 'NONE',  ( 12.40587428666008840, 0.4809231526954447222, -13.88880064789607616 ) ) ;
#32266=B_SPLINE_CURVE_WITH_KNOTS ( 'NONE', 1,
 ( #22375, #18526 ),
 .UNSPECIFIED., .F., .F.,
 ( 2, 2 ),
 ( 0.000000000000000000, 1.000000000000000000 ),
 .UNSPECIFIED. ) ;
#32267=CARTESIAN_POINT ( 'NONE',  ( 17.55505043854147118, -1.875000000000000000, -12.57541666120755863 ) ) ;
#32277=CARTESIAN_POINT ( 'NONE',  ( 17.87019584817734952, -3.039826384816739502, -12.30925258946623480 ) ) ;
#32280=ADVANCED_FACE ( 'NONE', ( #41700 ), #21400, .F. ) ;
#32285=CARTESIAN_POINT ( 'NONE',  ( 12.33448524795695889, 0.4118363585311526354, 13.89180007025485786 ) ) ;
#32311=CARTESIAN_POINT ( 'NONE',  ( 18.11618405632788864, 2.775422336685124947, -12.38314678680533021 ) ) ;
#32316=ADVANCED_FACE ( 'NONE', ( #27002 ), #24549, .T. ) ;
#32318=CARTESIAN_POINT ( 'NONE',  ( 18.27948916824811221, 2.669673601435039956, 12.31540264491035508 ) ) ;
#32319=ORIENTED_EDGE ( 'NONE', *, *, #29934, .T. ) ;
#32320=CARTESIAN_POINT ( 'NONE',  ( 12.44044950778751257, 0.5080407711865465581, -12.68632595416894837 ) ) ;
#32325=CARTESIAN_POINT ( 'NONE',  ( 5.700000000000000178, 13.04986661130000059, 1.811520473896000016 ) ) ;
#32330=CARTESIAN_POINT ( 'NONE',  ( 18.14735902879090190, 0.1997594608485829815, 12.69789023918054305 ) ) ;
#32338=CARTESIAN_POINT ( 'NONE',  ( 17.71863970650576192, 3.103558472751648090, -13.52675378075879387 ) ) ;
#32347=ORIENTED_EDGE ( 'NONE', *, *, #49837, .T. ) ;
#32350=CARTESIAN_POINT ( 'NONE',  ( 18.18005044212796051, -2.500000099754955851, 13.67345740034994783 ) ) ;
#32354=ORIENTED_EDGE ( 'NONE', *, *, #43008, .F. ) ;
#32356=CARTESIAN_POINT ( 'NONE',  ( 18.00922683609310937, -1.919385048924807657, -12.45295227646844793 ) ) ;
#32363=EDGE_CURVE ( 'NONE', #13791, #37829, #20058, .T. ) ;
#32371=CARTESIAN_POINT ( 'NONE',  ( 12.47325605351258559, 3.030051207268856128, -13.54664584463136556 ) ) ;
#32374=CARTESIAN_POINT ( 'NONE',  ( 18.17180502197784975, -0.1017048024283995350, 13.89950429703524826 ) ) ;
#32377=CARTESIAN_POINT ( 'NONE',  ( 12.35321263090786559, 0.4320316581265301603, 13.89096707190850211 ) ) ;
#32379=PLANE ( 'NONE',  #15689 ) ;
#32380=CARTESIAN_POINT ( 'NONE',  ( 17.93439120260890363, -0.4967442791062720020, -13.88805191678453177 ) ) ;
#32389=CARTESIAN_POINT ( 'NONE',  ( 18.16600380262988068, -0.1321628250398322602, 12.69908003149455133 ) ) ;
#32390=CARTESIAN_POINT ( 'NONE',  ( 7.100000000000000533, 13.04986661130000059, -1.811520473896000016 ) ) ;
#32404=CARTESIAN_POINT ( 'NONE',  ( 18.25219266138121554, 2.678721125794442326, -12.31196912072773308 ) ) ;
#32415=B_SPLINE_CURVE_WITH_KNOTS ( 'NONE', 3,
 ( #68376, #59271, #64167, #10003, #26091, #69078, #5453, #47417, #47075, #5102, #11374, #20497, #554, #41821, #26789, #52314, #63129, #21525, #68723, #37606, #53005, #42856, #36931, #20843, #58936, #32377, #53692, #5785, #42177, #16625, #27128, #48448, #21865, #58243, #10348, #64504, #7514, #48793, #902, #44256, #11718, #43550, #60660, #64850, #12774, #22215, #18366, #44602, #16961, #33060, #6827, #65552, #54374, #54026, #54726, #39687, #6129, #50177, #38294, #38998, #61006, #1585, #28159, #12076, #59968, #18023, #49473, #59623, #65200, #22902, #43898, #65893, #33409, #17319, #17675, #39339, #28513, #32715, #2280, #60317, #6477, #12426, #44939, #27466, #27826, #28869, #33757, #55072, #38644, #66244, #49131, #1243, #23596 ),
 .UNSPECIFIED., .F., .F.,
 ( 4, 2, 2, 2, 2, 2, 2, 2, 2, 1, 1, 2, 2, 2, 2, 2, 2, 2, 2, 2, 2, 2, 2, 2, 2, 2, 2, 2, 2, 2, 2, 2, 2, 1, 1, 2, 2, 2, 2, 1, 2, 2, 2, 2, 2, 2, 2, 2, 4 ),
 ( 0.000000000000000000, 0.03124999999999007738, 0.06249999999998015476, 0.09374999999997023215, 0.1093749999999640288, 0.1249999999999578115, 0.1562499999999453493, 0.1718749999999391043, 0.1874999999999328593, 0.2031249999999266143, 0.2109374999999235334, 0.2148437499999229505, 0.2187499999999223954, 0.2499999999999291678, 0.2656249999999332756, 0.2734374999999361622, 0.2812499999999390488, 0.2968749999999448219, 0.3124999999999505396, 0.3437499999999608646, 0.3593749999999660272, 0.3749999999999711897, 0.4062499999999815703, 0.4374999999999919509, 0.5000000000000133227, 0.5312500000000240918, 0.5625000000000347500, 0.5937500000000454081, 0.6093750000000502931, 0.6250000000000551781, 0.6562500000000650591, 0.6718750000000692779, 0.6875000000000736078, 0.7031250000000778266, 0.7109375000000800471, 0.7148437500000811573, 0.7187500000000821565, 0.7500000000000738298, 0.7656250000000696110, 0.7734375000000686118, 0.7773437500000668354, 0.7812500000000650591, 0.7968750000000613953, 0.8125000000000577316, 0.8437500000000506262, 0.8593750000000469624, 0.8750000000000432987, 0.9375000000000216493, 1.000000000000000000 ),
 .UNSPECIFIED. ) ;
#32420=CARTESIAN_POINT ( 'NONE',  ( 17.77532102045679352, -0.5849891190461622426, -13.88342664904962831 ) ) ;
#32435=CARTESIAN_POINT ( 'NONE',  ( 12.21176631991879447, -2.303170217796230546, -12.49524360984839433 ) ) ;
#32439=CARTESIAN_POINT ( 'NONE',  ( 12.50340631570018068, -1.853896141579339130, -13.87671057111554518 ) ) ;
#32443=CARTESIAN_POINT ( 'NONE',  ( 18.27898910297789925, -2.436826214745341446, 12.36212035235843487 ) ) ;
#32444=EDGE_CURVE ( 'NONE', #56658, #11513, #42828, .T. ) ;
#32455=EDGE_LOOP ( 'NONE', ( #16871, #42115, #19237, #6420 ) ) ;
#32464=CIRCLE ( 'NONE', #63, 13.89999852641999922 ) ;
#32473=CARTESIAN_POINT ( 'NONE',  ( 18.06560877808659882, 2.138932497554040246, 13.74340275081395113 ) ) ;
#32475=CIRCLE ( 'NONE', #62604, 2.000000000000001332 ) ;
#32478=CARTESIAN_POINT ( 'NONE',  ( 17.55505043854144276, -0.6250000000000001110, -13.88107975066922428 ) ) ;
#32483=VERTEX_POINT ( 'NONE', #20812 ) ;
#32485=CARTESIAN_POINT ( 'NONE',  ( 17.72189171626102322, -1.806990214763248392, -13.88289628861100766 ) ) ;
#32504=CARTESIAN_POINT ( 'NONE',  ( 12.37951367597793784, 1.897619119404204469, -12.45628731554757351 ) ) ;
#32513=ORIENTED_EDGE ( 'NONE', *, *, #51689, .T. ) ;
#32517=CARTESIAN_POINT ( 'NONE',  ( 5.500000000000000000, 12.87590651766999983, -2.791353855799999728 ) ) ;
#32520=CARTESIAN_POINT ( 'NONE',  ( 17.91829918956260315, -0.6226057762474851431, -12.58460959628226306 ) ) ;
#32527=ORIENTED_EDGE ( 'NONE', *, *, #20539, .T. ) ;
#32533=CARTESIAN_POINT ( 'NONE',  ( 18.27150181675463259, 2.367044107065569669, 12.37568780170008864 ) ) ;
#32539=CARTESIAN_POINT ( 'NONE',  ( 12.08085380679226262, -2.436412096897888180, 12.36221874022169587 ) ) ;
#32543=PLANE ( 'NONE',  #7497 ) ;
#32547=CARTESIAN_POINT ( 'NONE',  ( 12.78109913421143062, 0.7192906882580830663, 12.57945229568000123 ) ) ;
#32550=CARTESIAN_POINT ( 'NONE',  ( 12.70218814580025679, 3.116819717849788063, 12.28621950321773326 ) ) ;
#32558=CARTESIAN_POINT ( 'NONE',  ( 12.19849796498733951, 2.650903666209170062, 12.41512439138481128 ) ) ;
#32561=CARTESIAN_POINT ( 'NONE',  ( 12.22418410612670314, 0.2308773533104517828, 12.69717962854873150 ) ) ;
#32563=CARTESIAN_POINT ( 'NONE',  ( 17.55505043854144276, 0.7192913403693119712, -12.57945229203838267 ) ) ;
#32564=CARTESIAN_POINT ( 'NONE',  ( 17.74741402327983053, 1.780171064306780071, -12.47366677608254015 ) ) ;
#32565=CIRCLE ( 'NONE', #2427, 1.800000000000000044 ) ;
#32566=CARTESIAN_POINT ( 'NONE',  ( 12.13805290469199427, -2.231685852207996312, 13.82098778992224730 ) ) ;
#32575=CARTESIAN_POINT ( 'NONE',  ( 17.80628805164905870, 1.927626392034356595, -12.56668820897845329 ) ) ;
#32578=EDGE_CURVE ( 'NONE', #63182, #22430, #50163, .T. ) ;
#32586=VERTEX_POINT ( 'NONE', #24608 ) ;
#32590=CARTESIAN_POINT ( 'NONE',  ( 18.01279121882208045, -2.925678518064911859, 13.57390968381829488 ) ) ;
#32592=ORIENTED_EDGE ( 'NONE', *, *, #32578, .T. ) ;
#32599=CARTESIAN_POINT ( 'NONE',  ( 12.31508838510828951, 0.3880332711109533150, -13.89271023030988061 ) ) ;
#32610=EDGE_CURVE ( 'NONE', #58820, #62111, #61324, .T. ) ;
#32612=CARTESIAN_POINT ( 'NONE',  ( 18.00298204921611855, -3.099842930870032376, -13.65268125596126758 ) ) ;
#32613=CARTESIAN_POINT ( 'NONE',  ( 17.80118387294175974, -3.074517463812005857, -12.29895906470767919 ) ) ;
#32618=CARTESIAN_POINT ( 'NONE',  ( 12.23550883753393848, -0.2581888431706775844, 13.89679013629345228 ) ) ;
#32630=ORIENTED_EDGE ( 'NONE', *, *, #37871, .F. ) ;
#32632=CARTESIAN_POINT ( 'NONE',  ( 12.80505043854146940, -3.125000000000000000, -25.00000000000000000 ) ) ;
#32645=CARTESIAN_POINT ( 'NONE',  ( 5.634820040245294592, -12.96111452106133122, 2.364727959305737315 ) ) ;
#32667=CARTESIAN_POINT ( 'NONE',  ( 18.17906593022460626, 0.04061720351850793553, 12.69993396819095643 ) ) ;
#32674=CARTESIAN_POINT ( 'NONE',  ( 17.65850582825305892, 3.116720375661584441, -13.52313201004804277 ) ) ;
#32693=CARTESIAN_POINT ( 'NONE',  ( 18.07980642414615247, 0.3396162601617248034, -13.89441893193946775 ) ) ;
#32705=CARTESIAN_POINT ( 'NONE',  ( 12.75683046442381929, 1.789027279908999679, -13.88522190323555172 ) ) ;
#32711=CARTESIAN_POINT ( 'NONE',  ( 18.09667340657836121, -0.3125520594525368900, 13.89528657259775102 ) ) ;
#32715=CARTESIAN_POINT ( 'NONE',  ( 12.40639171141861929, -0.4813567170522365934, 13.88878047999798682 ) ) ;
#32716=CARTESIAN_POINT ( 'NONE',  ( 12.40965214754211843, -0.4840331165010965941, -13.88865521357928934 ) ) ;
#32718=CARTESIAN_POINT ( 'NONE',  ( 17.78593649205363647, -0.5808626952866734472, -13.88365973251372765 ) ) ;
#32727=CARTESIAN_POINT ( 'NONE',  ( 18.16408092502819116, 0.1418569258565852420, 12.69895512164409368 ) ) ;
#32730=VERTEX_POINT ( 'NONE', #17870 ) ;
#32743=CARTESIAN_POINT ( 'NONE',  ( 18.20615948710261733, 2.797893282243137492, -12.28544817418252855 ) ) ;
#32746=EDGE_LOOP ( 'NONE', ( #65773, #32846, #52878, #48937 ) ) ;
#32761=CARTESIAN_POINT ( 'NONE',  ( 17.88507584039978582, -0.5311540453515659621, -13.88634387573209494 ) ) ;
#32763=DIRECTION ( 'NONE',  ( 0.000000000000000000, 0.000000000000000000, 1.000000000000000000 ) ) ;
#32777=CARTESIAN_POINT ( 'NONE',  ( 12.46308409927492455, -1.976751580904480443, -12.55819113744975546 ) ) ;
#32782=CARTESIAN_POINT ( 'NONE',  ( 12.25828482332356728, -2.997587547359419791, -13.67532635696712440 ) ) ;
#32784=CARTESIAN_POINT ( 'NONE',  ( 12.15658143854451545, -2.853298863235071092, 12.27345178217744603 ) ) ;
#32785=CARTESIAN_POINT ( 'NONE',  ( 17.91266776300918551, -3.012678901972745571, 12.31722829471395464 ) ) ;
#32786=ORIENTED_EDGE ( 'NONE', *, *, #64769, .T. ) ;
#32804=VECTOR ( 'NONE', #14908, 1000.000000000000000 ) ;
#32808=FACE_OUTER_BOUND ( 'NONE', #56071, .T. ) ;
#32813=CARTESIAN_POINT ( 'NONE',  ( 18.13009756288981222, 2.254948952832145359, 13.72233930590318884 ) ) ;
#32823=ORIENTED_EDGE ( 'NONE', *, *, #45146, .T. ) ;
#32825=CARTESIAN_POINT ( 'NONE',  ( 17.87892170566136230, -1.864264957476227780, -13.87532524069350259 ) ) ;
#32846=ORIENTED_EDGE ( 'NONE', *, *, #39147, .F. ) ;
#32849=CARTESIAN_POINT ( 'NONE',  ( 12.18817755169812678, 2.859236737589999411, -12.27131451573979071 ) ) ;
#32858=CARTESIAN_POINT ( 'NONE',  ( 12.44013165738125615, -3.102068138921904694, -12.21217476962502069 ) ) ;
#32865=CARTESIAN_POINT ( 'NONE',  ( 17.93858415168864440, -0.6105138165312175014, -12.58520200551375368 ) ) ;
#32866=CARTESIAN_POINT ( 'NONE',  ( 12.19239630165612276, 2.623612345200928342, -12.42193400453944285 ) ) ;
#32870=VECTOR ( 'NONE', #11012, 1000.000000000000000 ) ;
#32875=CARTESIAN_POINT ( 'NONE',  ( 18.20792762907817419, 2.166426970554221842, 12.41237440719187290 ) ) ;
#32882=CARTESIAN_POINT ( 'NONE',  ( 12.11828080172250921, -2.711598415135501483, 12.30476978351483197 ) ) ;
#32889=CARTESIAN_POINT ( 'NONE',  ( 12.15464131684817950, -0.3178346465811148769, 12.59599179195193663 ) ) ;
#32892=CARTESIAN_POINT ( 'NONE',  ( 12.18852176789201813, 2.603049415106243103, 12.42696357550859787 ) ) ;
#32895=CARTESIAN_POINT ( 'NONE',  ( 18.05078025084782567, -0.5250004125410587807, 12.58906021966015842 ) ) ;
#32903=CARTESIAN_POINT ( 'NONE',  ( 12.47664625033035968, 0.5322368321508662570, 12.68499235032564521 ) ) ;
#32907=CARTESIAN_POINT ( 'NONE',  ( 12.17655141950255882, -2.882034090924107339, 13.70014555608275941 ) ) ;
#32918=CARTESIAN_POINT ( 'NONE',  ( 17.93883077754965072, 2.006280984399065659, -12.55302554764001499 ) ) ;
#32924=CARTESIAN_POINT ( 'NONE',  ( 12.70934146434746559, 1.792598170639653876, 13.88476440024012604 ) ) ;
#32934=CARTESIAN_POINT ( 'NONE',  ( 18.16447345601865848, -2.360953327207878871, 13.70196990072541077 ) ) ;
#32944=CARTESIAN_POINT ( 'NONE',  ( 17.55505043854147118, -1.760910691117812954, -12.47634535983622861 ) ) ;
#32952=CARTESIAN_POINT ( 'NONE',  ( 17.79094441639333013, -1.825864066368119598, -13.88043842654159299 ) ) ;
#32956=FACE_OUTER_BOUND ( 'NONE', #53881, .T. ) ;
#32957=CARTESIAN_POINT ( 'NONE',  ( 12.51718303290431678, 3.054853725429544919, 13.53993614671056811 ) ) ;
#32960=CARTESIAN_POINT ( 'NONE',  ( 12.66238154463050769, 0.6088408278571617593, 13.88204686096232621 ) ) ;
#32963=DIRECTION ( 'NONE',  ( 1.000000000000000000, -3.631529569662070274E-15, 1.174496025128702085E-14 ) ) ;
#32971=ORIENTED_EDGE ( 'NONE', *, *, #11180, .F. ) ;
#32987=CARTESIAN_POINT ( 'NONE',  ( 5.534341697420971151, -12.89488364876162763, 2.703816489143735513 ) ) ;
#32996=EDGE_CURVE ( 'NONE', #19638, #57425, #10254, .T. ) ;
#33005=CARTESIAN_POINT ( 'NONE',  ( 12.70687399448022425, 1.760978113263438560, 12.47633584387834027 ) ) ;
#33016=CARTESIAN_POINT ( 'NONE',  ( 17.81506173200506637, 3.068442049787682979, -13.53632421860061186 ) ) ;
#33031=CARTESIAN_POINT ( 'NONE',  ( 18.15949994905106735, -2.660112426196167057, -13.63815955517138789 ) ) ;
#33032=FACE_OUTER_BOUND ( 'NONE', #32006, .T. ) ;
#33044=CARTESIAN_POINT ( 'NONE',  ( 12.80505043854144276, 0.6600719421079697113, 13.91436771118226012 ) ) ;
#33046=DIRECTION ( 'NONE',  ( -1.000000000000000000, 0.000000000000000000, 0.000000000000000000 ) ) ;
#33049=CARTESIAN_POINT ( 'NONE',  ( 12.76358235960661780, 3.123961849445188843, -13.52113151862113938 ) ) ;
#33052=CARTESIAN_POINT ( 'NONE',  ( 18.16600461949966672, 0.1321590433901028427, 13.89915950722681970 ) ) ;
#33060=CARTESIAN_POINT ( 'NONE',  ( 12.18504202262453262, -0.08143095622523290056, 13.89969831568979153 ) ) ;
#33061=CARTESIAN_POINT ( 'NONE',  ( 12.32512809858833869, -0.4004137792110806782, -13.89223825656353739 ) ) ;
#33063=PLANE ( 'NONE',  #35058 ) ;
#33069=AXIS2_PLACEMENT_3D ( 'NONE', #13966, #30060, #67765 ) ;
#33072=AXIS2_PLACEMENT_3D ( 'NONE', #41886, #48166, #68789 ) ;
#33074=CARTESIAN_POINT ( 'NONE',  ( 17.86760901219547648, -0.5416145769730059678, 12.68445494689096087 ) ) ;
#33076=CARTESIAN_POINT ( 'NONE',  ( 18.01268549162643495, -2.926083040860917084, -12.34202569327525012 ) ) ;
#33089=CARTESIAN_POINT ( 'NONE',  ( 12.14465108362472634, -0.2970375428997896194, -12.59650273238872487 ) ) ;
#33091=CARTESIAN_POINT ( 'NONE',  ( 18.26113864896146666, 2.644667523736219827, -12.31932909903656537 ) ) ;
#33092=CARTESIAN_POINT ( 'NONE',  ( 5.648274849241552431, 12.08704511044957464, 3.737576519652656248 ) ) ;
#33106=CARTESIAN_POINT ( 'NONE',  ( 17.55505043854143565, 2.500000000000000000, -25.00000000000000000 ) ) ;
#33109=CARTESIAN_POINT ( 'NONE',  ( 17.74345116425200075, 0.7055305429986109544, -13.98221279804358019 ) ) ;
#33110=ORIENTED_EDGE ( 'NONE', *, *, #30811, .F. ) ;
#33111=CARTESIAN_POINT ( 'NONE',  ( 21.47500033997000202, -1.509903313490000218E-14, 4.329869796037999436E-14 ) ) ;
#33118=CARTESIAN_POINT ( 'NONE',  ( 17.99906018690873211, -1.940665501735332032, 13.86484298168863738 ) ) ;
#33123=CARTESIAN_POINT ( 'NONE',  ( 12.43764207941355338, -1.993980486415520614, -12.55516735266245121 ) ) ;
#33127=CARTESIAN_POINT ( 'NONE',  ( 12.08136008893002966, -2.567386246332875377, -13.76259835127842202 ) ) ;
#33132=CARTESIAN_POINT ( 'NONE',  ( 17.59659125555225145, -3.123958135111998491, 12.28406395290800823 ) ) ;
#33147=EDGE_CURVE ( 'NONE', #55276, #58820, #60818, .T. ) ;
#33161=CARTESIAN_POINT ( 'NONE',  ( 18.03429950922807734, 2.098690172523155262, 13.75037901049766731 ) ) ;
#33164=VERTEX_POINT ( 'NONE', #23159 ) ;
#33165=AXIS2_PLACEMENT_3D ( 'NONE', #7894, #22928, #65578 ) ;
#33173=CARTESIAN_POINT ( 'NONE',  ( 17.80546914520764545, -3.072731260628055683, -13.53510445278181962 ) ) ;
#33188=CARTESIAN_POINT ( 'NONE',  ( 17.55505043854143565, 1.787797342887044394, 13.88538010501570952 ) ) ;
#33192=EDGE_CURVE ( 'NONE', #48333, #66718, #3855, .T. ) ;
#33194=CARTESIAN_POINT ( 'NONE',  ( 12.51946955736927691, 3.141640009352831608, -12.20205326030422377 ) ) ;
#33204=CARTESIAN_POINT ( 'NONE',  ( 12.78084604758903886, -3.199697762315045768, -12.18695750762853258 ) ) ;
#33212=CARTESIAN_POINT ( 'NONE',  ( 17.88568294903051736, -0.5304820368560130284, -12.68508456201359991 ) ) ;
#33213=CARTESIAN_POINT ( 'NONE',  ( 12.20163823172845596, 2.663908709213365533, -12.41191052582379939 ) ) ;
#33221=CARTESIAN_POINT ( 'NONE',  ( 18.17187109576073567, 2.859211385468999556, 12.27132042014887148 ) ) ;
#33222=CARTESIAN_POINT ( 'NONE',  ( 4.599999999999999645, -3.199698446519375850, -12.18695736643652694 ) ) ;
#33231=CARTESIAN_POINT ( 'NONE',  ( 12.50301483199535468, -3.134404823497601633, 12.20391382861247109 ) ) ;
#33236=CARTESIAN_POINT ( 'NONE',  ( 12.70960625021945312, -0.7131288892044757022, 12.57980326738671906 ) ) ;
#33239=CARTESIAN_POINT ( 'NONE',  ( 12.64197434038399237, 3.103437838334064391, 12.29027179270079806 ) ) ;
#33243=CARTESIAN_POINT ( 'NONE',  ( 18.18297319953441971, -0.3597466176220683876, 12.59486741915706709 ) ) ;
#33252=AXIS2_PLACEMENT_3D ( 'NONE', #61292, #39277, #34731 ) ;
#33260=CARTESIAN_POINT ( 'NONE',  ( 12.63821499911166413, -1.807008444693748439, 13.88289391573714049 ) ) ;
#33264=ORIENTED_EDGE ( 'NONE', *, *, #59035, .F. ) ;
#33265=CARTESIAN_POINT ( 'NONE',  ( 5.500000000000000000, -6.661338147750999827E-14, 12.79999953825637427 ) ) ;
#33284=CARTESIAN_POINT ( 'NONE',  ( 18.14722095428672333, -2.700912180127440276, 13.62881044890620608 ) ) ;
#33302=CARTESIAN_POINT ( 'NONE',  ( 18.00364620838984919, -1.936356668767989397, -13.86561588859484395 ) ) ;
#33306=CARTESIAN_POINT ( 'NONE',  ( 12.24262961005303296, 2.226644062380152445, 13.72761226533214440 ) ) ;
#33357=CARTESIAN_POINT ( 'NONE',  ( 12.08078742596348576, 2.670354628897900540, 12.31525682382392084 ) ) ;
#33360=CARTESIAN_POINT ( 'NONE',  ( 12.13047358906990958, -0.2678304234474128687, -13.99744223245316199 ) ) ;
#33362=DIRECTION ( 'NONE',  ( 1.000000000000000000, 0.000000000000000000, 0.000000000000000000 ) ) ;
#33365=CARTESIAN_POINT ( 'NONE',  ( 5.657901059019435408, 12.07783836333738847, -3.734765664958211051 ) ) ;
#33368=CARTESIAN_POINT ( 'NONE',  ( 17.57587346436483600, 1.875000586273749992, -13.78631940097169739 ) ) ;
#33378=EDGE_LOOP ( 'NONE', ( #60851, #18492, #43770, #38743 ) ) ;
#33380=CARTESIAN_POINT ( 'NONE',  ( 18.17920330502697013, -2.539026862082569558, -13.66507545610718921 ) ) ;
#33388=CARTESIAN_POINT ( 'NONE',  ( 18.18389880332057018, -2.839229093938480997, -12.27596119698807975 ) ) ;
#33400=CARTESIAN_POINT ( 'NONE',  ( 12.18013031904082233, 2.522561724994068388, -13.66866813226131327 ) ) ;
#33403=CARTESIAN_POINT ( 'NONE',  ( 17.69685691690359164, 0.6090406077983143707, 13.88203505342131550 ) ) ;
#33409=CARTESIAN_POINT ( 'NONE',  ( 12.38151006044884639, -0.4597209098220048640, 13.88976952607801074 ) ) ;
#33418=EDGE_CURVE ( 'NONE', #68619, #46698, #18333, .T. ) ;
#33421=CARTESIAN_POINT ( 'NONE',  ( 18.17602447836047475, -0.07155418421575514276, 12.69973420405192144 ) ) ;
#33433=LINE ( 'NONE', #54749, #65541 ) ;
#33436=CARTESIAN_POINT ( 'NONE',  ( 12.15201606283210900, 0.3124912280145352161, -12.59612551846059780 ) ) ;
#33449=B_SPLINE_CURVE_WITH_KNOTS ( 'NONE', 3,
 ( #54303, #37197, #64433, #58515, #65128, #59552, #22144, #827, #37884 ),
 .UNSPECIFIED., .F., .F.,
 ( 4, 1, 2, 2, 4 ),
 ( 0.000000000000000000, 0.2500000000000002220, 0.3750000000000004441, 0.5000000000000006661, 1.000000000000000000 ),
 .UNSPECIFIED. ) ;
#33454=CARTESIAN_POINT ( 'NONE',  ( 18.17177275037307638, -0.1018973686818569341, -13.89950237059084870 ) ) ;
#33457=ORIENTED_EDGE ( 'NONE', *, *, #66716, .F. ) ;
#33465=CARTESIAN_POINT ( 'NONE',  ( 12.31588542589000390, -2.889160216960383387, -13.58313038422638286 ) ) ;
#33470=CARTESIAN_POINT ( 'NONE',  ( 12.18021258978589039, -2.482515821435917314, -12.45562150274660596 ) ) ;
#33478=CARTESIAN_POINT ( 'NONE',  ( 17.89002091993515720, -1.842089822799543253, 12.46461944294985358 ) ) ;
#33483=AXIS2_PLACEMENT_3D ( 'NONE', #21468, #68322, #64110 ) ;
#33493=CARTESIAN_POINT ( 'NONE',  ( 4.600000127571206576, -3.073097332162000125E-13, -5.595524044110998485E-14 ) ) ;
#33497=CARTESIAN_POINT ( 'NONE',  ( 12.80505043854144276, -0.7192913403693169672, -12.57945229203838267 ) ) ;
#33509=CARTESIAN_POINT ( 'NONE',  ( 18.06966903239548827, 2.854820418091308820, 13.59172178685414423 ) ) ;
#33520=CARTESIAN_POINT ( 'NONE',  ( 18.24298441323066555, -2.287290078788475345, -13.81189461436434307 ) ) ;
#33543=CARTESIAN_POINT ( 'NONE',  ( 12.63802361681258191, 3.180808137691514936, -12.19190235712761883 ) ) ;
#33556=CARTESIAN_POINT ( 'NONE',  ( 12.55449126378684532, -3.072671109762266095, -13.53512077903586786 ) ) ;
#33557=CARTESIAN_POINT ( 'NONE',  ( 18.11112283403659262, -0.2853680816562768063, -12.69568625917504257 ) ) ;
#33558=CARTESIAN_POINT ( 'NONE',  ( 12.19275557192769632, 2.625384353351010613, -12.42149591643997475 ) ) ;
#33569=CARTESIAN_POINT ( 'NONE',  ( 17.79060029153382416, 3.161091907734801865, 12.19703033907565981 ) ) ;
#33574=EDGE_LOOP ( 'NONE', ( #6769, #51674, #9533, #23945 ) ) ;
#33575=CARTESIAN_POINT ( 'NONE',  ( 12.11461379017079665, -2.700589376673579789, 12.30719081517757907 ) ) ;
#33583=EDGE_CURVE ( 'NONE', #62256, #52670, #4938, .T. ) ;
#33584=CARTESIAN_POINT ( 'NONE',  ( 12.25170120909046645, -0.4648927885597778920, 12.59142395508372836 ) ) ;
#33587=CARTESIAN_POINT ( 'NONE',  ( 12.33364337825305768, 2.910866508044257284, 12.34629936699908370 ) ) ;
#33593=CARTESIAN_POINT ( 'NONE',  ( 17.59542495535444218, -0.6250000000000002220, 12.67928922306855277 ) ) ;
#33601=CARTESIAN_POINT ( 'NONE',  ( 18.28104795956111062, 2.296528561426856019, -12.39041189979782409 ) ) ;
#33602=B_SPLINE_CURVE_WITH_KNOTS ( 'NONE', 3,
 ( #19669, #62315, #50803, #3915, #40639, #61974, #39619, #55703, #13058, #34728, #66519, #14430, #13739, #7801, #45216, #35072, #8146, #50448, #18642, #40306, #62981, #4955, #30849, #52856, #67895, #63327, #14770, #4264, #31537, #47958, #15792, #53546, #37123, #5636, #26291, #20013, #15457, #36087, #25601, #47617, #56, #15108, #21042, #31202, #37459, #20697, #58781, #36430, #21377, #10889, #68928, #42710, #64015, #57747, #42374, #16136, #32233, #63677, #41337, #62647, #58439, #26979, #31885, #57402, #9857, #20351, #41675, #52507, #4607 ),
 .UNSPECIFIED., .F., .F.,
 ( 4, 2, 2, 2, 2, 2, 2, 2, 2, 2, 2, 2, 2, 1, 2, 2, 2, 1, 2, 2, 2, 2, 1, 2, 2, 2, 2, 2, 2, 2, 2, 2, 2, 2, 2, 4 ),
 ( 0.000000000000000000, 0.06250000000002821354, 0.1250000000000564271, 0.1562500000000705269, 0.1875000000000846545, 0.2187500000000987543, 0.2343750000001060263, 0.2500000000001132983, 0.2812500000001282863, 0.2968750000001355582, 0.3125000000001428302, 0.3281250000001501022, 0.3437500000001573741, 0.3593750000001646461, 0.3671875000001683098, 0.3750000000001719735, 0.3906250000001779688, 0.3984375000001809108, 0.4023437500001826872, 0.4062500000001844636, 0.4218750000001930678, 0.4296875000001972866, 0.4335937500001988965, 0.4355468750001977307, 0.4375000000001965650, 0.4531250000001914580, 0.4687500000001863509, 0.4843750000001812439, 0.5000000000001760814, 0.5312500000001659783, 0.5468750000001606493, 0.5625000000001552092, 0.5937500000001438849, 0.6250000000001325606, 0.7500000000000878186, 1.000000000000000000 ),
 .UNSPECIFIED. ) ;
#33604=CARTESIAN_POINT ( 'NONE',  ( 12.10347303272475372, -2.332585440199567817, 13.80433171579881879 ) ) ;
#33608=EDGE_LOOP ( 'NONE', ( #44481, #44925, #47721, #15375 ) ) ;
#33610=CARTESIAN_POINT ( 'NONE',  ( 17.55505043854144631, -0.7192913403693119712, -12.57945229203838267 ) ) ;
#33617=CARTESIAN_POINT ( 'NONE',  ( 17.75825915738905536, 1.908867900852240673, -12.56984843829418530 ) ) ;
#33624=CARTESIAN_POINT ( 'NONE',  ( 18.20249159964110675, 0.3803681712634291445, -13.99548972733973073 ) ) ;
#33628=CARTESIAN_POINT ( 'NONE',  ( 12.19004578041274911, -2.611920287615140168, 12.42482035882550484 ) ) ;
#33633=CARTESIAN_POINT ( 'NONE',  ( 18.17485192111307057, -2.583003800953512563, 13.65552556266986350 ) ) ;
#33654=CARTESIAN_POINT ( 'NONE',  ( 12.41408225146703970, 2.012274740545226592, 13.76483611190083600 ) ) ;
#33658=CARTESIAN_POINT ( 'NONE',  ( 12.11457335221578369, 0.2229649748661308717, 13.99822903660538564 ) ) ;
#33670=AXIS2_PLACEMENT_3D ( 'NONE', #12760, #33046, #64839 ) ;
#33679=CARTESIAN_POINT ( 'NONE',  ( 4.650000881942629505, 3.375077994860000042E-14, 13.94999927503010362 ) ) ;
#33696=CARTESIAN_POINT ( 'NONE',  ( 5.700000000000000178, 13.04986661130000059, -1.811520473896000016 ) ) ;
#33699=CARTESIAN_POINT ( 'NONE',  ( 4.599999651764373532, 13.27499965161999818, -2.617296141720999949E-09 ) ) ;
#33701=CARTESIAN_POINT ( 'NONE',  ( 5.619513206070969602, 12.94695275831319492, 2.446394316580341233 ) ) ;
#33705=CARTESIAN_POINT ( 'NONE',  ( 12.78440349184324987, 0.6249994334955760733, -13.88107975403457495 ) ) ;
#33711=CARTESIAN_POINT ( 'NONE',  ( 5.602426839032992767, 12.13128594426812690, -3.749700506050852145 ) ) ;
#33713=VECTOR ( 'NONE', #29869, 1000.000000000000000 ) ;
#33714=B_SPLINE_CURVE_WITH_KNOTS ( 'NONE', 3,
 ( #53852, #16102, #53514, #27 ),
 .UNSPECIFIED., .F., .F.,
 ( 4, 4 ),
 ( 0.000000000000000000, 1.000000000000000000 ),
 .UNSPECIFIED. ) ;
#33716=CARTESIAN_POINT ( 'NONE',  ( 18.05294241905982133, 2.122066809870763127, -13.74638883949611845 ) ) ;
#33727=CARTESIAN_POINT ( 'NONE',  ( 18.10300909149178494, -2.800751615193656008, -13.60500513792289468 ) ) ;
#33735=CARTESIAN_POINT ( 'NONE',  ( 18.19141764354318269, -2.135256814392523683, -12.41776106013548464 ) ) ;
#33747=CARTESIAN_POINT ( 'NONE',  ( 17.55505043854147118, -3.125000000000000000, -13.52078605991414761 ) ) ;
#33748=CARTESIAN_POINT ( 'NONE',  ( 12.54527475442094442, 3.068547466015816294, -13.53629565290702352 ) ) ;
#33751=CARTESIAN_POINT ( 'NONE',  ( 18.17115727977514084, -0.3856318793704094361, 13.99470184309725695 ) ) ;
#33752=CARTESIAN_POINT ( 'NONE',  ( 17.93439120251456487, 0.4967442791785504075, 13.88805191678101458 ) ) ;
#33757=CARTESIAN_POINT ( 'NONE',  ( 12.54858531443457892, -0.5700392133465188582, 13.88426419246647292 ) ) ;
#33758=CARTESIAN_POINT ( 'NONE',  ( 12.72336452621133773, -0.6199804606865816359, -13.88138355690254855 ) ) ;
#33769=CARTESIAN_POINT ( 'NONE',  ( 18.05145864173986325, 0.3802890292809061323, 12.69234946364260708 ) ) ;
#33771=CARTESIAN_POINT ( 'NONE',  ( 17.88923853192078184, -3.028508370110811310, -12.31258559103177674 ) ) ;
#33785=CARTESIAN_POINT ( 'NONE',  ( 12.13986395842896648, -0.2863297863804592502, -12.59675086341328232 ) ) ;
#33786=LINE ( 'NONE', #8580, #17497 ) ;
#33789=EDGE_LOOP ( 'NONE', ( #28923, #68395, #36203, #63855 ) ) ;
#33802=CARTESIAN_POINT ( 'NONE',  ( 18.18003636789866917, -0.02080959496299032013, -13.89999914846831075 ) ) ;
#33825=CARTESIAN_POINT ( 'NONE',  ( 17.61541550669256395, -1.763241988052376641, 12.47601615708916789 ) ) ;
#33829=AXIS2_PLACEMENT_3D ( 'NONE', #35183, #62079, #14198 ) ;
#33854=CARTESIAN_POINT ( 'NONE',  ( 18.22207129059743380, 2.231684076289587981, 13.82098807703153476 ) ) ;
#33866=CARTESIAN_POINT ( 'NONE',  ( 18.00769469217373597, -3.088460579138319062, -13.65508963078420201 ) ) ;
#33873=EDGE_CURVE ( 'NONE', #42176, #32174, #15719, .T. ) ;
#33884=LINE ( 'NONE', #50304, #9401 ) ;
#33890=CARTESIAN_POINT ( 'NONE',  ( 12.61495819220210635, 3.174994159617164691, -12.19341885412869608 ) ) ;
#33893=B_SPLINE_CURVE_WITH_KNOTS ( 'NONE', 3,
 ( #11750, #16653, #48823, #15966, #54408, #48478, #47802, #585, #64195, #59653, #21894, #58618, #43231, #27498, #10717, #64536, #5482, #11405, #33092, #20872, #42210, #26817, #63512, #42888 ),
 .UNSPECIFIED., .F., .F.,
 ( 4, 2, 1, 1, 1, 2, 2, 1, 2, 2, 2, 2, 2, 4 ),
 ( 0.000000000000000000, 0.2499999999999175104, 0.3749999999998697708, 0.4374999999998425704, 0.4687499999998201994, 0.4843749999998034350, 0.4999999999997866706, 0.5624999999998281375, 0.5937499999998393507, 0.6249999999998505640, 0.6874999999998731015, 0.7499999999998955280, 0.8749999999999477085, 1.000000000000000000 ),
 .UNSPECIFIED. ) ;
#33898=CARTESIAN_POINT ( 'NONE',  ( 12.10796728133595579, -2.678710578830987288, -12.31197141455839272 ) ) ;
#33905=CARTESIAN_POINT ( 'NONE',  ( 12.42259655075935143, -2.994741173188553596, -13.55594337657172410 ) ) ;
#33906=CARTESIAN_POINT ( 'NONE',  ( 18.09636316215239660, 0.3125877143166576055, -12.69482668528969604 ) ) ;
#33912=CARTESIAN_POINT ( 'NONE',  ( 17.55505043854147118, -3.248147246781390329, -13.61798588129781074 ) ) ;
#33916=CARTESIAN_POINT ( 'NONE',  ( 18.09076461395649105, 2.178034604381229311, 12.52076370778328851 ) ) ;
#33922=CARTESIAN_POINT ( 'NONE',  ( 12.49755103297840542, -3.131894283645457300, 12.20455838002552795 ) ) ;
#33928=CARTESIAN_POINT ( 'NONE',  ( 12.09857507241189900, -0.1632583333441840756, 12.59896334813831764 ) ) ;
#33934=CARTESIAN_POINT ( 'NONE',  ( 12.30608813017793857, 2.123066299447892824, 12.53144042021393645 ) ) ;
#33940=CARTESIAN_POINT ( 'NONE',  ( 17.86524243499061271, -0.5426972542814749723, 12.68439075057083443 ) ) ;
#33947=CARTESIAN_POINT ( 'NONE',  ( 18.06384107467706102, -2.863137910839477662, 13.58970737937971229 ) ) ;
#33949=CARTESIAN_POINT ( 'NONE',  ( 12.33301873031884810, -1.963679441452091723, 13.86160245617593034 ) ) ;
#33951=CARTESIAN_POINT ( 'NONE',  ( 17.55505043854147118, -1.875000000000000000, 12.57545641911172396 ) ) ;
#33952=CARTESIAN_POINT ( 'NONE',  ( 17.55505043854143565, 3.248109929747637903, -13.61799478206225444 ) ) ;
#33960=VERTEX_POINT ( 'NONE', #37868 ) ;
#33970=CARTESIAN_POINT ( 'NONE',  ( 12.19275557201275362, -2.625384353767556078, 12.42149591633707573 ) ) ;
#33976=CARTESIAN_POINT ( 'NONE',  ( 18.18010564875750390, -2.481546250174181623, 13.67737493447378938 ) ) ;
#33984=PLANE ( 'NONE',  #27559 ) ;
#33989=AXIS2_PLACEMENT_3D ( 'NONE', #9869, #26300, #66 ) ;
#33993=DIRECTION ( 'NONE',  ( 1.000000000000000000, 0.000000000000000000, 0.000000000000000000 ) ) ;
#33995=CARTESIAN_POINT ( 'NONE',  ( 17.55505043854147118, -1.787797342887044172, -13.88538010501570774 ) ) ;
#33999=CARTESIAN_POINT ( 'NONE',  ( 12.55438499206305458, 1.927376109800345905, 13.77831414012769251 ) ) ;
#34005=CARTESIAN_POINT ( 'NONE',  ( 12.08612513405892841, 0.09509187666555039831, 13.99968209810982600 ) ) ;
#34054=CARTESIAN_POINT ( 'NONE',  ( 12.08006676141314983, 0.02431279293012172937, -13.99999914078080110 ) ) ;
#34061=CARTESIAN_POINT ( 'NONE',  ( 18.17249645628715626, 2.401006805677767808, -13.69397427989633620 ) ) ;
#34062=ORIENTED_EDGE ( 'NONE', *, *, #66295, .F. ) ;
#34070=ADVANCED_FACE ( 'NONE', ( #17587 ), #13387, .F. ) ;
#34072=ORIENTED_EDGE ( 'NONE', *, *, #68903, .F. ) ;
#34082=CARTESIAN_POINT ( 'NONE',  ( 18.08778676580602607, -1.991706414748710463, -12.44159931028328181 ) ) ;
#34092=CARTESIAN_POINT ( 'NONE',  ( 12.28091743413948578, 2.013400871504815282, -13.85446832019263397 ) ) ;
#34095=CARTESIAN_POINT ( 'NONE',  ( 17.91891929415153228, 0.5082612142235592989, 13.88749228919890122 ) ) ;
#34105=CARTESIAN_POINT ( 'NONE',  ( 12.19034750719213278, -2.613044105505787584, 13.64883414299444198 ) ) ;
#34117=CARTESIAN_POINT ( 'NONE',  ( 12.46489138696793475, -0.5244033890137438370, 12.68542455843550343 ) ) ;
#34118=CARTESIAN_POINT ( 'NONE',  ( 18.09718405123029328, -2.811158313956393151, -12.37360767970495701 ) ) ;
#34119=ORIENTED_EDGE ( 'NONE', *, *, #4267, .T. ) ;
#34121=CARTESIAN_POINT ( 'NONE',  ( 12.35578833716350822, -1.907710147612963203, -12.45493153468922287 ) ) ;
#34131=CARTESIAN_POINT ( 'NONE',  ( 12.23732871802942590, -0.4475098806653898253, -12.59205372277267720 ) ) ;
#34147=CARTESIAN_POINT ( 'NONE',  ( 18.27397574302396777, 0.09509187666554888563, -13.99968209810982067 ) ) ;
#34152=ADVANCED_FACE ( 'NONE', ( #2532 ), #1501, .F. ) ;
#34154=CARTESIAN_POINT ( 'NONE',  ( 18.18005043817898425, -2.519674554510558107, 12.44700836740716277 ) ) ;
#34159=CARTESIAN_POINT ( 'NONE',  ( 12.56936319536957214, -3.210092459286436828, 13.62701963584217957 ) ) ;
#34167=CARTESIAN_POINT ( 'NONE',  ( 12.75695018768104028, -1.789009927756594953, -13.88522413357867258 ) ) ;
#34169=CARTESIAN_POINT ( 'NONE',  ( 17.82442946238797887, -1.812220263014551858, 12.46899672597967523 ) ) ;
#34179=AXIS2_PLACEMENT_3D ( 'NONE', #69063, #35874, #5433 ) ;
#34200=CARTESIAN_POINT ( 'NONE',  ( 17.57920283571456110, 1.787797991197233038, 13.88537998700429554 ) ) ;
#34205=B_SPLINE_CURVE_WITH_KNOTS ( 'NONE', 3,
 ( #32350, #49802, #40341, #2931, #56074, #44576, #8528, #61325, #24259, #12745, #1909, #44228, #40010, #50150, #34765, #2255, #38972, #23569 ),
 .UNSPECIFIED., .F., .F.,
 ( 4, 2, 2, 2, 2, 2, 2, 2, 4 ),
 ( 0.5009155270902391210, 0.5633010862039588007, 0.5944938657608188626, 0.6256866453176790355, 0.6568794248745390973, 0.6880722044313991592, 0.7504577635451192830, 0.8752288817725597525, 1.000000000000000000 ),
 .UNSPECIFIED. ) ;
#34212=EDGE_LOOP ( 'NONE', ( #50932, #60843, #9724, #65173, #48918 ) ) ;
#34236=CARTESIAN_POINT ( 'NONE',  ( 12.25790434794250494, 2.952613167459276156, -12.24916959777017134 ) ) ;
#34245=CARTESIAN_POINT ( 'NONE',  ( 12.14231515301104736, -2.188169521966901065, -12.40854677421460295 ) ) ;
#34252=CARTESIAN_POINT ( 'NONE',  ( 12.46419745175926153, -3.023973028971910004, -13.54820305185628904 ) ) ;
#34253=CARTESIAN_POINT ( 'NONE',  ( 18.13658048666561484, -0.2292434675627126606, -12.69722039463305840 ) ) ;
#34261=VECTOR ( 'NONE', #46959, 1000.000000000000000 ) ;
#34262=CARTESIAN_POINT ( 'NONE',  ( 18.13782450322838358, 2.273941707540254598, 12.50136077393157308 ) ) ;
#34271=CARTESIAN_POINT ( 'NONE',  ( 12.29460735697735174, -2.139198256859472291, 12.52837235904283730 ) ) ;
#34278=CARTESIAN_POINT ( 'NONE',  ( 12.51625386035102316, -0.6598665579121884006, 12.58271022457860688 ) ) ;
#34281=CARTESIAN_POINT ( 'NONE',  ( 12.35269809054579149, 2.068595867586759063, 12.54166796000260398 ) ) ;
#34282=ORIENTED_EDGE ( 'NONE', *, *, #52792, .T. ) ;
#34293=CARTESIAN_POINT ( 'NONE',  ( 17.91802421017324320, -0.5088992770524164433, -12.68627498207444226 ) ) ;
#34295=CARTESIAN_POINT ( 'NONE',  ( 17.55505043854147118, -3.125000000000000000, 13.52084414783465860 ) ) ;
#34302=CARTESIAN_POINT ( 'NONE',  ( 17.55505043854144276, -0.6250000000000001110, -12.67928921589118474 ) ) ;
#34317=CARTESIAN_POINT ( 'NONE',  ( 17.55505043854147118, -3.199751711897561801, 12.18694338143115452 ) ) ;
#34319=CARTESIAN_POINT ( 'NONE',  ( 12.18432844470339127, -2.573800461448675136, 12.43409912879217849 ) ) ;
#34326=CARTESIAN_POINT ( 'NONE',  ( 18.23401891600715885, -2.774919967966536838, 13.72225625730859377 ) ) ;
#34350=CARTESIAN_POINT ( 'NONE',  ( 12.75679378108275586, 3.246933784478220009, 13.61827548339043581 ) ) ;
#34354=CARTESIAN_POINT ( 'NONE',  ( 12.08146951720330975, 0.04720351400547449089, 13.99992551180917388 ) ) ;
#34362=STYLED_ITEM ( 'NONE', ( #44059 ), #6030 ) ;
#34371=CARTESIAN_POINT ( 'NONE',  ( 12.80505043854144276, -0.7192913403693027563, 12.57945229203838267 ) ) ;
#34393=CARTESIAN_POINT ( 'NONE',  ( 18.21613312502037019, 2.776914653343697026, -12.29020858420810924 ) ) ;
#34401=CARTESIAN_POINT ( 'NONE',  ( 17.55505043854143565, 1.787816316115923954, -13.88537766212463254 ) ) ;
#34403=CARTESIAN_POINT ( 'NONE',  ( 12.60420804235854675, 0.5919407257947373324, -13.88303015925713879 ) ) ;
#34405=DIRECTION ( 'NONE',  ( 0.000000000000000000, 0.7198977633594745296, -0.6940801180771755119 ) ) ;
#34409=DIRECTION ( 'NONE',  ( 1.000000000000000000, 0.000000000000000000, 0.000000000000000000 ) ) ;
#34411=CARTESIAN_POINT ( 'NONE',  ( 17.81510163565844707, 1.931577867956977945, -13.77771208381435031 ) ) ;
#34415=VECTOR ( 'NONE', #61889, 1000.000000000000000 ) ;
#34419=ADVANCED_FACE ( 'NONE', ( #63997 ), #48625, .T. ) ;
#34420=CARTESIAN_POINT ( 'NONE',  ( 12.80505043854146940, -3.248109929747638347, 13.61799478206225444 ) ) ;
#34421=CARTESIAN_POINT ( 'NONE',  ( 17.78594645484335857, 0.5808586469753534987, -12.68211397078068003 ) ) ;
#34427=CARTESIAN_POINT ( 'NONE',  ( 18.03215848267582189, -2.904634633620106765, -13.57923905310026313 ) ) ;
#34433=CARTESIAN_POINT ( 'NONE',  ( 18.21786174063356967, -2.187645605293250917, -12.40865382983254506 ) ) ;
#34438=AXIS2_PLACEMENT_3D ( 'NONE', #45058, #7644, #2398 ) ;
#34442=DIRECTION ( 'NONE',  ( 0.7071067779452319124, 0.5091007393949228410, -0.4907305184431219325 ) ) ;
#34445=CARTESIAN_POINT ( 'NONE',  ( 12.11351653522380545, 2.298558756434998518, -13.81002389223456106 ) ) ;
#34449=CARTESIAN_POINT ( 'NONE',  ( 17.57569738523962144, 0.6249994334955766284, 13.88107975403459626 ) ) ;
#34455=CARTESIAN_POINT ( 'NONE',  ( 12.18008982747132229, -2.511713771506315140, 13.67097129485760476 ) ) ;
#34467=CARTESIAN_POINT ( 'NONE',  ( 17.85930819889520293, 0.5460377805369025506, 12.68419612078310621 ) ) ;
#34468=CARTESIAN_POINT ( 'NONE',  ( 12.66329582877813387, -0.6090237436603173071, 12.68033599931052713 ) ) ;
#34470=CARTESIAN_POINT ( 'NONE',  ( 18.11819331234647024, -2.771443073964306336, -12.38417569150683128 ) ) ;
#34473=CARTESIAN_POINT ( 'NONE',  ( 12.80505043854146940, -1.760910691117821614, -12.47634535983622683 ) ) ;
#34484=CARTESIAN_POINT ( 'NONE',  ( 12.18940205905204621, -0.3800566752825980110, -12.59427093624936767 ) ) ;
#34497=VERTEX_POINT ( 'NONE', #22039 ) ;
#34498=ORIENTED_EDGE ( 'NONE', *, *, #23750, .F. ) ;
#34501=CARTESIAN_POINT ( 'NONE',  ( 17.85480509960784445, 0.6653129401483860450, -13.98418548573916098 ) ) ;
#34511=CARTESIAN_POINT ( 'NONE',  ( 12.80505043854146940, -1.875000000000000444, -12.57541666120756396 ) ) ;
#34513=CARTESIAN_POINT ( 'NONE',  ( 12.80505043854146940, -3.125000000000000000, -13.52078605991414761 ) ) ;
#34517=EDGE_LOOP ( 'NONE', ( #60104, #67230, #56288, #55367 ) ) ;
#34523=CARTESIAN_POINT ( 'NONE',  ( 12.30864111941013128, -0.3802875570022061225, -13.89301034115781874 ) ) ;
#34524=CARTESIAN_POINT ( 'NONE',  ( 18.16360624365139742, -2.642789843301108554, 12.41718366361783232 ) ) ;
#34529=CARTESIAN_POINT ( 'NONE',  ( 18.17481653528710339, 2.416771143787688203, 13.69072451370120369 ) ) ;
#34554=CARTESIAN_POINT ( 'NONE',  ( 18.15197774836038036, 2.932501865601730984, 13.68943155935733991 ) ) ;
#34585=CARTESIAN_POINT ( 'NONE',  ( 12.20034797952038552, 2.341680320747017596, -12.48707311375845030 ) ) ;
#34589=EDGE_CURVE ( 'NONE', #31306, #26914, #54099, .T. ) ;
#34595=CARTESIAN_POINT ( 'NONE',  ( 17.55505043854144276, 0.7302158263239086899, 13.98094363220831049 ) ) ;
#34598=CARTESIAN_POINT ( 'NONE',  ( 12.13061620557594722, -2.744764576889035634, -12.29741386912397161 ) ) ;
#34604=CARTESIAN_POINT ( 'NONE',  ( 12.60230703261661667, -3.091556739796029074, -13.52998185037902346 ) ) ;
#34605=CARTESIAN_POINT ( 'NONE',  ( 18.17607568152034148, -0.07112609253419316380, -12.69973757146476778 ) ) ;
#34616=CARTESIAN_POINT ( 'NONE',  ( 17.88942345255911093, 3.118753088769705251, 12.20792418036210591 ) ) ;
#34622=CARTESIAN_POINT ( 'NONE',  ( 12.20034797952042105, -2.341680320747018484, 12.48707311375845208 ) ) ;
#34627=CARTESIAN_POINT ( 'NONE',  ( 12.22381919988786869, 0.2299973361971391905, 12.69720198919503495 ) ) ;
#34630=CARTESIAN_POINT ( 'NONE',  ( 12.48926758269842807, 1.960545016317334355, 12.56101064709213411 ) ) ;
#34642=B_SPLINE_CURVE_WITH_KNOTS ( 'NONE', 3,
 ( #47813, #54421, #17008, #21227, #64551, #32079, #5144, #5831, #38691, #26480, #1287, #42556, #59317, #60013, #12123, #43244 ),
 .UNSPECIFIED., .F., .F.,
 ( 4, 2, 2, 2, 2, 2, 2, 4 ),
 ( 0.000000000000000000, 0.06250000000000105471, 0.1250000000000021094, 0.2500000000000022204, 0.5000000000000011102, 0.7500000000000000000, 0.8750000000000000000, 1.000000000000000000 ),
 .UNSPECIFIED. ) ;
#34644=CARTESIAN_POINT ( 'NONE',  ( 18.12548766259744326, -0.2560639956372497972, -12.69654133872746726 ) ) ;
#34655=CARTESIAN_POINT ( 'NONE',  ( 17.94172469452077223, 2.002341272942101291, -13.76666224251748893 ) ) ;
#34658=ORIENTED_EDGE ( 'NONE', *, *, #46844, .F. ) ;
#34665=CARTESIAN_POINT ( 'NONE',  ( 12.80505043854143388, 1.760845406083386688, -12.47635457398814829 ) ) ;
#34668=CARTESIAN_POINT ( 'NONE',  ( 12.21062133715901332, -2.693099985139989272, 12.40450382423467346 ) ) ;
#34669=EDGE_CURVE ( 'NONE', #56202, #62522, #2608, .T. ) ;
#34672=CARTESIAN_POINT ( 'NONE',  ( 17.91291100103723011, -1.987489628841895062, 13.76889314140747622 ) ) ;
#34695=CARTESIAN_POINT ( 'NONE',  ( 12.80505043854144276, -0.6951438842159390896, 13.94765567169528531 ) ) ;
#34696=CARTESIAN_POINT ( 'NONE',  ( 12.33271654538601325, 2.090191715682863993, 13.75184336857263467 ) ) ;
#34698=EDGE_LOOP ( 'NONE', ( #44751, #14910, #60098, #49039 ) ) ;
#34699=CARTESIAN_POINT ( 'NONE',  ( 12.26182617413804365, 0.3097617570999572911, -12.69493148512597180 ) ) ;
#34700=CARTESIAN_POINT ( 'NONE',  ( 12.61664971283087233, 0.7055305429986050703, 13.98221279804358019 ) ) ;
#34701=VERTEX_POINT ( 'NONE', #42274 ) ;
#34710=CARTESIAN_POINT ( 'NONE',  ( 12.41985246593407766, 3.089908466900595396, 12.21525705840282150 ) ) ;
#34721=AXIS2_PLACEMENT_3D ( 'NONE', #44411, #1058, #54540 ) ;
#34726=CIRCLE ( 'NONE', #53719, 13.17499999999999893 ) ;
#34728=CARTESIAN_POINT ( 'NONE',  ( 12.43967993051476562, 3.007449918965190871, 13.55258931251708887 ) ) ;
#34731=DIRECTION ( 'NONE',  ( 0.000000000000000000, 0.000000000000000000, 1.000000000000000000 ) ) ;
#34732=CARTESIAN_POINT ( 'NONE',  ( 18.05438665931229636, 1.958444820271048270, -12.44686948166836338 ) ) ;
#34736=CARTESIAN_POINT ( 'NONE',  ( 12.20625471193361911, 2.679103183902759699, -13.63384013640462911 ) ) ;
#34740=CARTESIAN_POINT ( 'NONE',  ( 17.92262925329511347, 1.881361389459298650, -13.87306285015964669 ) ) ;
#34741=CARTESIAN_POINT ( 'NONE',  ( 12.10431174240585683, -0.1888260363403144737, -13.99874504378992590 ) ) ;
#34743=EDGE_CURVE ( 'NONE', #36489, #9530, #68463, .T. ) ;
#34744=CARTESIAN_POINT ( 'NONE',  ( 18.16413073598037187, -2.358269131811904007, -13.70246680370806835 ) ) ;
#34748=CARTESIAN_POINT ( 'NONE',  ( 43.76123417800000226, 11.06886219213000011, -1.536526853569999851 ) ) ;
#34752=CARTESIAN_POINT ( 'NONE',  ( 17.93785022694513742, 2.005837716635007428, -13.76593133495255650 ) ) ;
#34753=ORIENTED_EDGE ( 'NONE', *, *, #2019, .T. ) ;
#34759=CARTESIAN_POINT ( 'NONE',  ( 18.03350839574970266, 0.4021454017141842252, -12.69143011153355971 ) ) ;
#34765=CARTESIAN_POINT ( 'NONE',  ( 17.87143624847783130, -1.954798354107785796, 13.77413458886801934 ) ) ;
#34772=CARTESIAN_POINT ( 'NONE',  ( 18.10215020711902767, -2.952580169587739167, -12.24917755118609008 ) ) ;
#34776=AXIS2_PLACEMENT_3D ( 'NONE', #50071, #8456, #2858 ) ;
#34783=CARTESIAN_POINT ( 'NONE',  ( 12.30643338748584092, 1.987817336848021421, -13.85816184334709611 ) ) ;
#34786=CARTESIAN_POINT ( 'NONE',  ( 18.18884185737634951, 0.3547769576528340130, 13.99550803169339730 ) ) ;
#34787=CARTESIAN_POINT ( 'NONE',  ( 18.15916593610296559, -2.338515402807624710, 12.48776758576643964 ) ) ;
#34792=CARTESIAN_POINT ( 'NONE',  ( 12.18578014162844170, -2.585505937787686559, 13.65496065471434051 ) ) ;
#34804=CARTESIAN_POINT ( 'NONE',  ( 17.98256582722315144, 0.4560270868711856496, 12.68898073362800005 ) ) ;
#34805=CARTESIAN_POINT ( 'NONE',  ( 12.23478064047700009, -0.2559538865579775724, 12.69653251248904979 ) ) ;
#34818=CARTESIAN_POINT ( 'NONE',  ( 12.79307474260548538, 0.7192913015564709189, -12.57945229205062176 ) ) ;
#34827=DIRECTION ( 'NONE',  ( -0.000000000000000000, -0.000000000000000000, 1.000000000000000000 ) ) ;
#34837=CARTESIAN_POINT ( 'NONE',  ( 18.24183043734545961, 0.2342631834278595948, -13.99804438501501203 ) ) ;
#34851=ADVANCED_FACE ( 'NONE', ( #32808 ), #24038, .T. ) ;
#34856=CARTESIAN_POINT ( 'NONE',  ( 12.39285819377765918, 0.4699225802676940122, -13.88930950616751225 ) ) ;
#34857=CARTESIAN_POINT ( 'NONE',  ( 17.99286279921838982, -2.053846844283184758, 12.54442212638278775 ) ) ;
#34860=ORIENTED_EDGE ( 'NONE', *, *, #42775, .F. ) ;
#34882=CARTESIAN_POINT ( 'NONE',  ( 18.20001934199751759, -0.3287229608534071867, 12.59571550161850695 ) ) ;
#34890=CARTESIAN_POINT ( 'NONE',  ( 17.72189171626099125, 1.806990214763249059, 13.88289628861100589 ) ) ;
#34900=CARTESIAN_POINT ( 'NONE',  ( 18.18935690068784794, -2.871730747427968300, -13.70230915895854018 ) ) ;
#34914=CIRCLE ( 'NONE', #39349, 12.59999999999999964 ) ;
#34924=CARTESIAN_POINT ( 'NONE',  ( 12.37600679962888961, 2.954502784796254389, -12.33399089453511444 ) ) ;
#34934=CARTESIAN_POINT ( 'NONE',  ( 12.22840029456390099, -2.917071392396663576, -12.25769309035714905 ) ) ;
#34941=CARTESIAN_POINT ( 'NONE',  ( 12.66131753640905266, -3.108595072584062091, -13.52531149670802968 ) ) ;
#34946=CARTESIAN_POINT ( 'NONE',  ( 17.70945903195350724, -3.183352579998545373, 12.19123751323113325 ) ) ;
#34951=CARTESIAN_POINT ( 'NONE',  ( 18.18005043832643963, 2.519786135693555806, 13.66921024419250763 ) ) ;
#34954=CARTESIAN_POINT ( 'NONE',  ( 17.63760627221310173, 1.880133632725761172, 12.57457483776006768 ) ) ;
#34960=CARTESIAN_POINT ( 'NONE',  ( 12.20301641406255477, -2.331821773330018832, 12.48918929053770199 ) ) ;
#34966=CARTESIAN_POINT ( 'NONE',  ( 12.20412026884455692, 0.1720826094844745413, 12.69843621396828226 ) ) ;
#34970=CARTESIAN_POINT ( 'NONE',  ( 12.18180637322645055, 2.452078064253477407, 12.46259978693892556 ) ) ;
#34991=DIRECTION ( 'NONE',  ( -0.000000000000000000, -0.000000000000000000, 1.000000000000000000 ) ) ;
#34996=CARTESIAN_POINT ( 'NONE',  ( 5.500000000000000000, 0.000000000000000000, 0.000000000000000000 ) ) ;
#34998=CARTESIAN_POINT ( 'NONE',  ( 17.88386803574400830, -0.5319881936462144134, 13.88630234897559035 ) ) ;
#35011=CARTESIAN_POINT ( 'NONE',  ( 12.37651575366414924, -2.955073904877951296, 12.33383124654599072 ) ) ;
#35012=AXIS2_PLACEMENT_3D ( 'NONE', #64475, #58909, #38617 ) ;
#35015=AXIS2_PLACEMENT_3D ( 'NONE', #57644, #53443, #58335 ) ;
#35016=CARTESIAN_POINT ( 'NONE',  ( 17.94601859325910098, -2.012274714637017681, 13.76488447091686496 ) ) ;
#35027=CARTESIAN_POINT ( 'NONE',  ( 18.26845433917840822, -0.1286734328892429335, -12.59934825840596773 ) ) ;
#35032=VERTEX_POINT ( 'NONE', #32390 ) ;
#35039=CARTESIAN_POINT ( 'NONE',  ( 12.25828482332352820, 2.997587547359421123, 13.67532635696712440 ) ) ;
#35042=CARTESIAN_POINT ( 'NONE',  ( 12.18394763206765852, 0.08111188053566398271, -12.69973954613554135 ) ) ;
#35043=CARTESIAN_POINT ( 'NONE',  ( 12.68599131528412371, 0.7206971133477456659, 13.98143832535762954 ) ) ;
#35046=CARTESIAN_POINT ( 'NONE',  ( 12.80505043854144276, -0.6564304467897670303, 12.64601024127357931 ) ) ;
#35049=CARTESIAN_POINT ( 'NONE',  ( 4.599999999999999645, 0.7192913403693023122, 12.57945229203838267 ) ) ;
#35053=CARTESIAN_POINT ( 'NONE',  ( 12.44013165738121884, 3.102068138921894036, 12.21217476962502246 ) ) ;
#35058=AXIS2_PLACEMENT_3D ( 'NONE', #54377, #64855, #36934 ) ;
#35063=CARTESIAN_POINT ( 'NONE',  ( 12.18124154974186801, 2.460017072603256860, 12.46078795775544812 ) ) ;
#35072=CARTESIAN_POINT ( 'NONE',  ( 12.34838569214080550, 2.927120983257067710, 13.57349088381402247 ) ) ;
#35074=ORIENTED_EDGE ( 'NONE', *, *, #489, .T. ) ;
#35080=CARTESIAN_POINT ( 'NONE',  ( 17.94181191902910655, 1.871597878487315292, -12.46022310877026662 ) ) ;
#35084=B_SPLINE_CURVE_WITH_KNOTS ( 'NONE', 3,
 ( #20179, #46415, #15627, #51985, #41506, #67716, #41172, #9333, #62479, #36958, #25772, #58272, #14599, #47104, #63156, #10375 ),
 .UNSPECIFIED., .F., .F.,
 ( 4, 2, 2, 2, 2, 2, 2, 4 ),
 ( 0.000000000000000000, 0.06250000000000126288, 0.1250000000000025258, 0.2500000000000006106, 0.4999999999999993339, 0.7499999999999980016, 0.8749999999999990008, 1.000000000000000000 ),
 .UNSPECIFIED. ) ;
#35085=CARTESIAN_POINT ( 'NONE',  ( 12.19113298428035996, 2.617185168768731529, -13.64790684748345839 ) ) ;
#35087=DIRECTION ( 'NONE',  ( 0.000000000000000000, -0.000000000000000000, 1.000000000000000000 ) ) ;
#35091=CARTESIAN_POINT ( 'NONE',  ( 12.08965255773059155, 0.1190513140356027066, -13.99949878896183719 ) ) ;
#35097=EDGE_LOOP ( 'NONE', ( #32823, #39390, #6895, #62286, #65770 ) ) ;
#35099=CARTESIAN_POINT ( 'NONE',  ( 17.87817017025372834, 1.864246049947063666, -13.87532391830906420 ) ) ;
#35106=CARTESIAN_POINT ( 'NONE',  ( 18.02496081238558645, 0.4121104636170003777, -12.69099970358804086 ) ) ;
#35118=CARTESIAN_POINT ( 'NONE',  ( 18.10356236467040958, -2.200227019994205779, -12.51636715934673383 ) ) ;
#35124=DIRECTION ( 'NONE',  ( 0.000000000000000000, 0.9553735099700839672, 0.2954005017724949389 ) ) ;
#35127=CARTESIAN_POINT ( 'NONE',  ( 12.13805290469195874, 2.231685852207990095, -13.82098778992225441 ) ) ;
#35130=DIRECTION ( 'NONE',  ( 1.000000000000000000, 0.000000000000000000, 0.000000000000000000 ) ) ;
#35137=CARTESIAN_POINT ( 'NONE',  ( 12.18233509006626214, -2.554099910185274602, 13.66183974825599279 ) ) ;
#35150=CARTESIAN_POINT ( 'NONE',  ( 18.09667132770092834, 0.3125562302819395732, 12.69484091569602668 ) ) ;
#35151=CARTESIAN_POINT ( 'NONE',  ( 18.17924748726904838, -2.534358940396702842, -12.44349985638940304 ) ) ;
#35157=B_SPLINE_SURFACE_WITH_KNOTS ( 'NONE', 1, 3, ( 
 ( #36608, #21211, #10030, #31369, #47797, #42541, #53377, #21891, #43228, #32061, #582, #69105, #58615, #52681, #10714, #4777, #64532, #59298, #11402, #26117, #43578, #27495, #13154, #2306, #49157, #49854, #65581, #59996, #44283, #34131, #1966, #12451, #11747, #22240, #34484, #55448, #64878, #17706, #44630, #33089, #33785, #7207, #28898, #43926, #39029, #38320, #54405, #59650, #60344, #6505, #38675, #23289, #27850, #48820, #22585, #23626, #50205, #1615, #65232, #17347, #12107, #65922, #39367, #6154, #60686, #22931, #18049, #7543, #1269, #929, #6851, #33436, #54752, #16992, #49503, #44966, #28188, #12803, #66270, #55101, #18392, #39717, #28543, #61035, #24660, #40391, #46678, #40735, #2645, #55795, #45651, #56822, #61379, #51231, #29586, #2984, #50889, #30259, #67635, #24317, #8922, #56475, #61714, #20099, #14174, #3328, #13833, #8239, #35501, #62400, #34818, #30592 ),
 ( #35163, #51563, #3660, #25000, #19410, #29234, #66957, #46333, #67982, #29925, #45308, #19758, #45982, #41082, #14519, #19064, #41425, #56131, #35836, #57154, #9250, #8578, #51906, #62734, #67294, #62060, #4003, #25340, #14856, #23974, #7897, #50545, #66615, #18736, #40067, #13499, #9598, #68668, #31288, #43140, #58876, #26382, #37544, #58527, #48045, #5044, #37210, #15545, #10292, #42116, #52596, #31978, #10633, #63422, #4691, #10981, #36874, #147, #36178, #26034, #15878, #63767, #64107, #47708, #58190, #57490, #15196, #31627, #64443, #27069, #30940, #48386, #52256, #53290, #16222, #69018, #21133, #57844, #4352, #20785, #5391, #47363, #52947, #42458, #9951, #26729, #21465, #42801, #32320, #25684, #53633, #47017, #68319, #5728, #493, #21808, #20440, #41767, #63070, #36521, #65140, #6764, #838, #49074, #43495, #38942, #17261, #55017, #22153, #53968, #37894, #24502 ) ),
 .UNSPECIFIED., .F., .F., .F.,
 ( 2, 2 ),
 ( 4, 2, 2, 2, 2, 2, 2, 2, 2, 2, 2, 2, 2, 2, 2, 2, 2, 2, 2, 2, 2, 2, 2, 2, 2, 2, 2, 2, 2, 2, 2, 2, 2, 2, 2, 2, 2, 2, 2, 2, 2, 2, 2, 2, 2, 2, 2, 2, 2, 2, 2, 2, 2, 2, 2, 4 ),
 ( 0.000000000000000000, 1.000000000000000000 ),
 ( 0.000000000000000000, 7.083325941644376151E-05, 0.0001416665188328875230, 0.0002124997782493312981, 0.0002479164079575531992, 0.0002833330376657750460, 0.0003187496673739968929, 0.0003541662970822187940, 0.0004249995564986625961, 0.0004604161862068844972, 0.0004781245010609954478, 0.0004958328159151063983, 0.0005312494456233282994, 0.0005666660753315500921, 0.0006374993347479937858, 0.0006729159644562156869, 0.0007083325941644375880, 0.0007437492238726594890, 0.0007791658535808813901, 0.0008145824832891032912, 0.0008499991129973251923, 0.0008854157427055470934, 0.0009208323724137689945, 0.0009562490021219908955, 0.0009916656318302127966, 0.001027082261538434698, 0.001062498891246656599, 0.001133332150663100184, 0.001168748780371322085, 0.001204165410079543769, 0.001239582039787765671, 0.001274998669495987572, 0.001345831928912431374, 0.001381248558620653275, 0.001416665188328875176, 0.001452081818037097077, 0.001469790132891207919, 0.001487498447745318978, 0.001558331707161762780, 0.001629164966578206582, 0.001664581596286428484, 0.001699998225994650385, 0.001735414855702872286, 0.001770831485411094187, 0.001841664744827537989, 0.001877081374535759890, 0.001912498004243981791, 0.001947914633952203692, 0.001983331263660425593, 0.002018747893368647711, 0.002054164523076869395, 0.002124997782493313198, 0.002160414412201534882, 0.002195831041909756566, 0.002231247671617978684, 0.002266664301326200368 ),
 .UNSPECIFIED. ) ;
#35161=CARTESIAN_POINT ( 'NONE',  ( 21.35000154058000277, 0.000000000000000000, 0.000000000000000000 ) ) ;
#35163=CARTESIAN_POINT ( 'NONE',  ( 12.80505043854144276, -0.6250000000000006661, -12.67928921589118652 ) ) ;
#35170=CARTESIAN_POINT ( 'NONE',  ( 17.81164675503526951, 0.5699806461722944917, 12.68277882560270875 ) ) ;
#35180=CARTESIAN_POINT ( 'NONE',  ( 18.27977752388258281, 0.02332822437944338106, -13.99998565365491388 ) ) ;
#35183=CARTESIAN_POINT ( 'NONE',  ( 5.700000000000000178, -13.94845324556000143, 4.312847325879000770 ) ) ;
#35186=CARTESIAN_POINT ( 'NONE',  ( 18.13004437690753434, -2.745098799756841679, 12.39110308487445344 ) ) ;
#35194=CARTESIAN_POINT ( 'NONE',  ( 12.70933660604967130, -3.243304671741783274, 13.61914346456210012 ) ) ;
#35204=CARTESIAN_POINT ( 'NONE',  ( 12.66238154463050769, -0.6088408278571626475, -13.88204686096231733 ) ) ;
#35205=CARTESIAN_POINT ( 'NONE',  ( 18.06416738895852347, -2.863102795628076347, 12.35955380825001093 ) ) ;
#35210=CARTESIAN_POINT ( 'NONE',  ( 18.05677685604840832, 2.118334401049060567, 13.74715678132749019 ) ) ;
#35228=CARTESIAN_POINT ( 'NONE',  ( 17.55505043854144276, -0.7192913403693027563, 12.57945229203838267 ) ) ;
#35234=CARTESIAN_POINT ( 'NONE',  ( 18.16514092158336879, 2.912582788079544294, 13.69368340938387973 ) ) ;
#35253=AXIS2_PLACEMENT_3D ( 'NONE', #7675, #61502, #45770 ) ;
#35267=CARTESIAN_POINT ( 'NONE',  ( 12.30770095535949338, 2.879049501765980512, -12.35516346652264552 ) ) ;
#35274=CARTESIAN_POINT ( 'NONE',  ( 18.20249159964072661, -0.3803681712697531969, 13.99548972733949803 ) ) ;
#35276=CARTESIAN_POINT ( 'NONE',  ( 12.24851426484566908, -2.019008278824865332, -12.43718985311489966 ) ) ;
#35277=AXIS2_PLACEMENT_3D ( 'NONE', #12972, #60508, #55268 ) ;
#35284=CARTESIAN_POINT ( 'NONE',  ( 12.49029065891183343, -1.959656569402036475, -13.77327738386123279 ) ) ;
#35285=EDGE_CURVE ( 'NONE', #46698, #53716, #2426, .T. ) ;
#35293=CARTESIAN_POINT ( 'NONE',  ( 18.05135021982939492, 2.880031268700117941, 13.58542674995964994 ) ) ;
#35302=CARTESIAN_POINT ( 'NONE',  ( 12.23374516775632159, -2.245741837849043687, 12.50722324768529781 ) ) ;
#35308=CARTESIAN_POINT ( 'NONE',  ( 12.42881362571445436, 0.4990964484179714611, 12.68679736436866712 ) ) ;
#35312=CARTESIAN_POINT ( 'NONE',  ( 12.78420607872184966, 1.875260891907201133, 12.57537395219491216 ) ) ;
#35321=ORIENTED_EDGE ( 'NONE', *, *, #23039, .F. ) ;
#35324=CARTESIAN_POINT ( 'NONE',  ( 17.69809845378366120, -0.6087666915580426386, -12.68035271361765304 ) ) ;
#35332=CARTESIAN_POINT ( 'NONE',  ( 12.35242198444192674, -3.088429417998432847, 13.65509667848947473 ) ) ;
#35355=CARTESIAN_POINT ( 'NONE',  ( 17.55505043854147118, -3.248109929747638347, 13.61799478206225444 ) ) ;
#35356=CARTESIAN_POINT ( 'NONE',  ( 21.49999863197000138, 1.172395514003999961E-13, 13.99999975536035279 ) ) ;
#35366=EDGE_CURVE ( 'NONE', #57425, #53074, #51564, .T. ) ;
#35367=CARTESIAN_POINT ( 'NONE',  ( 18.27863132999453200, -0.04649795050485940051, -12.59991969135870526 ) ) ;
#35379=CARTESIAN_POINT ( 'NONE',  ( 12.18713711904774399, 2.135907760014737811, 13.83611243771405697 ) ) ;
#35382=CARTESIAN_POINT ( 'NONE',  ( 12.54851516836652969, 0.5702235046495642834, -12.68276536598757787 ) ) ;
#35383=CARTESIAN_POINT ( 'NONE',  ( 12.09168665071629967, -0.1308528744652237841, 13.99939340647621044 ) ) ;
#35389=DIRECTION ( 'NONE',  ( 0.000000000000000000, -0.7270098363383266094, -0.6866270442294852838 ) ) ;
#35393=CARTESIAN_POINT ( 'NONE',  ( 12.54729787553182341, 3.152819052640265518, 12.19917003430776248 ) ) ;
#35400=CARTESIAN_POINT ( 'NONE',  ( 12.18009741656777045, 2.512104454645549545, 12.44873738064200808 ) ) ;
#35404=CARTESIAN_POINT ( 'NONE',  ( 5.500000000000000000, -11.06886219213000011, -1.536526853569999851 ) ) ;
#35413=ORIENTED_EDGE ( 'NONE', *, *, #49352, .T. ) ;
#35418=CARTESIAN_POINT ( 'NONE',  ( 17.68813047654957771, 3.110753822336481011, -12.28807462416255092 ) ) ;
#35427=CARTESIAN_POINT ( 'NONE',  ( 12.57207325926688668, 0.6915911779535816040, -13.98290807251246548 ) ) ;
#35435=CARTESIAN_POINT ( 'NONE',  ( 18.27122651615330895, 2.402315819361971805, -13.79236889726217363 ) ) ;
#35456=CARTESIAN_POINT ( 'NONE',  ( 17.84060712062129639, -3.141591522576406614, -12.20206574396288346 ) ) ;
#35468=CARTESIAN_POINT ( 'NONE',  ( 12.10347303272471997, 2.332585440199563376, -13.80433171579881879 ) ) ;
#35470=CARTESIAN_POINT ( 'NONE',  ( 5.500000000000000000, 0.000000000000000000, 0.000000000000000000 ) ) ;
#35472=CARTESIAN_POINT ( 'NONE',  ( 18.05707515698670207, -2.118723117022102365, 12.53248177916035289 ) ) ;
#35474=VERTEX_POINT ( 'NONE', #32478 ) ;
#35479=CARTESIAN_POINT ( 'NONE',  ( 12.19818565438123414, -2.649653951396504503, 13.64057837019845998 ) ) ;
#35487=CARTESIAN_POINT ( 'NONE',  ( 12.43971800579959464, 0.6379138416539124057, 13.98550699733573133 ) ) ;
#35492=CARTESIAN_POINT ( 'NONE',  ( 5.700000000000000178, 13.04986661130000059, 1.811520473896000016 ) ) ;
#35501=CARTESIAN_POINT ( 'NONE',  ( 12.75722706473760226, 0.7178228174669301076, -12.57953618971562193 ) ) ;
#35502=CARTESIAN_POINT ( 'NONE',  ( 12.24474413009778750, -2.777098231000808326, -12.38267840003653752 ) ) ;
#35507=ORIENTED_EDGE ( 'NONE', *, *, #63340, .T. ) ;
#35520=CARTESIAN_POINT ( 'NONE',  ( 17.93787990420809209, -0.6205713442106968181, -13.98624562867392385 ) ) ;
#35532=CARTESIAN_POINT ( 'NONE',  ( 12.24918480870326043, -2.785872542151285547, -13.60860763679505325 ) ) ;
#35542=CARTESIAN_POINT ( 'NONE',  ( 12.80505043854144276, 0.6564304467897672524, 12.64601024127357931 ) ) ;
#35544=CARTESIAN_POINT ( 'NONE',  ( 12.20411985647183428, 0.1720826668005528137, -13.89857125525884207 ) ) ;
#35545=CARTESIAN_POINT ( 'NONE',  ( 18.14000279917957315, -2.720357798290598428, 12.39752072230842650 ) ) ;
#35570=CARTESIAN_POINT ( 'NONE',  ( 17.68572386047929967, 0.7076089047904873253, 12.58011506138060831 ) ) ;
#35601=CARTESIAN_POINT ( 'NONE',  ( 7.100000000000000533, -13.04986661130000059, 1.811520473896000016 ) ) ;
#35611=CARTESIAN_POINT ( 'NONE',  ( 12.18751053307000198, 2.401600969044472400, -12.47399295505824135 ) ) ;
#35622=CARTESIAN_POINT ( 'NONE',  ( 12.49051143973452227, -3.040180064579590891, -12.30914836342242680 ) ) ;
#35628=CARTESIAN_POINT ( 'NONE',  ( 12.54749102628331947, -3.200935012631489496, -13.62916378024774566 ) ) ;
#35636=CARTESIAN_POINT ( 'NONE',  ( 18.17607324740734143, 2.571217238393650906, 13.65805047069406974 ) ) ;
#35638=ADVANCED_FACE ( 'NONE', ( #13369 ), #8112, .T. ) ;
#35640=CARTESIAN_POINT ( 'NONE',  ( 17.80118387294172422, 3.074517463812005857, 12.29895906470767919 ) ) ;
#35645=CARTESIAN_POINT ( 'NONE',  ( 12.37479069268424148, -2.046560891103778701, 12.54575476380192534 ) ) ;
#35651=CARTESIAN_POINT ( 'NONE',  ( 12.61399029061283450, 0.5951698179256255106, 12.68122092285040559 ) ) ;
#35694=CARTESIAN_POINT ( 'NONE',  ( 18.20032535889736280, -2.850937372247259738, 13.70665064220730578 ) ) ;
#35695=CARTESIAN_POINT ( 'NONE',  ( 18.18005044212796051, -2.500000099754955851, 13.67345740034994783 ) ) ;
#35706=CARTESIAN_POINT ( 'NONE',  ( 18.27538032657187017, 0.08234928811777227076, -12.59973629603894274 ) ) ;
#35716=CARTESIAN_POINT ( 'NONE',  ( 12.13953890720636863, 2.807801093580546858, 13.71555245415304292 ) ) ;
#35718=ORIENTED_EDGE ( 'NONE', *, *, #22490, .T. ) ;
#35719=CARTESIAN_POINT ( 'NONE',  ( 12.41699802696285992, 0.4899468513230743061, -12.68727699267097719 ) ) ;
#35720=CARTESIAN_POINT ( 'NONE',  ( 12.75735126819566290, -0.7290235424212101467, 13.98100605002522734 ) ) ;
#35749=CARTESIAN_POINT ( 'NONE',  ( 21.47500033997000202, -1.509903313490000218E-14, 4.329869796037999436E-14 ) ) ;
#35753=ADVANCED_FACE ( 'NONE', ( #37088 ), #17819, .T. ) ;
#35758=CARTESIAN_POINT ( 'NONE',  ( 17.65791272883255303, 3.116819718221111035, -12.28623542600055174 ) ) ;
#35761=CARTESIAN_POINT ( 'NONE',  ( 12.19221373227584237, 2.622703613139459655, -13.64666900996694388 ) ) ;
#35765=CARTESIAN_POINT ( 'NONE',  ( 12.36383866360284145, 0.5795518042670567693, -13.98800095993140857 ) ) ;
#35775=CARTESIAN_POINT ( 'NONE',  ( 18.27043923978326490, 2.638421884002155160, -13.74915584829237680 ) ) ;
#35776=EDGE_LOOP ( 'NONE', ( #2762, #33457, #66364, #35321 ) ) ;
#35793=CARTESIAN_POINT ( 'NONE',  ( 17.55505043854147118, -3.199698446519380735, -12.18695736643652339 ) ) ;
#35796=ADVANCED_FACE ( 'NONE', ( #22293 ), #40633, .F. ) ;
#35799=ORIENTED_EDGE ( 'NONE', *, *, #27979, .T. ) ;
#35800=DIRECTION ( 'NONE',  ( 0.000000000000000000, 1.000000000000000000, 2.114232622412000242E-14 ) ) ;
#35805=CARTESIAN_POINT ( 'NONE',  ( 18.27538073532129914, 0.08359636179364303421, 13.99975542440154186 ) ) ;
#35816=AXIS2_PLACEMENT_3D ( 'NONE', #35161, #41080, #51902 ) ;
#35824=CARTESIAN_POINT ( 'NONE',  ( 17.55505043854143565, 1.787816316115923954, -13.88537766212463254 ) ) ;
#35836=CARTESIAN_POINT ( 'NONE',  ( 12.44117949531283784, -0.5082598251325813887, -12.68630931495243530 ) ) ;
#35837=CARTESIAN_POINT ( 'NONE',  ( 12.18236035867607292, -2.554391060938209446, -12.43872824569138480 ) ) ;
#35838=CARTESIAN_POINT ( 'NONE',  ( 12.80505043854146940, -1.787816316115923287, 13.88537766212463076 ) ) ;
#35840=DIRECTION ( 'NONE',  ( -1.000000000000000000, 0.000000000000000000, 0.000000000000000000 ) ) ;
#35844=CARTESIAN_POINT ( 'NONE',  ( 17.71610594224511814, 0.6042361945079729457, 12.68064620453998792 ) ) ;
#35849=VERTEX_POINT ( 'NONE', #27204 ) ;
#35856=ORIENTED_EDGE ( 'NONE', *, *, #57288, .F. ) ;
#35858=DIRECTION ( 'NONE',  ( -1.000000000000000000, 0.000000000000000000, 0.000000000000000000 ) ) ;
#35863=CARTESIAN_POINT ( 'NONE',  ( 17.81528574998987580, -3.068593513700731190, 12.30074760041515880 ) ) ;
#35866=CARTESIAN_POINT ( 'NONE',  ( 12.18133850337606461, -2.541372565769276282, -13.66455005695259572 ) ) ;
#35874=DIRECTION ( 'NONE',  ( -1.000000000000000000, 0.000000000000000000, 0.000000000000000000 ) ) ;
#35877=CARTESIAN_POINT ( 'NONE',  ( 12.24428838907443229, -0.2761834754990900032, -13.89631168292871344 ) ) ;
#35878=CARTESIAN_POINT ( 'NONE',  ( 17.83452421831951895, -1.940868773865736197, 12.56443418441918780 ) ) ;
#35896=CARTESIAN_POINT ( 'NONE',  ( 12.43708913302417152, 1.881554942472513314, -13.87303690248482013 ) ) ;
#35900=CARTESIAN_POINT ( 'NONE',  ( 18.27397540914052243, 0.09367178904473957846, 12.59965724591066483 ) ) ;
#35917=B_SPLINE_CURVE_WITH_KNOTS ( 'NONE', 3,
 ( #22254, #29856, #13424, #64891, #51162, #43592, #24589, #45911, #34744, #24240, #45578, #66884, #19335, #57766 ),
 .UNSPECIFIED., .F., .F.,
 ( 4, 2, 2, 2, 2, 2, 4 ),
 ( 0.000000000000000000, 0.2494049090184954909, 0.3741073635277432641, 0.4052829771550562343, 0.4364585907823692046, 0.4676342044096822304, 0.4988098180369952006 ),
 .UNSPECIFIED. ) ;
#35924=EDGE_LOOP ( 'NONE', ( #32354, #43468, #54693, #26926 ) ) ;
#35941=CARTESIAN_POINT ( 'NONE',  ( 12.20120475779644842, 2.662482513922677096, -12.41227208748767197 ) ) ;
#35944=ORIENTED_EDGE ( 'NONE', *, *, #48613, .T. ) ;
#35949=CARTESIAN_POINT ( 'NONE',  ( 12.61719528873172891, -3.096122730228594744, -12.29247817764211348 ) ) ;
#35955=CARTESIAN_POINT ( 'NONE',  ( 12.64211699103826270, -1.896258653787261217, -13.78307619201600254 ) ) ;
#35961=CARTESIAN_POINT ( 'NONE',  ( 12.07990818253658105, -0.1906559480948835372, -14.00000681886699461 ) ) ;
#35962=DIRECTION ( 'NONE',  ( 0.000000000000000000, 0.7198977633594747516, 0.6940801180771756229 ) ) ;
#35963=CARTESIAN_POINT ( 'NONE',  ( 18.09719409067036011, 2.811143122875886302, 13.60247644588032223 ) ) ;
#35966=CARTESIAN_POINT ( 'NONE',  ( 17.71888513161119505, 3.103492732303466450, 12.29025695670425300 ) ) ;
#35973=CARTESIAN_POINT ( 'NONE',  ( 12.24870215512123650, -2.784965704346237469, 12.38061966815949511 ) ) ;
#35980=CARTESIAN_POINT ( 'NONE',  ( 12.40062372901866894, 0.4766234715920624199, 12.68796191786312910 ) ) ;
#35981=CARTESIAN_POINT ( 'NONE',  ( 5.536227981748580440, -12.19240621326411578, -3.776122996998608983 ) ) ;
#35989=EDGE_CURVE ( 'NONE', #48764, #47657, #15664, .T. ) ;
#35990=CARTESIAN_POINT ( 'NONE',  ( 17.96975113184317152, 2.032288328865630156, 13.76155421333986695 ) ) ;
#36004=CARTESIAN_POINT ( 'NONE',  ( 17.96200919170520649, -2.025537500457071705, -13.76266550596354321 ) ) ;
#36026=CARTESIAN_POINT ( 'NONE',  ( 17.85668400807928080, -1.853912555516301630, 13.87670837816644109 ) ) ;
#36027=CARTESIAN_POINT ( 'NONE',  ( 17.55505043854144631, 0.7192913403693005359, 12.57945229203838267 ) ) ;
#36038=CARTESIAN_POINT ( 'NONE',  ( 18.27776587948808285, -0.05827135643914812396, -12.59987075990256855 ) ) ;
#36039=CARTESIAN_POINT ( 'NONE',  ( 12.29679984372382506, 2.863892094152995060, -12.35932590995903446 ) ) ;
#36049=CARTESIAN_POINT ( 'NONE',  ( 17.82422846108291736, 1.812210939693178924, 12.46899807711483987 ) ) ;
#36052=CARTESIAN_POINT ( 'NONE',  ( 12.19349437040516904, 2.125667349631279901, 13.83768917864515480 ) ) ;
#36056=CARTESIAN_POINT ( 'NONE',  ( 12.21982330446825316, -0.2196444115886839188, -12.69744877134248995 ) ) ;
#36059=CARTESIAN_POINT ( 'NONE',  ( 12.33239129661528821, -1.934538128658857881, 12.45060726317137423 ) ) ;
#36068=CARTESIAN_POINT ( 'NONE',  ( 12.21438802940094348, 2.898246740288908718, 12.26216014320957370 ) ) ;
#36080=CARTESIAN_POINT ( 'NONE',  ( 12.21236377911861659, -0.1994069032339068626, 12.69791261745780986 ) ) ;
#36086=CARTESIAN_POINT ( 'NONE',  ( 12.57359775157570247, -3.080655040460396954, 13.53300991339125225 ) ) ;
#36087=CARTESIAN_POINT ( 'NONE',  ( 12.20137260070325347, 2.663020830165313324, 13.63749600555738439 ) ) ;
#36096=CARTESIAN_POINT ( 'NONE',  ( 17.74533816909189454, 1.785653880132706872, -12.47283005504979592 ) ) ;
#36098=CARTESIAN_POINT ( 'NONE',  ( 18.05156413927919345, 2.879751443193474980, 12.35493952381846050 ) ) ;
#36103=CARTESIAN_POINT ( 'NONE',  ( 12.71024384884961478, 0.7243378955762067584, -13.98124959093732400 ) ) ;
#36106=CARTESIAN_POINT ( 'NONE',  ( 18.18004831022902934, 2.496998393545561967, 12.45226267664535413 ) ) ;
#36112=CARTESIAN_POINT ( 'NONE',  ( 18.26121249471881569, 2.684743402744599106, -13.74018592865772881 ) ) ;
#36116=AXIS2_PLACEMENT_3D ( 'NONE', #48253, #21676, #16095 ) ;
#36118=LINE ( 'NONE', #14799, #34261 ) ;
#36131=CARTESIAN_POINT ( 'NONE',  ( 17.75782926003070017, -1.908786995103509021, -12.56982197457662664 ) ) ;
#36145=CARTESIAN_POINT ( 'NONE',  ( 18.27977752388257571, -0.02332822437944303412, 13.99998565365491210 ) ) ;
#36148=EDGE_LOOP ( 'NONE', ( #8433, #67069, #31047, #18476 ) ) ;
#36152=CARTESIAN_POINT ( 'NONE',  ( 12.25852091198461302, -2.803392358766023662, 13.60441894874461610 ) ) ;
#36178=CARTESIAN_POINT ( 'NONE',  ( 12.18201988759300214, 0.05063260980701855818, -12.69986973508909323 ) ) ;
#36179=CARTESIAN_POINT ( 'NONE',  ( 12.22117151664400225, -2.723004124966011741, -12.39680780188599485 ) ) ;
#36186=CARTESIAN_POINT ( 'NONE',  ( 17.83819980912012326, 0.5572757172660935954, 12.68354006032474679 ) ) ;
#36203=ORIENTED_EDGE ( 'NONE', *, *, #6255, .F. ) ;
#36205=CARTESIAN_POINT ( 'NONE',  ( 12.19790361191645722, -2.648659039907943047, -13.64075350855048185 ) ) ;
#36207=EDGE_LOOP ( 'NONE', ( #48421, #35507, #40767, #48988 ) ) ;
#36215=AXIS2_PLACEMENT_3D ( 'NONE', #33106, #65248, #249 ) ;
#36220=EDGE_CURVE ( 'NONE', #38087, #57647, #41818, .T. ) ;
#36228=CARTESIAN_POINT ( 'NONE',  ( 12.30652006878821325, 2.122495540605185749, -13.74632343115108846 ) ) ;
#36230=DIRECTION ( 'NONE',  ( 0.000000000000000000, -1.000000000000000000, -0.000000000000000000 ) ) ;
#36244=CARTESIAN_POINT ( 'NONE',  ( 17.65049462686343773, 0.7131288892044757022, 12.57980326738671906 ) ) ;
#36276=CARTESIAN_POINT ( 'NONE',  ( 12.80505043854146940, -1.875000000000000444, -13.78627172894481667 ) ) ;
#36288=CARTESIAN_POINT ( 'NONE',  ( 17.55505043854144276, -0.7192913403693006469, 12.57945229203838444 ) ) ;
#36291=CARTESIAN_POINT ( 'NONE',  ( 12.61477885367313156, -1.785717119372570272, -12.47282100101237212 ) ) ;
#36296=CARTESIAN_POINT ( 'NONE',  ( 12.36142641661521147, -3.095968474609000154, -13.65339594101960330 ) ) ;
#36300=CARTESIAN_POINT ( 'NONE',  ( 17.77874050697768382, -3.164693776342190734, 12.19609433843463187 ) ) ;
#36312=CARTESIAN_POINT ( 'NONE',  ( 17.96903643132312567, 2.968342805378973992, 12.33002008018445217 ) ) ;
#36317=ORIENTED_EDGE ( 'NONE', *, *, #18421, .T. ) ;
#36318=CARTESIAN_POINT ( 'NONE',  ( 12.48990506108392395, -3.039826403548177236, 12.30927084193774057 ) ) ;
#36325=EDGE_CURVE ( 'NONE', #37829, #15559, #62787, .T. ) ;
#36327=CARTESIAN_POINT ( 'NONE',  ( 12.47441792805236815, -0.5304820368560169142, 12.68508456201358747 ) ) ;
#36330=CARTESIAN_POINT ( 'NONE',  ( 5.500000000000000000, 11.06886219213000011, -1.536526853569999851 ) ) ;
#36336=CARTESIAN_POINT ( 'NONE',  ( 17.75799838104445172, 1.908512137131851860, 13.78121285638385807 ) ) ;
#36342=CARTESIAN_POINT ( 'NONE',  ( 18.17506407531473656, -0.08141364318952959422, -12.69967032936936668 ) ) ;
#36348=CARTESIAN_POINT ( 'NONE',  ( 18.08647318473503773, -2.829117779091809393, -13.59807435138920439 ) ) ;
#36357=CARTESIAN_POINT ( 'NONE',  ( 17.95719809555263069, -0.4784561392272737579, 13.88891570267564113 ) ) ;
#36360=ORIENTED_EDGE ( 'NONE', *, *, #27979, .F. ) ;
#36370=CARTESIAN_POINT ( 'NONE',  ( 21.59999987243000064, 1.172395514003999961E-13, -2.486899575159999765E-14 ) ) ;
#36372=CARTESIAN_POINT ( 'NONE',  ( 18.25624423923971662, -2.332236704353563450, 13.80437652844154073 ) ) ;
#36373=CARTESIAN_POINT ( 'NONE',  ( 17.96849574074740730, 2.968826013471339564, -13.56277633467329125 ) ) ;
#36384=CARTESIAN_POINT ( 'NONE',  ( 18.27977754798708787, -0.02297882141078106538, -12.59998453421652442 ) ) ;
#36385=CARTESIAN_POINT ( 'NONE',  ( 12.54534433731234877, 3.068834427905941187, -12.30067458026015359 ) ) ;
#36397=CARTESIAN_POINT ( 'NONE',  ( 12.08963668261105617, 2.638435792642065625, 13.74915318082108762 ) ) ;
#36399=CARTESIAN_POINT ( 'NONE',  ( 12.42592538289389914, -0.4969854666067609616, -12.68691056894716773 ) ) ;
#36400=CARTESIAN_POINT ( 'NONE',  ( 12.32690743522623400, -0.5490318484135010557, 13.98923259457975909 ) ) ;
#36408=AXIS2_PLACEMENT_3D ( 'NONE', #13674, #18915, #67480 ) ;
#36409=ADVANCED_FACE ( 'NONE', ( #24368 ), #51617, .F. ) ;
#36411=CARTESIAN_POINT ( 'NONE',  ( 12.11859257910638554, 0.2316996085785973380, 12.59787430930301433 ) ) ;
#36414=CARTESIAN_POINT ( 'NONE',  ( 12.51357205051171562, 1.821485253447863384, 12.46764665430163532 ) ) ;
#36421=CARTESIAN_POINT ( 'NONE',  ( 12.19562994360508590, 2.360937373133742856, 12.48287347411684500 ) ) ;
#36423=ORIENTED_EDGE ( 'NONE', *, *, #32610, .F. ) ;
#36424=CARTESIAN_POINT ( 'NONE',  ( 12.29580549790138377, -0.3624889081508343991, 12.69304043450447850 ) ) ;
#36428=DIRECTION ( 'NONE',  ( 1.000000000000000000, 0.000000000000000000, 0.000000000000000000 ) ) ;
#36429=CARTESIAN_POINT ( 'NONE',  ( 12.18824001706384763, -2.602861674270837256, 13.65112526288235451 ) ) ;
#36430=CARTESIAN_POINT ( 'NONE',  ( 12.18817138782660514, 2.600938394344443960, 13.65148521156839045 ) ) ;
#36437=CARTESIAN_POINT ( 'NONE',  ( 18.15589597092046859, 2.672372730248489425, -12.40976522372663737 ) ) ;
#36439=CARTESIAN_POINT ( 'NONE',  ( 18.18005044388380043, 2.499999700417821380, 12.45156116530496604 ) ) ;
#36442=CARTESIAN_POINT ( 'NONE',  ( 17.74422827371068223, 3.224484589774872401, 13.62361160044438790 ) ) ;
#36446=CARTESIAN_POINT ( 'NONE',  ( 12.18940025506973335, 0.3858260082455223228, -13.99468631105252037 ) ) ;
#36447=CARTESIAN_POINT ( 'NONE',  ( 17.55505043854143565, 3.125000000000000000, 12.28373071562070074 ) ) ;
#36448=DIRECTION ( 'NONE',  ( 1.000000000000000000, -1.386239579945032070E-15, 9.986219791750131332E-15 ) ) ;
#36456=CARTESIAN_POINT ( 'NONE',  ( 17.95040605897955643, 3.130086699081791490, -13.64560748759990894 ) ) ;
#36462=CARTESIAN_POINT ( 'NONE',  ( 4.599999999999999645, -3.248109929747638347, 13.61799478206225622 ) ) ;
#36467=EDGE_CURVE ( 'NONE', #66715, #31306, #24713, .T. ) ;
#36473=CARTESIAN_POINT ( 'NONE',  ( 18.01423850902973101, -2.075512308681780382, -12.54039470262456568 ) ) ;
#36475=DIRECTION ( 'NONE',  ( 0.000000000000000000, 0.000000000000000000, -1.000000000000000000 ) ) ;
#36489=VERTEX_POINT ( 'NONE', #38289 ) ;
#36501=ORIENTED_EDGE ( 'NONE', *, *, #9133, .T. ) ;
#36509=CARTESIAN_POINT ( 'NONE',  ( 18.12484680926279879, 2.757022365696005117, -12.38798834874709875 ) ) ;
#36516=CARTESIAN_POINT ( 'NONE',  ( 17.92325670924426362, 1.853371315686558773, 12.46300045701071291 ) ) ;
#36519=ADVANCED_FACE ( 'NONE', ( #48100 ), #55215, .T. ) ;
#36520=ADVANCED_FACE ( 'NONE', ( #25306 ), #29555, .T. ) ;
#36521=CARTESIAN_POINT ( 'NONE',  ( 12.60374982967590185, 0.5917829749564897934, -12.68143435689272280 ) ) ;
#36522=CARTESIAN_POINT ( 'NONE',  ( 12.18035041863325851, -2.521826826373486874, -12.44645458621850942 ) ) ;
#36528=EDGE_CURVE ( 'NONE', #22723, #32483, #30226, .T. ) ;
#36540=CARTESIAN_POINT ( 'NONE',  ( 17.64985702823327784, -0.7243378955761968774, -13.98124959093732400 ) ) ;
#36541=EDGE_LOOP ( 'NONE', ( #3744, #64197, #9079, #43263 ) ) ;
#36545=CONICAL_SURFACE ( 'NONE', #45494, 1.899997304679999610, 0.7853981633972997312 ) ;
#36571=CARTESIAN_POINT ( 'NONE',  ( 12.80505043854143388, 1.874999999999999112, -13.78631952119025428 ) ) ;
#36576=CARTESIAN_POINT ( 'NONE',  ( 18.14887598846753036, 0.1995645667416934554, 13.89814765003537644 ) ) ;
#36577=ORIENTED_EDGE ( 'NONE', *, *, #30204, .T. ) ;
#36591=CARTESIAN_POINT ( 'NONE',  ( 18.18333067157141514, 0.3597103837127935133, 12.59488153751295769 ) ) ;
#36601=EDGE_LOOP ( 'NONE', ( #65768, #23554, #37452, #2592 ) ) ;
#36608=CARTESIAN_POINT ( 'NONE',  ( 12.80505043854144276, -0.7192913403693169672, -12.57945229203838267 ) ) ;
#36613=ORIENTED_EDGE ( 'NONE', *, *, #58725, .T. ) ;
#36627=ORIENTED_EDGE ( 'NONE', *, *, #60554, .T. ) ;
#36628=CARTESIAN_POINT ( 'NONE',  ( 18.14024860221783442, 0.2197089332467984102, -13.89766776387045866 ) ) ;
#36633=CARTESIAN_POINT ( 'NONE',  ( 12.46386834215124928, 3.023758766561084332, -12.31399102038137450 ) ) ;
#36636=EDGE_CURVE ( 'NONE', #58325, #44202, #31093, .T. ) ;
#36642=CARTESIAN_POINT ( 'NONE',  ( 12.19425446308167515, -2.632875717725343012, -12.41961888770621236 ) ) ;
#36647=CARTESIAN_POINT ( 'NONE',  ( 12.47274432058964422, -1.970265487500629353, -13.77159998682697051 ) ) ;
#36652=CARTESIAN_POINT ( 'NONE',  ( 17.95027792402082412, -3.083622039298903772, 12.21684579612696453 ) ) ;
#36663=CARTESIAN_POINT ( 'NONE',  ( 17.99149020822391165, 2.947405452019512317, 12.33598828993208585 ) ) ;
#36664=CARTESIAN_POINT ( 'NONE',  ( 17.92307254476367007, -3.107335109273783758, -12.21089239123762660 ) ) ;
#36670=CARTESIAN_POINT ( 'NONE',  ( 12.51684016020884549, -3.054675744551021754, 12.30488183412682801 ) ) ;
#36674=DIRECTION ( 'NONE',  ( -1.000000000000000000, -0.000000000000000000, -0.000000000000000000 ) ) ;
#36678=CARTESIAN_POINT ( 'NONE',  ( 12.34842979604855095, -0.4268810874232081276, 12.69034564040269508 ) ) ;
#36679=CARTESIAN_POINT ( 'NONE',  ( 5.592979883552142262, -12.14034187852487889, -3.752392258526793700 ) ) ;
#36696=CARTESIAN_POINT ( 'NONE',  ( 18.13616101475819775, -2.730220173702290420, 13.62193317602436338 ) ) ;
#36700=CARTESIAN_POINT ( 'NONE',  ( 17.92067731499820482, -3.006998531728875435, -13.55270476886629361 ) ) ;
#36704=ORIENTED_EDGE ( 'NONE', *, *, #4410, .F. ) ;
#36719=ORIENTED_EDGE ( 'NONE', *, *, #51140, .T. ) ;
#36722=CARTESIAN_POINT ( 'NONE',  ( 12.54704051454017133, 1.807816716204553087, -12.46963574575698352 ) ) ;
#36726=CARTESIAN_POINT ( 'NONE',  ( 17.72088406261403648, -1.806772466812839983, 13.88292461265716504 ) ) ;
#36727=CARTESIAN_POINT ( 'NONE',  ( 18.14647333857621092, 2.702177529323569694, -13.62849908386765208 ) ) ;
#36731=EDGE_LOOP ( 'NONE', ( #44177, #21216, #53653, #16586 ) ) ;
#36738=CARTESIAN_POINT ( 'NONE',  ( 18.02437627528318131, -0.5483668826291703269, -12.58806376549905082 ) ) ;
#36739=CARTESIAN_POINT ( 'NONE',  ( 12.27931543958120209, 2.838108479058770506, -12.36635919027451180 ) ) ;
#36748=CARTESIAN_POINT ( 'NONE',  ( 12.63921101284453741, 1.806754227364035126, 13.88292698645336642 ) ) ;
#36753=CARTESIAN_POINT ( 'NONE',  ( 12.42222097287479698, -0.6205713442106928213, 13.98624562867391496 ) ) ;
#36763=CARTESIAN_POINT ( 'NONE',  ( 12.14402373937349289, 2.776896049134141009, 12.29021278449864418 ) ) ;
#36773=CARTESIAN_POINT ( 'NONE',  ( 12.42592538302026206, 0.4969854667031534667, 12.68691056894229874 ) ) ;
#36778=CARTESIAN_POINT ( 'NONE',  ( 12.32580140628885879, -2.098690126660240463, 13.75042779764526912 ) ) ;
#36789=B_SPLINE_CURVE_WITH_KNOTS ( 'NONE', 3,
 ( #20782, #5724, #145, #53288, #20096, #36516, #31624, #10979, #69015, #32318, #30937, #52253, #4349, #20437, #25681, #42455 ),
 .UNSPECIFIED., .F., .F.,
 ( 4, 2, 2, 2, 2, 2, 2, 4 ),
 ( 0.000000000000000000, 0.06249999999999757139, 0.1249999999999951428, 0.2499999999999946154, 0.4999999999999963363, 0.7499999999999981126, 0.8749999999999991118, 1.000000000000000000 ),
 .UNSPECIFIED. ) ;
#36790=CARTESIAN_POINT ( 'NONE',  ( 18.06416738895848795, 2.863102795628076347, -12.35955380825000915 ) ) ;
#36792=CARTESIAN_POINT ( 'NONE',  ( 17.92143259511064457, 3.006721712956350601, 12.31894844866651439 ) ) ;
#36794=CARTESIAN_POINT ( 'NONE',  ( 18.00298204928587253, 3.099842930792937157, 13.65268125597837212 ) ) ;
#36803=ORIENTED_EDGE ( 'NONE', *, *, #62270, .F. ) ;
#36808=DIRECTION ( 'NONE',  ( -0.000000000000000000, -0.000000000000000000, 1.000000000000000000 ) ) ;
#36810=ORIENTED_EDGE ( 'NONE', *, *, #32610, .T. ) ;
#36816=CARTESIAN_POINT ( 'NONE',  ( 12.44874774236670945, 0.5136130429597132174, -13.88722741725625021 ) ) ;
#36828=CARTESIAN_POINT ( 'NONE',  ( 18.03321709926674998, -2.902596714178123261, -12.34859794581418413 ) ) ;
#36829=DIRECTION ( 'NONE',  ( 0.000000000000000000, 0.9905022095861402143, 0.1374968101629056305 ) ) ;
#36834=CARTESIAN_POINT ( 'NONE',  ( 7.100000000000000533, -12.03770622561999915, 3.722046322334000124 ) ) ;
#36857=CARTESIAN_POINT ( 'NONE',  ( 5.500000000000000000, -12.87590651766999983, 2.791353855799999728 ) ) ;
#36859=CARTESIAN_POINT ( 'NONE',  ( 18.06426550929511166, 2.862542805010156233, -12.35969564690516975 ) ) ;
#36871=CARTESIAN_POINT ( 'NONE',  ( 5.684131419941360619, 13.00367204040951385, -2.123909547228391759 ) ) ;
#36874=CARTESIAN_POINT ( 'NONE',  ( 12.18028569061553057, 0.01996654564806132556, -12.69998441237379971 ) ) ;
#36882=CARTESIAN_POINT ( 'NONE',  ( 18.06967961654933674, 0.3547743933919684789, 12.69333341030383444 ) ) ;
#36905=FACE_OUTER_BOUND ( 'NONE', #26049, .T. ) ;
#36908=CARTESIAN_POINT ( 'NONE',  ( 18.18005043853800373, 0.02024535615111898099, -13.89999992470869472 ) ) ;
#36909=CARTESIAN_POINT ( 'NONE',  ( 17.78508576848220812, -0.5812174491462164250, -12.68209204657794409 ) ) ;
#36913=DIRECTION ( 'NONE',  ( -1.000000000000000000, 0.000000000000000000, 0.000000000000000000 ) ) ;
#36914=CARTESIAN_POINT ( 'NONE',  ( 12.80505043854143210, 3.124999999999999556, 13.52078605991414939 ) ) ;
#36923=CARTESIAN_POINT ( 'NONE',  ( 12.29449213756044124, 2.138932443162071539, -13.74345175514785922 ) ) ;
#36931=CARTESIAN_POINT ( 'NONE',  ( 12.40965214746187684, 0.4840331164351866500, 13.88865521358243882 ) ) ;
#36934=DIRECTION ( 'NONE',  ( 0.000000000000000000, -0.000000000000000000, 1.000000000000000000 ) ) ;
#36941=B_SPLINE_CURVE_WITH_KNOTS ( 'NONE', 1,
 ( #32944, #32267 ),
 .UNSPECIFIED., .F., .F.,
 ( 2, 2 ),
 ( 0.000000000000000000, 1.000000000000000000 ),
 .UNSPECIFIED. ) ;
#36942=CARTESIAN_POINT ( 'NONE',  ( 18.23387849499154711, 0.2528603812084199154, 12.59746735456353051 ) ) ;
#36948=CARTESIAN_POINT ( 'NONE',  ( 17.55505043854143565, 3.248147246781391217, 13.61798588129781074 ) ) ;
#36956=ORIENTED_EDGE ( 'NONE', *, *, #40020, .T. ) ;
#36958=CARTESIAN_POINT ( 'NONE',  ( 18.28104795956118522, -2.296528561422030545, 12.39041189979879398 ) ) ;
#36977=CARTESIAN_POINT ( 'NONE',  ( 21.35000154058000277, 12.59999999999999964, 0.000000000000000000 ) ) ;
#36990=CARTESIAN_POINT ( 'NONE',  ( 12.49937493268697075, -3.045244672522429585, -12.30765407517399979 ) ) ;
#36994=CARTESIAN_POINT ( 'NONE',  ( 12.29798916261921704, -1.995979084551876559, -13.85698889012213186 ) ) ;
#36997=CARTESIAN_POINT ( 'NONE',  ( 18.23147373744593480, -2.220711592698070280, 12.40276429823314075 ) ) ;
#37005=CARTESIAN_POINT ( 'NONE',  ( 17.88331607686618341, 1.943250335976817622, -12.56477475324372683 ) ) ;
#37007=EDGE_CURVE ( 'NONE', #12411, #62256, #58861, .T. ) ;
#37008=CARTESIAN_POINT ( 'NONE',  ( 17.79128410735117782, -1.798519029228340615, -12.47099317247096906 ) ) ;
#37009=ADVANCED_FACE ( 'NONE', ( #68044 ), #20159, .F. ) ;
#37010=AXIS2_PLACEMENT_3D ( 'NONE', #8886, #29549, #35800 ) ;
#37034=CARTESIAN_POINT ( 'NONE',  ( 5.536712913963323324, -12.19258561490754111, 3.773936784948052292 ) ) ;
#37041=CARTESIAN_POINT ( 'NONE',  ( 18.08101717074209347, -2.837770499550322789, -13.59594328884928416 ) ) ;
#37066=CARTESIAN_POINT ( 'NONE',  ( 17.97013316094033542, -1.919230625394033662, 13.86782606946093743 ) ) ;
#37079=CARTESIAN_POINT ( 'NONE',  ( 17.90798944145351967, -0.6284163952874818326, -12.58432055988357767 ) ) ;
#37080=CARTESIAN_POINT ( 'NONE',  ( 12.47149800528992536, 3.028907606620561577, -12.31248708663812685 ) ) ;
#37088=FACE_OUTER_BOUND ( 'NONE', #6779, .T. ) ;
#37096=CARTESIAN_POINT ( 'NONE',  ( 12.32338852522668660, -1.942342658536881483, 12.44939237451325731 ) ) ;
#37105=CARTESIAN_POINT ( 'NONE',  ( 12.17603179862374674, 2.838932078785884716, 12.27602983002081771 ) ) ;
#37113=CARTESIAN_POINT ( 'NONE',  ( 18.17614054498634957, -0.08113966125565957865, 12.69973816840999170 ) ) ;
#37122=CARTESIAN_POINT ( 'NONE',  ( 12.42293806700078385, -2.994693046128884539, 13.55600569395198995 ) ) ;
#37123=CARTESIAN_POINT ( 'NONE',  ( 12.21587634993881188, 2.708625115168846520, 13.62694294273322804 ) ) ;
#37130=CARTESIAN_POINT ( 'NONE',  ( 18.09722825099190402, 2.811571021179180452, -12.37353494292365497 ) ) ;
#37132=CARTESIAN_POINT ( 'NONE',  ( 17.88923853191783664, 3.028508370112690251, 12.31258559103103245 ) ) ;
#37136=CARTESIAN_POINT ( 'NONE',  ( 12.61577834523377817, 1.811481987173967578, 13.88231333970316506 ) ) ;
#37139=CARTESIAN_POINT ( 'NONE',  ( 4.599999999999999645, -0.7302158263239085789, 13.98094363220830871 ) ) ;
#37164=CARTESIAN_POINT ( 'NONE',  ( 17.57591570971905170, -3.124999463061048921, -12.28373083832239132 ) ) ;
#37168=CARTESIAN_POINT ( 'NONE',  ( 12.52788616429852198, 0.5605600754933556251, 13.88478672247769552 ) ) ;
#37174=CARTESIAN_POINT ( 'NONE',  ( 12.80505043854143388, 3.248109929747637015, -13.61799478206225444 ) ) ;
#37195=CARTESIAN_POINT ( 'NONE',  ( 5.500000000000000000, 13.04986661130000059, 1.811520473896000016 ) ) ;
#37197=CARTESIAN_POINT ( 'NONE',  ( 5.700000000000000178, -13.03908314092542753, -1.889202648615756486 ) ) ;
#37199=CARTESIAN_POINT ( 'NONE',  ( 18.03251246674827257, 2.904216811361305162, -12.34819510225365669 ) ) ;
#37203=AXIS2_PLACEMENT_3D ( 'NONE', #8243, #65322, #56479 ) ;
#37210=CARTESIAN_POINT ( 'NONE',  ( 12.20137806200446029, -0.1622035078961271970, -12.69861136640060195 ) ) ;
#37227=FACE_OUTER_BOUND ( 'NONE', #35776, .T. ) ;
#37240=DIRECTION ( 'NONE',  ( 0.000000000000000000, -1.000000000000000000, -0.000000000000000000 ) ) ;
#37246=CARTESIAN_POINT ( 'NONE',  ( 17.97079960141762811, -1.890785106268467075, -12.45732622342820584 ) ) ;
#37247=DIRECTION ( 'NONE',  ( 0.000000000000000000, -1.000000000000000000, 0.000000000000000000 ) ) ;
#37260=CARTESIAN_POINT ( 'NONE',  ( 12.76347793713366130, 1.876036575608650780, -13.78616487348347519 ) ) ;
#37263=CARTESIAN_POINT ( 'NONE',  ( 18.12876426765905435, -0.2481576080865494083, 13.89702325994033671 ) ) ;
#37278=CARTESIAN_POINT ( 'NONE',  ( 18.10141690196193309, -0.3036663359794732342, 12.69511825016612860 ) ) ;
#37290=CARTESIAN_POINT ( 'NONE',  ( 17.55505043854143565, 3.125000000000000000, 13.52078605991414939 ) ) ;
#37309=CARTESIAN_POINT ( 'NONE',  ( 17.63737865760589330, 0.6198980793944587342, -13.88138779565238501 ) ) ;
#37317=CARTESIAN_POINT ( 'NONE',  ( 12.42229329081240152, 2.994506204212079137, -12.32251488760203628 ) ) ;
#37321=EDGE_LOOP ( 'NONE', ( #55453, #55143, #29784, #24399 ) ) ;
#37326=CARTESIAN_POINT ( 'NONE',  ( 12.18014475499754212, -2.522932601087060966, -12.44621172798972353 ) ) ;
#37330=CARTESIAN_POINT ( 'NONE',  ( 12.32410271629026255, -1.971482746313082179, -13.86049503924169457 ) ) ;
#37332=LINE ( 'NONE', #47486, #1815 ) ;
#37333=CARTESIAN_POINT ( 'NONE',  ( 18.00816351061650522, -3.042045466722126612, 12.22726353680069344 ) ) ;
#37349=CARTESIAN_POINT ( 'NONE',  ( 12.27338658866630716, -2.829189413748181892, 12.36878769217040919 ) ) ;
#37355=ADVANCED_FACE ( 'NONE', ( #65903 ), #1594, .F. ) ;
#37356=CARTESIAN_POINT ( 'NONE',  ( 12.79472656276096032, -0.6249999662751115626, 12.67928921590351798 ) ) ;
#37364=CARTESIAN_POINT ( 'NONE',  ( 17.81482613222762268, 3.068547461637707308, 13.53623828841520726 ) ) ;
#37379=CARTESIAN_POINT ( 'NONE',  ( 18.11274618065391095, -2.217676902473667777, -13.72925005197111048 ) ) ;
#37400=CARTESIAN_POINT ( 'NONE',  ( 12.38926598778390620, 1.890730539229748652, -12.45733450583996849 ) ) ;
#37403=CARTESIAN_POINT ( 'NONE',  ( 18.06384107466247357, 2.863137910860089175, -13.58970737937452533 ) ) ;
#37407=ORIENTED_EDGE ( 'NONE', *, *, #42718, .F. ) ;
#37415=CARTESIAN_POINT ( 'NONE',  ( 17.55505043854144631, -0.7192913403693169672, -12.57945229203838267 ) ) ;
#37423=CARTESIAN_POINT ( 'NONE',  ( 17.95087979294694591, 3.083166700081128475, 12.21696069964854736 ) ) ;
#37426=CARTESIAN_POINT ( 'NONE',  ( 12.40293124252145418, -0.4784650742344930818, -12.68786664692594535 ) ) ;
#37433=CARTESIAN_POINT ( 'NONE',  ( 5.599997304680200294, 13.94845324556000143, -4.312847325879000770 ) ) ;
#37438=CARTESIAN_POINT ( 'NONE',  ( 12.53842182639420599, 0.6689867242971689887, 12.58222862546947241 ) ) ;
#37441=EDGE_CURVE ( 'NONE', #13672, #67648, #14157, .T. ) ;
#37442=CARTESIAN_POINT ( 'NONE',  ( 12.48081329218149627, 1.836727633573117080, 12.46541050266128181 ) ) ;
#37450=CARTESIAN_POINT ( 'NONE',  ( 12.29671722859782079, 2.864281468083856197, 12.35920955626090745 ) ) ;
#37452=ORIENTED_EDGE ( 'NONE', *, *, #35366, .T. ) ;
#37458=CARTESIAN_POINT ( 'NONE',  ( 12.41482009541962128, -2.988314721215474812, 13.55768135971568356 ) ) ;
#37459=CARTESIAN_POINT ( 'NONE',  ( 12.19231142706649429, 2.623190749813627765, 13.64650702413893768 ) ) ;
#37463=CARTESIAN_POINT ( 'NONE',  ( 18.16451541383442247, 2.360124911612616394, -13.70214797745896895 ) ) ;
#37466=CARTESIAN_POINT ( 'NONE',  ( 18.12629019086303828, 2.246197018143532009, -12.50711533121134167 ) ) ;
#37468=CARTESIAN_POINT ( 'NONE',  ( 17.98440366585261074, 2.954302470115874435, 12.33403020158356078 ) ) ;
#37478=ORIENTED_EDGE ( 'NONE', *, *, #38625, .T. ) ;
#37484=B_SPLINE_CURVE_WITH_KNOTS ( 'NONE', 3,
 ( #67456, #13998, #51730, #35324, #25163, #45807, #8744, #66087, #56641, #51394, #23790, #60853, #40224, #2807, #34293, #8404, #67118, #45468, #61540, #55614, #29055, #50366, #19228, #3489, #19581, #2466, #45125, #66432, #62222, #13656, #18554, #14341, #40554, #61201, #13320, #34644, #55954, #29749, #51051, #24134, #66783, #46837, #36342, #19921, #21290, #14680 ),
 .UNSPECIFIED., .F., .F.,
 ( 4, 2, 2, 2, 2, 2, 2, 2, 2, 2, 2, 2, 2, 2, 1, 2, 2, 2, 2, 2, 1, 2, 2, 4 ),
 ( 0.000000000000000000, 0.06247329711058760560, 0.09370994566588143615, 0.1249465942211752667, 0.1405649184988197742, 0.1561832427764643094, 0.1874198913317580151, 0.2030382156094048540, 0.2186565398870516930, 0.2264657020258750708, 0.2342748641646984209, 0.2498931884423491734, 0.2811298369976507061, 0.2889389991364761379, 0.2967481612753015141, 0.3123664855529522666, 0.3279848098306030746, 0.3436031341082538271, 0.3748397826635555541, 0.3904581069412053074, 0.4060764312188550051, 0.4373130797741529019, 0.4685497283294507986, 0.4997863768847486954 ),
 .UNSPECIFIED. ) ;
#37491=CARTESIAN_POINT ( 'NONE',  ( 12.76469414194129115, 0.6249999999999995559, -13.88107975724710741 ) ) ;
#37498=B_SPLINE_CURVE_WITH_KNOTS ( 'NONE', 3,
 ( #6723, #1488, #54975, #24192, #40960, #45183, #3213, #7770, #2521, #29807, #24540, #35382, #3886, #25220, #14054, #41306, #56703, #29461, #14403, #62615, #35719, #56356, #46211, #13374, #66490, #29112, #18611, #57036, #62283, #66839, #67174, #67518, #23848, #9138, #3544, #8804, #34699, #39939, #50769, #61257, #67860, #30143, #50418, #45865, #46557, #35042, #19985, #56010, #14737, #24881, #18950, #30474, #45528, #2863, #8117, #36056, #40279, #61596, #13713, #51789, #8462, #19288, #51110, #40613, #61941, #51450, #19639, #15073, #26606, #16443, #21348, #68893, #53166, #48261, #64321, #37426, #47588, #68542, #9824, #36399, #62950, #4921, #63298, #31172, #15764, #57716, #43018, #42675, #25569, #57370, #25909, #52474, #4572 ),
 .UNSPECIFIED., .F., .F.,
 ( 4, 2, 2, 2, 2, 2, 2, 2, 2, 1, 1, 2, 2, 2, 2, 2, 2, 2, 2, 2, 2, 2, 2, 2, 2, 2, 2, 2, 2, 2, 2, 2, 2, 1, 1, 2, 2, 2, 2, 1, 2, 2, 2, 2, 2, 2, 2, 2, 4 ),
 ( 0.000000000000000000, 0.03124999999998657324, 0.06249999999997314648, 0.09374999999995972666, 0.1093749999999517192, 0.1249999999999437117, 0.1562499999999277522, 0.1718749999999209244, 0.1874999999999141242, 0.2031249999999072964, 0.2109374999999048816, 0.2148437499999037159, 0.2187499999999025779, 0.2499999999998959166, 0.2656249999998932521, 0.2734374999998928080, 0.2812499999998923084, 0.2968749999998929190, 0.3124999999998935296, 0.3437499999998948619, 0.3593749999998955835, 0.3749999999998963052, 0.4062499999998969158, 0.4374999999998974709, 0.4999999999998985256, 0.5312499999998990807, 0.5624999999998996358, 0.5937499999999001910, 0.6093749999999005240, 0.6249999999999007461, 0.6562499999999023004, 0.6718749999999037437, 0.6874999999999050759, 0.7031249999999065192, 0.7109374999999072964, 0.7148437499999084066, 0.7187499999999094058, 0.7499999999999189537, 0.7656249999999230615, 0.7734374999999250599, 0.7773437499999261702, 0.7812499999999272804, 0.7968749999999314992, 0.8124999999999358291, 0.8437499999999442668, 0.8593749999999483746, 0.8749999999999525935, 0.9374999999999763522, 1.000000000000000000 ),
 .UNSPECIFIED. ) ;
#37503=CARTESIAN_POINT ( 'NONE',  ( 18.16680584898033146, -2.371606440122840276, -12.48054868302275366 ) ) ;
#37506=CARTESIAN_POINT ( 'NONE',  ( 4.599999999999999645, -0.7192913403693023122, 12.57945229203838267 ) ) ;
#37507=CARTESIAN_POINT ( 'NONE',  ( 18.18005044388383240, -2.499999700414728743, -12.45156116530568902 ) ) ;
#37508=CARTESIAN_POINT ( 'NONE',  ( 12.18402495282434472, 0.07112389991331898031, 13.89976024287835799 ) ) ;
#37522=CARTESIAN_POINT ( 'NONE',  ( 17.79083366726184678, -1.825854556040602095, 13.88043960113447284 ) ) ;
#37529=ORIENTED_EDGE ( 'NONE', *, *, #3016, .T. ) ;
#37535=CARTESIAN_POINT ( 'NONE',  ( 18.15150620829238548, 2.686947401609460329, -12.40607332099752469 ) ) ;
#37539=AXIS2_PLACEMENT_3D ( 'NONE', #2148, #18224, #7038 ) ;
#37544=CARTESIAN_POINT ( 'NONE',  ( 12.22015141286114392, -0.2205037192104029042, -12.69742880170240085 ) ) ;
#37545=CARTESIAN_POINT ( 'NONE',  ( 17.55505043854144276, -0.7302158263239199032, -13.98094363220830871 ) ) ;
#37553=EDGE_CURVE ( 'NONE', #40048, #67932, #56312, .T. ) ;
#37571=EDGE_LOOP ( 'NONE', ( #56088, #20452, #31911, #28643 ) ) ;
#37575=VERTEX_POINT ( 'NONE', #67613 ) ;
#37582=CARTESIAN_POINT ( 'NONE',  ( 17.79030838958610872, -1.799800542995207309, -12.47079474911150143 ) ) ;
#37598=CIRCLE ( 'NONE', #52118, 13.17499999999999893 ) ;
#37599=CARTESIAN_POINT ( 'NONE',  ( 12.39034978066170645, 2.032288297489022177, -13.76160266677045563 ) ) ;
#37602=CARTESIAN_POINT ( 'NONE',  ( 17.83221471278435999, -0.5605600754933578456, 13.88478672247769730 ) ) ;
#37606=CARTESIAN_POINT ( 'NONE',  ( 12.42340929153268902, 0.4950008743410382883, 13.88813607082127355 ) ) ;
#37608=CARTESIAN_POINT ( 'NONE',  ( 18.08719402094173034, -0.3285636530950700740, -13.89479065952098935 ) ) ;
#37615=CARTESIAN_POINT ( 'NONE',  ( 18.15598060823833038, -0.1720826094844742082, 12.69843621396828226 ) ) ;
#37622=FACE_OUTER_BOUND ( 'NONE', #12817, .T. ) ;
#37632=CARTESIAN_POINT ( 'NONE',  ( 17.67439832720110005, 3.190335184669548241, -12.18941280901077739 ) ) ;
#37652=CARTESIAN_POINT ( 'NONE',  ( 17.77562957671592869, 0.5851376999905949505, -13.88342059653408533 ) ) ;
#37668=CARTESIAN_POINT ( 'NONE',  ( 12.30608813017797409, -2.123066299447895044, -12.53144042021394178 ) ) ;
#37673=CARTESIAN_POINT ( 'NONE',  ( 12.61605721975967498, -1.812633401299081903, -13.88216159563417307 ) ) ;
#37677=CARTESIAN_POINT ( 'NONE',  ( 18.08628618592430826, -2.970581112497159282, 12.24483314193593131 ) ) ;
#37681=VECTOR ( 'NONE', #7378, 1000.000000000000000 ) ;
#37687=CARTESIAN_POINT ( 'NONE',  ( 18.14129716922916558, 2.282346377865474008, -12.49966253006683381 ) ) ;
#37690=ORIENTED_EDGE ( 'NONE', *, *, #5284, .F. ) ;
#37699=CARTESIAN_POINT ( 'NONE',  ( 12.20981273398931499, -0.1908418880314488031, 12.69807545005479810 ) ) ;
#37709=CARTESIAN_POINT ( 'NONE',  ( 18.16473232272955229, 2.360987313248031239, 13.70192779769509528 ) ) ;
#37718=ORIENTED_EDGE ( 'NONE', *, *, #59386, .T. ) ;
#37720=CARTESIAN_POINT ( 'NONE',  ( 18.22207129059747288, -2.231684076289582208, -13.82098807703153476 ) ) ;
#37726=AXIS2_PLACEMENT_3D ( 'NONE', #27702, #16507, #44487 ) ;
#37727=EDGE_CURVE ( 'NONE', #47262, #19317, #60934, .T. ) ;
#37741=CARTESIAN_POINT ( 'NONE',  ( 12.21279934347909801, 2.064970636307569052, -12.42964156345203719 ) ) ;
#37745=CARTESIAN_POINT ( 'NONE',  ( 18.08128123658401520, 2.837338021505997343, -13.59610410465670682 ) ) ;
#37750=CARTESIAN_POINT ( 'NONE',  ( 12.34734069910711263, -3.038294257956349664, -12.22819623478419260 ) ) ;
#37757=CARTESIAN_POINT ( 'NONE',  ( 17.78855914542206307, -0.6810629908227162632, -12.58158054216573696 ) ) ;
#37768=CARTESIAN_POINT ( 'NONE',  ( 18.26479085099338562, 2.332519703358803209, 12.38222476794584814 ) ) ;
#37773=ORIENTED_EDGE ( 'NONE', *, *, #9295, .T. ) ;
#37774=CARTESIAN_POINT ( 'NONE',  ( 12.10652924560090860, -2.286704390305614787, 12.39076728011198547 ) ) ;
#37781=CARTESIAN_POINT ( 'NONE',  ( 12.14465108362473877, 0.2970375428997805711, 12.59650273238872487 ) ) ;
#37783=EDGE_CURVE ( 'NONE', #59809, #13672, #38943, .T. ) ;
#37786=VECTOR ( 'NONE', #56126, 1000.000000000000000 ) ;
#37787=CARTESIAN_POINT ( 'NONE',  ( 12.30801118402048111, 2.879457308712139785, 12.35502813289141599 ) ) ;
#37794=CARTESIAN_POINT ( 'NONE',  ( 18.06407908469787316, -0.3627935497759613437, 12.69302875402486741 ) ) ;
#37798=CARTESIAN_POINT ( 'NONE',  ( 12.28050398199685134, 0.3399395274153702573, 12.69387965975142407 ) ) ;
#37804=CARTESIAN_POINT ( 'NONE',  ( 12.24916914324846573, -2.049138926831462815, 13.84922804760273607 ) ) ;
#37814=CARTESIAN_POINT ( 'NONE',  ( 18.11622138774303892, 2.775899412256286336, -12.38303361670991443 ) ) ;
#37823=ORIENTED_EDGE ( 'NONE', *, *, #23375, .T. ) ;
#37827=CARTESIAN_POINT ( 'NONE',  ( 17.63808658539560170, -3.119809217581025251, 13.52227901589168901 ) ) ;
#37829=VERTEX_POINT ( 'NONE', #59116 ) ;
#37836=CARTESIAN_POINT ( 'NONE',  ( 12.23148617192921073, -0.2485195352517245160, -13.89701485918576296 ) ) ;
#37848=CARTESIAN_POINT ( 'NONE',  ( 17.82007478097248665, -3.066051200070172289, -12.30148382826351572 ) ) ;
#37853=CARTESIAN_POINT ( 'NONE',  ( 5.500000000000000000, 0.000000000000000000, 0.000000000000000000 ) ) ;
#37854=CARTESIAN_POINT ( 'NONE',  ( 12.18201982513761372, 0.05063168410658506341, 13.89988098555966012 ) ) ;
#37855=ORIENTED_EDGE ( 'NONE', *, *, #38201, .T. ) ;
#37868=CARTESIAN_POINT ( 'NONE',  ( 21.59999987243000064, 1.172395514003999961E-13, 13.89999852641997613 ) ) ;
#37871=EDGE_CURVE ( 'NONE', #18819, #44093, #28797, .T. ) ;
#37884=CARTESIAN_POINT ( 'NONE',  ( 5.500000000000000000, -12.87590651766999983, -2.791353855799999728 ) ) ;
#37894=CARTESIAN_POINT ( 'NONE',  ( 12.79472656276095854, 0.6249999662751102303, -12.67928921590352154 ) ) ;
#37896=DIRECTION ( 'NONE',  ( 0.000000000000000000, 0.000000000000000000, 1.000000000000000000 ) ) ;
#37902=CARTESIAN_POINT ( 'NONE',  ( 18.18005043824377154, 1.329526366183796371E-10, 12.70000000088145420 ) ) ;
#37930=CARTESIAN_POINT ( 'NONE',  ( 18.14736049945649299, 0.1997550941124134616, -13.89807248760371117 ) ) ;
#37942=CARTESIAN_POINT ( 'NONE',  ( 12.80505043854143388, 1.787816316115912407, -13.88537766212463431 ) ) ;
#37945=CARTESIAN_POINT ( 'NONE',  ( 17.71746485746498223, -0.6038715862870289719, 13.88233985103439494 ) ) ;
#37947=EDGE_LOOP ( 'NONE', ( #39033, #2679, #32347, #34753 ) ) ;
#37949=LINE ( 'NONE', #204, #45537 ) ;
#37951=CARTESIAN_POINT ( 'NONE',  ( 12.41269542047506391, -0.4865081001745747424, -13.88853895923323378 ) ) ;
#37954=CARTESIAN_POINT ( 'NONE',  ( 17.94293712298191679, -0.4901002082654778436, -13.88836944287707098 ) ) ;
#37963=CARTESIAN_POINT ( 'NONE',  ( 18.17481334264689607, 0.08139242733401001739, 12.69965452654166960 ) ) ;
#37978=CARTESIAN_POINT ( 'NONE',  ( 17.95027792402079569, 3.083622039298902884, -12.21684579612696808 ) ) ;
#37991=VECTOR ( 'NONE', #23462, 1000.000000000000000 ) ;
#37993=CARTESIAN_POINT ( 'NONE',  ( 17.59617041303008378, -0.6239795106976184780, -13.88114172264460322 ) ) ;
#38010=CARTESIAN_POINT ( 'NONE',  ( 12.34565325027257998, -2.076107717502759353, -12.54027567175044311 ) ) ;
#38014=CARTESIAN_POINT ( 'NONE',  ( 12.17501771842806768, -2.156544773268137316, -13.83291087807201691 ) ) ;
#38016=CARTESIAN_POINT ( 'NONE',  ( 12.07922409836651489, -2.296075726970902675, 12.39049400503303922 ) ) ;
#38017=CARTESIAN_POINT ( 'NONE',  ( 18.26259847173845330, -2.320949922530737286, 12.38441499264346390 ) ) ;
#38030=ADVANCED_FACE ( 'NONE', ( #56295 ), #14336, .F. ) ;
#38047=CARTESIAN_POINT ( 'NONE',  ( 18.16363222863425264, 2.642680409073417280, 13.64211442534931606 ) ) ;
#38051=EDGE_LOOP ( 'NONE', ( #39748, #17046, #56693, #33264 ) ) ;
#38052=CARTESIAN_POINT ( 'NONE',  ( 5.634824896761482016, -12.09997259267829506, 3.741298181620987151 ) ) ;
#38060=CARTESIAN_POINT ( 'NONE',  ( 17.85704948507095224, -1.853727412078939762, -13.87673533860537489 ) ) ;
#38079=CARTESIAN_POINT ( 'NONE',  ( 12.18657262959517595, 2.104614846739864209, -12.42298765743896816 ) ) ;
#38087=VERTEX_POINT ( 'NONE', #62552 ) ;
#38094=CARTESIAN_POINT ( 'NONE',  ( 4.599999999999999645, 1.760845406083394460, -12.47635457398814651 ) ) ;
#38097=CARTESIAN_POINT ( 'NONE',  ( 17.74345815918222868, -0.6949735217938798337, -12.58082105808779971 ) ) ;
#38099=CARTESIAN_POINT ( 'NONE',  ( 12.18396690406853544, 2.429413046084606620, -12.46775848778887408 ) ) ;
#38102=VERTEX_POINT ( 'NONE', #4166 ) ;
#38107=CARTESIAN_POINT ( 'NONE',  ( 18.23388167758333367, 2.733449996235734147, 12.29993400349665222 ) ) ;
#38114=CARTESIAN_POINT ( 'NONE',  ( 12.37983597880429265, -3.063558859249374766, 12.22189795429198966 ) ) ;
#38118=FACE_OUTER_BOUND ( 'NONE', #68566, .T. ) ;
#38121=CARTESIAN_POINT ( 'NONE',  ( 12.10431270533525527, -0.1860047152749652044, 12.59864695008082336 ) ) ;
#38124=CARTESIAN_POINT ( 'NONE',  ( 12.80505043854143388, 3.124999999999999556, 12.28373071562070074 ) ) ;
#38134=CARTESIAN_POINT ( 'NONE',  ( 12.40587394961001166, 0.4809228688204498225, 12.68774147672023744 ) ) ;
#38140=CARTESIAN_POINT ( 'NONE',  ( 12.14421144042239931, -2.819066901275895098, 13.71325475029871477 ) ) ;
#38163=CARTESIAN_POINT ( 'NONE',  ( 17.98481728017923942, -2.046093834626821817, 13.75931539188737496 ) ) ;
#38191=DIRECTION ( 'NONE',  ( 0.000000000000000000, -0.9586234969500269099, -0.2846769943204078834 ) ) ;
#38193=CARTESIAN_POINT ( 'NONE',  ( 12.21985227486504400, 0.2197089332467950795, 13.89766776387047642 ) ) ;
#38201=EDGE_CURVE ( 'NONE', #15133, #48764, #15010, .T. ) ;
#38204=CIRCLE ( 'NONE', #47152, 12.79999953825000070 ) ;
#38218=EDGE_LOOP ( 'NONE', ( #18331, #51562, #59534, #12302 ) ) ;
#38228=B_SPLINE_CURVE_WITH_KNOTS ( 'NONE', 3,
 ( #37507, #58487, #25991, #5687, #6031, #26339, #21764, #63380, #10939, #15155, #42417, #68279, #41723, #68977, #63723, #5348, #43101, #64403, #53243, #53928 ),
 .UNSPECIFIED., .F., .F.,
 ( 4, 2, 2, 2, 2, 2, 2, 2, 2, 4 ),
 ( 0.5011597829110069346, 0.5050569721070143903, 0.5089541613030218459, 0.5167485396950372012, 0.5323372964790684669, 0.5635148100471309984, 0.5946923236151935299, 0.6258698371832560614, 0.7505798914555037449, 1.000000000000000000 ),
 .UNSPECIFIED. ) ;
#38239=VERTEX_POINT ( 'NONE', #9757 ) ;
#38250=CARTESIAN_POINT ( 'NONE',  ( 18.08663229464169930, 2.829323725363764641, -13.59808899811970484 ) ) ;
#38255=EDGE_CURVE ( 'NONE', #62822, #28970, #64673, .T. ) ;
#38259=CARTESIAN_POINT ( 'NONE',  ( 17.67418791246058873, 1.797344534875185529, -13.88414834504120599 ) ) ;
#38285=CARTESIAN_POINT ( 'NONE',  ( 12.18118526251762646, 2.542711865659281312, -13.66432766657963427 ) ) ;
#38289=CARTESIAN_POINT ( 'NONE',  ( 5.500000000000000000, 12.65263727151999795, -3.063503113339999917 ) ) ;
#38294=CARTESIAN_POINT ( 'NONE',  ( 12.24298788041087782, -0.2740979068391591889, 13.89637745338051111 ) ) ;
#38295=CARTESIAN_POINT ( 'NONE',  ( 12.30787805051431150, -0.3788776035274156184, -13.89305317345212032 ) ) ;
#38307=CARTESIAN_POINT ( 'NONE',  ( 18.06882650195507978, -0.3560396104572058906, 12.69328656575055980 ) ) ;
#38311=ORIENTED_EDGE ( 'NONE', *, *, #30658, .T. ) ;
#38320=CARTESIAN_POINT ( 'NONE',  ( 12.10797143991210767, -0.1980440493285478276, -12.59844852634975254 ) ) ;
#38322=CARTESIAN_POINT ( 'NONE',  ( 18.24534165125340479, 2.701041880525440586, -12.30709158425920613 ) ) ;
#38339=CARTESIAN_POINT ( 'NONE',  ( 17.65055117253431050, 0.7242550212506057017, -13.98125389334239443 ) ) ;
#38351=CARTESIAN_POINT ( 'NONE',  ( 17.57920308108771934, -1.787817001021373420, 13.88537754104227417 ) ) ;
#38358=CARTESIAN_POINT ( 'NONE',  ( 12.18110988575103804, -2.462234709496985641, -12.46028276222759423 ) ) ;
#38363=CARTESIAN_POINT ( 'NONE',  ( 12.08963668261109525, -2.638435792642062960, -13.74915318082108939 ) ) ;
#38366=CARTESIAN_POINT ( 'NONE',  ( 17.72222400754431249, -1.779821952440184818, 12.47366250980180524 ) ) ;
#38395=CARTESIAN_POINT ( 'NONE',  ( 18.14812703077569367, 2.302545424703879462, 13.71331074879213219 ) ) ;
#38405=LINE ( 'NONE', #27234, #1179 ) ;
#38408=CARTESIAN_POINT ( 'NONE',  ( 18.18532329594574648, -2.156378744708864925, -13.83294935661368363 ) ) ;
#38429=CARTESIAN_POINT ( 'NONE',  ( 12.13037555192277850, 2.744322634620807388, -12.29751256722372865 ) ) ;
#38448=CARTESIAN_POINT ( 'NONE',  ( 18.15028814309356164, -0.1908418880314467214, -12.69807545005481053 ) ) ;
#38449=CARTESIAN_POINT ( 'NONE',  ( 12.21592886438546977, 2.708773148307667356, -12.40049785801472737 ) ) ;
#38461=CARTESIAN_POINT ( 'NONE',  ( 18.27481983568690183, 2.390134998303168778, 12.37124935920178714 ) ) ;
#38465=B_SPLINE_CURVE_WITH_KNOTS ( 'NONE', 3,
 ( #32325, #22850, #60266, #7122, #27414, #48390, #33701, #1191, #22500 ),
 .UNSPECIFIED., .F., .F.,
 ( 4, 1, 2, 2, 4 ),
 ( 0.000000000000000000, 0.2499999999999994449, 0.3749999999999998335, 0.5000000000000002220, 1.000000000000000000 ),
 .UNSPECIFIED. ) ;
#38468=CARTESIAN_POINT ( 'NONE',  ( 12.14412415395002398, -2.776584135961364108, 12.29026848248285475 ) ) ;
#38473=CARTESIAN_POINT ( 'NONE',  ( 12.11827192994441482, -0.2307628456012699170, 12.59789151516662997 ) ) ;
#38476=CARTESIAN_POINT ( 'NONE',  ( 12.57326805540220072, 3.080523641713201144, 12.29716358636311213 ) ) ;
#38480=CARTESIAN_POINT ( 'NONE',  ( 17.78803358707871141, -0.6812425322175436060, 12.58157083403807164 ) ) ;
#38483=CARTESIAN_POINT ( 'NONE',  ( 17.63846197668645743, -0.6206501420433685468, 12.67957965403709863 ) ) ;
#38492=CARTESIAN_POINT ( 'NONE',  ( 12.27274079034943455, -2.022162746929206278, 13.85319239000171265 ) ) ;
#38500=CARTESIAN_POINT ( 'NONE',  ( 12.80505043854144276, -0.7192913403693169672, -12.57945229203838267 ) ) ;
#38502=CARTESIAN_POINT ( 'NONE',  ( 18.09877017944540611, 2.191112624880879434, -12.51823083080036270 ) ) ;
#38518=CARTESIAN_POINT ( 'NONE',  ( 18.14041819333149519, -2.719953065120092273, 13.62436182279261843 ) ) ;
#38526=CARTESIAN_POINT ( 'NONE',  ( 12.35624619792629986, -1.936672541246387436, -13.86556857871296344 ) ) ;
#38528=CARTESIAN_POINT ( 'NONE',  ( 17.84362596415753544, 0.6599616342123957313, -12.58270523616455527 ) ) ;
#38542=B_SPLINE_CURVE_WITH_KNOTS ( 'NONE', 3,
 ( #23685, #65292, #60061, #33497 ),
 .UNSPECIFIED., .F., .F.,
 ( 4, 4 ),
 ( 0.000000000000000000, 1.000000000000000000 ),
 .UNSPECIFIED. ) ;
#38545=CARTESIAN_POINT ( 'NONE',  ( 12.47427908008582342, 0.5306878043354071872, 13.88636785578044375 ) ) ;
#38546=VERTEX_POINT ( 'NONE', #3166 ) ;
#38586=CARTESIAN_POINT ( 'NONE',  ( 12.26191093050522340, 2.190091418697194481, -13.73433605229142884 ) ) ;
#38591=CARTESIAN_POINT ( 'NONE',  ( 12.72332061973729012, 0.6199690124688018722, -13.88138352397877462 ) ) ;
#38602=CARTESIAN_POINT ( 'NONE',  ( 17.69802269633222735, 1.891226317878778485, -13.78388397175237223 ) ) ;
#38609=LINE ( 'NONE', #17985, #26670 ) ;
#38616=CARTESIAN_POINT ( 'NONE',  ( 18.07078568654538842, -2.853178104785935698, -13.59212922195714413 ) ) ;
#38617=DIRECTION ( 'NONE',  ( 0.000000000000000000, 0.9905022095861402143, -0.1374968101629056305 ) ) ;
#38623=CARTESIAN_POINT ( 'NONE',  ( 17.98022888730381652, -3.063516777430836502, -12.22190850126833794 ) ) ;
#38625=EDGE_CURVE ( 'NONE', #57125, #46362, #19525, .T. ) ;
#38630=CARTESIAN_POINT ( 'NONE',  ( 12.80505043854144276, 0.6951438842159390896, 13.94765567169528531 ) ) ;
#38635=CARTESIAN_POINT ( 'NONE',  ( 12.56965099582936674, 1.826966356815474368, -13.88028256676998495 ) ) ;
#38638=CARTESIAN_POINT ( 'NONE',  ( 18.24183043734545251, -0.2342631834278660341, 13.99804438501501380 ) ) ;
#38642=ORIENTED_EDGE ( 'NONE', *, *, #33583, .F. ) ;
#38644=CARTESIAN_POINT ( 'NONE',  ( 12.60522794357327747, -0.5937363471729734110, 13.88293910736614301 ) ) ;
#38660=CARTESIAN_POINT ( 'NONE',  ( 18.13628167719501505, -0.2299973361971393848, 12.69720198919503495 ) ) ;
#38662=CARTESIAN_POINT ( 'NONE',  ( 18.16744427651242688, -2.624922643435798619, -12.42158156183114848 ) ) ;
#38675=CARTESIAN_POINT ( 'NONE',  ( 12.08965323865563768, -0.1172743548790659562, -12.59945959730644205 ) ) ;
#38677=CARTESIAN_POINT ( 'NONE',  ( 17.55505043854143565, 3.199751711897557804, -12.18694338143115630 ) ) ;
#38691=CARTESIAN_POINT ( 'NONE',  ( 12.07922409836661792, 2.296075727005074008, -12.39049400502616827 ) ) ;
#38694=CARTESIAN_POINT ( 'NONE',  ( 18.12459203954894704, -0.2581888431706746978, -13.89679013629344517 ) ) ;
#38710=CARTESIAN_POINT ( 'NONE',  ( 12.73227166903755680, -1.879164230820285830, -12.57473389636349204 ) ) ;
#38717=CARTESIAN_POINT ( 'NONE',  ( 12.78440343889028874, -0.6249994633519880827, -13.88107975068472300 ) ) ;
#38718=CARTESIAN_POINT ( 'NONE',  ( 18.01290626049240728, -2.925915981747412076, 12.34209597222820420 ) ) ;
#38743=ORIENTED_EDGE ( 'NONE', *, *, #28667, .T. ) ;
#38748=CARTESIAN_POINT ( 'NONE',  ( 17.98492955360209322, 2.046199355803458353, 13.75924933913552728 ) ) ;
#38751=VERTEX_POINT ( 'NONE', #45051 ) ;
#38761=CARTESIAN_POINT ( 'NONE',  ( 18.08737871041812539, -2.022152854634004182, -13.85319383421289530 ) ) ;
#38782=CARTESIAN_POINT ( 'NONE',  ( 12.40918755490006831, 3.083210392534602828, -12.21694967330944870 ) ) ;
#38787=VERTEX_POINT ( 'NONE', #19506 ) ;
#38798=CARTESIAN_POINT ( 'NONE',  ( 7.100000000000000533, 12.59999999999999964, 0.000000000000000000 ) ) ;
#38799=CARTESIAN_POINT ( 'NONE',  ( 12.49912319420862872, -3.045104416349984966, -13.54255671968480357 ) ) ;
#38800=CARTESIAN_POINT ( 'NONE',  ( 18.17481334264689607, -0.08139242733401015617, -12.69965452654168026 ) ) ;
#38809=CARTESIAN_POINT ( 'NONE',  ( 18.08778676580599409, 1.991706414748727783, 12.44159931028328359 ) ) ;
#38817=CARTESIAN_POINT ( 'NONE',  ( 12.08949137858164669, -2.599319321963736495, 12.32899351683632005 ) ) ;
#38823=CARTESIAN_POINT ( 'NONE',  ( 12.30048768357420563, -0.5166535389540105605, 12.58940585649086508 ) ) ;
#38826=CARTESIAN_POINT ( 'NONE',  ( 12.39079901834617559, 2.968443430305769848, 12.32999838110539592 ) ) ;
#38832=EDGE_CURVE ( 'NONE', #58820, #38546, #25779, .T. ) ;
#38845=LINE ( 'NONE', #27666, #18453 ) ;
#38849=CARTESIAN_POINT ( 'NONE',  ( 12.11714050632482298, -2.287289704013994562, 13.81189467606769306 ) ) ;
#38856=CARTESIAN_POINT ( 'NONE',  ( 17.55505043854147118, -2.500000000000000000, -25.00000000000000000 ) ) ;
#38862=CARTESIAN_POINT ( 'NONE',  ( 17.99286279921835785, 2.053846844283184758, -12.54442212638278242 ) ) ;
#38865=CONICAL_SURFACE ( 'NONE', #14317, 2.100034213237000014, 0.7853981633972997312 ) ;
#38870=CARTESIAN_POINT ( 'NONE',  ( 12.19822292038682221, -2.649955820708161713, 12.41539170522314706 ) ) ;
#38874=CARTESIAN_POINT ( 'NONE',  ( 18.15689837892993097, -2.331154328543900700, 13.70782442673660206 ) ) ;
#38897=CARTESIAN_POINT ( 'NONE',  ( 12.21869931586264002, 2.282676242266353128, 13.71712068105209603 ) ) ;
#38900=VECTOR ( 'NONE', #53941, 1000.000000000000000 ) ;
#38902=CARTESIAN_POINT ( 'NONE',  ( 12.30894494036362019, 0.5330308249010283772, 13.98985951701901520 ) ) ;
#38913=DIRECTION ( 'NONE',  ( -0.000000000000000000, -0.000000000000000000, 1.000000000000000000 ) ) ;
#38917=CARTESIAN_POINT ( 'NONE',  ( 12.43982406843060851, -0.6284010951954579483, 12.58437167746757623 ) ) ;
#38929=PLANE ( 'NONE',  #17987 ) ;
#38938=EDGE_CURVE ( 'NONE', #42472, #18819, #57868, .T. ) ;
#38942=CARTESIAN_POINT ( 'NONE',  ( 12.72277096606028479, 0.6196453797482972536, -12.67964297675818308 ) ) ;
#38943=B_SPLINE_CURVE_WITH_KNOTS ( 'NONE', 3,
 ( #62633, #8138, #45884, #9157, #67194, #4252, #68219, #14422, #40296, #15097, #46916, #19306, #13731, #25240, #20337, #36421, #67537, #29484, #50791, #61615, #35063, #56379, #8482, #35400, #30165, #30494, #51468, #20003, #3565, #46576, #24900, #46230, #51807, #15445, #31192, #4943, #5971, #32558, #53190, #16124, #10532, #43395, #27310, #26630, #31524, #42365, #53536, #5288, #52846, #26281, #25930, #47948, #57735, #52498, #31872, #48, #37450, #53870, #48634, #64007, #58771, #736, #4594, #47260, #21706, #68564, #47607 ),
 .UNSPECIFIED., .F., .F.,
 ( 4, 2, 2, 2, 2, 2, 2, 2, 2, 2, 2, 2, 2, 2, 1, 1, 1, 2, 2, 2, 2, 2, 2, 2, 2, 2, 2, 2, 2, 2, 2, 2, 2, 2, 4 ),
 ( 0.000000000000000000, 0.1250000000000538458, 0.2500000000001076916, 0.3125000000001355582, 0.3437500000001494915, 0.3750000000001633693, 0.4062500000001773026, 0.4218750000001832978, 0.4375000000001892930, 0.4687500000002018385, 0.4843750000002080558, 0.5000000000002141620, 0.5156250000002204903, 0.5312500000002265965, 0.5468750000002328138, 0.5546875000002357003, 0.5585937500002366995, 0.5605468750002376987, 0.5625000000002385869, 0.5781250000002332579, 0.5859375000002308154, 0.5898437500002297051, 0.5937500000002284839, 0.6093750000002220446, 0.6171875000002184919, 0.6250000000002148282, 0.6406250000002076117, 0.6562500000002002842, 0.6718750000001930678, 0.6875000000001857403, 0.7187500000001714184, 0.7343750000001633138, 0.7500000000001553202, 0.8750000000000777156, 1.000000000000000000 ),
 .UNSPECIFIED. ) ;
#38949=CARTESIAN_POINT ( 'NONE',  ( 12.15446082633427771, 2.110350925085022311, 12.42276656535977075 ) ) ;
#38950=ORIENTED_EDGE ( 'NONE', *, *, #67649, .F. ) ;
#38952=CARTESIAN_POINT ( 'NONE',  ( 12.78109991897669673, -0.7302151993337216984, -13.98094363222392111 ) ) ;
#38960=CARTESIAN_POINT ( 'NONE',  ( 17.84276413147952312, 1.945066902726407365, -13.77561296414734038 ) ) ;
#38967=CARTESIAN_POINT ( 'NONE',  ( 17.55505043854144276, 0.6250000000000001110, -12.67928921589118474 ) ) ;
#38971=CARTESIAN_POINT ( 'NONE',  ( 18.16782992325282819, -2.622990444980092928, -13.64655204333130278 ) ) ;
#38972=CARTESIAN_POINT ( 'NONE',  ( 17.63765675170532532, -1.875000000000000666, 13.78631904427528809 ) ) ;
#38978=CARTESIAN_POINT ( 'NONE',  ( 18.12596594012301665, -2.036641643015561609, -12.43431447687783020 ) ) ;
#38989=CARTESIAN_POINT ( 'NONE',  ( 12.49074413817427853, 3.040604467177680181, -13.54382360563872822 ) ) ;
#38992=CARTESIAN_POINT ( 'NONE',  ( 17.93874521385978582, -0.6200266137005079337, 13.98626978124057807 ) ) ;
#38993=CARTESIAN_POINT ( 'NONE',  ( 17.55505043854144276, 0.6250000000000001110, 13.88107975066923316 ) ) ;
#38998=CARTESIAN_POINT ( 'NONE',  ( 12.25734203455823135, -0.3012395220628200643, 13.89560941713585684 ) ) ;
#38999=CARTESIAN_POINT ( 'NONE',  ( 12.57406875483051856, -0.5808247544188634981, -13.88366201036165570 ) ) ;
#39012=CARTESIAN_POINT ( 'NONE',  ( 17.69772537084632091, 0.6088395004560440693, 12.68034807294329447 ) ) ;
#39013=B_SPLINE_SURFACE_WITH_KNOTS ( 'NONE', 1, 3, ( 
 ( #29060, #50370, #2470, #23796, #66439, #45472, #66789, #40228, #8410, #25168, #10122, #26208, #47881, #57663, #30764, #36004, #3830, #31120, #62903, #31454, #46503, #31800, #58020, #52772, #53116, #5218, #15024, #37379, #47536, #20268, #52423, #67806, #32148, #46845, #52074, #4867, #68490, #26554, #9421, #20614, #68149, #41938, #68841, #21297, #20959, #42627, #41594, #42297, #63246, #19930, #63595, #41251, #15713, #69185, #63937, #36348, #37041, #9769, #16048, #25856, #4520, #58356, #62566, #15371, #14685, #57320, #47189, #36700, #10458, #58701, #10804, #4178, #25517, #48211, #33173, #23017, #6591, #17432, #22668, #60429, #44011, #59049, #21634, #5557, #53464, #49241 ),
 ( #44365, #1351, #318, #65316, #16393, #32485, #27581, #64623, #65664, #38060, #32825, #6935, #21978, #59384, #27932, #59732, #12537, #39105, #43665, #17787, #38761, #12192, #5896, #26899, #42969, #54141, #38408, #64276, #6239, #60086, #37720, #16731, #27238, #33520, #43319, #11151, #53799, #11485, #48562, #54839, #28270, #666, #11833, #49590, #48907, #1015, #22323, #1697, #64962, #17075, #54490, #45731, #2730, #34900, #13238, #7983, #55181, #67376, #56559, #13918, #67039, #23369, #2386, #55533, #19150, #33866, #50285, #13580, #12885, #44709, #50972, #66006, #49939, #19500, #40472, #23710, #39451, #3068, #51314, #62142, #28625, #3409, #24401, #56216, #24744, #45045 ) ),
 .UNSPECIFIED., .F., .F., .F.,
 ( 2, 2 ),
 ( 4, 2, 2, 2, 2, 2, 2, 2, 2, 2, 2, 2, 2, 2, 2, 2, 2, 2, 2, 2, 2, 2, 2, 2, 2, 2, 2, 2, 2, 2, 2, 2, 2, 2, 2, 2, 2, 2, 2, 2, 2, 2, 4 ),
 ( 0.000000000000000000, 1.000000000000000000 ),
 ( 0.000000000000000000, 7.142680049747107468E-05, 0.0001428536009949421494, 0.0002142804014924132240, 0.0002857072019898842987, 0.0003571340024873553734, 0.0004285608029848264481, 0.0004999876034822974685, 0.0005357010037310330330, 0.0005714144039797685974, 0.0006071278042285041619, 0.0006428412044772397263, 0.0007142680049747107468, 0.0007856948054721817672, 0.0008214082057209173317, 0.0008571216059696528961, 0.0008928350062183884606, 0.0009285484064671239166, 0.0009999752069645949371, 0.001071402007462066066, 0.001142828807959537195, 0.001214255608457008324, 0.001285682408954479453, 0.001321395809203215017, 0.001357109209451950581, 0.001428536009949421494, 0.001499962810446892406, 0.001535676210695627970, 0.001571389610944363534, 0.001607103011193099099, 0.001642816411441834663, 0.001714243211939305792, 0.001785670012436776921, 0.001821383412685512269, 0.001857096812934247833, 0.001928523613431718745, 0.001964237013680454093, 0.001999950413929189874, 0.002035663814177925655, 0.002071377214426661003, 0.002142804014924132132, 0.002214230815421603261, 0.002285657615919074390 ),
 .UNSPECIFIED. ) ;
#39020=CARTESIAN_POINT ( 'NONE',  ( 12.54469325725306916, -1.931433442391065958, 13.77773667378076006 ) ) ;
#39029=CARTESIAN_POINT ( 'NONE',  ( 12.11487221662461167, -0.2205548374446903714, -12.59807454672507809 ) ) ;
#39033=ORIENTED_EDGE ( 'NONE', *, *, #32444, .T. ) ;
#39045=CARTESIAN_POINT ( 'NONE',  ( 17.91054527438923216, -0.5141525164327350739, -13.88720023103245360 ) ) ;
#39053=CARTESIAN_POINT ( 'NONE',  ( 12.80505043854146940, -1.836970230372604318, -12.54239289408378255 ) ) ;
#39055=CARTESIAN_POINT ( 'NONE',  ( 12.56916471290668547, -1.825881566109255338, 13.88043612360053203 ) ) ;
#39063=EDGE_CURVE ( 'NONE', #63182, #11912, #31635, .T. ) ;
#39065=CARTESIAN_POINT ( 'NONE',  ( 17.81516833538384859, -3.068391096118999517, 12.30080513712135826 ) ) ;
#39093=CARTESIAN_POINT ( 'NONE',  ( 17.74496479089903289, 1.812889415971022933, 13.88212816151363782 ) ) ;
#39105=CARTESIAN_POINT ( 'NONE',  ( 18.05368493555554821, -1.987806113122535523, -13.85816345346370504 ) ) ;
#39113=VECTOR ( 'NONE', #55213, 1000.000000000000000 ) ;
#39127=CARTESIAN_POINT ( 'NONE',  ( 12.08949137858161293, 2.599319321963733387, -12.32899351683632005 ) ) ;
#39134=CARTESIAN_POINT ( 'NONE',  ( 12.15399652902990546, -2.797872959086246336, -12.28545279959702619 ) ) ;
#39143=CARTESIAN_POINT ( 'NONE',  ( 17.98256582722315144, -0.4560270868711831516, -12.68898073362800893 ) ) ;
#39147=EDGE_CURVE ( 'NONE', #59588, #19638, #48225, .T. ) ;
#39150=SHAPE_REPRESENTATION_RELATIONSHIP ( 'NONE' , 'NONE' ,  #8579, #6030 ) ;
#39155=CARTESIAN_POINT ( 'NONE',  ( 18.02785359611323912, 2.090732611440657251, 12.53755739145393555 ) ) ;
#39162=CARTESIAN_POINT ( 'NONE',  ( 12.41914228198398717, -3.089530644545724680, 12.21535262842080805 ) ) ;
#39168=CARTESIAN_POINT ( 'NONE',  ( 12.32674677874978642, -0.5406785836137757428, 12.58839662496522749 ) ) ;
#39171=CARTESIAN_POINT ( 'NONE',  ( 12.42261142450839984, 2.994360094170045450, 12.32252841079978189 ) ) ;
#39177=CARTESIAN_POINT ( 'NONE',  ( 18.03457482790186361, -0.4008908244505982599, 12.69148415474440661 ) ) ;
#39185=CARTESIAN_POINT ( 'NONE',  ( 17.98398272107413121, -2.954699841461171150, 13.56644208774973137 ) ) ;
#39188=CARTESIAN_POINT ( 'NONE',  ( 12.17479962224113166, -2.156383435693121520, 13.83294862407085724 ) ) ;
#39193=AXIS2_PLACEMENT_3D ( 'NONE', #68307, #8568, #19746 ) ;
#39197=CARTESIAN_POINT ( 'NONE',  ( 12.80505043854146763, -3.248147246781390329, -13.61798588129781074 ) ) ;
#39199=ORIENTED_EDGE ( 'NONE', *, *, #66211, .T. ) ;
#39202=CARTESIAN_POINT ( 'NONE',  ( 17.92245882712028759, 1.993980507605455310, -12.55520606452098775 ) ) ;
#39210=CARTESIAN_POINT ( 'NONE',  ( 12.20841262064594268, -2.686198882981354785, 12.40625987442081346 ) ) ;
#39211=ORIENTED_EDGE ( 'NONE', *, *, #59963, .T. ) ;
#39214=CARTESIAN_POINT ( 'NONE',  ( 18.14815926393673706, -2.301857555364728913, 13.71350736626465761 ) ) ;
#39221=CARTESIAN_POINT ( 'NONE',  ( 12.15689047902494835, -2.896806234243965328, -13.69773071446984858 ) ) ;
#39235=CARTESIAN_POINT ( 'NONE',  ( 4.599999999999999645, -0.7192913403693119712, -12.57945229203838267 ) ) ;
#39237=CARTESIAN_POINT ( 'NONE',  ( 12.21194158638444272, 2.301857635319167983, 13.71345735897205209 ) ) ;
#39241=CARTESIAN_POINT ( 'NONE',  ( 12.54917863858678118, 0.6836428945794205125, 13.98330131869062321 ) ) ;
#39250=CARTESIAN_POINT ( 'NONE',  ( 12.80505043854146940, -1.875000000000000000, 13.78631952119025073 ) ) ;
#39277=DIRECTION ( 'NONE',  ( 1.000000000000000000, 0.000000000000000000, 0.000000000000000000 ) ) ;
#39290=CARTESIAN_POINT ( 'NONE',  ( 12.52839348839893141, 0.5608030988280865436, -13.88477341743901050 ) ) ;
#39295=CARTESIAN_POINT ( 'NONE',  ( 5.630600923344116993, 12.10404814139731222, -3.742416328825069360 ) ) ;
#39297=CONICAL_SURFACE ( 'NONE', #23673, 12.72499970924999957, 0.7853981386146715593 ) ;
#39298=CARTESIAN_POINT ( 'NONE',  ( 18.16667230414093126, 2.370970514942110974, -13.69998174157045412 ) ) ;
#39305=CARTESIAN_POINT ( 'NONE',  ( 18.00675905371507923, 0.4321659195651227359, -12.69010673282157597 ) ) ;
#39311=CARTESIAN_POINT ( 'NONE',  ( 17.96842299892580996, -2.968890910988948750, -13.56270300416616692 ) ) ;
#39318=CARTESIAN_POINT ( 'NONE',  ( 18.17657007421214743, -2.109712673715142373, -12.42212297180517133 ) ) ;
#39328=EDGE_CURVE ( 'NONE', #39916, #66715, #16990, .T. ) ;
#39330=CARTESIAN_POINT ( 'NONE',  ( 12.26319456176230105, 2.811641923064096549, -13.60240885908115160 ) ) ;
#39334=CARTESIAN_POINT ( 'NONE',  ( 17.74345116425200075, -0.7055305429986051813, 13.98221279804358197 ) ) ;
#39339=CARTESIAN_POINT ( 'NONE',  ( 12.40292999696741028, -0.4784640315611758399, 13.88891505533309711 ) ) ;
#39346=B_SPLINE_CURVE_WITH_KNOTS ( 'NONE', 3,
 ( #1632, #55464, #945, #7221 ),
 .UNSPECIFIED., .F., .F.,
 ( 4, 4 ),
 ( 0.000000000000000000, 1.000000000000000000 ),
 .UNSPECIFIED. ) ;
#39349=AXIS2_PLACEMENT_3D ( 'NONE', #14893, #3111, #37247 ) ;
#39352=CARTESIAN_POINT ( 'NONE',  ( 17.59627748481874576, 0.6237239846186465320, 12.67937377942300614 ) ) ;
#39354=CARTESIAN_POINT ( 'NONE',  ( 17.86986266959569036, -3.040316756274647148, -12.30911383021075700 ) ) ;
#39361=AXIS2_PLACEMENT_3D ( 'NONE', #12837, #66305, #6887 ) ;
#39367=CARTESIAN_POINT ( 'NONE',  ( 12.09164653790447552, 0.1286734328892400470, -12.59934825840596773 ) ) ;
#39383=CARTESIAN_POINT ( 'NONE',  ( 17.83170738868395233, -0.5608030988280895413, -13.88477341743901050 ) ) ;
#39389=CARTESIAN_POINT ( 'NONE',  ( 18.17514718079836200, -2.578773340686874693, 12.43289648649885670 ) ) ;
#39390=ORIENTED_EDGE ( 'NONE', *, *, #39805, .F. ) ;
#39399=CARTESIAN_POINT ( 'NONE',  ( 12.07940096941462471, -2.330761819134298918, 13.80597083266311564 ) ) ;
#39407=CARTESIAN_POINT ( 'NONE',  ( 17.63949335857240186, -1.765638956106267310, 12.47567715783345221 ) ) ;
#39437=CARTESIAN_POINT ( 'NONE',  ( 18.27992102884630654, 2.544330805874857049, 13.76687901878135456 ) ) ;
#39451=CARTESIAN_POINT ( 'NONE',  ( 17.81237950545467896, -3.200707792931491547, -13.62921448194398977 ) ) ;
#39473=CARTESIAN_POINT ( 'NONE',  ( 12.57303446153994031, 1.919568987556538486, -12.56805043247348586 ) ) ;
#39479=ADVANCED_FACE ( 'NONE', ( #45412 ), #39297, .F. ) ;
#39484=CARTESIAN_POINT ( 'NONE',  ( 12.17603179862378404, -2.838932078785886048, -12.27602983002082304 ) ) ;
#39490=CARTESIAN_POINT ( 'NONE',  ( 12.18114782263376483, -2.542296328577542841, -13.66436634302259812 ) ) ;
#39491=CARTESIAN_POINT ( 'NONE',  ( 18.16373151406918041, 0.1422617729927601049, -12.69893308522357422 ) ) ;
#39496=VECTOR ( 'NONE', #36674, 1000.000000000000000 ) ;
#39501=CARTESIAN_POINT ( 'NONE',  ( 18.11779302252796597, 2.227307244339884917, 12.51093773244155472 ) ) ;
#39507=CARTESIAN_POINT ( 'NONE',  ( 12.78419053748688405, -1.875000590519850574, 12.57545628621517864 ) ) ;
#39513=CARTESIAN_POINT ( 'NONE',  ( 12.22921692136010563, -0.4376617689587176674, 12.59240970319242514 ) ) ;
#39517=CARTESIAN_POINT ( 'NONE',  ( 12.26133075698773212, 2.191112520879995973, 12.51819442860477771 ) ) ;
#39536=CARTESIAN_POINT ( 'NONE',  ( 12.44048633593779840, -3.149516123668035128, 13.64113935299650393 ) ) ;
#39537=DIRECTION ( 'NONE',  ( 1.000000000000000000, 0.000000000000000000, 0.000000000000000000 ) ) ;
#39549=CARTESIAN_POINT ( 'NONE',  ( 17.97023714413479567, 2.032719534845758069, -12.54827100236067139 ) ) ;
#39554=CARTESIAN_POINT ( 'NONE',  ( 12.80505043854143388, 1.798896937388929640, -12.50938852236267529 ) ) ;
#39556=CARTESIAN_POINT ( 'NONE',  ( 12.25778805737674837, -2.802014929519743180, 12.37607946563144878 ) ) ;
#39560=CARTESIAN_POINT ( 'NONE',  ( 18.25550288558785894, -2.707593611552288060, 13.73570038168180041 ) ) ;
#39582=CARTESIAN_POINT ( 'NONE',  ( 12.18760440664038391, 2.401006893892606353, 13.69392356709390945 ) ) ;
#39587=CARTESIAN_POINT ( 'NONE',  ( 12.61399518047280210, -0.5951713840684291768, 13.88284414672552991 ) ) ;
#39598=LINE ( 'NONE', #7430, #16415 ) ;
#39615=DIRECTION ( 'NONE',  ( 0.000000000000000000, -0.6884191022827257367, -0.7253131321107084695 ) ) ;
#39619=CARTESIAN_POINT ( 'NONE',  ( 12.52739587005665101, 3.060316261552512795, 13.53846823646895103 ) ) ;
#39631=CARTESIAN_POINT ( 'NONE',  ( 12.80505043854143388, 1.875000000000000000, -13.78631952119025428 ) ) ;
#39636=CARTESIAN_POINT ( 'NONE',  ( 12.70318375531252286, 0.6169787192598745751, -13.88156336867696616 ) ) ;
#39645=CARTESIAN_POINT ( 'NONE',  ( 17.94601859325906545, 2.012274714637017681, -13.76488447091686673 ) ) ;
#39652=CARTESIAN_POINT ( 'NONE',  ( 17.57920308108768381, 1.787817001021368313, -13.88537754104227417 ) ) ;
#39663=CARTESIAN_POINT ( 'NONE',  ( 18.17347573203825917, -2.104651709959060479, -12.42298141210392615 ) ) ;
#39673=ORIENTED_EDGE ( 'NONE', *, *, #28689, .F. ) ;
#39677=CARTESIAN_POINT ( 'NONE',  ( 12.32491409494622836, 3.065531103753988518, -13.66026219579215173 ) ) ;
#39680=CARTESIAN_POINT ( 'NONE',  ( 18.10090605892218107, -0.4811670829680718686, 13.99174107639406195 ) ) ;
#39681=CARTESIAN_POINT ( 'NONE',  ( 17.88331607686893321, -1.943250335979559429, 12.56477475324056847 ) ) ;
#39684=ORIENTED_EDGE ( 'NONE', *, *, #32363, .F. ) ;
#39687=CARTESIAN_POINT ( 'NONE',  ( 12.21982127435327214, -0.2196390008458968812, 13.89766917373561839 ) ) ;
#39689=CARTESIAN_POINT ( 'NONE',  ( 12.24478949869565447, -2.777190625952814962, 13.61075457644798448 ) ) ;
#39699=DIRECTION ( 'NONE',  ( -1.000000000000000000, 0.000000000000000000, 0.000000000000000000 ) ) ;
#39700=CARTESIAN_POINT ( 'NONE',  ( 12.19608323749910639, -0.1421782557229003263, 12.69895087450873383 ) ) ;
#39701=CARTESIAN_POINT ( 'NONE',  ( 18.16243401504203447, -2.647653207482971727, -12.41593780944610437 ) ) ;
#39711=VECTOR ( 'NONE', #8911, 1000.000000000000000 ) ;
#39712=LINE ( 'NONE', #13493, #37786 ) ;
#39717=CARTESIAN_POINT ( 'NONE',  ( 12.27537049189642637, 0.4912829912815125932, -12.59042165808840075 ) ) ;
#39733=EDGE_CURVE ( 'NONE', #64166, #4182, #11053, .T. ) ;
#39736=CARTESIAN_POINT ( 'NONE',  ( 18.20560607722003610, -0.3231860383015854876, -13.99628497142876249 ) ) ;
#39742=CARTESIAN_POINT ( 'NONE',  ( 18.13624123192029813, -2.730018939419430968, 12.39502206876364099 ) ) ;
#39748=ORIENTED_EDGE ( 'NONE', *, *, #63288, .T. ) ;
#39756=ADVANCED_FACE ( 'NONE', ( #24686 ), #66290, .F. ) ;
#39757=CARTESIAN_POINT ( 'NONE',  ( 12.18107303550440257, 0.04113803725886392565, -13.89993798560270122 ) ) ;
#39758=CARTESIAN_POINT ( 'NONE',  ( 17.98134286629680645, -1.897806848213326791, 12.45626380386397791 ) ) ;
#39779=CARTESIAN_POINT ( 'NONE',  ( 18.03319509584025582, -0.5408165383911034407, 12.58839068838662811 ) ) ;
#39787=CARTESIAN_POINT ( 'NONE',  ( 18.27904986288414690, 2.473365887482175118, 13.77980577478706792 ) ) ;
#39805=EDGE_CURVE ( 'NONE', #65648, #57880, #24443, .T. ) ;
#39808=AXIS2_PLACEMENT_3D ( 'NONE', #51478, #45562, #30505 ) ;
#39823=CARTESIAN_POINT ( 'NONE',  ( 12.27745450063681432, 2.164896879444428102, -12.52337953207688059 ) ) ;
#39832=CARTESIAN_POINT ( 'NONE',  ( 12.32336322858531474, -1.942450600934338745, -12.44937554728605100 ) ) ;
#39838=CARTESIAN_POINT ( 'NONE',  ( 12.18760440664042122, -2.401006893892608129, -13.69392356709392544 ) ) ;
#39839=CARTESIAN_POINT ( 'NONE',  ( 17.96738117868769535, -0.4698014501121463016, -12.68830453558793003 ) ) ;
#39849=CARTESIAN_POINT ( 'NONE',  ( 17.92067275948977212, 3.101661042832197790, 12.21227817455808307 ) ) ;
#39856=CARTESIAN_POINT ( 'NONE',  ( 12.70786224242106677, 0.7192245859875908698, -12.57945610904468303 ) ) ;
#39858=CARTESIAN_POINT ( 'NONE',  ( 12.33224723617690088, -2.090732662878786563, 12.53759506087955167 ) ) ;
#39865=CARTESIAN_POINT ( 'NONE',  ( 12.27431907826859714, 0.3302353423713642044, 12.69422546839060395 ) ) ;
#39869=CARTESIAN_POINT ( 'NONE',  ( 12.33197597414241997, 2.091428098900828925, 12.53741636228079948 ) ) ;
#39881=EDGE_CURVE ( 'NONE', #20140, #1557, #45926, .T. ) ;
#39887=CARTESIAN_POINT ( 'NONE',  ( 12.50373643672537582, -3.182160109867291808, 13.63355731004866556 ) ) ;
#39898=ORIENTED_EDGE ( 'NONE', *, *, #52522, .F. ) ;
#39909=CARTESIAN_POINT ( 'NONE',  ( 12.18214412808147884, -2.552249690271653826, 12.43927262873609685 ) ) ;
#39913=CARTESIAN_POINT ( 'NONE',  ( 18.27871553590501108, -2.567375067704839253, 13.76260043498214181 ) ) ;
#39916=VERTEX_POINT ( 'NONE', #15490 ) ;
#39918=CARTESIAN_POINT ( 'NONE',  ( 5.500000000000000000, -13.94845324556000143, 4.312847325879000770 ) ) ;
#39929=ORIENTED_EDGE ( 'NONE', *, *, #38832, .F. ) ;
#39935=CARTESIAN_POINT ( 'NONE',  ( 12.18828317886887902, 2.603111844536875275, 13.65101713889819557 ) ) ;
#39939=CARTESIAN_POINT ( 'NONE',  ( 12.24748280279661472, 0.2825744476584710618, -12.69577188568926474 ) ) ;
#39940=CARTESIAN_POINT ( 'NONE',  ( 12.48353988083098365, 0.6549277419692597357, 13.98467727287826889 ) ) ;
#39953=CARTESIAN_POINT ( 'NONE',  ( 12.36610530618393433, 3.052942130732427373, 12.22454734379039287 ) ) ;
#39980=CARTESIAN_POINT ( 'NONE',  ( 17.60337015074822276, 1.762344248314549944, -12.47614295832086206 ) ) ;
#39989=CARTESIAN_POINT ( 'NONE',  ( 12.08961512266908755, -0.1188263301541226807, -13.99950072926553979 ) ) ;
#39996=CARTESIAN_POINT ( 'NONE',  ( 18.15957959476899930, 2.341019627110876744, -13.70589624875886692 ) ) ;
#40000=VECTOR ( 'NONE', #20616, 1000.000000000000000 ) ;
#40004=CARTESIAN_POINT ( 'NONE',  ( 17.90980607984480244, 0.5146431972870012528, -12.68596244101704151 ) ) ;
#40005=FACE_OUTER_BOUND ( 'NONE', #11401, .T. ) ;
#40006=VERTEX_POINT ( 'NONE', #8522 ) ;
#40009=CARTESIAN_POINT ( 'NONE',  ( 18.17607324740604824, -2.571217238407994987, -13.65805047069065381 ) ) ;
#40010=CARTESIAN_POINT ( 'NONE',  ( 18.02726358178263766, -2.088564957048818727, 13.75219797955875123 ) ) ;
#40017=CARTESIAN_POINT ( 'NONE',  ( 18.21592075161434465, -2.776565552903150103, -12.29027267990593231 ) ) ;
#40020=EDGE_CURVE ( 'NONE', #4182, #9109, #19703, .T. ) ;
#40022=CARTESIAN_POINT ( 'NONE',  ( 17.55505043854144276, 0.7302158263239086899, 13.98094363220831049 ) ) ;
#40030=CARTESIAN_POINT ( 'NONE',  ( 12.14279580514167023, 2.220721880347445332, -13.82275356517831888 ) ) ;
#40033=CARTESIAN_POINT ( 'NONE',  ( 18.08578335600534714, 0.3302328523437053631, 13.89472426752322853 ) ) ;
#40041=EDGE_CURVE ( 'NONE', #63209, #9530, #28168, .T. ) ;
#40048=VERTEX_POINT ( 'NONE', #30203 ) ;
#40052=CARTESIAN_POINT ( 'NONE',  ( 18.11112283403659262, 0.2853680816562754741, 12.69568625917503013 ) ) ;
#40053=CARTESIAN_POINT ( 'NONE',  ( 12.18002295456098594, -0.03981407404452855930, 12.70000161046437981 ) ) ;
#40055=CARTESIAN_POINT ( 'NONE',  ( 17.96892410185106215, -2.968447989615301985, -12.32999203180362180 ) ) ;
#40060=CARTESIAN_POINT ( 'NONE',  ( 17.55505043854143565, 1.875000000000000000, 12.57541666120756041 ) ) ;
#40067=CARTESIAN_POINT ( 'NONE',  ( 12.27431907826859714, -0.3302353423713667580, -12.69422546839061461 ) ) ;
#40077=FACE_OUTER_BOUND ( 'NONE', #11058, .T. ) ;
#40086=CARTESIAN_POINT ( 'NONE',  ( 18.08442884140762175, -0.4994936913945470236, -13.99109680828866864 ) ) ;
#40090=CARTESIAN_POINT ( 'NONE',  ( 17.55505043854147118, -3.125000000000000000, 13.52084414783465860 ) ) ;
#40095=CARTESIAN_POINT ( 'NONE',  ( 12.37676482144654955, -2.955308392773306814, -13.56622858938219522 ) ) ;
#40097=CARTESIAN_POINT ( 'NONE',  ( 12.35647036338150606, -1.936369888838089137, 13.86561402904640161 ) ) ;
#40105=CARTESIAN_POINT ( 'NONE',  ( 12.27985112600388717, 0.3389646381316557822, -13.89444110642640773 ) ) ;
#40106=EDGE_CURVE ( 'NONE', #12254, #1557, #36941, .T. ) ;
#40107=CARTESIAN_POINT ( 'NONE',  ( 18.14833460798325859, -2.303170370814867862, 12.49527837666171415 ) ) ;
#40112=CARTESIAN_POINT ( 'NONE',  ( 17.55505043854143565, 1.875000000000000000, 13.78627172894481667 ) ) ;
#40130=CARTESIAN_POINT ( 'NONE',  ( 17.57900174287143358, -0.7192906882580816230, 12.57945229568000478 ) ) ;
#40131=DIRECTION ( 'NONE',  ( -0.000000000000000000, 0.7916053084224905501, 0.6110327615417471270 ) ) ;
#40136=CARTESIAN_POINT ( 'NONE',  ( 18.11095118117829728, 2.049130080444090396, 13.84922935676121902 ) ) ;
#40142=CARTESIAN_POINT ( 'NONE',  ( 4.599999999999999645, -1.787797342887044394, -13.88538010501570952 ) ) ;
#40163=CARTESIAN_POINT ( 'NONE',  ( 12.80505043854146940, -3.125000000000000000, 12.28374638332999780 ) ) ;
#40169=CARTESIAN_POINT ( 'NONE',  ( 12.36861073370954323, 2.947405515254781783, -12.33600917780097284 ) ) ;
#40172=ORIENTED_EDGE ( 'NONE', *, *, #51829, .T. ) ;
#40177=B_SPLINE_SURFACE_WITH_KNOTS ( 'NONE', 1, 3, ( 
 ( #58075, #31175, #62954, #68201, #41309, #21351, #21013, #20320, #52479, #4575, #42350, #20668, #62618, #4925, #31506, #14740, #41994, #42679, #63301, #15428, #26261, #53169, #41647, #63988, #15767, #36059, #37096, #58409, #26610, #16104, #5271, #58752, #32204, #57374, #53517, #26952, #67866, #52132, #46898, #48264, #43022, #1069, #65015, #6646, #44423, #65721, #54549, #37774, #27987, #49647, #65372, #27640, #55242, #32539, #64324, #11539, #43378, #17493, #38817, #60143, #12249, #33575, #32882, #64678, #7339, #1753, #38468, #23074, #1408, #54895, #17133, #49296, #48960, #22380, #16785, #371, #59100, #60485, #6995, #59788, #28327, #6295, #17845, #21688, #38114, #22724, #39162, #12594, #16446, #44071, #43721, #33922, #33231, #11202, #53854, #5953, #27294, #48618, #719, #22031, #59439, #54193, #11890, #66759 ),
 ( #55591, #39507, #19207, #13635, #56277, #61856, #61178, #45785, #7693, #2110, #45103, #46126, #3465, #24112, #67433, #62199, #40531, #40202, #60831, #3129, #29035, #67097, #56957, #13977, #61520, #24461, #19557, #35645, #8723, #18875, #39858, #50344, #2444, #34271, #24801, #13298, #23768, #12944, #28682, #55935, #18531, #8384, #35302, #66412, #45446, #8037, #30066, #34960, #34622, #29377, #50689, #23427, #51369, #29726, #2786, #51030, #56618, #40879, #14320, #44765, #49999, #66066, #18185, #57635, #31770, #31088, #68120, #20580, #35973, #47504, #37349, #42265, #41906, #4835, #69160, #16020, #58327, #68457, #20239, #30736, #57287, #14657, #53087, #62873, #9390, #41225, #9059, #36318, #41564, #36670, #68808, #4147, #25828, #9740, #10428, #63212, #14992, #25487, #52044, #51706, #5187, #10090, #46814, #52396 ) ),
 .UNSPECIFIED., .F., .F., .F.,
 ( 2, 2 ),
 ( 4, 2, 2, 2, 2, 2, 2, 2, 2, 2, 2, 2, 2, 2, 2, 2, 2, 2, 2, 2, 2, 2, 2, 2, 2, 2, 2, 2, 2, 2, 2, 2, 2, 2, 2, 2, 2, 2, 2, 2, 2, 2, 2, 2, 2, 2, 2, 2, 2, 2, 2, 4 ),
 ( 0.000000000000000000, 1.000000000000000000 ),
 ( 0.000000000000000000, 7.157624699936001862E-05, 0.0001431524939987200372, 0.0002147287409980800559, 0.0002326228027479200402, 0.0002505168644977600516, 0.0002863049879974400745, 0.0003220931114971200973, 0.0003578812349968001202, 0.0003936693584964801431, 0.0004294574819961601117, 0.0004652456054958400804, 0.0005010337289955201032, 0.0005368218524952001261, 0.0005726099759948801490, 0.0006441862229942401947, 0.0006799743464939202175, 0.0007157624699936002404, 0.0007336565317434402518, 0.0007515505934932802633, 0.0007873387169929602861, 0.0008589149639923202234, 0.0008947030874920001379, 0.0009304912109916801607, 0.0009662793344913601836, 0.001002067457991040206, 0.001073643704990400252, 0.001145219951989760298, 0.001216796198989120344, 0.001288372445988480389, 0.001359948692987840435, 0.001395736816487520458, 0.001431524939987200481, 0.001467313063486880504, 0.001503101186986560527, 0.001574677433985920572, 0.001646253680985280618, 0.001682041804484960424, 0.001717829927984640447, 0.001735723989734480350, 0.001753618051484320470, 0.001789406174984000276, 0.001860982421983360321, 0.001896770545483040344, 0.001932558668982720367, 0.001968346792482400173, 0.001986240854232240293, 0.002004134915982080413, 0.002075711162981440459, 0.002147287409980800504, 0.002218863656980160550, 0.002290439903979520596 ),
 .UNSPECIFIED. ) ;
#40178=CARTESIAN_POINT ( 'NONE',  ( 12.27207149905419925, -1.992391748285590181, -12.44148121715491584 ) ) ;
#40184=CARTESIAN_POINT ( 'NONE',  ( 12.37622832409311791, -2.954798090471129068, -13.56635979911537859 ) ) ;
#40185=CARTESIAN_POINT ( 'NONE',  ( 17.66769993992418364, -0.6148490057825423127, -12.67995724530760526 ) ) ;
#40197=CARTESIAN_POINT ( 'NONE',  ( 17.57925770490771100, 3.199697828486423923, 12.18695748817155078 ) ) ;
#40202=CARTESIAN_POINT ( 'NONE',  ( 12.49885887340288981, -1.955044097548215509, 12.56200003178136448 ) ) ;
#40206=DIRECTION ( 'NONE',  ( 0.000000000000000000, -1.000000000000000000, 0.000000000000000000 ) ) ;
#40209=CARTESIAN_POINT ( 'NONE',  ( 12.23574065127465182, 0.2580991232524050827, 12.69647497719789619 ) ) ;
#40212=CARTESIAN_POINT ( 'NONE',  ( 12.61159012396487000, 1.905606515074949714, 12.57035430044310154 ) ) ;
#40220=VECTOR ( 'NONE', #20555, 1000.000000000000000 ) ;
#40224=CARTESIAN_POINT ( 'NONE',  ( 17.88388243140133227, -0.5319787654676457755, -12.68500714331955237 ) ) ;
#40228=CARTESIAN_POINT ( 'NONE',  ( 17.75799838104448369, -1.908512137131851416, -13.78121285638385807 ) ) ;
#40229=CARTESIAN_POINT ( 'NONE',  ( 12.80505043854144276, -0.6250000000000001110, -25.00000000000000000 ) ) ;
#40230=CARTESIAN_POINT ( 'NONE',  ( 17.55505043854144276, 0.000000000000000000, -25.00000000000000000 ) ) ;
#40236=CARTESIAN_POINT ( 'NONE',  ( 17.63676827353077314, -0.6210358159598048378, 13.88132258802016494 ) ) ;
#40245=CARTESIAN_POINT ( 'NONE',  ( 4.600000127571202135, 3.375077994860000042E-14, 1.048050535245999973E-13 ) ) ;
#40247=CARTESIAN_POINT ( 'NONE',  ( 12.19400419524981238, -2.631361540944479049, 12.42001554595805857 ) ) ;
#40250=CARTESIAN_POINT ( 'NONE',  ( 17.81510163565847904, -1.931577867956977723, 13.77771208381435386 ) ) ;
#40262=CARTESIAN_POINT ( 'NONE',  ( 18.14418133822494283, 0.4193891200559174970, -12.59302195412780456 ) ) ;
#40266=PLANE ( 'NONE',  #3178 ) ;
#40272=ADVANCED_FACE ( 'NONE', ( #29097 ), #64643, .T. ) ;
#40276=CARTESIAN_POINT ( 'NONE',  ( 12.08611717550374820, 2.614944066661588185, 13.75364144501312680 ) ) ;
#40279=CARTESIAN_POINT ( 'NONE',  ( 12.22418410610920247, -0.2308773532682540375, -12.69717962855014193 ) ) ;
#40280=CARTESIAN_POINT ( 'NONE',  ( 12.80505043854144276, -0.6250000000000006661, 13.88107975066923316 ) ) ;
#40285=DIRECTION ( 'NONE',  ( 1.000000000000000000, 0.000000000000000000, 0.000000000000000000 ) ) ;
#40290=CARTESIAN_POINT ( 'NONE',  ( 12.27385967125947097, 2.970546648634948994, 12.24484150081281086 ) ) ;
#40296=CARTESIAN_POINT ( 'NONE',  ( 12.26155906745207602, 2.190709282217770948, 12.51827377313525780 ) ) ;
#40298=ORIENTED_EDGE ( 'NONE', *, *, #5087, .F. ) ;
#40299=VECTOR ( 'NONE', #47842, 1000.000000000000000 ) ;
#40305=DIRECTION ( 'NONE',  ( 1.000000000000000000, 0.000000000000000000, 0.000000000000000000 ) ) ;
#40306=CARTESIAN_POINT ( 'NONE',  ( 12.29692076506693965, 2.864061239608792331, 13.58942221845736853 ) ) ;
#40311=CARTESIAN_POINT ( 'NONE',  ( 18.03677854873447117, 1.942400312675097052, -12.44938339399086935 ) ) ;
#40320=CARTESIAN_POINT ( 'NONE',  ( 17.74675502965012086, 3.228624035226697053, -13.62268076944971362 ) ) ;
#40321=CARTESIAN_POINT ( 'NONE',  ( 12.75735126819566290, 0.7290235424212195836, -13.98100605002522734 ) ) ;
#40327=ORIENTED_EDGE ( 'NONE', *, *, #50518, .T. ) ;
#40329=CARTESIAN_POINT ( 'NONE',  ( 18.23515949175303064, 2.264077836046911596, -13.81573184862659431 ) ) ;
#40338=ORIENTED_EDGE ( 'NONE', *, *, #42337, .F. ) ;
#40340=DIRECTION ( 'NONE',  ( -0.7071067774168207087, 0.5091094021823148186, 0.4907215319718147839 ) ) ;
#40341=CARTESIAN_POINT ( 'NONE',  ( 18.17590806569061002, -2.418078130838746453, 13.69056546384896755 ) ) ;
#40345=CARTESIAN_POINT ( 'NONE',  ( 0.000000000000000000, 0.000000000000000000, 0.000000000000000000 ) ) ;
#40349=CARTESIAN_POINT ( 'NONE',  ( 17.94652436847578869, -2.012680451140230975, -12.55183781965936340 ) ) ;
#40358=CARTESIAN_POINT ( 'NONE',  ( 12.15287239299856559, 2.198919866763858089, -13.82623858331040267 ) ) ;
#40361=EDGE_CURVE ( 'NONE', #32483, #47064, #21945, .T. ) ;
#40362=CARTESIAN_POINT ( 'NONE',  ( 18.02418602114746093, 0.5568603909045788392, 13.98892293345219962 ) ) ;
#40369=CARTESIAN_POINT ( 'NONE',  ( 12.20440283798329517, -2.672818875560375673, 13.63528575797814568 ) ) ;
#40377=CARTESIAN_POINT ( 'NONE',  ( 12.75652363867536110, -0.7301778992647613986, 13.98094561311457440 ) ) ;
#40380=CARTESIAN_POINT ( 'NONE',  ( 18.02541143671232504, 0.4116921281473247540, 12.69102089861179472 ) ) ;
#40381=CARTESIAN_POINT ( 'NONE',  ( 18.17985377383712020, -2.516953534672679016, -12.44759707709438246 ) ) ;
#40387=DIRECTION ( 'NONE',  ( 1.000000000000000000, 0.000000000000000000, 0.000000000000000000 ) ) ;
#40389=EDGE_CURVE ( 'NONE', #25486, #59995, #34914, .T. ) ;
#40391=CARTESIAN_POINT ( 'NONE',  ( 12.32674677874978286, 0.5406785836137721901, -12.58839662496522749 ) ) ;
#40392=CARTESIAN_POINT ( 'NONE',  ( 12.72212784909656946, -1.875000000000001110, -12.57541659658316924 ) ) ;
#40405=VERTEX_POINT ( 'NONE', #43412 ) ;
#40409=CARTESIAN_POINT ( 'NONE',  ( 18.27776594916669239, 0.05915529127692104039, -13.99988012777929036 ) ) ;
#40415=CARTESIAN_POINT ( 'NONE',  ( 18.08697361609490173, -2.828309738116514094, 12.36901404293088724 ) ) ;
#40418=CARTESIAN_POINT ( 'NONE',  ( 12.20879664879744908, -2.687389840232196736, -13.63187458904427629 ) ) ;
#40428=CARTESIAN_POINT ( 'NONE',  ( 12.20096535489426692, -0.1616183441363955586, -13.89875400931294180 ) ) ;
#40429=CARTESIAN_POINT ( 'NONE',  ( 17.77761373051713178, -1.915879702936831519, 12.56867159344775153 ) ) ;
#40443=ADVANCED_FACE ( 'NONE', ( #22062 ), #49328, .F. ) ;
#40447=LINE ( 'NONE', #9658, #28781 ) ;
#40454=CARTESIAN_POINT ( 'NONE',  ( 17.93788416347130976, -0.6112845611542790936, 12.58516990776527145 ) ) ;
#40460=CARTESIAN_POINT ( 'NONE',  ( 17.60327209889952726, 1.789008353514935479, 13.88522434179080456 ) ) ;
#40472=CARTESIAN_POINT ( 'NONE',  ( 17.84552141390807378, -3.187082727966597417, -13.63240720791674931 ) ) ;
#40496=CARTESIAN_POINT ( 'NONE',  ( 12.28874679351406307, 2.147634260983757759, -12.52674262693623142 ) ) ;
#40500=VERTEX_POINT ( 'NONE', #33265 ) ;
#40506=CARTESIAN_POINT ( 'NONE',  ( 12.18809860077016971, -2.859021363400004567, -12.27136516364851815 ) ) ;
#40512=CARTESIAN_POINT ( 'NONE',  ( 12.45019282332729382, -3.154806840457492711, -13.63991304855491471 ) ) ;
#40525=CARTESIAN_POINT ( 'NONE',  ( 17.55505043854143565, 1.875000000000000000, 12.57541666120756041 ) ) ;
#40531=CARTESIAN_POINT ( 'NONE',  ( 12.51690604397277795, -1.945290150052898515, 12.56367745121459834 ) ) ;
#40538=CARTESIAN_POINT ( 'NONE',  ( 12.18402519556254404, -0.07112609253419358013, 12.69973757146476245 ) ) ;
#40542=CARTESIAN_POINT ( 'NONE',  ( 12.51634965191642301, 1.945578265428328457, 12.56358890505709169 ) ) ;
#40552=AXIS2_PLACEMENT_3D ( 'NONE', #53399, #5498, #10738 ) ;
#40554=CARTESIAN_POINT ( 'NONE',  ( 18.09779212077640764, -0.3101159433354428452, -12.69490728026826432 ) ) ;
#40560=CARTESIAN_POINT ( 'NONE',  ( 12.38095956647856610, -3.110256499846533185, 13.65014134263123857 ) ) ;
#40580=CARTESIAN_POINT ( 'NONE',  ( 18.02561562912592663, 0.4118363585311526354, -13.89180007025484720 ) ) ;
#40581=CARTESIAN_POINT ( 'NONE',  ( 12.80505043854144276, 0.6249999999999994449, -13.88107975066922428 ) ) ;
#40588=CARTESIAN_POINT ( 'NONE',  ( 17.69802269633226288, -1.891226317878778485, 13.78388397175237046 ) ) ;
#40600=CARTESIAN_POINT ( 'NONE',  ( 18.27393049982691764, 0.09400131084486958166, -12.59965472429369093 ) ) ;
#40603=CARTESIAN_POINT ( 'NONE',  ( 12.80505043854146940, -1.760845406083394016, 12.47635457398814829 ) ) ;
#40604=ORIENTED_EDGE ( 'NONE', *, *, #39733, .T. ) ;
#40610=CARTESIAN_POINT ( 'NONE',  ( 12.12491761308580074, 2.264077311857957575, 13.81573193591466797 ) ) ;
#40613=CARTESIAN_POINT ( 'NONE',  ( 12.29062685731073401, -0.3550721707632966129, -12.69332222954723655 ) ) ;
#40614=CARTESIAN_POINT ( 'NONE',  ( 12.64055492385137747, -0.7115697451012007457, 13.98190580764195801 ) ) ;
#40627=CARTESIAN_POINT ( 'NONE',  ( 12.80505043854144276, 0.6878608935795413881, -12.61273126665598454 ) ) ;
#40633=CONICAL_SURFACE ( 'NONE', #4891, 2.100030785748999929, 0.7853981633972997312 ) ;
#40638=CARTESIAN_POINT ( 'NONE',  ( 4.699998537092440642, 0.000000000000000000, 0.000000000000000000 ) ) ;
#40639=CARTESIAN_POINT ( 'NONE',  ( 12.60065541206203932, 3.091968277202242987, 13.52988132686268230 ) ) ;
#40648=CARTESIAN_POINT ( 'NONE',  ( 17.57591323121269511, 3.124999405572034927, -12.28374652565520009 ) ) ;
#40652=CARTESIAN_POINT ( 'NONE',  ( 12.21945847209102354, 2.718477924854734606, -13.62469170119612194 ) ) ;
#40666=CARTESIAN_POINT ( 'NONE',  ( 18.23401891600712688, 2.774919967966554157, -13.72225625730858667 ) ) ;
#40687=CARTESIAN_POINT ( 'NONE',  ( 18.09076461395652657, -2.178034604381228867, -12.52076370778329029 ) ) ;
#40696=CARTESIAN_POINT ( 'NONE',  ( 12.50373643672534030, 3.182160109867286479, -13.63355731004866378 ) ) ;
#40699=CARTESIAN_POINT ( 'NONE',  ( 17.74252317112528132, 0.7057854747025454900, 13.98219993205038669 ) ) ;
#40704=ORIENTED_EDGE ( 'NONE', *, *, #27085, .T. ) ;
#40705=ORIENTED_EDGE ( 'NONE', *, *, #57684, .F. ) ;
#40735=CARTESIAN_POINT ( 'NONE',  ( 12.36315700431396358, 0.5707228546306866157, -12.58707662888203771 ) ) ;
#40736=CARTESIAN_POINT ( 'NONE',  ( 12.18001542466667608, -2.493364570470032682, -12.45310825068047045 ) ) ;
#40743=CARTESIAN_POINT ( 'NONE',  ( 17.91195086076331577, 0.5131995812820130398, 12.68604179104477758 ) ) ;
#40754=CARTESIAN_POINT ( 'NONE',  ( 18.25212991285167519, -0.2010519787742862108, -13.99856097495847607 ) ) ;
#40763=CARTESIAN_POINT ( 'NONE',  ( 12.21224535004423117, -2.300944246481291255, -13.71363154655825767 ) ) ;
#40766=DIRECTION ( 'NONE',  ( 1.000000000000000000, 0.000000000000000000, 0.000000000000000000 ) ) ;
#40767=ORIENTED_EDGE ( 'NONE', *, *, #62314, .F. ) ;
#40768=CARTESIAN_POINT ( 'NONE',  ( 17.95596346652836672, 0.4795055876567429487, -13.88886709646117801 ) ) ;
#40769=FACE_OUTER_BOUND ( 'NONE', #17379, .T. ) ;
#40772=CARTESIAN_POINT ( 'NONE',  ( 12.20137680394560320, 0.1621987986621312994, -13.89873133405096617 ) ) ;
#40774=CARTESIAN_POINT ( 'NONE',  ( 18.09877017944544164, -2.191112624880879878, 12.51823083080035204 ) ) ;
#40800=CARTESIAN_POINT ( 'NONE',  ( 18.10839966799241552, 0.4648927885597754495, 12.59142395508373014 ) ) ;
#40840=CARTESIAN_POINT ( 'NONE',  ( 12.41357648242114919, 2.012680472106851859, -12.55187634341709213 ) ) ;
#40850=CARTESIAN_POINT ( 'NONE',  ( 12.74469048821896955, -1.763307075768893784, -12.47600695802491089 ) ) ;
#40857=CARTESIAN_POINT ( 'NONE',  ( 12.57340716663137670, -1.919420395509098931, -13.77954053360031672 ) ) ;
#40867=CARTESIAN_POINT ( 'NONE',  ( 18.16281717172225996, 2.646070501177852030, 13.64134067051623411 ) ) ;
#40879=CARTESIAN_POINT ( 'NONE',  ( 12.18529561036837983, -2.583342615503333217, 12.43180850209203037 ) ) ;
#40885=CARTESIAN_POINT ( 'NONE',  ( 12.18028569061552879, -0.01996654564806360846, 12.69998441237379083 ) ) ;
#40907=CARTESIAN_POINT ( 'NONE',  ( 12.51458961313714724, -3.187047769811533815, 13.63241538057482494 ) ) ;
#40928=CARTESIAN_POINT ( 'NONE',  ( 12.18936456685733916, -2.391983199617479627, 12.47610573829959435 ) ) ;
#40932=CARTESIAN_POINT ( 'NONE',  ( 17.55505043854147118, -1.875000000000000000, 13.78631952119025605 ) ) ;
#40934=ORIENTED_EDGE ( 'NONE', *, *, #48529, .T. ) ;
#40939=CIRCLE ( 'NONE', #46535, 12.60000000000000142 ) ;
#40944=CARTESIAN_POINT ( 'NONE',  ( 18.21574167892471152, -0.2964030593063894936, -12.59651778044212556 ) ) ;
#40949=EDGE_LOOP ( 'NONE', ( #18116, #36360, #1275, #48665 ) ) ;
#40957=CARTESIAN_POINT ( 'NONE',  ( 12.29798916261918329, 1.995979084551873450, 13.85698889012213186 ) ) ;
#40960=CARTESIAN_POINT ( 'NONE',  ( 12.70148909168772455, 0.6166679310397558123, -12.67983904305986087 ) ) ;
#40962=CARTESIAN_POINT ( 'NONE',  ( 12.08616987952487598, -0.09542514088231011937, 13.99967976774382272 ) ) ;
#40989=CARTESIAN_POINT ( 'NONE',  ( 17.55505043854144276, 0.6250000000000001110, 12.67928921589117586 ) ) ;
#40993=B_SPLINE_CURVE_WITH_KNOTS ( 'NONE', 3,
 ( #32563, #10885, #26974, #21373, #53195, #1434, #53876, #16469, #42707, #17157, #43401, #395, #49319, #5295, #54219, #64012 ),
 .UNSPECIFIED., .F., .F.,
 ( 4, 2, 2, 2, 2, 2, 2, 4 ),
 ( 0.000000000000000000, 0.06249999999999916733, 0.1249999999999983347, 0.2499999999999967248, 0.4999999999999966693, 0.7499999999999966693, 0.8749999999999983347, 1.000000000000000000 ),
 .UNSPECIFIED. ) ;
#40998=CARTESIAN_POINT ( 'NONE',  ( 17.68706105916309568, 1.772767334361405656, -12.47466639265151755 ) ) ;
#41002=CARTESIAN_POINT ( 'NONE',  ( 12.25852091194881588, 2.803392358698900910, -13.60441894876048252 ) ) ;
#41007=DIRECTION ( 'NONE',  ( 1.000000000000000000, -1.659086735363680163E-15, 1.195176146505341979E-14 ) ) ;
#41014=ORIENTED_EDGE ( 'NONE', *, *, #65166, .T. ) ;
#41016=CARTESIAN_POINT ( 'NONE',  ( 18.17294214856815060, 2.135913245783947811, -13.83611159055834960 ) ) ;
#41025=ORIENTED_EDGE ( 'NONE', *, *, #57509, .T. ) ;
#41034=CARTESIAN_POINT ( 'NONE',  ( 18.15708441975580811, -2.331821618626341852, -12.48915497634519411 ) ) ;
#41037=VECTOR ( 'NONE', #62645, 1000.000000000000000 ) ;
#41047=CARTESIAN_POINT ( 'NONE',  ( 12.12912605232851604, 2.253778109953301634, -13.81740241363613642 ) ) ;
#41051=ORIENTED_EDGE ( 'NONE', *, *, #52440, .F. ) ;
#41053=AXIS2_PLACEMENT_3D ( 'NONE', #13192, #22621, #44320 ) ;
#41070=CARTESIAN_POINT ( 'NONE',  ( 18.17221331276092755, -2.599179209475691366, -12.42790858714744218 ) ) ;
#41080=DIRECTION ( 'NONE',  ( -1.000000000000000000, 0.000000000000000000, 0.000000000000000000 ) ) ;
#41082=CARTESIAN_POINT ( 'NONE',  ( 12.52850951125299872, -0.5605836838512548992, -12.68334204399185694 ) ) ;
#41084=CARTESIAN_POINT ( 'NONE',  ( 12.26155906743356461, -2.190709282250366652, -12.51827377312864975 ) ) ;
#41110=CARTESIAN_POINT ( 'NONE',  ( 17.69835410963201028, -3.108690103393802584, 12.28870081726095087 ) ) ;
#41113=CARTESIAN_POINT ( 'NONE',  ( 12.18428608238523125, -2.573446268070838983, -13.65756128988527962 ) ) ;
#41123=CYLINDRICAL_SURFACE ( 'NONE', #42004, 0.6250000000000005551 ) ;
#41125=CARTESIAN_POINT ( 'NONE',  ( 12.34868974583248402, 0.4275223103465176644, -13.89116040406442032 ) ) ;
#41126=CARTESIAN_POINT ( 'NONE',  ( 18.02645743154362634, -2.910866584900386744, 12.34632125423082449 ) ) ;
#41127=EDGE_LOOP ( 'NONE', ( #42293, #1031, #58489, #22711 ) ) ;
#41136=EDGE_CURVE ( 'NONE', #4104, #6955, #26787, .T. ) ;
#41143=VERTEX_POINT ( 'NONE', #22047 ) ;
#41146=CARTESIAN_POINT ( 'NONE',  ( 12.80505043854144276, -0.6250000000000001110, -13.88107975066922428 ) ) ;
#41157=CARTESIAN_POINT ( 'NONE',  ( 18.27977754798707721, 0.02297882141078181478, 12.59998453421652620 ) ) ;
#41164=CARTESIAN_POINT ( 'NONE',  ( 4.599999999999999645, 0.000000000000000000, 0.000000000000000000 ) ) ;
#41172=CARTESIAN_POINT ( 'NONE',  ( 18.00351343198559917, -3.053300080839206121, 12.22464702761727651 ) ) ;
#41194=CARTESIAN_POINT ( 'NONE',  ( 12.46375379917804338, 1.976313547018315075, -12.55830662486076577 ) ) ;
#41202=CARTESIAN_POINT ( 'NONE',  ( 12.29593341745177781, -2.863102696958912841, -12.35953065740858570 ) ) ;
#41208=CARTESIAN_POINT ( 'NONE',  ( 12.44718984625871805, -1.987489649616605902, -13.76884489496295139 ) ) ;
#41211=CARTESIAN_POINT ( 'NONE',  ( 17.65081963855161362, -3.193844305817328255, 12.18849311783432654 ) ) ;
#41214=CARTESIAN_POINT ( 'NONE',  ( 12.08019303639704489, 0.1916560648979804826, -13.99999316327169296 ) ) ;
#41215=CARTESIAN_POINT ( 'NONE',  ( 18.18005043854147118, -2.500000000000000000, -25.00000000000000000 ) ) ;
#41216=CARTESIAN_POINT ( 'NONE',  ( 18.17052368433065368, 2.609308838564532884, 13.64962199042474289 ) ) ;
#41219=FACE_OUTER_BOUND ( 'NONE', #46304, .T. ) ;
#41220=CARTESIAN_POINT ( 'NONE',  ( 17.80592519432564913, 3.072462716380374381, 12.29957259991316576 ) ) ;
#41221=CARTESIAN_POINT ( 'NONE',  ( 5.599999772733899484, -9.503509090790997936E-14, 3.419486915844999993E-14 ) ) ;
#41225=CARTESIAN_POINT ( 'NONE',  ( 12.46386834215128303, -3.023758766561085665, 12.31399102038137272 ) ) ;
#41233=CARTESIAN_POINT ( 'NONE',  ( 12.41659929819182118, 0.4896501542853322064, 12.68729270499356510 ) ) ;
#41234=CARTESIAN_POINT ( 'NONE',  ( 5.630370665534807806, -12.10426712534045990, -3.742487578858010089 ) ) ;
#41240=CARTESIAN_POINT ( 'NONE',  ( 17.96200919170517096, 2.025537500457071260, 13.76266550596355209 ) ) ;
#41251=CARTESIAN_POINT ( 'NONE',  ( 18.12478797189200463, -2.757742546077707413, -13.61537068597722211 ) ) ;
#41263=ORIENTED_EDGE ( 'NONE', *, *, #4039, .F. ) ;
#41277=CARTESIAN_POINT ( 'NONE',  ( 12.63924565005606304, -1.875000000000000222, 12.57545536278439791 ) ) ;
#41278=FACE_OUTER_BOUND ( 'NONE', #36541, .T. ) ;
#41279=CARTESIAN_POINT ( 'NONE',  ( 18.08710802279909657, -2.021458498708258666, 13.85330284862006245 ) ) ;
#41280=CARTESIAN_POINT ( 'NONE',  ( 17.93700172729746356, 2.995132885295900493, -13.55589876081417522 ) ) ;
#41281=ORIENTED_EDGE ( 'NONE', *, *, #28984, .F. ) ;
#41292=CARTESIAN_POINT ( 'NONE',  ( 18.21544979345815563, 0.2970375428997837353, -12.59650273238872664 ) ) ;
#41302=CARTESIAN_POINT ( 'NONE',  ( 17.87873473849105110, 1.836456536727118394, 12.46545041361348716 ) ) ;
#41303=CARTESIAN_POINT ( 'NONE',  ( 12.08015713295724858, 2.543697886577362954, 13.76699599502173399 ) ) ;
#41306=CARTESIAN_POINT ( 'NONE',  ( 12.47604026673111477, 0.5315006616213344692, -12.68502792338267504 ) ) ;
#41308=VERTEX_POINT ( 'NONE', #26540 ) ;
#41309=CARTESIAN_POINT ( 'NONE',  ( 12.68566995881739601, -1.770266656024991114, 12.47502217142794478 ) ) ;
#41320=CARTESIAN_POINT ( 'NONE',  ( 12.28024471298226850, 1.983745382141952840, 12.44286253672009579 ) ) ;
#41330=CARTESIAN_POINT ( 'NONE',  ( 12.44983299104790397, -0.5143225250488896449, 12.68597987475963684 ) ) ;
#41337=CARTESIAN_POINT ( 'NONE',  ( 12.18808187646823882, 2.399650199051974298, 13.69418124938378156 ) ) ;
#41339=ORIENTED_EDGE ( 'NONE', *, *, #1484, .T. ) ;
#41345=CARTESIAN_POINT ( 'NONE',  ( 17.85753477061698646, 1.826313832178713126, -12.46694048874450900 ) ) ;
#41347=CARTESIAN_POINT ( 'NONE',  ( 18.17043869203643425, 2.609785213594550068, 12.42531509794201661 ) ) ;
#41349=CARTESIAN_POINT ( 'NONE',  ( 12.19167018792746227, 2.619965297409280414, -13.64728369052539847 ) ) ;
#41354=CARTESIAN_POINT ( 'NONE',  ( 12.09168665071629256, 0.1308528744652265041, -13.99939340647621222 ) ) ;
#41357=DIRECTION ( 'NONE',  ( -0.000000000000000000, -0.000000000000000000, 1.000000000000000000 ) ) ;
#41364=CARTESIAN_POINT ( 'NONE',  ( 18.00853468083866460, 1.948185427393965607, -13.86378859567400923 ) ) ;
#41382=CARTESIAN_POINT ( 'NONE',  ( 18.05338926791298704, -2.122656057830398790, -12.53150860927891941 ) ) ;
#41388=B_SPLINE_CURVE_WITH_KNOTS ( 'NONE', 1,
 ( #34317, #7736 ),
 .UNSPECIFIED., .F., .F.,
 ( 2, 2 ),
 ( 0.000000000000000000, 1.000000000000000000 ),
 .UNSPECIFIED. ) ;
#41394=CARTESIAN_POINT ( 'NONE',  ( 18.05077945915500592, 0.5329747956504938822, 13.98985355243729067 ) ) ;
#41398=ORIENTED_EDGE ( 'NONE', *, *, #19007, .F. ) ;
#41403=CARTESIAN_POINT ( 'NONE',  ( 12.80505043854146940, -3.125000000000000000, 13.52084414783465860 ) ) ;
#41421=PLANE ( 'NONE',  #47741 ) ;
#41425=CARTESIAN_POINT ( 'NONE',  ( 12.47502136616923352, -0.5311517451680624058, -12.68505220952107670 ) ) ;
#41426=CARTESIAN_POINT ( 'NONE',  ( 12.18494477642119378, -2.419331844715135738, -12.47000601354013227 ) ) ;
#41431=CARTESIAN_POINT ( 'NONE',  ( 17.55505043854147118, -1.875000000000000000, -25.00000000000000000 ) ) ;
#41433=ADVANCED_FACE ( 'NONE', ( #58008 ), #65794, .T. ) ;
#41436=CARTESIAN_POINT ( 'NONE',  ( 17.82925890460733598, 0.5617199691901461067, 12.68327559333872934 ) ) ;
#41446=EDGE_LOOP ( 'NONE', ( #308, #3703, #42781, #14469 ) ) ;
#41455=CARTESIAN_POINT ( 'NONE',  ( 12.23172337865274706, -2.748896841596946583, -13.61745941693682305 ) ) ;
#41460=PLANE ( 'NONE',  #58225 ) ;
#41469=CARTESIAN_POINT ( 'NONE',  ( 17.62782920531153863, -1.879164230502278210, 12.57477362212319250 ) ) ;
#41475=CARTESIAN_POINT ( 'NONE',  ( 12.78422835261024382, 1.875000554926936402, -13.78631940402569889 ) ) ;
#41483=FACE_OUTER_BOUND ( 'NONE', #34212, .T. ) ;
#41488=CARTESIAN_POINT ( 'NONE',  ( 12.80505043854146940, -3.149917237299187267, 12.25147871603038219 ) ) ;
#41490=CARTESIAN_POINT ( 'NONE',  ( 18.10066919781364803, 0.4738025322793226746, 12.59109159930368627 ) ) ;
#41497=CARTESIAN_POINT ( 'NONE',  ( 17.85637496866990404, 3.182194879603814197, 13.63354919460146064 ) ) ;
#41506=CARTESIAN_POINT ( 'NONE',  ( 17.79118476696444517, -3.162166141421065557, 12.19676423671824494 ) ) ;
#41521=CARTESIAN_POINT ( 'NONE',  ( 12.80505043854146940, -1.787797342887047947, -13.88538010501570774 ) ) ;
#41533=CARTESIAN_POINT ( 'NONE',  ( 18.20120694906496084, -0.3761765224146920716, 12.59508068834013983 ) ) ;
#41536=CARTESIAN_POINT ( 'NONE',  ( 12.70862826151954295, -1.767199679044274996, -12.47545624547677434 ) ) ;
#41543=CARTESIAN_POINT ( 'NONE',  ( 12.61529649622816507, -3.223097538158948616, -13.62393827815043679 ) ) ;
#41548=CARTESIAN_POINT ( 'NONE',  ( 21.54999911806000057, 1.172395514003999961E-13, 13.94999927502997572 ) ) ;
#41557=CARTESIAN_POINT ( 'NONE',  ( 17.65867742935359175, 3.116692472806303904, 12.28625815163619350 ) ) ;
#41561=ORIENTED_EDGE ( 'NONE', *, *, #28453, .F. ) ;
#41564=CARTESIAN_POINT ( 'NONE',  ( 12.49878241383753519, -3.044913063694495214, 12.30777011605604798 ) ) ;
#41571=CARTESIAN_POINT ( 'NONE',  ( 12.50079267818768614, -0.5460377805369048820, 12.68419612078310621 ) ) ;
#41591=CARTESIAN_POINT ( 'NONE',  ( 18.16751419062931205, -2.624553509083156211, 13.64625295323315513 ) ) ;
#41594=CARTESIAN_POINT ( 'NONE',  ( 18.16363222863429172, -2.642680409073418168, -13.64211442534931784 ) ) ;
#41604=CIRCLE ( 'NONE', #5859, 2.000000000000001332 ) ;
#41616=CARTESIAN_POINT ( 'NONE',  ( 12.21202437720818601, -2.301604982168444558, 12.49562318899339708 ) ) ;
#41618=CARTESIAN_POINT ( 'NONE',  ( 17.87817017025377098, -1.864246049947076100, 13.87532391830906597 ) ) ;
#41631=CARTESIAN_POINT ( 'NONE',  ( 18.02418542278644509, 0.5485298171726687988, -12.58805670501782359 ) ) ;
#41642=CARTESIAN_POINT ( 'NONE',  ( 12.48178274919584752, 3.171647819517038336, 13.63600670097293843 ) ) ;
#41645=CARTESIAN_POINT ( 'NONE',  ( 12.09897931881621425, -0.1662062226620466543, 13.99901824074930978 ) ) ;
#41647=CARTESIAN_POINT ( 'NONE',  ( 12.37951367597797159, -1.897619119404206467, 12.45628731554757351 ) ) ;
#41648=CARTESIAN_POINT ( 'NONE',  ( 12.80505043854143388, 1.787816316115912185, -13.88537766212463254 ) ) ;
#41653=CARTESIAN_POINT ( 'NONE',  ( 12.13082219998073974, 0.2646961475753737414, 12.59722401988189411 ) ) ;
#41658=CARTESIAN_POINT ( 'NONE',  ( 12.37879419969803685, 1.897860824706880889, 12.45625557883629853 ) ) ;
#41665=CARTESIAN_POINT ( 'NONE',  ( 5.500000000000000000, -6.661338147750999827E-14, -1.931788062847999572E-14 ) ) ;
#41669=CARTESIAN_POINT ( 'NONE',  ( 12.64392860550861819, -0.6042188441982559999, 12.68064732209123946 ) ) ;
#41674=CARTESIAN_POINT ( 'NONE',  ( 12.33243540359738866, -2.090896859126742502, 13.75176201293517408 ) ) ;
#41675=CARTESIAN_POINT ( 'NONE',  ( 12.47652830181506012, 1.943388387788944405, 13.77651117150486115 ) ) ;
#41678=AXIS2_PLACEMENT_3D ( 'NONE', #17290, #37240, #16934 ) ;
#41684=CARTESIAN_POINT ( 'NONE',  ( 17.84275129854000852, 3.054939169952809230, -12.30480372676524858 ) ) ;
#41686=CARTESIAN_POINT ( 'NONE',  ( 18.18003600477297610, 2.504879791473498596, 12.45042248975033061 ) ) ;
#41687=CARTESIAN_POINT ( 'NONE',  ( 18.20500217920490016, 2.141655701468109019, 13.83591107702473266 ) ) ;
#41691=CARTESIAN_POINT ( 'NONE',  ( 12.10478902330476281, 0.1895042076700467759, -13.99872220539657519 ) ) ;
#41700=FACE_OUTER_BOUND ( 'NONE', #9643, .T. ) ;
#41702=CARTESIAN_POINT ( 'NONE',  ( 18.21576355877873965, 2.818661318639662294, -13.71332454644887555 ) ) ;
#41715=FACE_OUTER_BOUND ( 'NONE', #41127, .T. ) ;
#41721=CARTESIAN_POINT ( 'NONE',  ( 17.80610932905897315, -1.927548246225502249, -12.56666212246289405 ) ) ;
#41723=CARTESIAN_POINT ( 'NONE',  ( 18.15926133227551631, -2.338854968149422842, -12.48766092793498217 ) ) ;
#41731=CARTESIAN_POINT ( 'NONE',  ( 18.27544000105304534, -0.08309727575450792658, 13.99975851644561864 ) ) ;
#41742=CARTESIAN_POINT ( 'NONE',  ( 12.35418469966212562, -2.932966736140843800, 13.57204261866825235 ) ) ;
#41767=CARTESIAN_POINT ( 'NONE',  ( 12.57501510860068272, 0.5812174491462186454, -12.68209204657794231 ) ) ;
#41768=CARTESIAN_POINT ( 'NONE',  ( 12.19254223304418083, -2.624341220734839109, -12.42172529697063865 ) ) ;
#41779=VECTOR ( 'NONE', #57135, 1000.000000000000000 ) ;
#41795=CARTESIAN_POINT ( 'NONE',  ( 12.47652830184861372, -1.943388387755060398, -13.77651117150767668 ) ) ;
#41801=ORIENTED_EDGE ( 'NONE', *, *, #3768, .T. ) ;
#41803=CARTESIAN_POINT ( 'NONE',  ( 17.86532676353943572, 0.5429298016611214805, -13.88573085157339726 ) ) ;
#41808=CARTESIAN_POINT ( 'NONE',  ( 12.80505043854143388, 3.199751711897557804, -12.18694338143115630 ) ) ;
#41818=LINE ( 'NONE', #25051, #23871 ) ;
#41821=CARTESIAN_POINT ( 'NONE',  ( 12.50370260266017830, 0.5476489826676945727, 13.88547809940294719 ) ) ;
#41825=DIRECTION ( 'NONE',  ( -1.000000000000000000, 0.000000000000000000, 0.000000000000000000 ) ) ;
#41833=CARTESIAN_POINT ( 'NONE',  ( 18.24182894713846892, 0.2307628456012671414, 12.59789151516662997 ) ) ;
#41845=VECTOR ( 'NONE', #28050, 1000.000000000000000 ) ;
#41854=ORIENTED_EDGE ( 'NONE', *, *, #51321, .F. ) ;
#41867=CARTESIAN_POINT ( 'NONE',  ( 18.11117642456258992, 0.2854033456632677490, -13.89606078824646929 ) ) ;
#41871=EDGE_CURVE ( 'NONE', #2693, #66715, #28526, .T. ) ;
#41879=CARTESIAN_POINT ( 'NONE',  ( 4.699998537092440642, 2.033928548242059464E-13, 13.17499999999999893 ) ) ;
#41882=CARTESIAN_POINT ( 'NONE',  ( 12.42261142450843536, -2.994360094170046338, -12.32252841079977834 ) ) ;
#41886=CARTESIAN_POINT ( 'NONE',  ( 4.599999999999999645, -3.125000000000000000, -13.52078605991414761 ) ) ;
#41887=CARTESIAN_POINT ( 'NONE',  ( 12.21869931586267732, -2.282676242266354016, -13.71712068105209958 ) ) ;
#41891=CARTESIAN_POINT ( 'NONE',  ( 18.24165222613601500, -2.712088604378295464, 12.30466175173927290 ) ) ;
#41898=CIRCLE ( 'NONE', #57507, 1.999999999999999556 ) ;
#41899=CARTESIAN_POINT ( 'NONE',  ( 17.82007478097245112, 3.066051200070172289, 12.30148382826351394 ) ) ;
#41906=CARTESIAN_POINT ( 'NONE',  ( 12.30770095535952358, -2.879049501765980956, 12.35516346652265263 ) ) ;
#41916=CARTESIAN_POINT ( 'NONE',  ( 5.695281798977684495, -12.04221271193012477, -3.723442287066820899 ) ) ;
#41935=CARTESIAN_POINT ( 'NONE',  ( 4.700001368028300597, 3.375077994860000042E-14, 13.99999975535615171 ) ) ;
#41938=CARTESIAN_POINT ( 'NONE',  ( 18.17997055489867719, -2.522561811188516856, -13.66861645680632620 ) ) ;
#41955=CIRCLE ( 'NONE', #1728, 12.84999890301999947 ) ;
#41960=CARTESIAN_POINT ( 'NONE',  ( 12.75685216135443945, 1.762044409276926515, -12.47618552084819576 ) ) ;
#41963=CARTESIAN_POINT ( 'NONE',  ( 18.10291081608028918, -2.039210736883937169, 13.85070288166277663 ) ) ;
#41964=DIRECTION ( 'NONE',  ( 1.000000000000000000, -3.631529569662070274E-15, 1.174496025128702085E-14 ) ) ;
#41969=( LENGTH_UNIT ( ) NAMED_UNIT ( * ) SI_UNIT ( .MILLI., .METRE. ) );
#41977=CARTESIAN_POINT ( 'NONE',  ( 17.82189142195447928, -0.6689034848678687695, -12.58223305319197571 ) ) ;
#41978=CARTESIAN_POINT ( 'NONE',  ( 12.33505003431745273, 2.912475392612775327, -12.34587402707887449 ) ) ;
#41988=CARTESIAN_POINT ( 'NONE',  ( 12.41959488098031095, 1.899094099299810212, 13.87060288894783255 ) ) ;
#41994=CARTESIAN_POINT ( 'NONE',  ( 12.47072553654366267, -1.841758158201590945, 12.46466843114748890 ) ) ;
#42002=ADVANCED_FACE ( 'NONE', ( #6845 ), #49609, .T. ) ;
#42004=AXIS2_PLACEMENT_3D ( 'NONE', #62436, #52989, #9289 ) ;
#42005=CARTESIAN_POINT ( 'NONE',  ( 12.32690578124262970, 0.5408165383911035518, 12.58839068838662811 ) ) ;
#42009=CARTESIAN_POINT ( 'NONE',  ( 12.08892279761558086, 2.366838896507799550, 12.37571060269619139 ) ) ;
#42019=CARTESIAN_POINT ( 'NONE',  ( 12.37275785075365597, 0.4515912410345762629, 12.68919663783466234 ) ) ;
#42024=DIRECTION ( 'NONE',  ( -0.7071068090162534459, 0.000000000000000000, 0.7071067533568404784 ) ) ;
#42025=CARTESIAN_POINT ( 'NONE',  ( 12.26168426244257326, -2.190490593926008867, 13.73426451135289916 ) ) ;
#42033=CARTESIAN_POINT ( 'NONE',  ( 17.94956985871012733, 2.984774188598619649, -12.32531689504261685 ) ) ;
#42048=CIRCLE ( 'NONE', #67726, 13.89999852641999922 ) ;
#42049=CARTESIAN_POINT ( 'NONE',  ( 12.80505043854144276, -5.963111948670274387E-16, -25.00000000000000000 ) ) ;
#42058=CARTESIAN_POINT ( 'NONE',  ( 12.40292999708903565, 0.4784640316632534640, -13.88891505532827075 ) ) ;
#42068=CARTESIAN_POINT ( 'NONE',  ( 18.17892392841396187, -2.542707335428990856, -12.44153274845740498 ) ) ;
#42072=ORIENTED_EDGE ( 'NONE', *, *, #51607, .T. ) ;
#42079=ADVANCED_FACE ( 'NONE', ( #7719 ), #39013, .T. ) ;
#42106=CARTESIAN_POINT ( 'NONE',  ( 18.18005043817894872, 2.519674551049350786, -12.44700836821350620 ) ) ;
#42115=ORIENTED_EDGE ( 'NONE', *, *, #22641, .F. ) ;
#42116=CARTESIAN_POINT ( 'NONE',  ( 12.19008233596125557, -0.1120021961262563370, -12.69934078656688925 ) ) ;
#42117=CARTESIAN_POINT ( 'NONE',  ( 12.23179573713378510, -2.749250017956391012, -12.38999654619789403 ) ) ;
#42126=CARTESIAN_POINT ( 'NONE',  ( 17.95596512695399127, 0.4795041973588453632, 12.68781427220483771 ) ) ;
#42162=AXIS2_PLACEMENT_3D ( 'NONE', #48087, #36913, #11361 ) ;
#42171=CARTESIAN_POINT ( 'NONE',  ( 12.72203378256778983, 1.880187905311241581, -13.78554362285502677 ) ) ;
#42174=CARTESIAN_POINT ( 'NONE',  ( 18.17602483311041439, 0.07155107330948734523, 13.89975717292031376 ) ) ;
#42176=VERTEX_POINT ( 'NONE', #51649 ) ;
#42177=CARTESIAN_POINT ( 'NONE',  ( 12.33180813479861904, 0.4082709497317869030, 13.89192968283204088 ) ) ;
#42180=DIRECTION ( 'NONE',  ( 0.000000000000000000, 1.000000000000000000, 0.000000000000000000 ) ) ;
#42185=VECTOR ( 'NONE', #66193, 1000.000000000000000 ) ;
#42188=CONICAL_SURFACE ( 'NONE', #66877, 12.69999976913000062, 0.7853981453603698926 ) ;
#42190=CARTESIAN_POINT ( 'NONE',  ( 17.78855914542205952, 0.6810629908226980556, 12.58158054216573341 ) ) ;
#42198=CARTESIAN_POINT ( 'NONE',  ( 17.84552141390803115, 3.187082727966593865, 13.63240720791674576 ) ) ;
#42210=CARTESIAN_POINT ( 'NONE',  ( 5.664191326658419179, 12.07183080424314525, 3.732901064425761639 ) ) ;
#42223=CARTESIAN_POINT ( 'NONE',  ( 18.06357043707759402, 0.3639325664385109627, -13.89360161040561970 ) ) ;
#42230=EDGE_CURVE ( 'NONE', #33960, #11762, #42048, .T. ) ;
#42232=ORIENTED_EDGE ( 'NONE', *, *, #8050, .F. ) ;
#42239=CARTESIAN_POINT ( 'NONE',  ( 17.55505043854144276, -0.6250000000000001110, 12.67928921589117586 ) ) ;
#42241=CARTESIAN_POINT ( 'NONE',  ( 12.80505043854146940, -1.760910691117822280, -12.47634535983623216 ) ) ;
#42244=CARTESIAN_POINT ( 'NONE',  ( 12.08015713295728411, -2.543697886577363843, -13.76699599502173044 ) ) ;
#42248=CARTESIAN_POINT ( 'NONE',  ( 18.27458182272990328, -2.390008000232556107, 12.37125705564431932 ) ) ;
#42262=ORIENTED_EDGE ( 'NONE', *, *, #19990, .F. ) ;
#42265=CARTESIAN_POINT ( 'NONE',  ( 12.29572644340314724, -2.862796356722884461, 12.35963739789472626 ) ) ;
#42272=CARTESIAN_POINT ( 'NONE',  ( 12.52804317529070133, -0.5603556898929450414, 12.68335562943300232 ) ) ;
#42274=CARTESIAN_POINT ( 'NONE',  ( 12.80505043854144276, 0.6249999999999994449, -13.88107975066922428 ) ) ;
#42278=CARTESIAN_POINT ( 'NONE',  ( 5.700000000000000178, 12.50865771883999855, -2.924687089724999911 ) ) ;
#42286=CARTESIAN_POINT ( 'NONE',  ( 5.630600923344347919, -12.10404814139707419, 3.742416328825248328 ) ) ;
#42293=ORIENTED_EDGE ( 'NONE', *, *, #68898, .F. ) ;
#42296=AXIS2_PLACEMENT_3D ( 'NONE', #17156, #65395, #44445 ) ;
#42297=CARTESIAN_POINT ( 'NONE',  ( 18.15864108120893050, -2.662504769557529904, -13.63760133890561121 ) ) ;
#42314=B_SPLINE_SURFACE_WITH_KNOTS ( 'NONE', 1, 3, ( 
 ( #58984, #45830, #48148, #37309, #26830, #42903, #47120, #10049, #37652, #64208, #29773, #68769, #26138, #67142, #51078, #20887, #19253, #31386, #40580, #3512, #42223, #68421, #47464, #41867, #15642, #20543, #63174, #15302, #36628, #57951, #49871, #28559, #64897, #17010, #12469, #11085, #44646, #43946, #49178, #22259, #22947, #33802, #1289, #48494, #54769, #33454, #64553, #16668, #946, #17722, #59320, #55119, #12125, #38694, #65250, #6523, #49520, #6870, #28206, #1634, #17366, #21908, #22602, #44303, #18064, #60015, #43599, #1984, #23306, #65598, #39045, #32761, #65938, #39383, #598, #60361, #32420, #7222, #53735, #43246, #5833, #27171, #27868, #37993, #11419, #54075 ),
 ( #6171, #27513, #48838, #38339, #59669, #11765, #33109, #54423, #29947, #34501, #23991, #23644, #44981, #55814, #2323, #19430, #61731, #66636, #7916, #13852, #45326, #30279, #13516, #29254, #24681, #28916, #56148, #60704, #55466, #34837, #8256, #19082, #56842, #8940, #66974, #34147, #7562, #40409, #51584, #35180, #46001, #51250, #67652, #3677, #66286, #29604, #12822, #50221, #56492, #18411, #40754, #25019, #46351, #8597, #39736, #3345, #61054, #13173, #50906, #2663, #19776, #18754, #40086, #14193, #50563, #61395, #67312, #62076, #3004, #24336, #45668, #35520, #5413, #58208, #5065, #47383, #57172, #30610, #47035, #57508, #58547, #15898, #36540, #68688, #63090, #25359 ) ),
 .UNSPECIFIED., .F., .F., .F.,
 ( 2, 2 ),
 ( 4, 2, 2, 2, 2, 2, 2, 2, 2, 2, 2, 2, 2, 2, 2, 2, 2, 2, 2, 2, 2, 2, 2, 2, 2, 2, 2, 2, 2, 2, 2, 2, 2, 2, 2, 2, 2, 2, 2, 2, 2, 2, 4 ),
 ( 0.000000000000000000, 1.000000000000000000 ),
 ( 0.000000000000000000, 7.083094307561129462E-05, 0.0001416618861512225892, 0.0002124928292268338974, 0.0002833237723024451785, 0.0003541547153780564595, 0.0004249856584536677948, 0.0004958166015292791301, 0.0005666475446048903570, 0.0006374784876805015838, 0.0007083094307561129191, 0.0007791403738317242544, 0.0008145558453695299220, 0.0008499713169073355896, 0.0008853867884451412573, 0.0009208022599829469249, 0.0009916332030585582602, 0.001027048674596363819, 0.001062464146134169379, 0.001097879617671975155, 0.001133295089209780714, 0.001204126032285392049, 0.001239541503823197608, 0.001274956975361003168, 0.001310372446898808944, 0.001345787918436614503, 0.001416618861512225838, 0.001487449804587837173, 0.001522865276125642733, 0.001558280747663448509, 0.001629111690739059844, 0.001699942633814671179, 0.001735358105352476955, 0.001770773576890282515, 0.001806189048428088074, 0.001841604519965893850, 0.001912435463041505185, 0.001983266406117116520, 0.002018681877654922296, 0.002054097349192727639, 0.002124928292268338757, 0.002195759235343950309, 0.002266590178419561428 ),
 .UNSPECIFIED. ) ;
#42316=CARTESIAN_POINT ( 'NONE',  ( 12.29727795756345365, 1.966522083383872799, -12.44559612467660514 ) ) ;
#42317=EDGE_CURVE ( 'NONE', #34701, #1963, #9682, .T. ) ;
#42321=CARTESIAN_POINT ( 'NONE',  ( 18.27991844657871212, -2.543687620403382255, 13.76699789025506071 ) ) ;
#42322=CARTESIAN_POINT ( 'NONE',  ( 7.100000000000000533, 13.94845324556000143, 4.312847325879000770 ) ) ;
#42323=ORIENTED_EDGE ( 'NONE', *, *, #41136, .T. ) ;
#42328=DIRECTION ( 'NONE',  ( -1.000000000000000000, 6.086974017450460374E-15, -6.313390726318450536E-15 ) ) ;
#42332=CARTESIAN_POINT ( 'NONE',  ( 17.84068610406497868, 0.5560043133243454117, -12.68361349193355103 ) ) ;
#42336=ORIENTED_EDGE ( 'NONE', *, *, #40041, .F. ) ;
#42337=EDGE_CURVE ( 'NONE', #5820, #58325, #35084, .T. ) ;
#42350=CARTESIAN_POINT ( 'NONE',  ( 12.56405804856029995, -1.801709437036785433, 12.47051912880706226 ) ) ;
#42358=CARTESIAN_POINT ( 'NONE',  ( 12.10480575880360909, 2.667436721895840801, 12.31441907085212151 ) ) ;
#42365=CARTESIAN_POINT ( 'NONE',  ( 12.22117151670427226, 2.723004125123300589, 12.39680780184485975 ) ) ;
#42368=CARTESIAN_POINT ( 'NONE',  ( 12.60523857549420690, 0.5937411427826001509, 12.68132466675082348 ) ) ;
#42373=CARTESIAN_POINT ( 'NONE',  ( 12.25820678327527347, -2.802802780256933080, 13.60456178155848406 ) ) ;
#42374=CARTESIAN_POINT ( 'NONE',  ( 12.17999101424761577, 2.480063841773443301, 13.67763837793895298 ) ) ;
#42381=CARTESIAN_POINT ( 'NONE',  ( 18.14833460798322307, 2.303170370814867862, -12.49527837666172125 ) ) ;
#42383=CARTESIAN_POINT ( 'NONE',  ( 18.17924748727732620, 2.534358940238659486, 12.44349985642685041 ) ) ;
#42386=CARTESIAN_POINT ( 'NONE',  ( 12.61333915116789051, 3.228660600395449887, 13.62267210748412616 ) ) ;
#42404=CARTESIAN_POINT ( 'NONE',  ( 12.42592716733844860, 0.4969868315108272316, -13.88804154506775923 ) ) ;
#42406=LINE ( 'NONE', #15826, #47441 ) ;
#42414=CARTESIAN_POINT ( 'NONE',  ( 17.65867742935362728, -3.116692472806303904, -12.28625815163619883 ) ) ;
#42417=CARTESIAN_POINT ( 'NONE',  ( 18.17241432537605306, -2.400344151260349168, -12.47423995686379072 ) ) ;
#42418=CARTESIAN_POINT ( 'NONE',  ( 12.54664124763763944, 0.5694488842926255234, 13.88429844810378277 ) ) ;
#42446=CARTESIAN_POINT ( 'NONE',  ( 17.55505043854143565, 1.875000000000000000, -12.57545641911172751 ) ) ;
#42455=CARTESIAN_POINT ( 'NONE',  ( 17.55505043854143565, 3.199698446519375850, 12.18695736643652694 ) ) ;
#42457=EDGE_LOOP ( 'NONE', ( #370, #33110, #5894, #2666 ) ) ;
#42458=CARTESIAN_POINT ( 'NONE',  ( 12.37008254743958169, 0.4489258298041860495, -12.68932177688765606 ) ) ;
#42472=VERTEX_POINT ( 'NONE', #17348 ) ;
#42475=CARTESIAN_POINT ( 'NONE',  ( 17.83374359992749447, 3.059519611938945172, -13.53873550554769345 ) ) ;
#42476=ORIENTED_EDGE ( 'NONE', *, *, #38255, .F. ) ;
#42494=CARTESIAN_POINT ( 'NONE',  ( 17.94097423839755479, -1.871151600930998748, -12.46029012432409466 ) ) ;
#42501=FACE_OUTER_BOUND ( 'NONE', #32746, .T. ) ;
#42509=CARTESIAN_POINT ( 'NONE',  ( 12.20884949286983279, 2.312191565065523147, -13.71150332431687247 ) ) ;
#42512=CARTESIAN_POINT ( 'NONE',  ( 18.05145975767274535, -0.3802875570022093421, 13.89301034115782940 ) ) ;
#42517=CARTESIAN_POINT ( 'NONE',  ( 18.11689869015255994, -0.2739455837727965970, -13.89636968673228878 ) ) ;
#42526=CARTESIAN_POINT ( 'NONE',  ( 17.88507951091365911, -0.5311517451680607405, 12.68505220952105184 ) ) ;
#42538=CARTESIAN_POINT ( 'NONE',  ( 17.55505043854143565, 3.248147246781390329, 13.61798588129781074 ) ) ;
#42541=CARTESIAN_POINT ( 'NONE',  ( 12.64055030734118645, -0.7009231686363676106, -12.58048995873114073 ) ) ;
#42543=CARTESIAN_POINT ( 'NONE',  ( 18.22954180134188817, 2.744780546098122720, -12.29741030561552861 ) ) ;
#42556=CARTESIAN_POINT ( 'NONE',  ( 12.35703415364444346, 3.053811614356524373, -12.22452321716938251 ) ) ;
#42564=CARTESIAN_POINT ( 'NONE',  ( 12.72186720215634459, 3.119790641632218087, -12.28533200497074063 ) ) ;
#42573=CARTESIAN_POINT ( 'NONE',  ( 12.78420607872188342, -1.875260891907202243, -12.57537395219491749 ) ) ;
#42577=FACE_OUTER_BOUND ( 'NONE', #67839, .T. ) ;
#42578=CARTESIAN_POINT ( 'NONE',  ( 12.53635786351538606, -1.839692799137185641, -13.87860051966028152 ) ) ;
#42582=CARTESIAN_POINT ( 'NONE',  ( 18.26113864896150218, -2.644667523736221604, 12.31932909903656181 ) ) ;
#42591=DIRECTION ( 'NONE',  ( -0.000000000000000000, -0.000000000000000000, 1.000000000000000000 ) ) ;
#42592=CARTESIAN_POINT ( 'NONE',  ( 18.17483763482896109, 2.416937413673594381, -12.47057468851364348 ) ) ;
#42604=CARTESIAN_POINT ( 'NONE',  ( 12.72277096606028834, -0.6196453797482989190, 12.67964297675817598 ) ) ;
#42614=EDGE_CURVE ( 'NONE', #16254, #28416, #37598, .T. ) ;
#42615=CARTESIAN_POINT ( 'NONE',  ( 17.86935674558754528, 3.040604463256959100, 13.54376658945627909 ) ) ;
#42627=CARTESIAN_POINT ( 'NONE',  ( 18.16587897468629009, -2.632730956727242333, -13.64436436691515731 ) ) ;
#42637=CARTESIAN_POINT ( 'NONE',  ( 18.04064113778062861, -0.3934955819137399557, 13.89250369607185398 ) ) ;
#42646=CARTESIAN_POINT ( 'NONE',  ( 12.56977253056424004, 1.799738463188376825, -12.47080370841241503 ) ) ;
#42650=CARTESIAN_POINT ( 'NONE',  ( 17.99250848602325803, 2.946479007099335412, -13.56856542436401369 ) ) ;
#42655=PRESENTATION_STYLE_ASSIGNMENT (( #25199 ) ) ;
#42662=CARTESIAN_POINT ( 'NONE',  ( 17.83159136582989035, 0.5605836838512537890, -12.68334204399185694 ) ) ;
#42664=CARTESIAN_POINT ( 'NONE',  ( 12.34817707643961526, 2.926896462515248487, -12.34181790736438522 ) ) ;
#42672=CARTESIAN_POINT ( 'NONE',  ( 18.02641336659266003, 3.027085105403482412, 12.23097768044556055 ) ) ;
#42675=CARTESIAN_POINT ( 'NONE',  ( 12.55586324466750270, -0.5732756865038156624, -12.68257855878029439 ) ) ;
#42677=CARTESIAN_POINT ( 'NONE',  ( 12.80505043854144276, 0.6249999999999994449, -12.67928921589118652 ) ) ;
#42679=CARTESIAN_POINT ( 'NONE',  ( 12.44978597066681836, -1.852986171447666974, 12.46300423074626451 ) ) ;
#42682=CARTESIAN_POINT ( 'NONE',  ( 17.55505043854147118, -1.875000000000000000, -13.78627172894481667 ) ) ;
#42686=CARTESIAN_POINT ( 'NONE',  ( 12.15475987602171770, 0.3182341284860636388, 12.59598505207571861 ) ) ;
#42690=CARTESIAN_POINT ( 'NONE',  ( 12.08977223171467763, 2.598917558143519102, 12.32906181315049210 ) ) ;
#42700=CARTESIAN_POINT ( 'NONE',  ( 18.12515139794508912, -0.2563289266217783635, 12.69652241465665732 ) ) ;
#42707=CARTESIAN_POINT ( 'NONE',  ( 18.27990737420740786, 0.1887961029076866970, -12.59999260960568712 ) ) ;
#42709=CARTESIAN_POINT ( 'NONE',  ( 12.47325605351262290, -3.030051207268857461, 13.54664584463135135 ) ) ;
#42710=CARTESIAN_POINT ( 'NONE',  ( 12.18133850337987134, 2.541372565827187735, 13.66455005694026603 ) ) ;
#42718=EDGE_CURVE ( 'NONE', #66385, #61133, #33786, .T. ) ;
#42719=CARTESIAN_POINT ( 'NONE',  ( 17.75769270374269482, 3.091259753241552666, -12.29395838111494754 ) ) ;
#42721=CARTESIAN_POINT ( 'NONE',  ( 17.96110074834104253, 2.975239710473370103, 12.32804434199381483 ) ) ;
#42738=CARTESIAN_POINT ( 'NONE',  ( 4.699999740790709701, 13.17499974068000057, -1.948182422444000466E-09 ) ) ;
#42742=CARTESIAN_POINT ( 'NONE',  ( 12.72381130742976474, 0.6210784669310237538, -13.88131957737374300 ) ) ;
#42745=ORIENTED_EDGE ( 'NONE', *, *, #7961, .F. ) ;
#42753=CARTESIAN_POINT ( 'NONE',  ( 18.18011893007464153, -2.482032845566130241, -12.45575022786950647 ) ) ;
#42757=CARTESIAN_POINT ( 'NONE',  ( 12.27431752107754015, -0.3302328523437085273, 13.89472426752322853 ) ) ;
#42775=EDGE_CURVE ( 'NONE', #15559, #22723, #24173, .T. ) ;
#42781=ORIENTED_EDGE ( 'NONE', *, *, #64174, .T. ) ;
#42801=CARTESIAN_POINT ( 'NONE',  ( 12.42410782380136425, 0.4959072410923918706, -12.68697406334525546 ) ) ;
#42806=VERTEX_POINT ( 'NONE', #37545 ) ;
#42809=CARTESIAN_POINT ( 'NONE',  ( 18.16417820191648858, 0.1413121814401153697, 12.69896133444684949 ) ) ;
#42813=ORIENTED_EDGE ( 'NONE', *, *, #21703, .T. ) ;
#42815=CARTESIAN_POINT ( 'NONE',  ( 18.09702113181629457, 2.811936484508641865, -13.60234957393456945 ) ) ;
#42828=LINE ( 'NONE', #58557, #32870 ) ;
#42835=CARTESIAN_POINT ( 'NONE',  ( 17.55505043854147118, -1.760910691117821836, -12.47634535983622861 ) ) ;
#42848=CARTESIAN_POINT ( 'NONE',  ( 21.59999987243000064, -13.89999852641999922, 0.000000000000000000 ) ) ;
#42849=CARTESIAN_POINT ( 'NONE',  ( 12.35317296531419551, 2.068098628661974470, -13.75563068618459184 ) ) ;
#42852=CARTESIAN_POINT ( 'NONE',  ( 17.96752346481819984, -0.4700078255514594794, 13.88931146942756634 ) ) ;
#42856=CARTESIAN_POINT ( 'NONE',  ( 12.41269542049148455, 0.4865081001878581168, 13.88853895923280746 ) ) ;
#42858=CARTESIAN_POINT ( 'NONE',  ( 18.14887598841489691, -0.1995645668690017027, -13.89814765003239216 ) ) ;
#42869=CARTESIAN_POINT ( 'NONE',  ( 17.77532606275349991, -0.5849872192492382439, 12.68185863724641216 ) ) ;
#42888=CARTESIAN_POINT ( 'NONE',  ( 5.700000000000000178, 12.03770622561999915, 3.722046322334000124 ) ) ;
#42894=VECTOR ( 'NONE', #40340, 1000.000000000000000 ) ;
#42896=ORIENTED_EDGE ( 'NONE', *, *, #17203, .F. ) ;
#42903=CARTESIAN_POINT ( 'NONE',  ( 17.69771933245237605, 0.6088408278571637577, -13.88204686096231733 ) ) ;
#42909=CARTESIAN_POINT ( 'NONE',  ( 12.64121575286206323, 3.103492734220864691, -12.29027329182863149 ) ) ;
#42918=CARTESIAN_POINT ( 'NONE',  ( 12.66096866354273409, -1.891485216129972446, -12.57270334283925806 ) ) ;
#42923=CARTESIAN_POINT ( 'NONE',  ( 12.12491761308583449, -2.264077311857971342, -13.81573193591466442 ) ) ;
#42927=CARTESIAN_POINT ( 'NONE',  ( 18.26836321268588392, -2.610382005543646855, 12.32663954618810997 ) ) ;
#42956=CARTESIAN_POINT ( 'NONE',  ( 18.15591411656198773, 2.672312740310635260, 13.63535347231577077 ) ) ;
#42958=AXIS2_PLACEMENT_3D ( 'NONE', #46866, #58044, #62924 ) ;
#42961=CARTESIAN_POINT ( 'NONE',  ( 5.641095281751840496, -12.09393047400899412, 3.739612655151788978 ) ) ;
#42969=CARTESIAN_POINT ( 'NONE',  ( 18.14726809210094416, -2.096144380837183352, -13.84220294531915307 ) ) ;
#42987=CARTESIAN_POINT ( 'NONE',  ( 12.25647171456040319, 2.009180677272484949, -12.43879158508227611 ) ) ;
#42990=CARTESIAN_POINT ( 'NONE',  ( 18.16751419051670879, 2.624553509637494564, -13.64625295310859165 ) ) ;
#42995=CARTESIAN_POINT ( 'NONE',  ( 12.36135608140801345, -3.049327969019417051, -12.22544940668144697 ) ) ;
#43004=CARTESIAN_POINT ( 'NONE',  ( 17.71666921258853478, 0.6040886362899379192, -12.68065483099175417 ) ) ;
#43008=EDGE_CURVE ( 'NONE', #7987, #31711, #57545, .T. ) ;
#43010=ORIENTED_EDGE ( 'NONE', *, *, #11180, .T. ) ;
#43014=CARTESIAN_POINT ( 'NONE',  ( 18.19141764354314716, 2.135256814392525460, 12.41776106013548464 ) ) ;
#43018=CARTESIAN_POINT ( 'NONE',  ( 12.54858945020884065, -0.5700410258314839718, -12.68277524907877130 ) ) ;
#43022=CARTESIAN_POINT ( 'NONE',  ( 12.16862919417109268, -2.135222488495310600, 12.41776696322756735 ) ) ;
#43028=B_SPLINE_SURFACE_WITH_KNOTS ( 'NONE', 1, 3, ( 
 ( #66743, #56944, #30381, #41211, #14976, #34946, #9374, #61843, #18861, #61504, #36300, #56260, #59007, #59343, #58312, #5855, #47487, #64232, #68444, #26505, #58657, #10758, #36652, #21589, #32102, #27196, #48515, #37333, #64579, #53419, #52723, #37677, #5516, #15325, #26857, #57974, #275, #10072, #20564, #52377, #48170, #41891, #11108, #25811, #624, #42582, #21933, #42927, #43271, #63197, #31409, #4820, #26162, #68793, #16349, #32443, #20911, #4473, #42248, #16689, #53758, #38017, #63553, #31071, #47143, #15668, #36997, #10413, #31755, #53073, #5172, #69145, #47836, #21253, #63890, #16005, #49543, #54447, #27890, #22284, #59691, #43625, #55488, #23327, #39758, #44667, #22972, #7243, #64919, #33478, #54793, #49202, #17033, #34169, #972, #7588, #28938, #65274, #38366, #11792, #1655, #12490, #39407, #33825, #2004, #6548, #28228, #60038 ),
 ( #65961, #17388, #33132, #6195, #6892, #50241, #48863, #28581, #12842, #27538, #2345, #1309, #60727, #44322, #23665, #65619, #39065, #17745, #60385, #22624, #11444, #55140, #49895, #32785, #12150, #43969, #54100, #45002, #18085, #66309, #18433, #38718, #41126, #3702, #35205, #50929, #30636, #13196, #7938, #18777, #35545, #46025, #25041, #56514, #62098, #34524, #3028, #13874, #55834, #8621, #29969, #14560, #56863, #68023, #29274, #61755, #8960, #30300, #8282, #67333, #51606, #51272, #19107, #19801, #40107, #19453, #46720, #3366, #24703, #66996, #13538, #40774, #61420, #20139, #46373, #50588, #61077, #29625, #66658, #34857, #2688, #4045, #56172, #24014, #14216, #67673, #62439, #51946, #45348, #24358, #35878, #57193, #25382, #45690, #40429, #9294, #27368, #11971, #28062, #49372, #48341, #54626, #41469, #52297, #16866, #1144, #22454, #64750 ) ),
 .UNSPECIFIED., .F., .F., .F.,
 ( 2, 2 ),
 ( 4, 2, 2, 2, 2, 2, 2, 2, 2, 2, 2, 2, 2, 2, 2, 2, 2, 2, 2, 2, 2, 2, 2, 2, 2, 2, 2, 2, 2, 2, 2, 2, 2, 2, 2, 2, 2, 2, 2, 2, 2, 2, 2, 2, 2, 2, 2, 2, 2, 2, 2, 2, 2, 4 ),
 ( 0.000000000000000000, 1.000000000000000000 ),
 ( 0.000000000000000000, 7.157214214794704388E-05, 0.0001431442842958940878, 0.0001789303553698675894, 0.0002147164264438411181, 0.0002326094619808278825, 0.0002505024975178146468, 0.0002862885685917881755, 0.0003220746396657616500, 0.0003578607107397351788, 0.0003936467818137087075, 0.0004294328528876822362, 0.0004652189239616557649, 0.0004831119594986425293, 0.0005010049950356292936, 0.0005725771371835763511, 0.0006441492793315233001, 0.0007157214214794703575, 0.0007872935636274174150, 0.0008588657057753644724, 0.0008946517768493380011, 0.0009304378479233115298, 0.0009662239189972850585, 0.001002009990071258587, 0.001037796061145232224, 0.001073582132219205645, 0.001145154274367152702, 0.001180940345441126339, 0.001216726416515099760, 0.001252512487589073180, 0.001288298558663046600, 0.001359870700810993658, 0.001395656771884967295, 0.001431442842958940715, 0.001467228914032914135, 0.001503014985106887772, 0.001574587127254834830, 0.001646159269402781887, 0.001681945340476755524, 0.001717731411550728945, 0.001753517482624702365, 0.001789303553698676002, 0.001860875695846623060, 0.001896661766920596480, 0.001932447837994570117, 0.001968233909068543754, 0.002004019980142517175, 0.002039806051216491029, 0.002075592122290464449, 0.002147164264438411289, 0.002182950335512384710, 0.002218736406586358130, 0.002254522477660331550, 0.002290308548734305404 ),
 .UNSPECIFIED. ) ;
#43033=CARTESIAN_POINT ( 'NONE',  ( 12.22009801487423175, 2.720357631080353666, 12.39749406087476302 ) ) ;
#43044=CARTESIAN_POINT ( 'NONE',  ( 12.21982330445614195, 0.2196444115568565170, 12.69744877134261429 ) ) ;
#43048=CARTESIAN_POINT ( 'NONE',  ( 17.92259505138787290, 3.107618780086595311, -12.21081961728242504 ) ) ;
#43050=CARTESIAN_POINT ( 'NONE',  ( 12.54721708147389059, -1.835134883933975392, 13.87920628830545411 ) ) ;
#43052=CARTESIAN_POINT ( 'NONE',  ( 12.80505043854143388, 1.845932447629014872, 13.81930785430178155 ) ) ;
#43058=CARTESIAN_POINT ( 'NONE',  ( 17.88706890093970259, 3.029615921040858861, -12.31227368058699767 ) ) ;
#43063=CARTESIAN_POINT ( 'NONE',  ( 12.15646016996021217, 2.140061664406224917, 13.83614491990443085 ) ) ;
#43081=CARTESIAN_POINT ( 'NONE',  ( 12.18002302684027960, -0.03981422837198456133, -13.90000146831368255 ) ) ;
#43090=ORIENTED_EDGE ( 'NONE', *, *, #52164, .F. ) ;
#43094=ORIENTED_EDGE ( 'NONE', *, *, #45146, .F. ) ;
#43096=CARTESIAN_POINT ( 'NONE',  ( 17.93780763597379391, -2.994506166037827821, -12.32249531978309065 ) ) ;
#43101=CARTESIAN_POINT ( 'NONE',  ( 18.05693606625744252, -2.118559450820218792, -12.53247283883959007 ) ) ;
#43102=CARTESIAN_POINT ( 'NONE',  ( 12.30864111941012951, 0.3802875570022034579, 13.89301034115782940 ) ) ;
#43115=CARTESIAN_POINT ( 'NONE',  ( 17.92254446318295535, -3.154612309593181507, 13.64000973912208003 ) ) ;
#43132=CARTESIAN_POINT ( 'NONE',  ( 18.05168367658140838, 2.879595443362037432, -12.35500515152453538 ) ) ;
#43140=CARTESIAN_POINT ( 'NONE',  ( 12.23574065127464827, -0.2580991232524066925, -12.69647497719791573 ) ) ;
#43156=CARTESIAN_POINT ( 'NONE',  ( 18.12467946932835616, 2.757395321821673129, -13.61549383066601138 ) ) ;
#43171=PLANE ( 'NONE',  #41678 ) ;
#43178=CARTESIAN_POINT ( 'NONE',  ( 18.16417894366983177, 0.1413088920345111354, -13.89905105385967943 ) ) ;
#43194=CARTESIAN_POINT ( 'NONE',  ( 12.58320380180958509, 3.084393765090617467, -13.53199207997350584 ) ) ;
#43197=CARTESIAN_POINT ( 'NONE',  ( 4.600000127571202135, -13.89999852641999922, 0.000000000000000000 ) ) ;
#43198=CARTESIAN_POINT ( 'NONE',  ( 18.13658220607009142, -0.2292390942789229447, 13.89746050377130793 ) ) ;
#43212=CARTESIAN_POINT ( 'NONE',  ( 18.15872281507842345, -0.1622035078961262533, 12.69861136640059129 ) ) ;
#43218=CARTESIAN_POINT ( 'NONE',  ( 17.55505043854143565, 1.760910691117812954, 12.47634535983622861 ) ) ;
#43228=CARTESIAN_POINT ( 'NONE',  ( 12.57206729000417056, -0.6812425322175689191, -12.58157083403807164 ) ) ;
#43230=CARTESIAN_POINT ( 'NONE',  ( 18.00816351061646969, 3.042045466722131941, -12.22726353680069344 ) ) ;
#43231=CARTESIAN_POINT ( 'NONE',  ( 5.614176421965364483, 12.11993299477459551, 3.746642824816280637 ) ) ;
#43238=CONICAL_SURFACE ( 'NONE', #3018, 1.900023899775999947, 0.7853981633972997312 ) ;
#43240=ORIENTED_EDGE ( 'NONE', *, *, #27478, .T. ) ;
#43244=CARTESIAN_POINT ( 'NONE',  ( 12.80505043854143388, 3.199751711897557804, -12.18694338143115630 ) ) ;
#43246=CARTESIAN_POINT ( 'NONE',  ( 17.71666486338982338, -0.6040897852209337060, -13.88232707694115398 ) ) ;
#43250=AXIS2_PLACEMENT_3D ( 'NONE', #63348, #36448, #4624 ) ;
#43263=ORIENTED_EDGE ( 'NONE', *, *, #20204, .F. ) ;
#43264=CARTESIAN_POINT ( 'NONE',  ( 12.22973370829438622, -2.255582799352161327, -12.50515469879591812 ) ) ;
#43265=DIRECTION ( 'NONE',  ( 0.000000000000000000, 0.9905022095861402143, 0.1374968101629056305 ) ) ;
#43268=CARTESIAN_POINT ( 'NONE',  ( 12.25061842917687827, -2.988573241473616360, -13.67729937646034344 ) ) ;
#43270=CARTESIAN_POINT ( 'NONE',  ( 12.56879673637879691, -1.798456840550200830, 12.47100214317080358 ) ) ;
#43271=CARTESIAN_POINT ( 'NONE',  ( 18.27038927661327961, -2.598921547761774420, 12.32906097307313686 ) ) ;
#43300=B_SPLINE_SURFACE_WITH_KNOTS ( 'NONE', 1, 3, ( 
 ( #36571, #41475, #37260, #42171, #52646, #48096, #4053, #69071, #26084, #62783, #47412, #30994, #10682, #53343, #68717, #16273, #37599, #198, #20837, #42849, #63470, #14905, #15593, #36228, #36923, #11033, #57543, #58238, #4400, #9647, #52303, #47068, #21177, #58581, #42509, #21859, #1929, #59957, #59613, #1235, #60309, #33400, #38285, #48785, #12068, #54716, #44592, #55063, #54365, #65542, #892, #6120, #22205, #6815, #39330, #44245, #12416, #43542, #11710, #28151, #5778, #27121, #49463, #23249, #1576, #17665, #22894, #60650, #65885, #32371, #38989, #18013, #53686, #33748, #64842, #48437, #43194, #7165, #546, #64497, #16617, #28504, #49817, #33049, #43888, #11367 ),
 ( #37942, #59264, #32705, #54018, #27458, #22546, #6469, #38635, #16954, #27816, #49121, #65191, #17310, #2270, #45271, #51200, #45948, #34783, #12765, #34092, #44930, #18355, #66577, #56791, #55412, #61680, #45615, #28859, #40358, #40030, #35127, #41047, #51532, #13796, #34445, #35468, #62025, #67258, #23588, #50507, #55759, #24281, #8202, #50168, #56441, #7861, #67598, #8889, #46298, #61342, #8544, #29552, #13460, #19374, #24964, #3628, #7505, #23938, #18697, #29893, #13117, #2607, #66234, #30224, #39677, #19723, #3293, #50853, #56092, #19031, #60996, #24628, #29195, #40696, #2947, #66920, #14139, #31592, #26345, #15161, #62368, #14485, #25305, #67950, #25652, #37174 ) ),
 .UNSPECIFIED., .F., .F., .F.,
 ( 2, 2 ),
 ( 4, 2, 2, 2, 2, 2, 2, 2, 2, 2, 2, 2, 2, 2, 2, 2, 2, 2, 2, 2, 2, 2, 2, 2, 2, 2, 2, 2, 2, 2, 2, 2, 2, 2, 2, 2, 2, 2, 2, 2, 2, 2, 4 ),
 ( 0.000000000000000000, 1.000000000000000000 ),
 ( 0.000000000000000000, 7.142430198406409696E-05, 0.0001428486039681281939, 0.0002142729059521922773, 0.0002856972079362563879, 0.0003571215099203204442, 0.0004285458119043845547, 0.0004999701138884486652, 0.0005356822648804807204, 0.0005713944158725127757, 0.0006071065668645447225, 0.0006428187178565767778, 0.0007142430198406408883, 0.0007856673218247049988, 0.0008213794728167370541, 0.0008570916238087691093, 0.0008928037748008011646, 0.0009285159257928332199, 0.0009999402277768973304, 0.001071364529760961441, 0.001142788831745025551, 0.001214213133729089445, 0.001285637435713153556, 0.001321349586705185611, 0.001357061737697217666, 0.001428486039681281777, 0.001499910341665345887, 0.001535622492657377942, 0.001571334643649409998, 0.001607046794641442053, 0.001642758945633474108, 0.001714183247617538219, 0.001785607549601602329, 0.001821319700593634384, 0.001857031851585666440, 0.001928456153569730550, 0.001964168304561762605, 0.001999880455553794661, 0.002035592606545826716, 0.002071304757537858771, 0.002142729059521922882, 0.002214153361505986992, 0.002285577663490051103 ),
 .UNSPECIFIED. ) ;
#43304=CARTESIAN_POINT ( 'NONE',  ( 18.05358084703146559, 2.122495591609770305, 13.74627451715323012 ) ) ;
#43319=CARTESIAN_POINT ( 'NONE',  ( 18.24660850951287472, -2.298559566806798404, -13.81002375772540702 ) ) ;
#43341=CARTESIAN_POINT ( 'NONE',  ( 12.12470607006057399, 2.231004149372982415, -12.40091715157283936 ) ) ;
#43354=CARTESIAN_POINT ( 'NONE',  ( 12.27385967125950650, -2.970546648634963649, -12.24484150081280553 ) ) ;
#43360=DIRECTION ( 'NONE',  ( -1.000000000000000000, 0.000000000000000000, 0.000000000000000000 ) ) ;
#43361=CARTESIAN_POINT ( 'NONE',  ( 18.01141060613105793, 0.4275228316712895160, -12.69032453495386648 ) ) ;
#43363=CARTESIAN_POINT ( 'NONE',  ( 12.22895615647772516, 2.742396662204058977, -12.39180484752808020 ) ) ;
#43372=CARTESIAN_POINT ( 'NONE',  ( 18.18564075751665143, 2.124969003714952898, 12.41952547471440482 ) ) ;
#43378=CARTESIAN_POINT ( 'NONE',  ( 12.08118961495429744, -2.529460273524984704, 12.34351656561901223 ) ) ;
#43383=CARTESIAN_POINT ( 'NONE',  ( 12.09168743772587362, 0.1288995356414812388, 12.59934597632939735 ) ) ;
#43386=DIRECTION ( 'NONE',  ( 0.000000000000000000, -0.9553735099700839672, 0.2954005017724949389 ) ) ;
#43388=CARTESIAN_POINT ( 'NONE',  ( 12.19649458927090357, 2.642789655208612754, 12.41715525233005479 ) ) ;
#43395=CARTESIAN_POINT ( 'NONE',  ( 12.20626853909072906, 2.679149498294548071, 12.40801937966798008 ) ) ;
#43397=ORIENTED_EDGE ( 'NONE', *, *, #23182, .T. ) ;
#43399=CARTESIAN_POINT ( 'NONE',  ( 12.20071720273219462, 0.1607023182928339899, 12.69865132254282436 ) ) ;
#43401=CARTESIAN_POINT ( 'NONE',  ( 18.20247741961644650, -0.3746922849188884519, -12.59513687152069572 ) ) ;
#43403=VECTOR ( 'NONE', #29713, 1000.000000000000000 ) ;
#43406=CARTESIAN_POINT ( 'NONE',  ( 12.12630585043898535, -2.775512167237639716, 13.72213635400578013 ) ) ;
#43412=CARTESIAN_POINT ( 'NONE',  ( 17.55505043854147118, -1.787797342887044172, -13.88538010501570774 ) ) ;
#43431=CARTESIAN_POINT ( 'NONE',  ( 18.02738429465122039, -2.090191673117356874, 13.75189211025434233 ) ) ;
#43438=CARTESIAN_POINT ( 'NONE',  ( 12.80505043854146763, -3.248147246781390329, -13.61798588129781074 ) ) ;
#43439=CARTESIAN_POINT ( 'NONE',  ( 12.18006436421865679, 0.02054912266423991260, -13.89999925486820231 ) ) ;
#43449=CARTESIAN_POINT ( 'NONE',  ( 4.599999999999999645, 3.199698446519374073, 12.18695736643652694 ) ) ;
#43450=CARTESIAN_POINT ( 'NONE',  ( 18.15889616939342233, -2.662482328103963791, -12.41224410776443321 ) ) ;
#43459=CARTESIAN_POINT ( 'NONE',  ( 12.37737328439355444, 0.4562271229319652677, 13.88993195058941410 ) ) ;
#43468=ORIENTED_EDGE ( 'NONE', *, *, #7820, .F. ) ;
#43495=CARTESIAN_POINT ( 'NONE',  ( 12.70247988648370452, 0.6166112555940446160, -12.67984200623736513 ) ) ;
#43497=CARTESIAN_POINT ( 'NONE',  ( 21.54999911806000057, 1.172395514003999961E-13, -2.486899575159999765E-14 ) ) ;
#43510=ORIENTED_EDGE ( 'NONE', *, *, #41871, .T. ) ;
#43511=CARTESIAN_POINT ( 'NONE',  ( 17.59665311020856393, 3.123961325934789812, -13.52113166927136589 ) ) ;
#43528=CARTESIAN_POINT ( 'NONE',  ( 7.100000000000000533, 0.000000000000000000, 0.000000000000000000 ) ) ;
#43536=ADVANCED_FACE ( 'NONE', ( #54137 ), #43238, .T. ) ;
#43542=CARTESIAN_POINT ( 'NONE',  ( 12.29043182814382007, 2.854820394136931672, -13.59177665069740293 ) ) ;
#43545=CARTESIAN_POINT ( 'NONE',  ( 17.63737865760588974, -0.6198980793944591783, 13.88138779565240100 ) ) ;
#43550=CARTESIAN_POINT ( 'NONE',  ( 12.21931057678297528, 0.2190559830119534757, 13.89769592719668445 ) ) ;
#43554=CARTESIAN_POINT ( 'NONE',  ( 17.69618303672615056, -0.6091729397527337886, -13.88202727520719648 ) ) ;
#43563=CARTESIAN_POINT ( 'NONE',  ( 17.80382244274732528, -0.5734477787136644800, 12.68256797703445038 ) ) ;
#43578=CARTESIAN_POINT ( 'NONE',  ( 12.36386718854188160, -0.5708113556792973053, -12.58706429964239071 ) ) ;
#43580=CARTESIAN_POINT ( 'NONE',  ( 17.72109462663381052, 3.180738073285645839, -12.19192004217519099 ) ) ;
#43592=CARTESIAN_POINT ( 'NONE',  ( 18.14117786275458855, -2.282023444416175995, -13.71724589037892983 ) ) ;
#43599=CARTESIAN_POINT ( 'NONE',  ( 17.95947766544255231, -0.4766231184928892417, -13.88900205690511136 ) ) ;
#43609=CARTESIAN_POINT ( 'NONE',  ( 18.20740272079784816, -2.198619098391816795, 13.82629845589066520 ) ) ;
#43618=CARTESIAN_POINT ( 'NONE',  ( 12.39760546513567263, -2.025954772141364213, -12.54945441499613423 ) ) ;
#43622=CARTESIAN_POINT ( 'NONE',  ( 12.19349437040520634, -2.125667349631288339, -13.83768917864515302 ) ) ;
#43625=CARTESIAN_POINT ( 'NONE',  ( 18.03677854873450670, -1.942400312675104157, 12.44938339399087290 ) ) ;
#43633=CARTESIAN_POINT ( 'NONE',  ( 5.599969214251100169, -11.06886219213000011, -1.536526853569999851 ) ) ;
#43654=CARTESIAN_POINT ( 'NONE',  ( 18.10189407302235409, 2.802802817710309924, 13.60450747121971204 ) ) ;
#43665=CARTESIAN_POINT ( 'NONE',  ( 18.06232794982562595, -1.996188719851625715, -13.85695876210811228 ) ) ;
#43679=EDGE_CURVE ( 'NONE', #44093, #24800, #21973, .T. ) ;
#43686=CARTESIAN_POINT ( 'NONE',  ( 12.64184255386818201, 1.896331190223614405, -12.57194050387412076 ) ) ;
#43689=B_SPLINE_CURVE_WITH_KNOTS ( 'NONE', 3,
 ( #50926, #35542, #56861, #24355 ),
 .UNSPECIFIED., .F., .F.,
 ( 4, 4 ),
 ( 0.000000000000000000, 1.000000000000000000 ),
 .UNSPECIFIED. ) ;
#43703=CARTESIAN_POINT ( 'NONE',  ( 18.17902769456078360, 0.04114048977874683322, -12.69993211551499535 ) ) ;
#43705=CARTESIAN_POINT ( 'NONE',  ( 12.18526316313925406, 2.581188759499452701, -12.43231204083059005 ) ) ;
#43713=CARTESIAN_POINT ( 'NONE',  ( 18.10980516112008942, 2.943705546998117484, 12.25131356140272310 ) ) ;
#43721=CARTESIAN_POINT ( 'NONE',  ( 12.48129647765401451, -3.124180215534335225, 12.20653620603298073 ) ) ;
#43724=FACE_OUTER_BOUND ( 'NONE', #38051, .T. ) ;
#43726=CARTESIAN_POINT ( 'NONE',  ( 12.42151672539423934, -0.6105138165312035126, 12.58520200551375545 ) ) ;
#43729=CARTESIAN_POINT ( 'NONE',  ( 12.72061467711774974, 1.765703846569725011, 12.47566797393135651 ) ) ;
#43733=CARTESIAN_POINT ( 'NONE',  ( 18.23353331006402200, -0.2537702651956276201, 12.59744904646397679 ) ) ;
#43738=CARTESIAN_POINT ( 'NONE',  ( 17.92176999521577230, -0.5062894561356391376, 12.68641719396355860 ) ) ;
#43744=FACE_OUTER_BOUND ( 'NONE', #46409, .T. ) ;
#43749=CARTESIAN_POINT ( 'NONE',  ( 12.22896558337872897, -2.961354171198312457, 13.68321881638708604 ) ) ;
#43759=CARTESIAN_POINT ( 'NONE',  ( 18.08840168032788398, 2.173540213500963159, -12.52169971385178115 ) ) ;
#43770=ORIENTED_EDGE ( 'NONE', *, *, #58517, .T. ) ;
#43773=CARTESIAN_POINT ( 'NONE',  ( 17.98387256218937225, -2.954798081836346846, 13.56641578797404790 ) ) ;
#43801=CARTESIAN_POINT ( 'NONE',  ( 12.18829585510503577, 0.1017048024283954966, 13.89950429703524826 ) ) ;
#43836=EDGE_CURVE ( 'NONE', #65244, #1839, #15960, .T. ) ;
#43842=CARTESIAN_POINT ( 'NONE',  ( 12.30534114219160635, 2.122480415404790932, -13.74636906787548263 ) ) ;
#43847=LINE ( 'NONE', #52956, #25404 ) ;
#43854=CARTESIAN_POINT ( 'NONE',  ( 18.02642401515173631, 2.910531091912870405, -13.57777274349195906 ) ) ;
#43873=CARTESIAN_POINT ( 'NONE',  ( 17.84632148815561692, -1.821395309707484422, -12.46765979085770937 ) ) ;
#43878=EDGE_CURVE ( 'NONE', #38751, #31059, #6650, .T. ) ;
#43885=DIRECTION ( 'NONE',  ( -0.000000000000000000, -0.000000000000000000, 1.000000000000000000 ) ) ;
#43888=CARTESIAN_POINT ( 'NONE',  ( 12.78422499708364768, 3.124999410541264400, -13.52084427634423314 ) ) ;
#43892=CARTESIAN_POINT ( 'NONE',  ( 17.78863088638135537, -0.6916885356984026068, 13.98290438115173373 ) ) ;
#43898=CARTESIAN_POINT ( 'NONE',  ( 12.34379246237138261, -0.4226248004909251010, 13.89137006862893209 ) ) ;
#43899=CARTESIAN_POINT ( 'NONE',  ( 12.78475456307759828, -0.6250000000000008882, -13.88107975066922783 ) ) ;
#43901=LINE ( 'NONE', #54729, #29479 ) ;
#43912=CARTESIAN_POINT ( 'NONE',  ( 18.12436022580822836, -0.2580991232524050272, 12.69647497719789975 ) ) ;
#43914=CARTESIAN_POINT ( 'NONE',  ( 18.16560600438747386, -2.633677674594984808, -12.41941284408005153 ) ) ;
#43926=CARTESIAN_POINT ( 'NONE',  ( 12.11859257910637844, -0.2316996085786171000, -12.59787430930301433 ) ) ;
#43928=CARTESIAN_POINT ( 'NONE',  ( 17.94028104512295485, 3.089952709746675463, -12.21524586714253147 ) ) ;
#43938=CARTESIAN_POINT ( 'NONE',  ( 12.80505043854143388, 1.760910691117811844, 12.47634535983622861 ) ) ;
#43946=CARTESIAN_POINT ( 'NONE',  ( 18.17808105194527002, 0.05063168410658663854, -13.89988098555964946 ) ) ;
#43960=CARTESIAN_POINT ( 'NONE',  ( 12.36723811880913892, -2.053846804184053632, -12.54438404081591507 ) ) ;
#43967=CARTESIAN_POINT ( 'NONE',  ( 12.61298032308283190, -3.180483649554697312, 12.19204447432963612 ) ) ;
#43969=CARTESIAN_POINT ( 'NONE',  ( 17.93339585188542529, -2.997500062648085883, 12.32163866699053578 ) ) ;
#43981=ORIENTED_EDGE ( 'NONE', *, *, #9919, .T. ) ;
#43986=EDGE_CURVE ( 'NONE', #19784, #1839, #33433, .T. ) ;
#43998=CARTESIAN_POINT ( 'NONE',  ( 17.92067731499815864, 3.006998531728875435, 13.55270476886629716 ) ) ;
#44011=CARTESIAN_POINT ( 'NONE',  ( 17.69797138021026939, -3.108785234939712261, -13.52525919603468552 ) ) ;
#44013=ADVANCED_FACE ( 'NONE', ( #49500 ), #55790, .F. ) ;
#44029=DIRECTION ( 'NONE',  ( 0.000000000000000000, -0.9905022095861402143, -0.1374968101629056305 ) ) ;
#44035=CARTESIAN_POINT ( 'NONE',  ( 12.27369669298500021, 2.970039040581486045, -12.24495604130072124 ) ) ;
#44044=CARTESIAN_POINT ( 'NONE',  ( 12.65065493613389513, -3.183300664725537743, -12.19125106909030443 ) ) ;
#44051=CARTESIAN_POINT ( 'NONE',  ( 18.14024703743436717, -0.2197131112048710255, -12.69744725510432914 ) ) ;
#44052=CARTESIAN_POINT ( 'NONE',  ( 12.18517285595358501, 2.419552247719690019, -12.46997200859132704 ) ) ;
#44059=PRESENTATION_STYLE_ASSIGNMENT (( #12581 ) ) ;
#44064=CONICAL_SURFACE ( 'NONE', #25076, 13.94999927503000059, 0.7853981058017837080 ) ;
#44065=CARTESIAN_POINT ( 'NONE',  ( 18.05281416665457428, 3.003450933888335950, 12.23680105844127475 ) ) ;
#44071=CARTESIAN_POINT ( 'NONE',  ( 12.47064909367912477, -3.118799700203786607, 12.20791227269315371 ) ) ;
#44080=CARTESIAN_POINT ( 'NONE',  ( 12.50535913667519949, -0.6550687562476263937, 12.58296113213902068 ) ) ;
#44083=CARTESIAN_POINT ( 'NONE',  ( 12.58288255545463130, 3.084271795211692258, 12.29604036100131914 ) ) ;
#44093=VERTEX_POINT ( 'NONE', #31284 ) ;
#44101=CARTESIAN_POINT ( 'NONE',  ( 12.78089888617687109, -1.787816964400932296, 13.88537754411822078 ) ) ;
#44108=CARTESIAN_POINT ( 'NONE',  ( 18.18005044212792143, 2.500000099754956739, -13.67345740034994250 ) ) ;
#44123=CARTESIAN_POINT ( 'NONE',  ( 12.28979759249027204, -2.853877291415200634, 12.36206589978998593 ) ) ;
#44127=CARTESIAN_POINT ( 'NONE',  ( 17.75779383521795296, -3.091556742956585779, 13.53003950643004671 ) ) ;
#44136=CARTESIAN_POINT ( 'NONE',  ( 17.91761838490639036, 0.6233258800551639833, -12.58457734799054784 ) ) ;
#44140=ADVANCED_FACE ( 'NONE', ( #67632, #14516 ), #41421, .T. ) ;
#44152=CARTESIAN_POINT ( 'NONE',  ( 12.76358260308698611, 1.876037923228466298, 13.78611687077048842 ) ) ;
#44155=CARTESIAN_POINT ( 'NONE',  ( 12.44165070291072439, 0.6323113780857038124, 13.98571806661952976 ) ) ;
#44166=CARTESIAN_POINT ( 'NONE',  ( 17.55505043854144276, -0.6250000000000001110, 13.88107975066923316 ) ) ;
#44177=ORIENTED_EDGE ( 'NONE', *, *, #1880, .F. ) ;
#44187=VECTOR ( 'NONE', #27012, 1000.000000000000114 ) ;
#44202=VERTEX_POINT ( 'NONE', #64104 ) ;
#44204=CARTESIAN_POINT ( 'NONE',  ( 12.54683519492311738, 0.5695321295966281339, -13.88429381145914299 ) ) ;
#44213=CARTESIAN_POINT ( 'NONE',  ( 17.80571586434983544, 1.927376100771097223, -13.77836213227538131 ) ) ;
#44214=VERTEX_POINT ( 'NONE', #21804 ) ;
#44221=CARTESIAN_POINT ( 'NONE',  ( 18.01482197226484416, 0.4234835433089234047, -12.69049809664633166 ) ) ;
#44227=CARTESIAN_POINT ( 'NONE',  ( 18.16776742079022000, -2.623333169985007096, -13.64647547701515506 ) ) ;
#44228=CARTESIAN_POINT ( 'NONE',  ( 18.05387017988397957, -2.121311586850259001, 13.74657283405556285 ) ) ;
#44235=CARTESIAN_POINT ( 'NONE',  ( 17.92067275948981475, -3.101661042832208004, -12.21227817455808129 ) ) ;
#44240=CARTESIAN_POINT ( 'NONE',  ( 4.700001368028300597, -14.00000000000000000, 0.000000000000000000 ) ) ;
#44245=CARTESIAN_POINT ( 'NONE',  ( 12.27362767355643136, 2.829117748835542123, -13.59812893905842479 ) ) ;
#44249=CARTESIAN_POINT ( 'NONE',  ( 17.93540541742265404, 0.4960449563116372529, 13.88808666890938248 ) ) ;
#44250=AXIS2_PLACEMENT_3D ( 'NONE', #33111, #27515, #32763 ) ;
#44251=CARTESIAN_POINT ( 'NONE',  ( 17.78593649203479643, 0.5808626952944924149, 13.88365973251299401 ) ) ;
#44256=CARTESIAN_POINT ( 'NONE',  ( 12.23477845768578831, 0.2559490221015915390, 13.89683205629558316 ) ) ;
#44257=CARTESIAN_POINT ( 'NONE',  ( 12.33489288317253418, -0.4118289862746280505, -13.89178842664826519 ) ) ;
#44268=CARTESIAN_POINT ( 'NONE',  ( 18.10875687686965918, 0.2899325138666226653, 12.69554708236671914 ) ) ;
#44275=CARTESIAN_POINT ( 'NONE',  ( 12.64132288496830547, -1.896477787946246440, 13.78309086827115770 ) ) ;
#44280=ORIENTED_EDGE ( 'NONE', *, *, #59386, .F. ) ;
#44283=CARTESIAN_POINT ( 'NONE',  ( 12.25981900110941325, -0.4746736627229765637, -12.59106879393900691 ) ) ;
#44297=AXIS2_PLACEMENT_3D ( 'NONE', #65256, #16673, #951 ) ;
#44303=CARTESIAN_POINT ( 'NONE',  ( 17.98979471028674126, -0.4491394412341178088, -13.89023495843588840 ) ) ;
#44305=LINE ( 'NONE', #10737, #10734 ) ;
#44309=CARTESIAN_POINT ( 'NONE',  ( 18.18005043799237086, -2.500000011518549670, 12.45159158845318359 ) ) ;
#44318=PLANE ( 'NONE',  #46047 ) ;
#44320=DIRECTION ( 'NONE',  ( 0.000000000000000000, 0.9905022095861402143, 0.1374968101629056305 ) ) ;
#44322=CARTESIAN_POINT ( 'NONE',  ( 17.77721830936824077, -3.084271799839129358, 12.29605728393572228 ) ) ;
#44323=ORIENTED_EDGE ( 'NONE', *, *, #48657, .T. ) ;
#44334=ORIENTED_EDGE ( 'NONE', *, *, #39328, .T. ) ;
#44352=CARTESIAN_POINT ( 'NONE',  ( 18.20725128760094691, 2.198916822427670947, 13.82623906782133005 ) ) ;
#44365=CARTESIAN_POINT ( 'NONE',  ( 17.55505043854147118, -1.787797342887048391, -13.88538010501571129 ) ) ;
#44379=ORIENTED_EDGE ( 'NONE', *, *, #64235, .T. ) ;
#44388=CARTESIAN_POINT ( 'NONE',  ( 12.61707675448779398, 1.903914349653179627, -12.57067604690442764 ) ) ;
#44395=CARTESIAN_POINT ( 'NONE',  ( 18.00086112087972268, -0.5837697426893185826, 13.98798827748170481 ) ) ;
#44397=CARTESIAN_POINT ( 'NONE',  ( 12.54729787553185716, -3.152819052640251307, -12.19917003430776958 ) ) ;
#44403=CARTESIAN_POINT ( 'NONE',  ( 12.51718303290435763, -3.054853725429545808, -13.53993614671057166 ) ) ;
#44404=CARTESIAN_POINT ( 'NONE',  ( 18.16600380262988423, 0.1321628250398309556, -12.69908003149456377 ) ) ;
#44406=CARTESIAN_POINT ( 'NONE',  ( 12.18432844470346232, 2.573800461449739618, -12.43409912879210566 ) ) ;
#44411=CARTESIAN_POINT ( 'NONE',  ( 21.59999953993000332, -1.509903313490000218E-14, 4.329869796037999436E-14 ) ) ;
#44415=CARTESIAN_POINT ( 'NONE',  ( 17.83404768640021487, 1.940633243441993283, 12.56443520114847345 ) ) ;
#44416=LINE ( 'NONE', #33222, #19394 ) ;
#44423=CARTESIAN_POINT ( 'NONE',  ( 12.12470607006060597, -2.231004149372987744, 12.40091715157283936 ) ) ;
#44429=CARTESIAN_POINT ( 'NONE',  ( 12.08032332909581186, -0.02297882141078348359, 12.59998453421652798 ) ) ;
#44432=CARTESIAN_POINT ( 'NONE',  ( 12.46441593768242839, 3.024116347931779636, 12.31386760464157781 ) ) ;
#44445=DIRECTION ( 'NONE',  ( 0.000000000000000000, 0.000000000000000000, -1.000000000000000000 ) ) ;
#44448=CARTESIAN_POINT ( 'NONE',  ( 17.96066850196192632, -2.975608638376130877, 13.56100830561149095 ) ) ;
#44450=AXIS2_PLACEMENT_3D ( 'NONE', #14234, #20157, #45706 ) ;
#44451=CARTESIAN_POINT ( 'NONE',  ( 12.08961158949552228, -2.638129719752023927, 13.74921199938403937 ) ) ;
#44460=CARTESIAN_POINT ( 'NONE',  ( 18.18005043857343139, 2.459498578984884443, -13.68200151021915545 ) ) ;
#44461=AXIS2_PLACEMENT_3D ( 'NONE', #41431, #20792, #10298 ) ;
#44463=CARTESIAN_POINT ( 'NONE',  ( 18.18005043854143565, 2.500000000000000000, -25.00000000000000000 ) ) ;
#44466=CARTESIAN_POINT ( 'NONE',  ( 18.05401280175960110, 2.123066371663036023, -12.53147770072749267 ) ) ;
#44472=CARTESIAN_POINT ( 'NONE',  ( 17.64997652425314811, -0.7254930141145078393, -13.98119259374181311 ) ) ;
#44474=CARTESIAN_POINT ( 'NONE',  ( 12.49090498479077560, -3.040702594595472874, 12.30901830445581346 ) ) ;
#44479=CARTESIAN_POINT ( 'NONE',  ( 18.10320344748336652, -2.199570933858661537, 13.73260621368703482 ) ) ;
#44481=ORIENTED_EDGE ( 'NONE', *, *, #58887, .T. ) ;
#44487=DIRECTION ( 'NONE',  ( 0.000000000000000000, 0.000000000000000000, 1.000000000000000000 ) ) ;
#44500=CARTESIAN_POINT ( 'NONE',  ( 12.37528356179625710, 2.046093867836325852, 13.75926687192407094 ) ) ;
#44504=CARTESIAN_POINT ( 'NONE',  ( 12.44118158293134613, -0.5082612142235585218, 13.88749228919890122 ) ) ;
#44505=ORIENTED_EDGE ( 'NONE', *, *, #56275, .T. ) ;
#44507=DIRECTION ( 'NONE',  ( 1.000000000000000000, 0.000000000000000000, 0.000000000000000000 ) ) ;
#44512=LINE ( 'NONE', #18618, #14654 ) ;
#44514=PRODUCT_DEFINITION ( 'UNKNOWN', '', #54158, #15707 ) ;
#44528=ORIENTED_EDGE ( 'NONE', *, *, #47992, .T. ) ;
#44549=CARTESIAN_POINT ( 'NONE',  ( 12.63945631780503831, 1.891770379291387361, -13.78384844198478021 ) ) ;
#44555=CARTESIAN_POINT ( 'NONE',  ( 12.36315992512968265, -0.5793931417437993003, -13.98801390351337837 ) ) ;
#44560=CARTESIAN_POINT ( 'NONE',  ( 5.647168941335773518, 12.08810193142241474, -3.737902345522961856 ) ) ;
#44563=CARTESIAN_POINT ( 'NONE',  ( 18.16447345601862651, 2.360953327207878871, -13.70196990072541610 ) ) ;
#44575=CARTESIAN_POINT ( 'NONE',  ( 18.18005043832647161, -2.519786138815505616, -13.66921024352858538 ) ) ;
#44576=CARTESIAN_POINT ( 'NONE',  ( 18.14740543753015345, -2.299612738903852982, 13.71393688410694622 ) ) ;
#44581=CARTESIAN_POINT ( 'NONE',  ( 18.10358258445732815, -2.009225442943083806, -12.43878435193940568 ) ) ;
#44592=CARTESIAN_POINT ( 'NONE',  ( 12.19646863228097367, 2.642680340209512924, -13.64216715890480636 ) ) ;
#44595=CARTESIAN_POINT ( 'NONE',  ( 17.94354858665102981, 0.4896942981276218299, 13.88839019180477052 ) ) ;
#44602=CARTESIAN_POINT ( 'NONE',  ( 12.18006436421859107, -0.02054912257076008456, 13.89999925486856824 ) ) ;
#44603=CARTESIAN_POINT ( 'NONE',  ( 12.66331021905145349, -0.6090267839202087030, -13.88203573366523358 ) ) ;
#44611=CARTESIAN_POINT ( 'NONE',  ( 12.80505043854144276, -0.7302158263239078018, 13.98094363220830871 ) ) ;
#44613=CARTESIAN_POINT ( 'NONE',  ( 18.08617525414963367, 0.3300695133819673832, 12.69424233780834754 ) ) ;
#44630=CARTESIAN_POINT ( 'NONE',  ( 12.15475987602170882, -0.3182341284860687458, -12.59598505207571506 ) ) ;
#44631=CARTESIAN_POINT ( 'NONE',  ( 12.41685245973976137, -2.003519757431140302, -12.55365090558318997 ) ) ;
#44640=EDGE_LOOP ( 'NONE', ( #57609, #11082, #18679, #16550 ) ) ;
#44646=CARTESIAN_POINT ( 'NONE',  ( 18.17607592425854079, 0.07112389991332046524, -13.89976024287834910 ) ) ;
#44663=FACE_OUTER_BOUND ( 'NONE', #59403, .T. ) ;
#44667=CARTESIAN_POINT ( 'NONE',  ( 17.95182328287553375, -1.877974217481241714, 12.45926392518878068 ) ) ;
#44681=ORIENTED_EDGE ( 'NONE', *, *, #39063, .F. ) ;
#44697=CARTESIAN_POINT ( 'NONE',  ( 18.27869735329872114, 2.567871808702999914, 13.76250717860552264 ) ) ;
#44709=CARTESIAN_POINT ( 'NONE',  ( 17.93991242251033924, -3.137220474326288588, -13.64397427468588120 ) ) ;
#44731=CARTESIAN_POINT ( 'NONE',  ( 12.59734647783783856, 1.910499211092021365, -12.56957462197894060 ) ) ;
#44740=CARTESIAN_POINT ( 'NONE',  ( 12.51357205051175114, -1.821485253447858055, -12.46764665430163710 ) ) ;
#44746=CARTESIAN_POINT ( 'NONE',  ( 12.21968270649331245, -2.719953125373908875, -13.62430835208222923 ) ) ;
#44747=CARTESIAN_POINT ( 'NONE',  ( 18.08024441302280039, 0.3389720875425278890, -12.69391532355469110 ) ) ;
#44748=CARTESIAN_POINT ( 'NONE',  ( 12.30233513030038317, 2.119611855453280569, -12.53231127769398690 ) ) ;
#44751=ORIENTED_EDGE ( 'NONE', *, *, #8369, .F. ) ;
#44753=DIRECTION ( 'NONE',  ( -1.000000000000000000, 0.000000000000000000, 0.000000000000000000 ) ) ;
#44756=CARTESIAN_POINT ( 'NONE',  ( 18.01423850902969903, 2.075512308681780382, 12.54039470262457634 ) ) ;
#44762=CARTESIAN_POINT ( 'NONE',  ( 12.75651925146921606, -0.7192569394295693641, -12.57945425907935544 ) ) ;
#44765=CARTESIAN_POINT ( 'NONE',  ( 12.19628620791409723, -2.642962752853494912, 12.41715721841834785 ) ) ;
#44771=CARTESIAN_POINT ( 'NONE',  ( 12.17677020551147393, -0.3597103837128051707, 12.59488153751295769 ) ) ;
#44774=CARTESIAN_POINT ( 'NONE',  ( 12.22973370829435069, 2.255582799352162660, 12.50515469879591102 ) ) ;
#44788=CARTESIAN_POINT ( 'NONE',  ( 17.86939907854621978, -3.040585884638498992, 13.54383026114072130 ) ) ;
#44791=LINE ( 'NONE', #40229, #65441 ) ;
#44803=CARTESIAN_POINT ( 'NONE',  ( 17.87083331331561098, 1.960545027353535863, -12.56104967893682200 ) ) ;
#44810=CARTESIAN_POINT ( 'NONE',  ( 17.60357723836707322, -0.7301778992647969257, -13.98094561311457618 ) ) ;
#44812=CARTESIAN_POINT ( 'NONE',  ( 12.39197104280896511, -2.969147788937597010, 12.32981191671119348 ) ) ;
#44816=CARTESIAN_POINT ( 'NONE',  ( 18.06505946208164559, -2.138585121884149398, 13.74350169411782829 ) ) ;
#44825=CARTESIAN_POINT ( 'NONE',  ( 12.75598089126020618, -1.787835849362730434, -13.88537514715539878 ) ) ;
#44829=LINE ( 'NONE', #28751, #41845 ) ;
#44838=CARTESIAN_POINT ( 'NONE',  ( 12.70233692021770011, 1.883156082608297366, 13.78505115204620068 ) ) ;
#44842=CARTESIAN_POINT ( 'NONE',  ( 12.22921562908471316, 0.4443071882833232178, 13.99296005428181822 ) ) ;
#44858=CARTESIAN_POINT ( 'NONE',  ( 12.35913603387738036, 0.5748214922496756030, 12.58705572532742600 ) ) ;
#44865=ORIENTED_EDGE ( 'NONE', *, *, #55982, .T. ) ;
#44882=LINE ( 'NONE', #33699, #49877 ) ;
#44884=CARTESIAN_POINT ( 'NONE',  ( 17.55505043854147118, -1.875000000000000000, -25.00000000000000000 ) ) ;
#44888=CARTESIAN_POINT ( 'NONE',  ( 12.09857429938280582, -0.1657344298535316507, -13.99903850390423798 ) ) ;
#44897=CARTESIAN_POINT ( 'NONE',  ( 18.17537916830624312, 2.421093501972792605, -13.68989611939600159 ) ) ;
#44904=CARTESIAN_POINT ( 'NONE',  ( 17.81145623651324428, 0.5702806495112531238, -12.68276204030717125 ) ) ;
#44909=CARTESIAN_POINT ( 'NONE',  ( 18.13614788755254636, -2.730255577220590979, -13.62187136675007082 ) ) ;
#44912=AXIS2_PLACEMENT_3D ( 'NONE', #23167, #28780, #66502 ) ;
#44917=CARTESIAN_POINT ( 'NONE',  ( 18.06277981064212668, -1.966570380498759540, -12.44558849270348944 ) ) ;
#44925=ORIENTED_EDGE ( 'NONE', *, *, #68001, .F. ) ;
#44930=CARTESIAN_POINT ( 'NONE',  ( 12.27274079034939902, 2.022162746929204058, -13.85319239000171265 ) ) ;
#44934=CARTESIAN_POINT ( 'NONE',  ( 17.81092223849609368, -0.6836428945794228440, 13.98330131869062321 ) ) ;
#44939=CARTESIAN_POINT ( 'NONE',  ( 12.47664075725316479, -0.5322329922416514369, 13.88628950328731548 ) ) ;
#44940=CARTESIAN_POINT ( 'NONE',  ( 12.23612747310287041, -2.758947143698455395, 13.61512400665175981 ) ) ;
#44949=ADVANCED_FACE ( 'NONE', ( #40077 ), #28552, .F. ) ;
#44950=CARTESIAN_POINT ( 'NONE',  ( 12.80505043854146940, -3.125000000000000000, -12.28373071562070074 ) ) ;
#44953=CARTESIAN_POINT ( 'NONE',  ( 12.41269347227960118, -0.4865065285064677503, 12.68745508179905457 ) ) ;
#44954=CARTESIAN_POINT ( 'NONE',  ( 18.08677744228779005, -2.828625537410247581, -12.36890451986435124 ) ) ;
#44959=CARTESIAN_POINT ( 'NONE',  ( 12.36772010770948249, -2.053374490018978538, 13.75810180220398671 ) ) ;
#44965=ORIENTED_EDGE ( 'NONE', *, *, #53541, .F. ) ;
#44966=CARTESIAN_POINT ( 'NONE',  ( 12.17677020551147038, 0.3597103837127930692, -12.59488153751296657 ) ) ;
#44981=CARTESIAN_POINT ( 'NONE',  ( 17.93874521385978937, 0.6200266137005103761, -13.98626978124057629 ) ) ;
#44992=CARTESIAN_POINT ( 'NONE',  ( 12.39223264510079758, -2.969378069107369456, -13.56257646889492285 ) ) ;
#45000=CARTESIAN_POINT ( 'NONE',  ( 12.78089695109148494, -1.787798027819077040, -13.88537998392834893 ) ) ;
#45001=CARTESIAN_POINT ( 'NONE',  ( 12.64263601961789085, -0.6038715862870278617, -13.88233985103438251 ) ) ;
#45002=CARTESIAN_POINT ( 'NONE',  ( 17.94557471909619295, -2.987998163485180214, 12.32438680867657332 ) ) ;
#45027=CARTESIAN_POINT ( 'NONE',  ( 18.02418542278644153, -0.5485298171726814553, 12.58805670501782181 ) ) ;
#45034=CARTESIAN_POINT ( 'NONE',  ( 17.87892170566133032, 1.864264957476230222, 13.87532524069350082 ) ) ;
#45045=CARTESIAN_POINT ( 'NONE',  ( 17.55505043854147118, -3.248147246781389885, -13.61798588129780896 ) ) ;
#45051=CARTESIAN_POINT ( 'NONE',  ( 17.55505043854143565, 3.248147246781390329, 13.61798588129781074 ) ) ;
#45058=CARTESIAN_POINT ( 'NONE',  ( 21.49999863197000138, 0.000000000000000000, 0.000000000000000000 ) ) ;
#45060=ORIENTED_EDGE ( 'NONE', *, *, #24000, .F. ) ;
#45070=CARTESIAN_POINT ( 'NONE',  ( 12.51690604397273887, 1.945290150052898515, -12.56367745121460011 ) ) ;
#45078=CARTESIAN_POINT ( 'NONE',  ( 18.27990784067583618, 0.1916560647487305369, 13.99999316327169119 ) ) ;
#45080=CARTESIAN_POINT ( 'NONE',  ( 12.29711362085067528, -1.966768764679983184, -12.44555721978030860 ) ) ;
#45086=CARTESIAN_POINT ( 'NONE',  ( 12.18011073905427111, -2.522020058064991410, -13.66873259811635677 ) ) ;
#45087=CARTESIAN_POINT ( 'NONE',  ( 18.10141690196193309, 0.3036663359794742334, -12.69511825016613749 ) ) ;
#45097=CARTESIAN_POINT ( 'NONE',  ( 17.59659105803583756, 1.876041592512284195, 12.57524627323323330 ) ) ;
#45101=CARTESIAN_POINT ( 'NONE',  ( 12.15889392793075530, -0.3761765223121792956, -12.59508068834428052 ) ) ;
#45103=CARTESIAN_POINT ( 'NONE',  ( 12.59734647783787409, -1.910499211092022476, 12.56957462197894415 ) ) ;
#45109=CARTESIAN_POINT ( 'NONE',  ( 12.41256632787946756, 0.4864235087029698534, 12.68745975172790530 ) ) ;
#45110=VECTOR ( 'NONE', #18958, 1000.000000000000000 ) ;
#45113=CARTESIAN_POINT ( 'NONE',  ( 12.32534826942432282, 2.099231811413890814, 12.53595023114330331 ) ) ;
#45120=CARTESIAN_POINT ( 'NONE',  ( 17.94293909943462850, -0.4900986450237151959, 12.68726951834787897 ) ) ;
#45125=CARTESIAN_POINT ( 'NONE',  ( 18.04536347370801508, -0.3876168848819628310, -12.69203885981792368 ) ) ;
#45127=CARTESIAN_POINT ( 'NONE',  ( 17.88876225152345611, -3.028809290952733324, 13.54697662062045005 ) ) ;
#45146=EDGE_CURVE ( 'NONE', #11513, #57880, #27282, .T. ) ;
#45153=CARTESIAN_POINT ( 'NONE',  ( 12.31573549172491866, -2.888971355233717286, 12.35241121500909856 ) ) ;
#45157=CARTESIAN_POINT ( 'NONE',  ( 17.96192083627962788, -2.025460433975771579, 13.76272661095429228 ) ) ;
#45164=CARTESIAN_POINT ( 'NONE',  ( 12.80505043854143388, 3.149917237299187267, -12.25147871603038219 ) ) ;
#45169=CARTESIAN_POINT ( 'NONE',  ( 17.64985999057966026, 0.7135009822675021374, -12.57978225961209162 ) ) ;
#45178=DIRECTION ( 'NONE',  ( -0.000000000000000000, 0.7270098363383213913, 0.6866270442294909460 ) ) ;
#45180=CARTESIAN_POINT ( 'NONE',  ( 12.61529649622812954, 3.223097538158945952, 13.62393827815043501 ) ) ;
#45183=CARTESIAN_POINT ( 'NONE',  ( 12.66329582868160131, 0.6090237436409963179, -12.68033599931248290 ) ) ;
#45184=CARTESIAN_POINT ( 'NONE',  ( 12.42469545966024214, -0.4960449563116401950, 13.88808666890938248 ) ) ;
#45189=CARTESIAN_POINT ( 'NONE',  ( 12.80505043854143388, 1.875000000000000000, -25.00000000000000000 ) ) ;
#45198=CARTESIAN_POINT ( 'NONE',  ( 12.70928935905665291, 3.193791526923301927, 12.18850694772984333 ) ) ;
#45215=DIRECTION ( 'NONE',  ( -1.000000000000000000, 0.000000000000000000, 0.000000000000000000 ) ) ;
#45216=CARTESIAN_POINT ( 'NONE',  ( 12.36816014207664161, 2.947033975320460630, 13.56836638442238296 ) ) ;
#45221=CARTESIAN_POINT ( 'NONE',  ( 18.17388115328630960, 2.104502522679955856, -12.42302150255121340 ) ) ;
#45229=CARTESIAN_POINT ( 'NONE',  ( 17.65355681324606252, 3.248032782086212489, -13.61801318301548491 ) ) ;
#45231=CARTESIAN_POINT ( 'NONE',  ( 12.80505043854144098, -0.7302158263239267866, -13.98094363220830871 ) ) ;
#45240=CARTESIAN_POINT ( 'NONE',  ( 18.17895306041983972, 2.542296241241985832, -13.66441818551904674 ) ) ;
#45241=EDGE_LOOP ( 'NONE', ( #15578, #6363, #38950, #57960 ) ) ;
#45242=CARTESIAN_POINT ( 'NONE',  ( 18.18005043854144276, 0.000000000000000000, -25.00000000000000000 ) ) ;
#45250=ORIENTED_EDGE ( 'NONE', *, *, #26406, .F. ) ;
#45252=CARTESIAN_POINT ( 'NONE',  ( 17.88831561177691398, -3.029094439784365544, -13.54684341222245436 ) ) ;
#45260=CARTESIAN_POINT ( 'NONE',  ( 18.28023629128827565, -2.459623831379296632, -12.35762167929922839 ) ) ;
#45267=VERTEX_POINT ( 'NONE', #12727 ) ;
#45268=CARTESIAN_POINT ( 'NONE',  ( 17.55505043854147118, -1.787816316115923954, 13.88537766212463254 ) ) ;
#45271=CARTESIAN_POINT ( 'NONE',  ( 12.36046591005674777, 1.940744226335691103, -13.86483863263027416 ) ) ;
#45275=CARTESIAN_POINT ( 'NONE',  ( 18.20015658150181892, -0.3334496638227529841, 13.99603244703262739 ) ) ;
#45276=CARTESIAN_POINT ( 'NONE',  ( 18.18005043799237086, -2.500000011518549670, 12.45159158845318359 ) ) ;
#45283=CARTESIAN_POINT ( 'NONE',  ( 12.19334556251213186, -2.628630844604569194, 13.64533835530551009 ) ) ;
#45289=CARTESIAN_POINT ( 'NONE',  ( 12.80505043854143388, 3.199698446519374517, 12.18695736643652694 ) ) ;
#45293=CARTESIAN_POINT ( 'NONE',  ( 17.62710295837867847, 0.6209187240130098484, 12.67955909024709094 ) ) ;
#45294=CARTESIAN_POINT ( 'NONE',  ( 12.30788008590002391, -0.3788802694180442021, 12.69239629738001973 ) ) ;
#45308=CARTESIAN_POINT ( 'NONE',  ( 12.57519818727761951, -0.5812897767837165164, -12.68208758371478595 ) ) ;
#45326=CARTESIAN_POINT ( 'NONE',  ( 18.14493363608989540, 0.4251989115648961426, -13.99355557726514299 ) ) ;
#45339=CARTESIAN_POINT ( 'NONE',  ( 12.15832103307001155, -2.898357473903109494, 13.69738840704686389 ) ) ;
#45342=EDGE_CURVE ( 'NONE', #53037, #5820, #22856, .T. ) ;
#45347=CARTESIAN_POINT ( 'NONE',  ( 12.23550883753394025, 0.2581888431706758635, -13.89679013629344517 ) ) ;
#45348=CARTESIAN_POINT ( 'NONE',  ( 17.86190681601109631, -1.955416883085901558, 12.56193573862144852 ) ) ;
#45369=ADVANCED_FACE ( 'NONE', ( #27303, #11215 ), #383, .F. ) ;
#45378=CARTESIAN_POINT ( 'NONE',  ( 18.08737871041808987, 2.022152854634007291, 13.85319383421289530 ) ) ;
#45407=VERTEX_POINT ( 'NONE', #10526 ) ;
#45412=FACE_OUTER_BOUND ( 'NONE', #45241, .T. ) ;
#45414=CARTESIAN_POINT ( 'NONE',  ( 12.36494524851998023, 2.943800415886788091, -12.33703218264929902 ) ) ;
#45422=CARTESIAN_POINT ( 'NONE',  ( 12.08418858410078300, -2.401692437127227464, -12.36899414651120921 ) ) ;
#45429=CARTESIAN_POINT ( 'NONE',  ( 12.39133745138803810, -2.968584063660574479, -13.56278128057737398 ) ) ;
#45433=ORIENTED_EDGE ( 'NONE', *, *, #36636, .T. ) ;
#45436=CARTESIAN_POINT ( 'NONE',  ( 4.599999999999999645, 0.7302158263239085789, 13.98094363220830871 ) ) ;
#45440=CARTESIAN_POINT ( 'NONE',  ( 17.69826591161632834, 1.891282299241872522, 12.57273691359006129 ) ) ;
#45446=CARTESIAN_POINT ( 'NONE',  ( 12.21868246241199962, -2.283434118842408100, 12.49941978418538646 ) ) ;
#45452=CARTESIAN_POINT ( 'NONE',  ( 12.18004360525213414, -0.009762034906140630575, 12.70000045436730751 ) ) ;
#45457=CARTESIAN_POINT ( 'NONE',  ( 12.52557666887732957, 1.940868768839140390, 12.56439497327412624 ) ) ;
#45468=CARTESIAN_POINT ( 'NONE',  ( 17.95596512699729885, -0.4795041973233179489, -12.68781427220655011 ) ) ;
#45472=CARTESIAN_POINT ( 'NONE',  ( 17.69888641710121746, -1.891428316105117746, -13.78380564104365291 ) ) ;
#45483=CARTESIAN_POINT ( 'NONE',  ( 17.82923902994810916, -0.5617296174771665429, 13.88472048964353611 ) ) ;
#45494=AXIS2_PLACEMENT_3D ( 'NONE', #37433, #10861, #26955 ) ;
#45497=CARTESIAN_POINT ( 'NONE',  ( 12.18822406275262438, -2.601257609840999407, 12.42743042555770572 ) ) ;
#45501=CARTESIAN_POINT ( 'NONE',  ( 17.80571586434987097, -1.927376100771097223, 13.77836213227538487 ) ) ;
#45514=CARTESIAN_POINT ( 'NONE',  ( 17.77668021070434889, 0.6849607937330790541, -12.58136878870645248 ) ) ;
#45525=CARTESIAN_POINT ( 'NONE',  ( 12.18114782263372753, 2.542296328577541953, 13.66436634302260167 ) ) ;
#45528=CARTESIAN_POINT ( 'NONE',  ( 12.20071720274720661, -0.1607023183492722884, -12.69865132254261120 ) ) ;
#45530=CARTESIAN_POINT ( 'NONE',  ( 12.37030616679613892, -0.4491394412341195297, 13.89023495843590261 ) ) ;
#45537=VECTOR ( 'NONE', #32036, 1000.000000000000000 ) ;
#45544=CARTESIAN_POINT ( 'NONE',  ( 12.30701392268162309, 3.003682976637727986, 12.23675526868967367 ) ) ;
#45562=DIRECTION ( 'NONE',  ( -0.000000000000000000, -0.000000000000000000, 1.000000000000000000 ) ) ;
#45568=CARTESIAN_POINT ( 'NONE',  ( 18.18591139755467623, 2.124730565513604841, -12.41957995629783973 ) ) ;
#45571=CARTESIAN_POINT ( 'NONE',  ( 12.27416439412415450, 2.829982835813917408, -13.59791655271627064 ) ) ;
#45576=CARTESIAN_POINT ( 'NONE',  ( 12.15994429558105239, -0.3334496638227552046, -13.99603244703262739 ) ) ;
#45578=CARTESIAN_POINT ( 'NONE',  ( 18.17481653531215358, -2.416771143973758029, -13.69072451366435672 ) ) ;
#45584=CARTESIAN_POINT ( 'NONE',  ( 18.08228063350337678, 2.164202898012135723, -13.73897034938254968 ) ) ;
#45585=ORIENTED_EDGE ( 'NONE', *, *, #156, .T. ) ;
#45592=CARTESIAN_POINT ( 'NONE',  ( 17.94293909947463561, 0.4900986449918856569, -12.68726951834973349 ) ) ;
#45600=ORIENTED_EDGE ( 'NONE', *, *, #28113, .F. ) ;
#45604=CARTESIAN_POINT ( 'NONE',  ( 18.05281416665461336, -3.003450933888336838, -12.23680105844127652 ) ) ;
#45610=ORIENTED_EDGE ( 'NONE', *, *, #15055, .T. ) ;
#45615=CARTESIAN_POINT ( 'NONE',  ( 12.17479962224109435, 2.156383435693109529, -13.83294862407085901 ) ) ;
#45618=CARTESIAN_POINT ( 'NONE',  ( 18.24178265820143352, 0.2353130933619127785, 13.99804086085458721 ) ) ;
#45627=CARTESIAN_POINT ( 'NONE',  ( 12.18501279890337052, -2.418803504714349017, 13.69036126159378775 ) ) ;
#45633=DIRECTION ( 'NONE',  ( -0.7071058580588949205, -0.7071077043129949669, 4.007446525297969874E-09 ) ) ;
#45639=CARTESIAN_POINT ( 'NONE',  ( 17.80401300531091024, 0.5733651658914310500, 12.68257300503909590 ) ) ;
#45640=CARTESIAN_POINT ( 'NONE',  ( 12.40964703146719650, -0.4840289222540395397, 12.68758247551644125 ) ) ;
#45641=CARTESIAN_POINT ( 'NONE',  ( 5.500000000000000000, -12.65263727151999795, 3.063503113339999917 ) ) ;
#45651=CARTESIAN_POINT ( 'NONE',  ( 12.42151672539423579, 0.6105138165312113951, -12.58520200551375545 ) ) ;
#45652=CARTESIAN_POINT ( 'NONE',  ( 12.80505043854146940, -1.875000000000000444, -12.57541666120756396 ) ) ;
#45668=CARTESIAN_POINT ( 'NONE',  ( 17.96742444759811974, -0.6007076874295256275, -13.98710814480368114 ) ) ;
#45675=CARTESIAN_POINT ( 'NONE',  ( 17.83355475040677973, -3.059894173690222541, 12.30333952404826370 ) ) ;
#45678=CARTESIAN_POINT ( 'NONE',  ( 12.18524893065073655, -2.418966797217242171, -13.69026124204716588 ) ) ;
#45689=CARTESIAN_POINT ( 'NONE',  ( 12.18832812670980914, 0.1018973686818595847, -13.89950237059084870 ) ) ;
#45690=CARTESIAN_POINT ( 'NONE',  ( 17.78721996965305507, -1.919630126996079600, 12.56804012644223079 ) ) ;
#45706=DIRECTION ( 'NONE',  ( 0.000000000000000000, 0.9549051095264925459, -0.2969111513570973915 ) ) ;
#45713=CARTESIAN_POINT ( 'NONE',  ( 17.64985999057966026, -0.7135009822674878155, 12.57978225961208807 ) ) ;
#45719=CARTESIAN_POINT ( 'NONE',  ( 18.18935690068781241, 2.871730747427965191, 13.70230915895854018 ) ) ;
#45731=CARTESIAN_POINT ( 'NONE',  ( 18.21591247723855034, -2.819087736749462003, -13.71325046847544193 ) ) ;
#45752=CARTESIAN_POINT ( 'NONE',  ( 12.31295406811161719, 2.114551508724274775, -12.53308940647968761 ) ) ;
#45759=CARTESIAN_POINT ( 'NONE',  ( 17.60357723839708299, 0.7301778992647629529, 13.98094561311457618 ) ) ;
#45762=CARTESIAN_POINT ( 'NONE',  ( 12.10312773382969453, -2.298350437047144812, -12.38862788998081754 ) ) ;
#45768=CARTESIAN_POINT ( 'NONE',  ( 12.19623795424366897, -2.642762699020543060, -13.64211084970869692 ) ) ;
#45769=CARTESIAN_POINT ( 'NONE',  ( 17.55505043854144631, -0.6250000000000001110, -12.67928921589118652 ) ) ;
#45770=DIRECTION ( 'NONE',  ( 1.000000000000000000, 0.000000000000000000, 0.000000000000000000 ) ) ;
#45774=VERTEX_POINT ( 'NONE', #29321 ) ;
#45776=CARTESIAN_POINT ( 'NONE',  ( 17.86920599199770265, 3.040695425030093713, 13.54374392800313132 ) ) ;
#45779=CARTESIAN_POINT ( 'NONE',  ( 17.94652436847575672, 2.012680451140230531, 12.55183781965936696 ) ) ;
#45785=CARTESIAN_POINT ( 'NONE',  ( 12.61707675448782773, -1.903914349653180516, 12.57067604690442586 ) ) ;
#45791=CARTESIAN_POINT ( 'NONE',  ( 12.18201988759300036, -0.05063260980701941860, 12.69986973508908079 ) ) ;
#45794=CARTESIAN_POINT ( 'NONE',  ( 12.60184172746868114, 1.908867898185655054, 12.56980895172865687 ) ) ;
#45807=CARTESIAN_POINT ( 'NONE',  ( 17.75512362481055106, -0.5924617913105076905, -12.68139389763045521 ) ) ;
#45812=CARTESIAN_POINT ( 'NONE',  ( 12.61614725291588890, -3.223296771745977285, 13.62389115065821699 ) ) ;
#45830=CARTESIAN_POINT ( 'NONE',  ( 17.57569743819256658, 0.6249994633519876386, -13.88107975068472300 ) ) ;
#45832=CARTESIAN_POINT ( 'NONE',  ( 12.25748074642598695, -2.187380181826345193, 12.51928400914606954 ) ) ;
#45835=CARTESIAN_POINT ( 'NONE',  ( 18.10946311474936721, -2.988545908040631804, 13.67730534870324277 ) ) ;
#45839=DIRECTION ( 'NONE',  ( 1.000000000000000000, 0.000000000000000000, 0.000000000000000000 ) ) ;
#45850=CARTESIAN_POINT ( 'NONE',  ( 18.14493211602550105, -0.4188397444781337686, -12.59305179380755213 ) ) ;
#45862=CARTESIAN_POINT ( 'NONE',  ( 12.15267534726961607, 2.198616041048513381, 13.82629894333309295 ) ) ;
#45865=CARTESIAN_POINT ( 'NONE',  ( 12.20062903853931147, 0.1603600964535310536, -12.69865684038602360 ) ) ;
#45866=CARTESIAN_POINT ( 'NONE',  ( 12.12629894760563509, -0.2577288767859198249, 13.99764474128114600 ) ) ;
#45869=EDGE_CURVE ( 'NONE', #93, #44093, #23933, .T. ) ;
#45872=PLANE ( 'NONE',  #23887 ) ;
#45877=CARTESIAN_POINT ( 'NONE',  ( 12.61585440497580990, 3.174879747171424960, 12.19344691178322471 ) ) ;
#45884=CARTESIAN_POINT ( 'NONE',  ( 12.63917144495449207, 1.891830949853918975, 12.57269938248749064 ) ) ;
#45901=CARTESIAN_POINT ( 'NONE',  ( 18.22257245894167710, 2.198943951577544631, -12.40664208059732587 ) ) ;
#45903=CARTESIAN_POINT ( 'NONE',  ( 17.55505043854143565, 3.125000000000000000, 12.28373071562070074 ) ) ;
#45904=CARTESIAN_POINT ( 'NONE',  ( 12.22115613568263903, 2.722964197629289984, -13.62363865701805210 ) ) ;
#45909=CARTESIAN_POINT ( 'NONE',  ( 12.22983020848963065, 0.4451122480341365151, -13.99293440828418511 ) ) ;
#45911=CARTESIAN_POINT ( 'NONE',  ( 18.15909587492906496, -2.338249772828220774, -13.70640098171541155 ) ) ;
#45912=CARTESIAN_POINT ( 'NONE',  ( 18.17974523563204414, 2.479825770664845663, 12.45623811633683431 ) ) ;
#45917=CARTESIAN_POINT ( 'NONE',  ( 18.26447107791328861, 2.367226376531800458, -13.79841952404521166 ) ) ;
#45919=CARTESIAN_POINT ( 'NONE',  ( 5.700000000000000178, 12.50865771883999855, 2.924687089724999911 ) ) ;
#45926=LINE ( 'NONE', #63012, #16972 ) ;
#45938=CARTESIAN_POINT ( 'NONE',  ( 17.86124198984734690, -1.955044089803213536, -12.56196094884553638 ) ) ;
#45940=AXIS2_PLACEMENT_3D ( 'NONE', #27812, #1232, #45945 ) ;
#45942=DIRECTION ( 'NONE',  ( 1.000000000000000000, 0.000000000000000000, 0.000000000000000000 ) ) ;
#45945=DIRECTION ( 'NONE',  ( 0.000000000000000000, 0.000000000000000000, 1.000000000000000000 ) ) ;
#45948=CARTESIAN_POINT ( 'NONE',  ( 12.32403884885180645, 1.971565993173698850, -13.86048321094706637 ) ) ;
#45950=CARTESIAN_POINT ( 'NONE',  ( 18.03319344185665329, 0.5490318484135021659, 13.98923259457976087 ) ) ;
#45955=ORIENTED_EDGE ( 'NONE', *, *, #17203, .T. ) ;
#45972=DIRECTION ( 'NONE',  ( 0.000000000000000000, 1.000000000000000000, 0.000000000000000000 ) ) ;
#45974=CARTESIAN_POINT ( 'NONE',  ( 4.599999999999999645, -3.248147246781390329, -13.61798588129781251 ) ) ;
#45982=CARTESIAN_POINT ( 'NONE',  ( 12.54694134722857513, -0.5693054069933395356, -12.68281928773557787 ) ) ;
#45983=CARTESIAN_POINT ( 'NONE',  ( 12.19038559394824972, -2.613250548335406265, -12.42445786901186722 ) ) ;
#46001=CARTESIAN_POINT ( 'NONE',  ( 18.28005834358923920, 0.01140630886273286473, -14.00000041621361291 ) ) ;
#46013=ADVANCED_FACE ( 'NONE', ( #52953 ), #68325, .F. ) ;
#46014=CARTESIAN_POINT ( 'NONE',  ( 12.19290954905150315, -2.626136292398727701, -13.64584403834836479 ) ) ;
#46019=CARTESIAN_POINT ( 'NONE',  ( 17.94287402913520069, 0.4902502636344967524, -13.88836422973777296 ) ) ;
#46024=CARTESIAN_POINT ( 'NONE',  ( 12.60368798324988404, -0.5920240553917492932, -13.88302649426327307 ) ) ;
#46025=CARTESIAN_POINT ( 'NONE',  ( 18.14681149257599913, -2.701359571199342113, 12.40239981104076072 ) ) ;
#46037=CARTESIAN_POINT ( 'NONE',  ( 17.55505043854143565, 1.875000000000000000, -25.00000000000000000 ) ) ;
#46046=CARTESIAN_POINT ( 'NONE',  ( 12.75534451565254201, 1.787855198891418418, -13.88537265576022861 ) ) ;
#46047=AXIS2_PLACEMENT_3D ( 'NONE', #65955, #54440, #22968 ) ;
#46053=CARTESIAN_POINT ( 'NONE',  ( 17.81083341652436758, 0.6731412448965020667, 12.58200685883813108 ) ) ;
#46054=CARTESIAN_POINT ( 'NONE',  ( 4.599999999999999645, -3.199698446519374073, -12.18695736643652694 ) ) ;
#46060=CARTESIAN_POINT ( 'NONE',  ( 18.13115538416114703, 2.961380457613811412, 13.68321312766445175 ) ) ;
#46091=CARTESIAN_POINT ( 'NONE',  ( 12.35410221487141591, 2.932869452542227418, -12.34012701440640747 ) ) ;
#46102=CARTESIAN_POINT ( 'NONE',  ( 12.72061467711778171, -1.765703846569735669, -12.47566797393135474 ) ) ;
#46108=CARTESIAN_POINT ( 'NONE',  ( 12.32516769934784584, -3.065409648700736511, -13.66028300215598534 ) ) ;
#46111=DIRECTION ( 'NONE',  ( 0.9999999999999473754, -3.241492823037153003E-07, -2.435227350522113568E-09 ) ) ;
#46113=ORIENTED_EDGE ( 'NONE', *, *, #65217, .F. ) ;
#46118=CARTESIAN_POINT ( 'NONE',  ( 17.55505043854144276, -0.6250000000000001110, -13.88107975066922428 ) ) ;
#46121=CARTESIAN_POINT ( 'NONE',  ( 17.81536569913635759, 3.068232145164245583, 12.30083422255798631 ) ) ;
#46126=CARTESIAN_POINT ( 'NONE',  ( 12.58267958641587114, -1.915804698272715934, 12.56868422206429869 ) ) ;
#46133=PRODUCT ( 'Airflow Sleeve', 'Airflow Sleeve', '', ( #51238 ) ) ;
#46135=CARTESIAN_POINT ( 'NONE',  ( 12.60420289721210985, 0.5919389804100245733, 12.68142457171642157 ) ) ;
#46155=CARTESIAN_POINT ( 'NONE',  ( 18.17508454104073934, -2.579277621784283436, 13.65633006993621557 ) ) ;
#46157=CARTESIAN_POINT ( 'NONE',  ( 12.78089499409917451, -3.248109241121374335, 13.61799491149520946 ) ) ;
#46183=CARTESIAN_POINT ( 'NONE',  ( 17.65776394871757660, -1.883156081309886432, 13.78509897404221718 ) ) ;
#46194=CARTESIAN_POINT ( 'NONE',  ( 17.96742813929299132, 0.5917181940048636957, -12.58609996267493258 ) ) ;
#46206=CARTESIAN_POINT ( 'NONE',  ( 17.67442079356964868, 1.770331164897448684, 12.47501301698789433 ) ) ;
#46208=CARTESIAN_POINT ( 'NONE',  ( 12.10694218860113125, 2.320713384140923097, 13.80631828123456906 ) ) ;
#46211=CARTESIAN_POINT ( 'NONE',  ( 12.40964703161358607, 0.4840289223742854641, -12.68758247551030038 ) ) ;
#46212=CARTESIAN_POINT ( 'NONE',  ( 12.50552075632584881, -0.6654101994098641226, 13.98418081573739435 ) ) ;
#46222=CARTESIAN_POINT ( 'NONE',  ( 12.47126843887705938, 3.119056300612241373, 12.20784669583219895 ) ) ;
#46230=CARTESIAN_POINT ( 'NONE',  ( 12.19116924869954310, 2.617374924051761642, 12.42344294663814530 ) ) ;
#46241=CARTESIAN_POINT ( 'NONE',  ( 21.35000154058000277, 0.000000000000000000, 0.000000000000000000 ) ) ;
#46248=CARTESIAN_POINT ( 'NONE',  ( 17.92144340210919395, 1.859318429515440796, -12.46206136722992319 ) ) ;
#46257=CARTESIAN_POINT ( 'NONE',  ( 12.15449479986285830, 0.3231860383015842109, -13.99628497142876071 ) ) ;
#46268=CARTESIAN_POINT ( 'NONE',  ( 18.12530810765558087, 2.066994332627597686, -13.84657437950017922 ) ) ;
#46281=EDGE_LOOP ( 'NONE', ( #21078, #61915, #67594, #22192 ) ) ;
#46286=CARTESIAN_POINT ( 'NONE',  ( 17.74796797082753130, -1.905496177146738690, -12.57037238745254548 ) ) ;
#46298=CARTESIAN_POINT ( 'NONE',  ( 12.10810820711261471, 2.719264802799586267, -13.73338027651840321 ) ) ;
#46299=CARTESIAN_POINT ( 'NONE',  ( 18.10028295948236732, 0.4818816852691620300, 13.99171642476389721 ) ) ;
#46304=EDGE_LOOP ( 'NONE', ( #27359, #22859, #31330, #12161, #8551, #11665, #11435, #23491 ) ) ;
#46307=CARTESIAN_POINT ( 'NONE',  ( 12.24279999538967623, -2.226287937550149199, 13.72772666894641880 ) ) ;
#46313=DIRECTION ( 'NONE',  ( 0.000000000000000000, -1.000000000000000000, 0.000000000000000000 ) ) ;
#46319=EDGE_CURVE ( 'NONE', #4104, #16477, #23802, .T. ) ;
#46333=CARTESIAN_POINT ( 'NONE',  ( 12.61399029061283450, -0.5951698179256268428, -12.68122092285041624 ) ) ;
#46334=CARTESIAN_POINT ( 'NONE',  ( 12.18412391182395815, -2.571774448735478558, -12.43455553904774646 ) ) ;
#46351=CARTESIAN_POINT ( 'NONE',  ( 18.23380192947725931, -0.2577288767859217122, -13.99764474128114777 ) ) ;
#46360=CARTESIAN_POINT ( 'NONE',  ( 12.19259091212767210, -2.624575865053327295, -13.64619539123898839 ) ) ;
#46362=VERTEX_POINT ( 'NONE', #61639 ) ;
#46371=CARTESIAN_POINT ( 'NONE',  ( 12.23133660942382583, -0.2481576080865461609, -13.89702325994032961 ) ) ;
#46373=CARTESIAN_POINT ( 'NONE',  ( 18.05401280175963663, -2.123066371663036023, 12.53147770072749623 ) ) ;
#46382=DIRECTION ( 'NONE',  ( -0.000000000000000000, -0.000000000000000000, 1.000000000000000000 ) ) ;
#46398=CARTESIAN_POINT ( 'NONE',  ( 17.82189142195447573, 0.6689034848678535594, 12.58223305319197394 ) ) ;
#46402=ORIENTED_EDGE ( 'NONE', *, *, #61237, .T. ) ;
#46409=EDGE_LOOP ( 'NONE', ( #51528, #42072, #12105, #62682, #37690, #7394, #40172, #30748 ) ) ;
#46415=CARTESIAN_POINT ( 'NONE',  ( 17.60408629075383047, -3.199716927301871738, 12.18695251432577464 ) ) ;
#46437=CARTESIAN_POINT ( 'NONE',  ( 12.24413029362356831, 2.775858423521469387, -12.38303112237259640 ) ) ;
#46446=CARTESIAN_POINT ( 'NONE',  ( 12.18120961385786849, -2.543048387066361382, -12.44145101111442919 ) ) ;
#46454=CARTESIAN_POINT ( 'NONE',  ( 12.33271654538604523, -2.090191715682863993, -13.75184336857262402 ) ) ;
#46461=CARTESIAN_POINT ( 'NONE',  ( 12.15888864299428640, 0.3818843737314618902, -13.99543728850283131 ) ) ;
#46463=CARTESIAN_POINT ( 'NONE',  ( 18.12469242171570372, 2.757364536613152062, 13.61544764691891629 ) ) ;
#46466=CARTESIAN_POINT ( 'NONE',  ( 18.11139879660519014, 2.784965558754640913, 12.38059455073776505 ) ) ;
#46478=CARTESIAN_POINT ( 'NONE',  ( 12.42472005158248294, 0.4959841406075979342, 12.68696163625449103 ) ) ;
#46483=DIRECTION ( 'NONE',  ( 1.000000000000000000, 0.000000000000000000, 0.000000000000000000 ) ) ;
#46489=CARTESIAN_POINT ( 'NONE',  ( 17.92197813837931619, 1.993632751867237207, 13.76786175838295279 ) ) ;
#46493=ORIENTED_EDGE ( 'NONE', *, *, #38832, .T. ) ;
#46497=UNCERTAINTY_MEASURE_WITH_UNIT (LENGTH_MEASURE( 1.000000000000000082E-05 ), #17480, 'distance_accuracy_value', 'NONE');
#46503=CARTESIAN_POINT ( 'NONE',  ( 18.01397738364139300, -2.075598766708243836, -13.75431519107022815 ) ) ;
#46513=CARTESIAN_POINT ( 'NONE',  ( 17.98741890697079882, -0.4515201817464164491, 13.89013314510155261 ) ) ;
#46515=ORIENTED_EDGE ( 'NONE', *, *, #64570, .F. ) ;
#46526=CARTESIAN_POINT ( 'NONE',  ( 18.06104743845540384, -3.040966990778160017, 13.66574534766771620 ) ) ;
#46527=CARTESIAN_POINT ( 'NONE',  ( 17.75978284915347771, 3.091857219545061763, -13.52996931830681149 ) ) ;
#46532=ORIENTED_EDGE ( 'NONE', *, *, #60776, .T. ) ;
#46535=AXIS2_PLACEMENT_3D ( 'NONE', #43528, #48420, #526 ) ;
#46540=CARTESIAN_POINT ( 'NONE',  ( 18.17069881803083931, 0.3800566752825912387, -12.59427093624936767 ) ) ;
#46554=CARTESIAN_POINT ( 'NONE',  ( 12.22752497338536415, 2.076440593937394219, 13.84516123709150826 ) ) ;
#46557=CARTESIAN_POINT ( 'NONE',  ( 12.19608323748815160, 0.1421782556677775866, -12.69895087450945503 ) ) ;
#46558=CARTESIAN_POINT ( 'NONE',  ( 12.78109998040213213, -0.7302151644511187811, 13.98094363559787467 ) ) ;
#46567=CARTESIAN_POINT ( 'NONE',  ( 12.17424305300934151, 2.124765750614183712, 12.41957393385126451 ) ) ;
#46576=CARTESIAN_POINT ( 'NONE',  ( 12.18869345029320606, 2.603827955627350477, 12.42676989083816252 ) ) ;
#46577=CARTESIAN_POINT ( 'NONE',  ( 12.80505043854143388, 1.875000000000000000, -13.78631952119025073 ) ) ;
#46598=CARTESIAN_POINT ( 'NONE',  ( 17.77951638133172452, 1.796077334879280896, -12.47133186514445313 ) ) ;
#46600=CARTESIAN_POINT ( 'NONE',  ( 18.11819331236293706, 2.771443073929879208, 12.38417569151564734 ) ) ;
#46601=CARTESIAN_POINT ( 'NONE',  ( 12.22548351784790199, 2.734003476504523800, -13.62103941680929076 ) ) ;
#46606=CARTESIAN_POINT ( 'NONE',  ( 12.53842061970401467, 0.6791475903684074389, -13.98351814429473094 ) ) ;
#46614=CARTESIAN_POINT ( 'NONE',  ( 17.94045008455784185, 3.136494811772696067, -13.64413575143460911 ) ) ;
#46615=ORIENTED_EDGE ( 'NONE', *, *, #13827, .T. ) ;
#46632=CARTESIAN_POINT ( 'NONE',  ( 17.65155715295180627, -3.193702317672024282, -12.18853033496119842 ) ) ;
#46644=CARTESIAN_POINT ( 'NONE',  ( 18.28003411566973213, 0.02431279293010887507, 13.99999914078079932 ) ) ;
#46655=ADVANCED_FACE ( 'NONE', ( #31551 ), #52871, .F. ) ;
#46673=EDGE_CURVE ( 'NONE', #46748, #45774, #62185, .T. ) ;
#46678=CARTESIAN_POINT ( 'NONE',  ( 12.33572460179970065, 0.5483668826291651088, -12.58806376549905082 ) ) ;
#46679=CARTESIAN_POINT ( 'NONE',  ( 12.18009741656738854, -2.512104454550815991, -12.44873738066442925 ) ) ;
#46698=VERTEX_POINT ( 'NONE', #54236 ) ;
#46706=CARTESIAN_POINT ( 'NONE',  ( 12.24260983038517914, -2.772891244653861609, -13.61173698548923028 ) ) ;
#46720=CARTESIAN_POINT ( 'NONE',  ( 18.13803896488302669, -2.274492816832912823, 12.50128160305151503 ) ) ;
#46734=CYLINDRICAL_SURFACE ( 'NONE', #54986, 13.17499999999999893 ) ;
#46738=CARTESIAN_POINT ( 'NONE',  ( 12.35713445931008359, 3.099811329670646209, -13.65268841750417650 ) ) ;
#46744=CARTESIAN_POINT ( 'NONE',  ( 18.26841343935701190, -0.1288995356414823490, 12.59934597632939912 ) ) ;
#46748=VERTEX_POINT ( 'NONE', #6690 ) ;
#46772=ORIENTED_EDGE ( 'NONE', *, *, #65040, .F. ) ;
#46773=LINE ( 'NONE', #57247, #66344 ) ;
#46775=LINE ( 'NONE', #20888, #8549 ) ;
#46780=CARTESIAN_POINT ( 'NONE',  ( 12.49885887340285961, 1.955044097548213733, -12.56200003178136448 ) ) ;
#46788=CARTESIAN_POINT ( 'NONE',  ( 12.66194203315991906, -3.108482559131308332, -12.28874639354599374 ) ) ;
#46795=CARTESIAN_POINT ( 'NONE',  ( 12.38032181885351513, -3.110191202103278485, -13.65016103957348825 ) ) ;
#46805=CARTESIAN_POINT ( 'NONE',  ( 18.10300909156940818, 2.800751615046049192, 13.60500513795867583 ) ) ;
#46808=CARTESIAN_POINT ( 'NONE',  ( 17.93780763597375483, 2.994506166037827377, 12.32249531978309243 ) ) ;
#46813=EDGE_LOOP ( 'NONE', ( #68509, #21754, #32235, #15283 ) ) ;
#46814=CARTESIAN_POINT ( 'NONE',  ( 12.78418516728952703, -3.124999463064650929, 12.28374650604039786 ) ) ;
#46823=CARTESIAN_POINT ( 'NONE',  ( 12.78441639972302113, -0.6247443594537136491, 12.67930618256805886 ) ) ;
#46831=CARTESIAN_POINT ( 'NONE',  ( 17.57587252603347494, 1.875000554927097607, 13.78627161177572624 ) ) ;
#46837=CARTESIAN_POINT ( 'NONE',  ( 18.17180710801086008, -0.1030387082853383846, -12.69945707558994563 ) ) ;
#46838=EDGE_CURVE ( 'NONE', #42806, #32174, #59708, .T. ) ;
#46844=EDGE_CURVE ( 'NONE', #15133, #18184, #14643, .T. ) ;
#46845=CARTESIAN_POINT ( 'NONE',  ( 18.14812703077573275, -2.302545424703879462, -13.71331074879213219 ) ) ;
#46866=CARTESIAN_POINT ( 'NONE',  ( 17.55505043854147118, -2.500000000000000000, -25.00000000000000000 ) ) ;
#46880=CARTESIAN_POINT ( 'NONE',  ( 18.18297319953442681, 0.3597466176220722178, -12.59486741915706531 ) ) ;
#46881=CARTESIAN_POINT ( 'NONE',  ( 12.64175205088856657, 3.104634757609924467, -12.28992885563447146 ) ) ;
#46883=EDGE_CURVE ( 'NONE', #50331, #47262, #68983, .T. ) ;
#46884=EDGE_CURVE ( 'NONE', #5820, #38087, #41388, .T. ) ;
#46892=CARTESIAN_POINT ( 'NONE',  ( 12.08550557360779365, 2.425787521189699980, 13.78826042901831528 ) ) ;
#46896=CARTESIAN_POINT ( 'NONE',  ( 12.08032335320031159, 0.02332822437943948488, 13.99998565365491210 ) ) ;
#46898=CARTESIAN_POINT ( 'NONE',  ( 12.18347802452938211, -2.109676230065137936, 12.42212916133884981 ) ) ;
#46909=CARTESIAN_POINT ( 'NONE',  ( 12.09756245983758127, 2.320968861236844649, 12.38441143973091485 ) ) ;
#46916=CARTESIAN_POINT ( 'NONE',  ( 12.23322259332536355, 2.246983130377972149, 12.50693187469323497 ) ) ;
#46919=CARTESIAN_POINT ( 'NONE',  ( 12.33180295219017353, -0.4082649239379795847, 12.69116688080143618 ) ) ;
#46927=CARTESIAN_POINT ( 'NONE',  ( 12.70235978774141294, -3.116847232384803323, 13.52309701207074966 ) ) ;
#46936=CARTESIAN_POINT ( 'NONE',  ( 17.74784205817676863, 3.094544633123687216, -12.29297002796977800 ) ) ;
#46938=CARTESIAN_POINT ( 'NONE',  ( 18.14655301447361779, 2.701944876897162562, 12.40222020712343998 ) ) ;
#46939=CARTESIAN_POINT ( 'NONE',  ( 12.18578014164085488, 2.585505937877283333, -13.65496065469440268 ) ) ;
#46946=CARTESIAN_POINT ( 'NONE',  ( 18.17956732773302164, 2.474903466559772891, 12.45737214977695828 ) ) ;
#46953=CARTESIAN_POINT ( 'NONE',  ( 17.97013316094029989, 1.919230625394029888, -13.86782606946093743 ) ) ;
#46959=DIRECTION ( 'NONE',  ( -0.000000000000000000, -0.000000000000000000, 1.000000000000000000 ) ) ;
#46972=CARTESIAN_POINT ( 'NONE',  ( 17.55505043854147118, -1.875000000000000000, -12.57541666120756041 ) ) ;
#46985=CARTESIAN_POINT ( 'NONE',  ( 17.91761384724883399, 0.6327954766588940183, 13.98569611075749286 ) ) ;
#46993=CARTESIAN_POINT ( 'NONE',  ( 12.48673873075621188, -3.044366353203134423, 13.54286685750151165 ) ) ;
#47006=DIRECTION ( 'NONE',  ( 1.000000000000000000, -4.332706595949694629E-15, 1.401268137124204108E-14 ) ) ;
#47017=CARTESIAN_POINT ( 'NONE',  ( 12.49190496432325226, 0.5409888710114135746, -12.68448745112149645 ) ) ;
#47018=CARTESIAN_POINT ( 'NONE',  ( 12.27188044046201654, -2.173264662115791168, -12.52171693736153557 ) ) ;
#47035=CARTESIAN_POINT ( 'NONE',  ( 17.77667453761836214, -0.6953657024348838256, -13.98272072176121483 ) ) ;
#47042=CARTESIAN_POINT ( 'NONE',  ( 18.08168818188836724, -2.836704670462161904, 12.36674034547891488 ) ) ;
#47047=CARTESIAN_POINT ( 'NONE',  ( 12.25785601948557257, -2.186712656597046056, -13.73518136002139478 ) ) ;
#47054=CARTESIAN_POINT ( 'NONE',  ( 17.75510503584834865, 0.5924680672296399608, -13.88300198246877315 ) ) ;
#47058=DIRECTION ( 'NONE',  ( 0.7071067987106167685, 0.000000000000000000, 0.7071067636624778219 ) ) ;
#47064=VERTEX_POINT ( 'NONE', #16324 ) ;
#47066=ADVANCED_FACE ( 'NONE', ( #15981 ), #42314, .T. ) ;
#47068=CARTESIAN_POINT ( 'NONE',  ( 12.22230712497529304, 2.273859679217653973, -13.71882920742291923 ) ) ;
#47073=CARTESIAN_POINT ( 'NONE',  ( 18.03351232763409939, 0.4021407113610637185, 13.89217057782673592 ) ) ;
#47075=CARTESIAN_POINT ( 'NONE',  ( 12.60487368084097604, 0.5921679928993447417, 13.88301795523195459 ) ) ;
#47086=CARTESIAN_POINT ( 'NONE',  ( 18.28005836700933529, 0.01123479547583059769, 12.60000044989513412 ) ) ;
#47093=CARTESIAN_POINT ( 'NONE',  ( 17.57920672810397278, 3.248146558128239381, 13.61798601073640924 ) ) ;
#47094=CYLINDRICAL_SURFACE ( 'NONE', #15390, 14.00000000000000000 ) ;
#47104=CARTESIAN_POINT ( 'NONE',  ( 17.74741402337964047, -1.780171064341584453, 12.47366677607746333 ) ) ;
#47119=ORIENTED_EDGE ( 'NONE', *, *, #57395, .F. ) ;
#47120=CARTESIAN_POINT ( 'NONE',  ( 17.71746485746498223, 0.6038715862870291939, -13.88233985103438251 ) ) ;
#47135=EDGE_LOOP ( 'NONE', ( #35944, #32971, #39929, #52858 ) ) ;
#47136=CARTESIAN_POINT ( 'NONE',  ( 12.60240816447944034, -3.091259750208972701, -12.29394167103376923 ) ) ;
#47140=CARTESIAN_POINT ( 'NONE',  ( 12.58303802678793559, -1.915668549203847437, -13.78011653961192629 ) ) ;
#47143=CARTESIAN_POINT ( 'NONE',  ( 18.24341944916329794, -2.253723043306040008, 12.39680838072757574 ) ) ;
#47145=ORIENTED_EDGE ( 'NONE', *, *, #19922, .T. ) ;
#47151=CARTESIAN_POINT ( 'NONE',  ( 18.17176891181418341, 2.603394967838109864, 12.42689558795375682 ) ) ;
#47152=AXIS2_PLACEMENT_3D ( 'NONE', #48881, #22299, #12165 ) ;
#47165=CARTESIAN_POINT ( 'NONE',  ( 12.23548902587310216, -0.2575478136180257005, 12.69649014468029335 ) ) ;
#47173=CARTESIAN_POINT ( 'NONE',  ( 12.56893612375087876, -3.162115968203192740, -12.19677724224617599 ) ) ;
#47179=CARTESIAN_POINT ( 'NONE',  ( 5.670648345173091798, -12.06568050912973611, 3.730933605404522790 ) ) ;
#47184=CARTESIAN_POINT ( 'NONE',  ( 18.16657332793047175, -2.629115782240843302, 13.64522528451933425 ) ) ;
#47189=CARTESIAN_POINT ( 'NONE',  ( 17.93716281226434717, -2.994693044426598671, -13.55594923565225329 ) ) ;
#47198=VECTOR ( 'NONE', #66111, 1000.000000000000000 ) ;
#47209=CARTESIAN_POINT ( 'NONE',  ( 12.07980306947240301, 2.459616342362515695, -12.35762317364247487 ) ) ;
#47212=CARTESIAN_POINT ( 'NONE',  ( 18.23515949175306261, -2.264077836046926251, 13.81573184862659431 ) ) ;
#47217=B_SPLINE_CURVE_WITH_KNOTS ( 'NONE', 3,
 ( #36288, #30705, #52015, #4116, #20554, #25453, #10061, #41533, #1646, #27183, #49191, #54087, #16339, #263, #12137, #1300 ),
 .UNSPECIFIED., .F., .F.,
 ( 4, 2, 2, 2, 2, 2, 2, 4 ),
 ( 0.000000000000000000, 0.06249999999999733546, 0.1249999999999946709, 0.2499999999999935607, 0.4999999999999946709, 0.7499999999999957812, 0.8749999999999978906, 1.000000000000000000 ),
 .UNSPECIFIED. ) ;
#47226=CARTESIAN_POINT ( 'NONE',  ( 18.07652645701808325, -0.4998493492227053525, -12.59008424712975227 ) ) ;
#47227=CARTESIAN_POINT ( 'NONE',  ( 12.42339251324506222, 2.995356603752234115, -12.32227076304033275 ) ) ;
#47237=CARTESIAN_POINT ( 'NONE',  ( 12.50345261626379845, 3.182071724319534223, 13.63357796689959933 ) ) ;
#47241=CARTESIAN_POINT ( 'NONE',  ( 12.58342633946452338, -0.6953657024348739446, 13.98272072176121661 ) ) ;
#47249=CARTESIAN_POINT ( 'NONE',  ( 12.19582542658656976, 0.3901114995139722819, 12.59396323349878166 ) ) ;
#47253=CARTESIAN_POINT ( 'NONE',  ( 12.12451730110971582, 2.231694252990110261, 12.40079297172318107 ) ) ;
#47260=CARTESIAN_POINT ( 'NONE',  ( 12.48631554272296640, 3.044136704961973638, 12.30804282041555275 ) ) ;
#47262=VERTEX_POINT ( 'NONE', #51847 ) ;
#47263=CARTESIAN_POINT ( 'NONE',  ( 12.32623904992082942, -0.4017251368573808157, 12.69144801866960037 ) ) ;
#47269=LINE ( 'NONE', #20695, #3112 ) ;
#47270=CARTESIAN_POINT ( 'NONE',  ( 12.27207468729466022, -2.172927540677619618, 13.73742275803506452 ) ) ;
#47281=CARTESIAN_POINT ( 'NONE',  ( 18.17157907633050939, 2.603049611614717485, -12.42699283961531265 ) ) ;
#47283=CARTESIAN_POINT ( 'NONE',  ( 17.86986266960968450, 3.040316756266463027, 12.30911383021309824 ) ) ;
#47299=ORIENTED_EDGE ( 'NONE', *, *, #61873, .T. ) ;
#47301=VECTOR ( 'NONE', #47925, 1000.000000000000000 ) ;
#47305=CARTESIAN_POINT ( 'NONE',  ( 12.31853810485765877, 0.3923498215458492977, -13.89254714539060132 ) ) ;
#47316=CARTESIAN_POINT ( 'NONE',  ( 18.17997390458975460, -2.522451123844925203, -12.44632513475228031 ) ) ;
#47320=EDGE_CURVE ( 'NONE', #28416, #49162, #17193, .T. ) ;
#47344=ORIENTED_EDGE ( 'NONE', *, *, #51321, .T. ) ;
#47360=CARTESIAN_POINT ( 'NONE',  ( 5.634820038283264054, 12.96111451950602245, -2.364727967815067888 ) ) ;
#47363=CARTESIAN_POINT ( 'NONE',  ( 12.34842979604855273, 0.4268810874232075170, -12.69034564040270396 ) ) ;
#47364=CARTESIAN_POINT ( 'NONE',  ( 12.64124574432627313, -3.108970204240351975, -12.28865804429000264 ) ) ;
#47365=DIRECTION ( 'NONE',  ( -1.000000000000000000, 0.000000000000000000, 0.000000000000000000 ) ) ;
#47366=FACE_OUTER_BOUND ( 'NONE', #15563, .T. ) ;
#47373=EDGE_CURVE ( 'NONE', #64966, #1839, #6221, .T. ) ;
#47377=ORIENTED_EDGE ( 'NONE', *, *, #30982, .F. ) ;
#47383=CARTESIAN_POINT ( 'NONE',  ( 17.82168025737886552, -0.6791475903684105475, -13.98351814429472917 ) ) ;
#47398=CARTESIAN_POINT ( 'NONE',  ( 17.77476912162670430, 0.5854932480697117025, -13.88340087527083000 ) ) ;
#47405=CARTESIAN_POINT ( 'NONE',  ( 12.24414859480283901, 2.775896286417996794, 13.61101139974200791 ) ) ;
#47412=CARTESIAN_POINT ( 'NONE',  ( 12.52583694058614938, 1.940453150098576662, -13.77633667721135602 ) ) ;
#47414=CARTESIAN_POINT ( 'NONE',  ( 17.98272759268933285, -0.4562271229319647681, 13.88993195058941410 ) ) ;
#47415=CARTESIAN_POINT ( 'NONE',  ( 18.11245875488958390, 0.2828881520042535458, 13.89612849061349387 ) ) ;
#47417=CARTESIAN_POINT ( 'NONE',  ( 12.61467092241713850, 0.5953860544200658689, 13.88283270324807184 ) ) ;
#47426=CYLINDRICAL_SURFACE ( 'NONE', #1227, 2.000000000000000444 ) ;
#47428=CARTESIAN_POINT ( 'NONE',  ( 18.17115522622102830, 0.3798658283128530377, 12.59428767283704786 ) ) ;
#47439=B_SPLINE_CURVE_WITH_KNOTS ( 'NONE', 3,
 ( #16700, #6208, #48876, #26518, #37008, #58324, #984, #10425, #22295, #63208, #69157, #31767, #36664, #57986, #21265, #10083 ),
 .UNSPECIFIED., .F., .F.,
 ( 4, 2, 2, 2, 2, 2, 2, 4 ),
 ( 0.000000000000000000, 0.06249999999999894529, 0.1249999999999978906, 0.2500000000000000000, 0.5000000000000008882, 0.7500000000000017764, 0.8750000000000008882, 1.000000000000000000 ),
 .UNSPECIFIED. ) ;
#47441=VECTOR ( 'NONE', #17560, 1000.000000000000000 ) ;
#47464=CARTESIAN_POINT ( 'NONE',  ( 18.09667340657836476, 0.3125520594525350027, -13.89528657259774391 ) ) ;
#47469=CARTESIAN_POINT ( 'NONE',  ( 12.54002611783803012, 3.066051210233499802, -12.30150130090889427 ) ) ;
#47479=CARTESIAN_POINT ( 'NONE',  ( 12.21010952511930903, -2.691762936255614580, -12.40482162467503890 ) ) ;
#47484=CARTESIAN_POINT ( 'NONE',  ( 12.21441178144108619, -2.942030139115490606, -13.68739795509152479 ) ) ;
#47486=CARTESIAN_POINT ( 'NONE',  ( 4.599999999999999645, -14.00000000000000000, 1.714505518806294638E-15 ) ) ;
#47487=CARTESIAN_POINT ( 'NONE',  ( 17.85685707441191639, -3.134587784889875106, 12.20386770240991403 ) ) ;
#47496=CARTESIAN_POINT ( 'NONE',  ( 17.59673268120277356, 3.123957167259608259, 12.28404855389177719 ) ) ;
#47504=CARTESIAN_POINT ( 'NONE',  ( 12.26301939624444870, -2.811829068737872639, 12.37346575716766672 ) ) ;
#47511=CARTESIAN_POINT ( 'NONE',  ( 12.33468944037056225, -0.4116921281473252536, 12.69102089861179294 ) ) ;
#47512=CARTESIAN_POINT ( 'NONE',  ( 5.642739276337546350, -12.09235441392642052, -3.739144582074775958 ) ) ;
#47514=CARTESIAN_POINT ( 'NONE',  ( 21.49999863197000138, 0.000000000000000000, 0.000000000000000000 ) ) ;
#47525=CIRCLE ( 'NONE', #14045, 2.200000000000001954 ) ;
#47530=VECTOR ( 'NONE', #4944, 1000.000000000000000 ) ;
#47534=ORIENTED_EDGE ( 'NONE', *, *, #20539, .F. ) ;
#47536=CARTESIAN_POINT ( 'NONE',  ( 18.11732105061185649, -2.226901518982100203, -13.72755281718820797 ) ) ;
#47546=CARTESIAN_POINT ( 'NONE',  ( 18.12548987800779088, -0.2560590259945930147, 13.89684012171511540 ) ) ;
#47558=CARTESIAN_POINT ( 'NONE',  ( 12.27226887596751759, 1.991660198615914590, -12.44160671058018863 ) ) ;
#47562=CARTESIAN_POINT ( 'NONE',  ( 18.14661026973002933, -2.095745652224531685, 13.84225217829565580 ) ) ;
#47563=CARTESIAN_POINT ( 'NONE',  ( 18.17918907329175227, 2.539311109804731181, -13.66506621000817212 ) ) ;
#47570=CARTESIAN_POINT ( 'NONE',  ( 6.633333333559363609, -12.50865242394284493, 2.924692581576780803 ) ) ;
#47574=CARTESIAN_POINT ( 'NONE',  ( 18.05074276561662572, 0.3808128809978812979, -12.69231869260113754 ) ) ;
#47575=CARTESIAN_POINT ( 'NONE',  ( 12.24260341322176870, 2.772876882482055994, -12.38382274644487602 ) ) ;
#47581=LINE ( 'NONE', #21341, #23581 ) ;
#47586=EDGE_CURVE ( 'NONE', #56864, #23992, #1814, .T. ) ;
#47588=CARTESIAN_POINT ( 'NONE',  ( 12.40587394967876556, -0.4809228688773738991, -12.68774147671740415 ) ) ;
#47596=CARTESIAN_POINT ( 'NONE',  ( 12.38296014331787553, 0.5849390254007664769, 12.58641711472857594 ) ) ;
#47599=CARTESIAN_POINT ( 'NONE',  ( 12.33234491188476767, 1.934664193338946792, 12.45058764867823164 ) ) ;
#47607=CARTESIAN_POINT ( 'NONE',  ( 12.80505043854143388, 3.124999999999999556, 12.28373071562070074 ) ) ;
#47616=CARTESIAN_POINT ( 'NONE',  ( 12.31461592258506421, -2.887558836668430828, 13.58358613427759032 ) ) ;
#47617=CARTESIAN_POINT ( 'NONE',  ( 12.19454236369542244, 2.633904202154401908, 13.64409272134985862 ) ) ;
#47626=CARTESIAN_POINT ( 'NONE',  ( 18.18008862603425158, 2.492635669256734854, -12.45330984115723361 ) ) ;
#47629=CARTESIAN_POINT ( 'NONE',  ( 17.93744643711270115, 2.994789699037250230, 12.32241545780499159 ) ) ;
#47630=CARTESIAN_POINT ( 'NONE',  ( 17.60475804966352342, 1.787836225788080879, 13.88537509868915087 ) ) ;
#47649=CARTESIAN_POINT ( 'NONE',  ( 17.55505043854144276, 0.000000000000000000, -25.00000000000000000 ) ) ;
#47650=CARTESIAN_POINT ( 'NONE',  ( 12.29893553432339282, 0.3669576687960916517, -13.89348614081305655 ) ) ;
#47657=VERTEX_POINT ( 'NONE', #1959 ) ;
#47659=CARTESIAN_POINT ( 'NONE',  ( 17.81536569913638601, -3.068232145164245583, -12.30083422255797565 ) ) ;
#47673=AXIS2_PLACEMENT_3D ( 'NONE', #66848, #3896, #62295 ) ;
#47681=CONICAL_SURFACE ( 'NONE', #51027, 13.94999927503000059, 0.7853981058017837080 ) ;
#47697=CARTESIAN_POINT ( 'NONE',  ( 17.55505043854143565, 3.125000000000000000, -12.28374638332999602 ) ) ;
#47708=CARTESIAN_POINT ( 'NONE',  ( 12.19601995205470324, 0.1418569258565841595, -12.69895512164410079 ) ) ;
#47721=ORIENTED_EDGE ( 'NONE', *, *, #41871, .F. ) ;
#47731=LINE ( 'NONE', #51927, #66582 ) ;
#47741=AXIS2_PLACEMENT_3D ( 'NONE', #9947, #15192, #8574 ) ;
#47745=CARTESIAN_POINT ( 'NONE',  ( 18.15698508547102819, 0.1703860850723086517, -13.89862588397357790 ) ) ;
#47746=CARTESIAN_POINT ( 'NONE',  ( 17.75635104740698722, -0.5917829749564899045, -12.68143435689272280 ) ) ;
#47764=CARTESIAN_POINT ( 'NONE',  ( 18.17607592425854079, -0.07112389991332161709, 13.89976024287835799 ) ) ;
#47765=CARTESIAN_POINT ( 'NONE',  ( 18.06844887843520908, 0.3566139488609988417, 13.89384732035922632 ) ) ;
#47769=AXIS2_PLACEMENT_3D ( 'NONE', #63108, #58226, #62092 ) ;
#47781=CARTESIAN_POINT ( 'NONE',  ( 17.84068610406497868, -0.5560043133243457447, 12.68361349193353860 ) ) ;
#47783=VECTOR ( 'NONE', #45215, 1000.000000000000000 ) ;
#47797=CARTESIAN_POINT ( 'NONE',  ( 12.68688152457048268, -0.7100593550700113887, -12.57997761080729582 ) ) ;
#47799=CARTESIAN_POINT ( 'NONE',  ( 12.80505043854144276, 0.6249999999999994449, -25.00000000000000000 ) ) ;
#47801=EDGE_CURVE ( 'NONE', #32730, #31652, #12940, .T. ) ;
#47802=CARTESIAN_POINT ( 'NONE',  ( 5.592979883553708120, 12.14034187852289115, 3.752392258527085467 ) ) ;
#47809=VERTEX_POINT ( 'NONE', #5720 ) ;
#47813=CARTESIAN_POINT ( 'NONE',  ( 12.80505043854143388, 1.760845406083386688, -12.47635457398814829 ) ) ;
#47828=CARTESIAN_POINT ( 'NONE',  ( 12.76340515712447221, -1.876302067334185475, -12.57520337466226223 ) ) ;
#47832=CARTESIAN_POINT ( 'NONE',  ( 12.41959488098034292, -1.899094099299829530, -13.87060288894783433 ) ) ;
#47836=CARTESIAN_POINT ( 'NONE',  ( 18.17388115328634868, -2.104502522679969179, 12.42302150255120807 ) ) ;
#47842=DIRECTION ( 'NONE',  ( -0.000000000000000000, -0.000000000000000000, 1.000000000000000000 ) ) ;
#47846=CARTESIAN_POINT ( 'NONE',  ( 18.17229989573655047, 2.399660445438212442, -12.47442500975356872 ) ) ;
#47859=CARTESIAN_POINT ( 'NONE',  ( 12.22352039041727245, -0.2292434675627123553, 12.69722039463304952 ) ) ;
#47860=CARTESIAN_POINT ( 'NONE',  ( 5.500000000000000000, -12.22296174243999900, -3.800101973039000214 ) ) ;
#47881=CARTESIAN_POINT ( 'NONE',  ( 17.88807090798128741, -1.970716457409874778, -13.77152834881607468 ) ) ;
#47890=CARTESIAN_POINT ( 'NONE',  ( 17.93438719500359824, -0.4968219660327466980, 13.88804946350949976 ) ) ;
#47897=ORIENTED_EDGE ( 'NONE', *, *, #29393, .T. ) ;
#47900=CARTESIAN_POINT ( 'NONE',  ( 12.12887591290035338, 2.220077349933747168, -12.40287778440552557 ) ) ;
#47914=CARTESIAN_POINT ( 'NONE',  ( 17.59617179617751859, 0.6239794389693675836, -12.67935706666153450 ) ) ;
#47915=CARTESIAN_POINT ( 'NONE',  ( 12.30936054499994725, 2.880824963415391959, -12.35466577907433638 ) ) ;
#47924=CARTESIAN_POINT ( 'NONE',  ( 18.25660817874744168, 2.298073654326294957, 12.38866391276716961 ) ) ;
#47925=DIRECTION ( 'NONE',  ( -1.000000000000000000, -0.000000000000000000, -0.000000000000000000 ) ) ;
#47937=CARTESIAN_POINT ( 'NONE',  ( 12.30932062623505807, 0.5250004125410563383, 12.58906021966015842 ) ) ;
#47940=CARTESIAN_POINT ( 'NONE',  ( 12.10312773382966434, 2.298350437047141259, 12.38862788998081754 ) ) ;
#47948=CARTESIAN_POINT ( 'NONE',  ( 12.24831336537904036, 2.784226791580946436, 12.38079107516542798 ) ) ;
#47957=CARTESIAN_POINT ( 'NONE',  ( 12.18088137079345579, -2.461818645006702777, 13.68150212747531214 ) ) ;
#47958=CARTESIAN_POINT ( 'NONE',  ( 12.22895947712403952, 2.742405092596572391, 13.61899867097569050 ) ) ;
#47965=CARTESIAN_POINT ( 'NONE',  ( 17.83364017334648111, 3.059569048391924451, -12.30342972110860167 ) ) ;
#47967=CARTESIAN_POINT ( 'NONE',  ( 18.14478511896022184, 2.707036753601618440, 12.40091620380301407 ) ) ;
#47988=CARTESIAN_POINT ( 'NONE',  ( 12.64261640806205200, 0.6049408601271634156, -13.88227884472453155 ) ) ;
#47992=EDGE_CURVE ( 'NONE', #67648, #31059, #67193, .T. ) ;
#48001=CARTESIAN_POINT ( 'NONE',  ( 18.08671436482210026, -2.829189290800525391, -12.36876367364216911 ) ) ;
#48004=CARTESIAN_POINT ( 'NONE',  ( 12.49177480397739615, 0.5412024733746015892, 13.88582008197803219 ) ) ;
#48006=CARTESIAN_POINT ( 'NONE',  ( 21.59999953993000332, -12.84999890301999947, 0.000000000000000000 ) ) ;
#48019=CARTESIAN_POINT ( 'NONE',  ( 12.26369778072670691, -2.812515541958659604, 13.60219590381264254 ) ) ;
#48044=EDGE_CURVE ( 'NONE', #40500, #22839, #1777, .T. ) ;
#48045=CARTESIAN_POINT ( 'NONE',  ( 12.21006921427117398, -0.1916424759571759007, -12.69805926625132919 ) ) ;
#48055=CARTESIAN_POINT ( 'NONE',  ( 18.07980528506707074, 0.3396180385544777525, 12.69389128024067936 ) ) ;
#48067=CARTESIAN_POINT ( 'NONE',  ( 17.55505043854147118, -1.875000000000000000, -13.78627172894481667 ) ) ;
#48081=CARTESIAN_POINT ( 'NONE',  ( 17.96719322760356974, 0.4698824118409584694, -13.88931020048284815 ) ) ;
#48087=CARTESIAN_POINT ( 'NONE',  ( 43.76123417800000226, -13.94845324556000143, 4.312847325879000770 ) ) ;
#48088=ORIENTED_EDGE ( 'NONE', *, *, #53701, .T. ) ;
#48096=CARTESIAN_POINT ( 'NONE',  ( 12.66121447289696000, 1.891428313113427073, -13.78385349382385527 ) ) ;
#48100=FACE_OUTER_BOUND ( 'NONE', #48353, .T. ) ;
#48101=CARTESIAN_POINT ( 'NONE',  ( 17.96218347287557648, 0.4743995194917912661, 13.88910611340307533 ) ) ;
#48103=B_SPLINE_CURVE_WITH_KNOTS ( 'NONE', 1,
 ( #66749, #46118 ),
 .UNSPECIFIED., .F., .F.,
 ( 2, 2 ),
 ( 0.000000000000000000, 1.000000000000000000 ),
 .UNSPECIFIED. ) ;
#48114=CARTESIAN_POINT ( 'NONE',  ( 17.96724410757352786, -0.4699213205053990872, 12.68829855189361844 ) ) ;
#48148=CARTESIAN_POINT ( 'NONE',  ( 17.59627693841142104, 0.6239806250735592252, -13.88114166035887997 ) ) ;
#48150=DIRECTION ( 'NONE',  ( 1.000000000000000000, 0.000000000000000000, 0.000000000000000000 ) ) ;
#48158=VERTEX_POINT ( 'NONE', #31191 ) ;
#48163=CARTESIAN_POINT ( 'NONE',  ( 12.24247500090515928, -2.227530134987962818, -12.51087939115179104 ) ) ;
#48166=DIRECTION ( 'NONE',  ( 0.000000000000000000, 0.6195591179857981023, -0.7849499979748136846 ) ) ;
#48167=CARTESIAN_POINT ( 'NONE',  ( 12.08002314427570312, -2.496413253464126569, -13.77564875264238253 ) ) ;
#48170=CARTESIAN_POINT ( 'NONE',  ( 18.23375231277521635, -2.733957939387008818, 12.29982111303847603 ) ) ;
#48188=FACE_BOUND ( 'NONE', #28481, .T. ) ;
#48192=CARTESIAN_POINT ( 'NONE',  ( 12.57501510860068272, -0.5812174491462195336, 12.68209204657793165 ) ) ;
#48193=AXIS2_PLACEMENT_3D ( 'NONE', #7499, #3288, #45942 ) ;
#48200=CARTESIAN_POINT ( 'NONE',  ( 17.71791196170127591, 3.103760126671077035, 13.52664063941735151 ) ) ;
#48204=CARTESIAN_POINT ( 'NONE',  ( 5.563312991718063927, -12.16892724396389447, 3.760371626689057223 ) ) ;
#48211=CARTESIAN_POINT ( 'NONE',  ( 17.81482613222766531, -3.068547461637705975, -13.53623828841521259 ) ) ;
#48225=CIRCLE ( 'NONE', #24771, 2.000000000000001776 ) ;
#48231=CARTESIAN_POINT ( 'NONE',  ( 12.48133867187396007, 1.836397482308027129, -12.46545911376217042 ) ) ;
#48235=CARTESIAN_POINT ( 'NONE',  ( 7.100000000000000533, 12.03770622561999915, -3.722046322334000124 ) ) ;
#48247=CARTESIAN_POINT ( 'NONE',  ( 17.63863136176617985, -0.7145943380091489550, -12.57972004139934974 ) ) ;
#48248=CARTESIAN_POINT ( 'NONE',  ( 12.72076653474564978, 3.120601141701319747, -12.28508997180393436 ) ) ;
#48253=CARTESIAN_POINT ( 'NONE',  ( 4.599999999999999645, -1.760910691117812954, -12.47634535983622861 ) ) ;
#48257=CARTESIAN_POINT ( 'NONE',  ( 18.14725124545925539, 2.065010783240463166, 12.42963489304855962 ) ) ;
#48258=LINE ( 'NONE', #26947, #47301 ) ;
#48261=CARTESIAN_POINT ( 'NONE',  ( 12.39297475254648262, -0.4699412923507725881, -12.68829632720558465 ) ) ;
#48264=CARTESIAN_POINT ( 'NONE',  ( 12.17440657078186028, -2.124933824806643390, 12.41953149444585769 ) ) ;
#48272=CARTESIAN_POINT ( 'NONE',  ( 12.11487221662462055, 0.2205548374446844873, 12.59807454672507632 ) ) ;
#48275=CARTESIAN_POINT ( 'NONE',  ( 12.24387941792141099, 2.775899267521869884, 12.38300827451278607 ) ) ;
#48284=CARTESIAN_POINT ( 'NONE',  ( 18.18005043855005809, -0.04052604701685407623, 12.70000016496815221 ) ) ;
#48292=CARTESIAN_POINT ( 'NONE',  ( 12.21197387330461481, -2.302545343651723808, 13.71336076199744625 ) ) ;
#48295=ORIENTED_EDGE ( 'NONE', *, *, #4410, .T. ) ;
#48302=CARTESIAN_POINT ( 'NONE',  ( 17.71812653075899391, 3.103437839927554176, -12.29028812931823644 ) ) ;
#48319=CARTESIAN_POINT ( 'NONE',  ( 17.55505043854147118, -3.125000000000000000, 13.52084414783465860 ) ) ;
#48328=CARTESIAN_POINT ( 'NONE',  ( 12.44245189064305457, 0.5091685953835116685, -13.88744776337133402 ) ) ;
#48333=VERTEX_POINT ( 'NONE', #29048 ) ;
#48338=CARTESIAN_POINT ( 'NONE',  ( 17.92152980461526468, -3.006687145500352543, -12.31895938800957957 ) ) ;
#48340=PLANE ( 'NONE',  #10599 ) ;
#48341=CARTESIAN_POINT ( 'NONE',  ( 17.65865034516105325, -1.883559157718814880, 12.57405095325165334 ) ) ;
#48343=CARTESIAN_POINT ( 'NONE',  ( 12.19008165514798669, -0.1119984579798063151, 13.89939774083726576 ) ) ;
#48353=EDGE_LOOP ( 'NONE', ( #41014, #26768, #32527, #19182, #42262 ) ) ;
#48359=CARTESIAN_POINT ( 'NONE',  ( 12.75651925148578414, 0.7192569394297179119, 12.57945425907934300 ) ) ;
#48367=AXIS2_PLACEMENT_3D ( 'NONE', #46054, #40131, #19481 ) ;
#48374=CARTESIAN_POINT ( 'NONE',  ( 18.15015087275886074, 2.691082634156150899, -12.40501869842431937 ) ) ;
#48383=VECTOR ( 'NONE', #5356, 1000.000000000000000 ) ;
#48386=CARTESIAN_POINT ( 'NONE',  ( 12.24208977126479070, 0.2715269968477689311, -12.69609476950841831 ) ) ;
#48390=CARTESIAN_POINT ( 'NONE',  ( 5.660639688932317171, 12.98305835826268151, 2.241106542164481130 ) ) ;
#48401=CARTESIAN_POINT ( 'NONE',  ( 17.63808658539555907, 3.119809217581025251, -13.52227901589168546 ) ) ;
#48420=DIRECTION ( 'NONE',  ( -1.000000000000000000, 0.000000000000000000, 0.000000000000000000 ) ) ;
#48421=ORIENTED_EDGE ( 'NONE', *, *, #49081, .T. ) ;
#48437=CARTESIAN_POINT ( 'NONE',  ( 12.57359775157566695, 3.080655040460396066, -13.53300991339124870 ) ) ;
#48441=CARTESIAN_POINT ( 'NONE',  ( 18.11587426570509862, 0.2766185922798710117, 13.89631150889696798 ) ) ;
#48448=CARTESIAN_POINT ( 'NONE',  ( 12.31443335393315586, 0.3873583149501338418, 13.89273910398916279 ) ) ;
#48458=CARTESIAN_POINT ( 'NONE',  ( 17.95947714806421658, -0.4766234715920697473, 12.68796191786312910 ) ) ;
#48477=CARTESIAN_POINT ( 'NONE',  ( 17.60324894539389717, 3.198552395131802228, -12.18725844837785210 ) ) ;
#48478=CARTESIAN_POINT ( 'NONE',  ( 5.584969860380273765, 12.14796130796948859, 3.754865623502155358 ) ) ;
#48494=CARTESIAN_POINT ( 'NONE',  ( 18.17602483311041439, -0.07155107330948752564, -13.89975717292030311 ) ) ;
#48508=CARTESIAN_POINT ( 'NONE',  ( 12.29407742813166493, -2.139519579705956076, -12.52828553530646793 ) ) ;
#48512=CARTESIAN_POINT ( 'NONE',  ( 12.09886375431306682, -2.684759089869698467, -13.74018286504950659 ) ) ;
#48514=CARTESIAN_POINT ( 'NONE',  ( 12.75601781081296693, -1.760880198315417200, 12.47634966360013919 ) ) ;
#48515=CARTESIAN_POINT ( 'NONE',  ( 17.99878237954355598, -3.049368882785702173, 12.22543920180491384 ) ) ;
#48529=EDGE_CURVE ( 'NONE', #19729, #10762, #14167, .T. ) ;
#48548=CARTESIAN_POINT ( 'NONE',  ( 18.15864108120890208, 2.662504769557530793, 13.63760133890561654 ) ) ;
#48557=DIRECTION ( 'NONE',  ( -0.000000000000000000, -0.000000000000000000, 1.000000000000000000 ) ) ;
#48562=CARTESIAN_POINT ( 'NONE',  ( 18.27459401263896055, -2.425695574333701199, -13.78827716170582107 ) ) ;
#48582=CARTESIAN_POINT ( 'NONE',  ( 12.58121427537365022, 1.795950320080887730, -12.47134981075813087 ) ) ;
#48591=CARTESIAN_POINT ( 'NONE',  ( 12.56425374667833950, -3.158898859712414797, -12.19759658245784628 ) ) ;
#48599=CARTESIAN_POINT ( 'NONE',  ( 17.98240372392063335, 0.4561785182478261813, -12.68897339690747295 ) ) ;
#48600=CARTESIAN_POINT ( 'NONE',  ( 12.19483627237708134, 2.635236894562234866, -12.41905446250361678 ) ) ;
#48606=FACE_OUTER_BOUND ( 'NONE', #57449, .T. ) ;
#48608=CARTESIAN_POINT ( 'NONE',  ( 18.15405049586274444, 2.074720874654909064, 12.42801810613654823 ) ) ;
#48613=EDGE_CURVE ( 'NONE', #66385, #55988, #19401, .T. ) ;
#48618=CARTESIAN_POINT ( 'NONE',  ( 12.61495819220213832, -3.174994159617159806, 12.19341885412869964 ) ) ;
#48623=CARTESIAN_POINT ( 'NONE',  ( 12.23004733766517838, 0.4382646521645816584, 12.59237917444261434 ) ) ;
#48625=CYLINDRICAL_SURFACE ( 'NONE', #359, 2.000000000000000444 ) ;
#48626=CARTESIAN_POINT ( 'NONE',  ( 12.21010952511927350, 2.691762936255612360, 12.40482162467503535 ) ) ;
#48632=CARTESIAN_POINT ( 'NONE',  ( 17.55505043854143565, 1.787816316115923954, -13.88537766212463254 ) ) ;
#48634=CARTESIAN_POINT ( 'NONE',  ( 12.32868821305151563, 2.904730879156684153, 12.34800599561342516 ) ) ;
#48639=CARTESIAN_POINT ( 'NONE',  ( 12.52212199951356020, 0.5573870966591139009, 12.68353347973583389 ) ) ;
#48644=CARTESIAN_POINT ( 'NONE',  ( 12.08553199184723681, -2.425689856710292247, 13.78827816593212141 ) ) ;
#48652=CARTESIAN_POINT ( 'NONE',  ( 18.06602350563007775, 2.139519659637397986, -12.52832261142687642 ) ) ;
#48657=EDGE_CURVE ( 'NONE', #47657, #65244, #24569, .T. ) ;
#48658=CARTESIAN_POINT ( 'NONE',  ( 12.80505043854143210, 3.248147246781388553, 13.61798588129781251 ) ) ;
#48665=ORIENTED_EDGE ( 'NONE', *, *, #38201, .F. ) ;
#48666=CARTESIAN_POINT ( 'NONE',  ( 17.92121436125180978, -3.006915247989151219, 13.55278817016120385 ) ) ;
#48674=CARTESIAN_POINT ( 'NONE',  ( 12.08061556837366091, -2.709898641945338138, -13.73658242091784309 ) ) ;
#48682=VECTOR ( 'NONE', #24504, 1000.000000000000000 ) ;
#48685=CARTESIAN_POINT ( 'NONE',  ( 18.27929200419409028, -2.710634889731355912, -13.73643850021282020 ) ) ;
#48687=CARTESIAN_POINT ( 'NONE',  ( 17.59673268120281264, -3.123957167259608259, -12.28404855389177541 ) ) ;
#48696=CARTESIAN_POINT ( 'NONE',  ( 12.29698918160474364, -0.3645810575750318971, 13.89357890581305099 ) ) ;
#48720=VERTEX_POINT ( 'NONE', #20428 ) ;
#48751=DIRECTION ( 'NONE',  ( 0.000000000000000000, 0.7506664619968553831, -0.6606813625592322659 ) ) ;
#48760=ORIENTED_EDGE ( 'NONE', *, *, #48529, .F. ) ;
#48764=VERTEX_POINT ( 'NONE', #42446 ) ;
#48771=CARTESIAN_POINT ( 'NONE',  ( 18.11727536442213093, 0.2737665426068931485, -13.89638618295544248 ) ) ;
#48785=CARTESIAN_POINT ( 'NONE',  ( 12.18523880347860811, 2.582858790010647887, -13.65555696386475582 ) ) ;
#48793=CARTESIAN_POINT ( 'NONE',  ( 12.24748039825137624, 0.2825697096154566323, 13.89613713856509136 ) ) ;
#48794=CARTESIAN_POINT ( 'NONE',  ( 12.35321263090787269, -0.4320316581265434275, -13.89096707190848790 ) ) ;
#48796=CARTESIAN_POINT ( 'NONE',  ( 18.01482774842505918, -0.4234772792228427285, -13.89131919812468929 ) ) ;
#48805=CARTESIAN_POINT ( 'NONE',  ( 18.14682445378390341, -0.2013262877421428398, 12.69785743964334834 ) ) ;
#48808=ORIENTED_EDGE ( 'NONE', *, *, #40106, .T. ) ;
#48819=ORIENTED_EDGE ( 'NONE', *, *, #3525, .F. ) ;
#48820=CARTESIAN_POINT ( 'NONE',  ( 12.08123681970976193, -0.04734719685817544849, -12.59993264914401401 ) ) ;
#48822=CARTESIAN_POINT ( 'NONE',  ( 17.96998260175200102, 3.070456082915652640, -12.22016143605431004 ) ) ;
#48823=CARTESIAN_POINT ( 'NONE',  ( 5.536227981746089988, 12.19240621326732388, 3.776122996995809888 ) ) ;
#48838=CARTESIAN_POINT ( 'NONE',  ( 17.60287317832943543, 0.7290248443971264480, -13.98100598729141097 ) ) ;
#48850=CARTESIAN_POINT ( 'NONE',  ( 18.13255570286232654, -2.076448383791634544, 13.84516006853288950 ) ) ;
#48856=CARTESIAN_POINT ( 'NONE',  ( 12.18001225342677607, -2.492635468222105910, -12.45327835951381346 ) ) ;
#48859=CYLINDRICAL_SURFACE ( 'NONE', #5111, 0.6250000000000005551 ) ;
#48860=CARTESIAN_POINT ( 'NONE',  ( 12.27297424062793141, -2.021448577728832685, -13.85330429709570765 ) ) ;
#48863=CARTESIAN_POINT ( 'NONE',  ( 17.69815883927268985, -3.108482560213371215, 12.28876257455221221 ) ) ;
#48876=CARTESIAN_POINT ( 'NONE',  ( 17.65093666541812212, -1.765655615497803588, -12.47567830514637066 ) ) ;
#48878=CIRCLE ( 'NONE', #18739, 13.17499999999999893 ) ;
#48881=CARTESIAN_POINT ( 'NONE',  ( 5.500000000000000000, -6.661338147750999827E-14, -1.931788062847999572E-14 ) ) ;
#48895=CARTESIAN_POINT ( 'NONE',  ( 18.16587897468625812, 2.632730956727242333, 13.64436436691515908 ) ) ;
#48907=CARTESIAN_POINT ( 'NONE',  ( 18.27051424461486562, -2.638143613628455064, -13.74920933505747733 ) ) ;
#48911=VERTEX_POINT ( 'NONE', #1175 ) ;
#48918=ORIENTED_EDGE ( 'NONE', *, *, #51913, .F. ) ;
#48921=CARTESIAN_POINT ( 'NONE',  ( 18.28072526159958144, 2.330763871450813429, 13.80597059069190458 ) ) ;
#48929=CARTESIAN_POINT ( 'NONE',  ( 12.78084111884633600, 3.199751093817826408, -12.18694350317453079 ) ) ;
#48937=ORIENTED_EDGE ( 'NONE', *, *, #29934, .F. ) ;
#48945=CARTESIAN_POINT ( 'NONE',  ( 18.09667132770093545, -0.3125562302819428484, -12.69484091569604089 ) ) ;
#48954=CARTESIAN_POINT ( 'NONE',  ( 18.06277981064209115, 1.966570380498756654, 12.44558849270348944 ) ) ;
#48960=CARTESIAN_POINT ( 'NONE',  ( 12.22799143493891627, -2.916631933635871476, 12.25779765684317191 ) ) ;
#48966=CARTESIAN_POINT ( 'NONE',  ( 12.08004251007355023, -0.01123479547583346692, 12.60000044989513412 ) ) ;
#48971=CARTESIAN_POINT ( 'NONE',  ( 12.61719528873169338, 3.096122730228594300, 12.29247817764211348 ) ) ;
#48981=CARTESIAN_POINT ( 'NONE',  ( 12.31853785129944434, 0.3923495136273177364, 12.69184251826150955 ) ) ;
#48984=CARTESIAN_POINT ( 'NONE',  ( 17.65093748396062523, 3.195004315067500045, -12.18819265947668207 ) ) ;
#48985=CARTESIAN_POINT ( 'NONE',  ( 12.20814394425996419, -2.932476687367341128, 13.68943695263251570 ) ) ;
#48988=ORIENTED_EDGE ( 'NONE', *, *, #67649, .T. ) ;
#48994=CARTESIAN_POINT ( 'NONE',  ( 17.56547987801834410, 1.875000035136120458, -12.57545641098305289 ) ) ;
#49003=ADVANCED_FACE ( 'NONE', ( #24908 ), #61018, .F. ) ;
#49011=CARTESIAN_POINT ( 'NONE',  ( 17.88731995174124734, -3.029458325253037820, 13.54679862780130151 ) ) ;
#49038=CARTESIAN_POINT ( 'NONE',  ( 12.19601928331639051, 0.1418539764880151210, 13.89904537328360767 ) ) ;
#49039=ORIENTED_EDGE ( 'NONE', *, *, #13240, .T. ) ;
#49051=ADVANCED_FACE ( 'NONE', ( #24571 ), #2550, .F. ) ;
#49065=CARTESIAN_POINT ( 'NONE',  ( 5.684131420607005936, -13.00367204148822253, 2.123909540366339499 ) ) ;
#49074=CARTESIAN_POINT ( 'NONE',  ( 12.69240093715870188, 0.6148490057825425348, -12.67995724530760526 ) ) ;
#49078=CARTESIAN_POINT ( 'NONE',  ( 12.70917152006029660, 3.194951439744890820, 12.18820651941773470 ) ) ;
#49081=EDGE_CURVE ( 'NONE', #17996, #40048, #66544, .T. ) ;
#49083=EDGE_CURVE ( 'NONE', #15974, #18846, #33602, .T. ) ;
#49091=CARTESIAN_POINT ( 'NONE',  ( 18.12879638218879208, 2.748081584522202192, -13.61770999214558486 ) ) ;
#49103=CARTESIAN_POINT ( 'NONE',  ( 17.75984001016927394, -3.091833346833228191, -13.52991597408320068 ) ) ;
#49110=CARTESIAN_POINT ( 'NONE',  ( 18.04064113784076184, 0.3934955818404124450, -13.89250369607471036 ) ) ;
#49121=CARTESIAN_POINT ( 'NONE',  ( 12.48119050255584739, 1.864280969780519825, -13.87532308892432553 ) ) ;
#49125=CARTESIAN_POINT ( 'NONE',  ( 18.22962728801296350, -0.2678304234474040424, 13.99744223245316199 ) ) ;
#49131=CARTESIAN_POINT ( 'NONE',  ( 12.72381130736580346, -0.6210784669183123663, 13.88131957737377675 ) ) ;
#49132=CARTESIAN_POINT ( 'NONE',  ( 12.47605349752420523, -0.5315089155663856868, -13.88632137824048485 ) ) ;
#49134=CARTESIAN_POINT ( 'NONE',  ( 17.77470470791479684, -0.5852235853112173203, -13.88341353704719161 ) ) ;
#49143=CARTESIAN_POINT ( 'NONE',  ( 17.98979505986429572, -0.4491390935506889281, 12.68931154995401123 ) ) ;
#49145=CARTESIAN_POINT ( 'NONE',  ( 18.12474152633276958, -2.757110843054713989, -12.38793583424880040 ) ) ;
#49150=B_SPLINE_CURVE_WITH_KNOTS ( 'NONE', 3,
 ( #44108, #44460, #16141, #37463, #17878, #50724, #66796, #24838, #55279, #29069, #8417, #66447, #7726, #34655, #65755, #28716, #2142, #50379 ),
 .UNSPECIFIED., .F., .F.,
 ( 4, 2, 2, 2, 2, 2, 2, 2, 4 ),
 ( 0.5009155270902381218, 0.5633010862039566913, 0.5944938657608158650, 0.6256866453176750387, 0.6568794248745342124, 0.6880722044313933861, 0.7504577635451146200, 0.8752288817725573100, 1.000000000000000000 ),
 .UNSPECIFIED. ) ;
#49157=CARTESIAN_POINT ( 'NONE',  ( 12.32690578124262615, -0.5408165383911121005, -12.58839068838662456 ) ) ;
#49159=CARTESIAN_POINT ( 'NONE',  ( 18.27387565520746193, 2.575953525795611210, -12.33388021351436770 ) ) ;
#49162=VERTEX_POINT ( 'NONE', #68574 ) ;
#49178=CARTESIAN_POINT ( 'NONE',  ( 18.17882709566423216, 0.04040202251154540597, -13.89992604541789589 ) ) ;
#49187=CARTESIAN_POINT ( 'NONE',  ( 18.03598133453871810, -1.971494603937298029, 13.86049335245054337 ) ) ;
#49191=CARTESIAN_POINT ( 'NONE',  ( 18.20247741952565690, 0.3746922850090889101, 12.59513687151705241 ) ) ;
#49193=B_SPLINE_SURFACE_WITH_KNOTS ( 'NONE', 1, 3, ( 
 ( #35228, #40130, #24382, #45713, #18802, #50953, #28961, #22396, #38480, #3051, #17148, #56198, #61443, #2369, #59803, #3390, #40454, #23693, #24726, #67022, #61781, #55858, #66679, #45027, #39779, #32895, #24037, #50611, #8644, #13900, #66332, #29994, #51294, #11552, #54206, #33243, #13562, #34882, #6307, #7963, #27654, #1081, #43733, #54564, #18456, #7613, #61100, #29300, #2713, #46744, #67699, #5113, #68737, #31352, #10014, #47086, #41157, #26102, #57917, #20163, #35900, #15612, #67357, #62123, #3729, #63491, #41833, #36942, #9318, #68387, #19480, #57216, #68049, #30323, #51969, #36591, #47428, #20507, #53017, #40800, #41490, #14242, #52665, #51633, #30660, #63142, #14921, #4072, #4761, #25064, #31014, #31694, #62802, #20854, #52324, #15267, #58256, #46398, #46053, #42190, #25409, #10360, #62463, #35570, #56885, #36244, #4419, #25757, #19826, #8983, #14583, #57563 ),
 ( #9664, #11387, #65214, #27837, #5797, #59979, #6490, #59635, #26449, #42869, #6140, #43563, #69089, #64517, #47781, #33074, #42526, #63835, #27140, #21195, #568, #64863, #15949, #48458, #48114, #54739, #49143, #11732, #54388, #27481, #21535, #1254, #38307, #21878, #16292, #17331, #37278, #58599, #53361, #43912, #22226, #38660, #58947, #48805, #10700, #37615, #43212, #32045, #32389, #16976, #22569, #914, #33421, #5463, #16635, #26800, #12090, #217, #11054, #64178, #37963, #53703, #59283, #32727, #54040, #61704, #23610, #13483, #13138, #23959, #19053, #7190, #13821, #40052, #44268, #35150, #44613, #12437, #33769, #49488, #40380, #28527, #6838, #29218, #34804, #7526, #66942, #29573, #7884, #2972, #60331, #55434, #34467, #49839, #1598, #61021, #45639, #28171, #22915, #65565, #50530, #17687, #39012, #2632, #56114, #8226, #45293, #18718, #39352, #55084, #1950, #50875 ) ),
 .UNSPECIFIED., .F., .F., .F.,
 ( 2, 2 ),
 ( 4, 2, 2, 2, 2, 2, 2, 2, 2, 2, 2, 2, 2, 2, 2, 2, 2, 2, 2, 2, 2, 2, 2, 2, 2, 2, 2, 2, 2, 2, 2, 2, 2, 2, 2, 2, 2, 2, 2, 2, 2, 2, 2, 2, 2, 2, 2, 2, 2, 2, 2, 2, 2, 2, 2, 4 ),
 ( 0.000000000000000000, 1.000000000000000000 ),
 ( 0.000000000000000000, 7.083325941644265020E-05, 0.0001416665188328853004, 0.0002124997782493279370, 0.0002479164079575492960, 0.0002833330376657706008, 0.0003187496673739919056, 0.0003541662970822132646, 0.0004249995564986558741, 0.0004604161862068772331, 0.0004781245010609879126, 0.0004958328159150985921, 0.0005312494456233198426, 0.0005666660753315412016, 0.0006374993347479838111, 0.0006729159644562051701, 0.0007083325941644265291, 0.0007437492238726477797, 0.0007791658535808691386, 0.0008145824832890904976, 0.0008499991129973117482, 0.0008854157427055331072, 0.0009208323724137544661, 0.0009562490021219758251, 0.0009916656318301971841, 0.001027082261538418435, 0.001062498891246639685, 0.001133332150663082403, 0.001168748780371303871, 0.001204165410079525121, 0.001239582039787746372, 0.001274998669495967622, 0.001345831928912410340, 0.001381248558620631808, 0.001416665188328853058, 0.001452081818037074309, 0.001469790132891184934, 0.001487498447745295559, 0.001558331707161738277, 0.001629164966578180995, 0.001664581596286402246, 0.001699998225994623496, 0.001735414855702844747, 0.001770831485411066214, 0.001841664744827508932, 0.001877081374535730183, 0.001912498004243951650, 0.001947914633952173118, 0.001983331263660394368, 0.002018747893368615619, 0.002054164523076836869, 0.002124997782493279370, 0.002160414412201500621, 0.002195831041909721872, 0.002231247671617943122, 0.002266664301326164806 ),
 .UNSPECIFIED. ) ;
#49194=CARTESIAN_POINT ( 'NONE',  ( 12.60184172746871845, -1.908867898185656165, -12.56980895172865687 ) ) ;
#49201=CARTESIAN_POINT ( 'NONE',  ( 12.35703415365825997, -3.053811614365077531, 12.22452321716729529 ) ) ;
#49202=CARTESIAN_POINT ( 'NONE',  ( 17.85753477061702199, -1.826313832178724228, 12.46694048874451077 ) ) ;
#49229=CARTESIAN_POINT ( 'NONE',  ( 18.04548494004247772, 2.887558854919742402, 13.58353091070611107 ) ) ;
#49232=ORIENTED_EDGE ( 'NONE', *, *, #21455, .T. ) ;
#49241=CARTESIAN_POINT ( 'NONE',  ( 17.55505043854147118, -3.125000000000000000, -13.52078605991414761 ) ) ;
#49258=CARTESIAN_POINT ( 'NONE',  ( 17.74540238977778728, 1.811773551572771757, 13.88227535917423339 ) ) ;
#49263=CARTESIAN_POINT ( 'NONE',  ( 12.31158149911128596, 3.007516552431691359, -12.23580242208396562 ) ) ;
#49280=CARTESIAN_POINT ( 'NONE',  ( 18.17477462772146524, 0.08167875237853183812, -12.69965198491187230 ) ) ;
#49282=CARTESIAN_POINT ( 'NONE',  ( 12.17997668546742318, 2.480562828885295446, -12.45612489592983074 ) ) ;
#49289=CARTESIAN_POINT ( 'NONE',  ( 18.06139486453144372, 2.995281757671052425, 12.23880324656448693 ) ) ;
#49291=DIRECTION ( 'NONE',  ( -1.000000000000000000, -0.000000000000000000, -0.000000000000000000 ) ) ;
#49294=CARTESIAN_POINT ( 'NONE',  ( 12.35923484894303748, 0.5750310236204370096, -12.58704914195723568 ) ) ;
#49296=CARTESIAN_POINT ( 'NONE',  ( 12.21409778435358184, -2.897922531322536077, 12.26223633105722222 ) ) ;
#49302=CARTESIAN_POINT ( 'NONE',  ( 12.14435919815819176, -0.2964030593063875507, 12.59651778044212378 ) ) ;
#49307=CARTESIAN_POINT ( 'NONE',  ( 12.60240816447940837, 3.091259750208972701, 12.29394167103376390 ) ) ;
#49319=CARTESIAN_POINT ( 'NONE',  ( 17.92027680870444328, -0.6284010951786941357, -12.58437167746846264 ) ) ;
#49320=CARTESIAN_POINT ( 'NONE',  ( 18.00351343197331389, 3.053300080854057796, -12.22464702761365807 ) ) ;
#49322=CARTESIAN_POINT ( 'NONE',  ( 12.15287239299860289, -2.198919866763854092, 13.82623858331039912 ) ) ;
#49328=CYLINDRICAL_SURFACE ( 'NONE', #24823, 0.6250000000000005551 ) ;
#49334=EDGE_CURVE ( 'NONE', #68619, #93, #24142, .T. ) ;
#49342=CARTESIAN_POINT ( 'NONE',  ( 4.599999999999999645, -3.199751711897561801, 12.18694338143115452 ) ) ;
#49347=CARTESIAN_POINT ( 'NONE',  ( 18.08663229464172773, -2.829323725363763753, 13.59808899811969773 ) ) ;
#49352=EDGE_CURVE ( 'NONE', #2919, #11428, #44791, .T. ) ;
#49357=CARTESIAN_POINT ( 'NONE',  ( 17.88638781139529144, 0.6398865404514834099, -12.58374251866278648 ) ) ;
#49371=CARTESIAN_POINT ( 'NONE',  ( 12.28917444793833269, 2.147008681356603610, 13.74197010666757635 ) ) ;
#49372=CARTESIAN_POINT ( 'NONE',  ( 17.66882634972352761, -1.885356762137523345, 12.57375482825836421 ) ) ;
#49374=CARTESIAN_POINT ( 'NONE',  ( 12.18407604397246580, -0.07155107330948952404, 13.89975717292031376 ) ) ;
#49375=ORIENTED_EDGE ( 'NONE', *, *, #10664, .T. ) ;
#49377=DIRECTION ( 'NONE',  ( 0.000000000000000000, -0.9553735099700839672, -0.2954005017724949389 ) ) ;
#49394=CARTESIAN_POINT ( 'NONE',  ( 12.07990771228651461, -0.1878083608152754658, 12.60000737103648660 ) ) ;
#49408=ORIENTED_EDGE ( 'NONE', *, *, #4656, .F. ) ;
#49418=CARTESIAN_POINT ( 'NONE',  ( 12.20071655345841677, 2.340273578635414076, -13.70604138522239523 ) ) ;
#49420=ORIENTED_EDGE ( 'NONE', *, *, #68552, .F. ) ;
#49422=CARTESIAN_POINT ( 'NONE',  ( 12.68599131528412371, -0.7206971133477613201, -13.98143832535762776 ) ) ;
#49431=CARTESIAN_POINT ( 'NONE',  ( 17.63746348810182951, 1.880115813469444230, -13.78555441649718460 ) ) ;
#49446=CARTESIAN_POINT ( 'NONE',  ( 18.11601457983865515, -2.775767521436611318, -13.61104273374189511 ) ) ;
#49451=ORIENTED_EDGE ( 'NONE', *, *, #353, .F. ) ;
#49453=CARTESIAN_POINT ( 'NONE',  ( 18.07822721942930855, -2.978550302103504688, -12.24288824562991174 ) ) ;
#49463=CARTESIAN_POINT ( 'NONE',  ( 12.34743845434965159, 2.926178772989069365, -13.57378949252271028 ) ) ;
#49468=CARTESIAN_POINT ( 'NONE',  ( 18.02507847443574818, 0.4124479947379854905, 13.89177559470776302 ) ) ;
#49473=CARTESIAN_POINT ( 'NONE',  ( 12.31508838531384420, -0.3880332713699820024, 13.89271023030023500 ) ) ;
#49474=ADVANCED_FACE ( 'NONE', ( #61545, #2134, #56305, #23454 ), #24831, .F. ) ;
#49475=CARTESIAN_POINT ( 'NONE',  ( 12.49453886781196310, -0.5425156946746918507, -13.88574935928999921 ) ) ;
#49483=CIRCLE ( 'NONE', #40552, 2.200000000000001954 ) ;
#49488=CARTESIAN_POINT ( 'NONE',  ( 18.03207563512528111, 0.4039503557775008247, 12.69135589213615667 ) ) ;
#49490=CARTESIAN_POINT ( 'NONE',  ( 18.14478511901992874, -2.707036753431580678, -12.40091620384611026 ) ) ;
#49496=CARTESIAN_POINT ( 'NONE',  ( 12.80505043854146940, -1.875000000000000000, 13.78631952119025605 ) ) ;
#49500=FACE_OUTER_BOUND ( 'NONE', #7246, .T. ) ;
#49503=CARTESIAN_POINT ( 'NONE',  ( 12.16275096843966885, 0.3336735144251337659, -12.59558214381612551 ) ) ;
#49520=CARTESIAN_POINT ( 'NONE',  ( 18.09636517151066215, -0.3125842563278192210, -13.89527356689842996 ) ) ;
#49522=FACE_OUTER_BOUND ( 'NONE', #64493, .T. ) ;
#49543=CARTESIAN_POINT ( 'NONE',  ( 18.10394395700119929, -2.009981277211916328, 12.43865165640890069 ) ) ;
#49546=B_SPLINE_CURVE_WITH_KNOTS ( 'NONE', 1,
 ( #9020, #16671 ),
 .UNSPECIFIED., .F., .F.,
 ( 2, 2 ),
 ( 0.000000000000000000, 1.000000000000000000 ),
 .UNSPECIFIED. ) ;
#49576=CARTESIAN_POINT ( 'NONE',  ( 17.91230600709723220, 3.012931617833825904, 13.55113455194568495 ) ) ;
#49577=ADVANCED_FACE ( 'NONE', ( #22242 ), #55203, .T. ) ;
#49589=DIRECTION ( 'NONE',  ( 0.000000000000000000, -1.000000000000000000, -0.000000000000000000 ) ) ;
#49590=CARTESIAN_POINT ( 'NONE',  ( 18.27399547846089689, -2.614774648920896727, -13.75367307402544270 ) ) ;
#49609=B_SPLINE_SURFACE_WITH_KNOTS ( 'NONE', 1, 3, ( 
 ( #49496, #55786, #3914, #25248, #1606, #22924, #44275, #65573, #17696, #39020, #12444, #7198, #60680, #12795, #7534, #28889, #50198, #23618, #44959, #18384, #25600, #41674, #36778, #4606, #32232, #47270, #42025, #16135, #31201, #68573, #15791, #68927, #397, #48292, #52855, #5298, #26978, #10541, #26640, #47957, #58438, #21714, #53545, #31536, #36429, #20696, #31884, #58100, #57746, #9856, #52506, #4954, #25940, #42373, #63326, #15456, #10203, #62646, #21041, #26290, #47616, #15107, #63676, #55, #62980, #37458, #37122, #53197, #21376, #42709, #10888, #64014, #58780, #5635, #14769, #36086, #57401, #9506, #30848, #52160, #4263, #46927, #68230, #20350, #1784, #64702 ),
 ( #60511, #44101, #12620, #59466, #65400, #33260, #59125, #28015, #43050, #12278, #23100, #17871, #16813, #17519, #6319, #33949, #65044, #11564, #7024, #11229, #38492, #64352, #37804, #17159, #59815, #1437, #39188, #55272, #49322, #16474, #32566, #22752, #7368, #38849, #28359, #33604, #50026, #54923, #48644, #53878, #5978, #27318, #60172, #745, #44451, #28709, #2133, #49675, #22058, #65747, #43406, #38140, #11919, #54221, #32907, #27670, #22406, #48985, #1095, #43749, #54578, #6673, #30426, #9087, #13660, #35332, #56984, #40560, #56646, #29753, #39536, #12975, #29409, #39887, #40907, #67461, #18903, #62229, #61887, #45812, #14346, #61207, #2811, #51736, #46157, #24489 ) ),
 .UNSPECIFIED., .F., .F., .F.,
 ( 2, 2 ),
 ( 4, 2, 2, 2, 2, 2, 2, 2, 2, 2, 2, 2, 2, 2, 2, 2, 2, 2, 2, 2, 2, 2, 2, 2, 2, 2, 2, 2, 2, 2, 2, 2, 2, 2, 2, 2, 2, 2, 2, 2, 2, 2, 4 ),
 ( 0.000000000000000000, 1.000000000000000000 ),
 ( 0.000000000000000000, 7.142430198406411052E-05, 0.0001428486039681282210, 0.0002142729059521923315, 0.0002856972079362564421, 0.0003571215099203205526, 0.0004285458119043846631, 0.0004999701138884487736, 0.0005356822648804808289, 0.0005713944158725128841, 0.0006071065668645449394, 0.0006428187178565769946, 0.0007142430198406411052, 0.0007856673218247052157, 0.0008213794728167372709, 0.0008570916238087693262, 0.0008928037748008013814, 0.0009285159257928334367, 0.0009999402277768975472, 0.001071364529760961658, 0.001142788831745025768, 0.001214213133729089879, 0.001285637435713153989, 0.001321349586705186045, 0.001357061737697218100, 0.001428486039681282210, 0.001499910341665346321, 0.001535622492657378376, 0.001571334643649410431, 0.001607046794641442487, 0.001642758945633474542, 0.001714183247617538652, 0.001785607549601602763, 0.001821319700593634818, 0.001857031851585666873, 0.001928456153569730984, 0.001964168304561763039, 0.001999880455553795094, 0.002035592606545827150, 0.002071304757537859205, 0.002142729059521923315, 0.002214153361505987426, 0.002285577663490051536 ),
 .UNSPECIFIED. ) ;
#49612=CARTESIAN_POINT ( 'NONE',  ( 12.43939714311201428, 3.101706251878831644, -12.21226669259267794 ) ) ;
#49622=CARTESIAN_POINT ( 'NONE',  ( 12.60431942020951546, -3.171686099353038024, -12.19427817519220625 ) ) ;
#49630=CARTESIAN_POINT ( 'NONE',  ( 18.17882706751078814, -0.04040257046694439164, -12.69991905489011685 ) ) ;
#49631=CARTESIAN_POINT ( 'NONE',  ( 12.19537138483636873, 2.360847786583726737, -12.48294616049518524 ) ) ;
#49640=CARTESIAN_POINT ( 'NONE',  ( 17.84060712062126086, 3.141591522576398177, 12.20206574396288524 ) ) ;
#49647=CARTESIAN_POINT ( 'NONE',  ( 12.09778329087094839, -2.320992115139767886, 12.38439064982923021 ) ) ;
#49648=EDGE_CURVE ( 'NONE', #9344, #24123, #59856, .T. ) ;
#49655=CARTESIAN_POINT ( 'NONE',  ( 12.27537049189643525, -0.4912829912815118716, 12.59042165808839897 ) ) ;
#49658=CARTESIAN_POINT ( 'NONE',  ( 12.67197039647509982, 3.110753821461598623, 12.28805851341191158 ) ) ;
#49664=CARTESIAN_POINT ( 'NONE',  ( 17.85612272112348364, -0.5477996803818093730, 12.68409554377261905 ) ) ;
#49673=CARTESIAN_POINT ( 'NONE',  ( 18.00435067848273718, 1.907656978610660081, -12.45493970930200511 ) ) ;
#49675=CARTESIAN_POINT ( 'NONE',  ( 12.10494519979310368, -2.707806787687958572, 13.73564420130113994 ) ) ;
#49688=CARTESIAN_POINT ( 'NONE',  ( 17.57589479786107844, 1.875260891896569415, -12.57541370809468440 ) ) ;
#49690=AXIS2_PLACEMENT_3D ( 'NONE', #26686, #31931, #36829 ) ;
#49696=CARTESIAN_POINT ( 'NONE',  ( 12.60033281152288964, -3.091857377022406705, 12.29379371307645208 ) ) ;
#49700=CARTESIAN_POINT ( 'NONE',  ( 17.99129208686614945, -2.947687251868547520, 13.56825406139790680 ) ) ;
#49724=CARTESIAN_POINT ( 'NONE',  ( 12.31340688242389625, 2.113974262928780767, 13.74774419251637880 ) ) ;
#49728=CARTESIAN_POINT ( 'NONE',  ( 12.40062321164033499, -0.4766231184928889086, 13.88900205690512735 ) ) ;
#49738=LINE ( 'NONE', #59875, #17948 ) ;
#49774=CARTESIAN_POINT ( 'NONE',  ( 12.43753697073189279, 3.107573092027756001, 12.21083123505777479 ) ) ;
#49777=CARTESIAN_POINT ( 'NONE',  ( 12.08233492791619490, -0.05915529127692992217, -13.99988012777929036 ) ) ;
#49782=CARTESIAN_POINT ( 'NONE',  ( 5.536712913981922668, 12.19258561489269255, -3.773936784932935051 ) ) ;
#49784=B_SPLINE_CURVE_WITH_KNOTS ( 'NONE', 3,
 ( #45903, #68585, #57757, #58451, #9516, #15466, #16146, #47283, #37132, #36792, #47629, #42721, #30859, #37468, #63689, #67905, #58795, #68240, #36098, #57414, #3924, #25262, #20022, #21051, #15120, #14779, #46600, #25610, #15804, #4275, #68938, #52174, #47967, #46938, #58113, #10554, #63338, #5309, #25950, #10213, #20707, #30514, #41347, #4968, #31896, #53208, #52866, #42383, #62992, #20362, #41686, #26651, #36439 ),
 .UNSPECIFIED., .F., .F.,
 ( 4, 2, 2, 2, 2, 2, 2, 2, 2, 2, 2, 2, 2, 1, 2, 2, 2, 2, 2, 2, 2, 2, 2, 2, 1, 1, 2, 4 ),
 ( 0.000000000000000000, 0.06264497286344758442, 0.1252899457268951688, 0.1566124321586186696, 0.1879349185903421704, 0.2192574050220656989, 0.2349186482379256591, 0.2505798914537856192, 0.2819023778855022089, 0.2975636211013604759, 0.3132248643172187430, 0.3288861075330770101, 0.3445473507489353326, 0.3602085939647935997, 0.3680392155727237880, 0.3758698371806540317, 0.3915310803965136865, 0.3993617020044440968, 0.4071923236123745071, 0.4228535668282352722, 0.4306841884361666262, 0.4385148100440979246, 0.4541760532599614653, 0.4698372964758249504, 0.4854985396916884910, 0.4933291612996200115, 0.4972444721035861326, 0.5011597829075521426 ),
 .UNSPECIFIED. ) ;
#49786=CARTESIAN_POINT ( 'NONE',  ( 17.74479774746056293, 3.223061189501813750, -13.62394687717147335 ) ) ;
#49794=ADVANCED_FACE ( 'NONE', ( #61220 ), #5161, .T. ) ;
#49795=CARTESIAN_POINT ( 'NONE',  ( 17.81256277267584309, 1.835326726223542426, -13.87917840078988263 ) ) ;
#49796=CARTESIAN_POINT ( 'NONE',  ( 17.97807132158231980, 0.4608801934710635706, -12.68876176375646736 ) ) ;
#49802=CARTESIAN_POINT ( 'NONE',  ( 18.18005043857346692, -2.459498578984929296, 13.68200151021939348 ) ) ;
#49807=CARTESIAN_POINT ( 'NONE',  ( 18.17187109576076764, -2.859211385468993782, -12.27132042014886970 ) ) ;
#49817=CARTESIAN_POINT ( 'NONE',  ( 12.72264977853953027, 3.119885623323980006, -13.52225790872756228 ) ) ;
#49820=CARTESIAN_POINT ( 'NONE',  ( 18.01141113125041571, 0.4275223103465155550, 13.89116040406442032 ) ) ;
#49837=EDGE_CURVE ( 'NONE', #31652, #25814, #61902, .T. ) ;
#49839=CARTESIAN_POINT ( 'NONE',  ( 17.84124069827834091, 0.5557204214162413392, 12.68363025601216520 ) ) ;
#49854=CARTESIAN_POINT ( 'NONE',  ( 12.30932062623504741, -0.5250004125410564493, -12.58906021966015842 ) ) ;
#49871=CARTESIAN_POINT ( 'NONE',  ( 18.15028930682391106, 0.1908382484571590487, -13.89824168789394854 ) ) ;
#49877=VECTOR ( 'NONE', #66531, 1000.000000000000227 ) ;
#49880=CARTESIAN_POINT ( 'NONE',  ( 18.16572637375661969, -2.633126308906749369, 12.41957822429843539 ) ) ;
#49884=CARTESIAN_POINT ( 'NONE',  ( 12.49122810692607288, -3.040889930152274268, -13.54369178477776714 ) ) ;
#49895=CARTESIAN_POINT ( 'NONE',  ( 17.89568490471444662, -3.024116370425395939, 12.31388631808445133 ) ) ;
#49900=CARTESIAN_POINT ( 'NONE',  ( 18.15909587493458233, 2.338249772848897123, 13.70640098171117671 ) ) ;
#49927=CARTESIAN_POINT ( 'NONE',  ( 18.27459401263892502, 2.425695574333697646, 13.78827716170582285 ) ) ;
#49939=CARTESIAN_POINT ( 'NONE',  ( 17.87779404330691690, -3.171907921506158967, -13.63594617280361199 ) ) ;
#49959=CARTESIAN_POINT ( 'NONE',  ( 12.33364759508187802, 3.027124203391257762, -12.23096800428945663 ) ) ;
#49969=CARTESIAN_POINT ( 'NONE',  ( 12.47010838183371462, -1.842148406394420013, -12.46461078478868423 ) ) ;
#49976=CARTESIAN_POINT ( 'NONE',  ( 12.36880880067038291, -2.947687262017098409, -13.56819815501604154 ) ) ;
#49977=CARTESIAN_POINT ( 'NONE',  ( 18.03207563512528111, -0.4039503557775012688, -12.69135589213616377 ) ) ;
#49980=CARTESIAN_POINT ( 'NONE',  ( 12.21062133718143627, 2.693099985209356451, -12.40450382421715680 ) ) ;
#49985=ADVANCED_FACE ( 'NONE', ( #19201, #67426, #68113, #41219 ), #20231, .F. ) ;
#49987=SURFACE_STYLE_FILL_AREA ( #22714 ) ;
#49989=DIRECTION ( 'NONE',  ( 0.000000000000000000, 1.000000000000000000, 0.000000000000000000 ) ) ;
#49992=CARTESIAN_POINT ( 'NONE',  ( 17.86252378965066612, 3.131846597291652046, 12.20457061699601731 ) ) ;
#49993=CARTESIAN_POINT ( 'NONE',  ( 17.55505043854144276, 0.6250000000000001110, -13.88107975066922428 ) ) ;
#49997=CARTESIAN_POINT ( 'NONE',  ( 12.15762345757241825, 0.3746922850242029313, -12.59513687151644845 ) ) ;
#49999=CARTESIAN_POINT ( 'NONE',  ( 12.20120475779648572, -2.662482513922677985, 12.41227208748765598 ) ) ;
#50002=DIRECTION ( 'NONE',  ( 1.000000000000000000, 0.000000000000000000, 0.000000000000000000 ) ) ;
#50004=CARTESIAN_POINT ( 'NONE',  ( 12.68606859785047725, -0.7096370184368634426, 12.58000072970462924 ) ) ;
#50007=CARTESIAN_POINT ( 'NONE',  ( 12.80505043854143388, 1.875000000000000000, -13.78631952119025428 ) ) ;
#50015=CARTESIAN_POINT ( 'NONE',  ( 17.72542258371771950, -0.6019459913954784414, 12.68079480700004957 ) ) ;
#50024=CARTESIAN_POINT ( 'NONE',  ( 18.09696660045537442, -2.811537062166766354, 13.60243477577289717 ) ) ;
#50026=CARTESIAN_POINT ( 'NONE',  ( 12.09788000779848183, -2.355563551342477968, 13.80043034480240394 ) ) ;
#50039=CARTESIAN_POINT ( 'NONE',  ( 17.83452421831947987, 1.940868773865736197, -12.56443418441918425 ) ) ;
#50047=CARTESIAN_POINT ( 'NONE',  ( 12.52707377837015024, -3.060156797972230169, 12.30326077405791274 ) ) ;
#50054=CARTESIAN_POINT ( 'NONE',  ( 18.08228063350341230, -2.164202898012135279, 13.73897034938254613 ) ) ;
#50071=CARTESIAN_POINT ( 'NONE',  ( 5.700000000000000178, 11.06886219213000011, -1.536526853569999851 ) ) ;
#50076=CARTESIAN_POINT ( 'NONE',  ( 12.30715842069478505, 2.122066859011512818, 13.74633992746440114 ) ) ;
#50080=CARTESIAN_POINT ( 'NONE',  ( 12.70954970454857502, 0.7242550212505937113, 13.98125389334239799 ) ) ;
#50103=EDGE_LOOP ( 'NONE', ( #19069, #22616, #62761, #18196, #25383 ) ) ;
#50126=CARTESIAN_POINT ( 'NONE',  ( 17.65075606732844449, 1.792616958745788525, -13.88476197432903092 ) ) ;
#50127=CARTESIAN_POINT ( 'NONE',  ( 12.64343601369307279, 0.6040897852209334840, -13.88232707694115398 ) ) ;
#50134=CARTESIAN_POINT ( 'NONE',  ( 5.666085114159494118, 12.07002994274871099, -3.732314430517552850 ) ) ;
#50137=CARTESIAN_POINT ( 'NONE',  ( 18.17999014114397482, 2.522019970189117277, -13.66878426939142877 ) ) ;
#50145=CARTESIAN_POINT ( 'NONE',  ( 17.93439305972981401, 0.4967428619047934979, -12.68692192486979486 ) ) ;
#50146=CARTESIAN_POINT ( 'NONE',  ( 21.54999911806000057, -1.749711486808999826E-13, -3.819167204710999825E-14 ) ) ;
#50150=CARTESIAN_POINT ( 'NONE',  ( 17.94172469444382401, -2.002341272864497146, 13.76666224253383142 ) ) ;
#50156=CARTESIAN_POINT ( 'NONE',  ( 18.23533704695771362, -2.231030541001939760, -12.40091240268597694 ) ) ;
#50163=B_SPLINE_CURVE_WITH_KNOTS ( 'NONE', 3,
 ( #23229, #44575, #33380, #40009, #65519, #60632, #22877, #44227, #38971, #54697, #7486, #55044, #60980, #33031, #18335, #29178, #28131, #13092, #44909, #12396, #60289, #49446, #1555, #33727, #28839, #66213, #28483, #38616, #65867, #2254, #34427, #12047, #6446, #6794, #39311, #55739, #50485, #45252, #54343, #66558, #27796, #49103, #1215, #22527, #13778, #19357 ),
 .UNSPECIFIED., .F., .F.,
 ( 4, 2, 2, 2, 2, 1, 2, 2, 2, 1, 2, 2, 2, 2, 2, 2, 1, 2, 2, 1, 2, 2, 2, 2, 4 ),
 ( 0.4988098180369952006, 0.5301342044096829520, 0.5457963975960268277, 0.5614585907823708144, 0.5653741390789567278, 0.5692896873755427523, 0.5771207839687148011, 0.5927829771550601201, 0.6006140737482328351, 0.6084451703414054391, 0.6241073635277518683, 0.6397695567140984085, 0.6554317499004448377, 0.6710939430867912669, 0.6867561362731376962, 0.7024183294594841254, 0.7180805226458306656, 0.7494049090185193052, 0.7650671022048636249, 0.7807292953912079447, 0.8120536817638925875, 0.8433780681365772303, 0.8747024545092618730, 0.9373512272546309365, 1.000000000000000000 ),
 .UNSPECIFIED. ) ;
#50168=CARTESIAN_POINT ( 'NONE',  ( 12.08613047971136467, 2.614761652440394268, -13.75367554324229680 ) ) ;
#50171=CARTESIAN_POINT ( 'NONE',  ( 18.09636517151065860, 0.3125842563278199426, 13.89527356689843884 ) ) ;
#50172=CARTESIAN_POINT ( 'NONE',  ( 17.72543224092255798, 0.6019432101436682503, 13.88245510389148230 ) ) ;
#50177=CARTESIAN_POINT ( 'NONE',  ( 12.23478023522865321, -0.2564316839802910364, 13.89683092737489822 ) ) ;
#50178=CARTESIAN_POINT ( 'NONE',  ( 12.22445506978716168, -2.731418685756656473, 13.62164890397837347 ) ) ;
#50183=DIRECTION ( 'NONE',  ( 1.000000000000000000, 0.000000000000000000, 0.000000000000000000 ) ) ;
#50189=EDGE_CURVE ( 'NONE', #59809, #18846, #283, .T. ) ;
#50192=CARTESIAN_POINT ( 'NONE',  ( 12.21931228141710690, -0.2190605493744586796, 12.69747807323868116 ) ) ;
#50193=CARTESIAN_POINT ( 'NONE',  ( 18.15011306042656969, -2.691200174357349706, -12.40496142758472509 ) ) ;
#50196=CARTESIAN_POINT ( 'NONE',  ( 12.61270316628418975, -1.780234759020672852, -12.47365767676673798 ) ) ;
#50198=CARTESIAN_POINT ( 'NONE',  ( 12.39034978066174197, -2.032288297489023066, 13.76160266677045740 ) ) ;
#50205=CARTESIAN_POINT ( 'NONE',  ( 12.08032332909579765, 0.02297882141077639551, -12.59998453421652442 ) ) ;
#50206=DIRECTION ( 'NONE',  ( 1.000000000000000000, 0.000000000000000000, 0.000000000000000000 ) ) ;
#50214=CARTESIAN_POINT ( 'NONE',  ( 12.80505043854143388, 1.798940460745208636, 12.50936912696000469 ) ) ;
#50221=CARTESIAN_POINT ( 'NONE',  ( 18.26375728754769767, -0.1544074001204070734, -13.99915345895492003 ) ) ;
#50227=CARTESIAN_POINT ( 'NONE',  ( 18.14658900058367408, -2.701839613306171728, 12.40227423849764321 ) ) ;
#50240=CARTESIAN_POINT ( 'NONE',  ( 12.34820889858482396, -0.4270206790917092654, -13.89118144889037509 ) ) ;
#50241=CARTESIAN_POINT ( 'NONE',  ( 17.68813047654961323, -3.110753822336481011, 12.28807462416255092 ) ) ;
#50274=CARTESIAN_POINT ( 'NONE',  ( 18.23381869303822356, 2.775531333002567713, 13.72213247881303033 ) ) ;
#50285=CARTESIAN_POINT ( 'NONE',  ( 17.99827832423969909, -3.095912246742690499, -13.65340184222058184 ) ) ;
#50304=CARTESIAN_POINT ( 'NONE',  ( 12.80505043854144276, -0.6250000000000001110, -13.88107975066922428 ) ) ;
#50310=CARTESIAN_POINT ( 'NONE',  ( 12.15423239032306668, 2.797846099084077665, -12.28544569950199516 ) ) ;
#50319=CARTESIAN_POINT ( 'NONE',  ( 12.21223476585298862, -2.065380716993684196, -12.42958554107382163 ) ) ;
#50325=CARTESIAN_POINT ( 'NONE',  ( 12.80505043854146940, -1.875000000000000444, -25.00000000000000000 ) ) ;
#50326=CARTESIAN_POINT ( 'NONE',  ( 12.26307976823776968, -2.811936524129938331, -13.60229516772050040 ) ) ;
#50327=CARTESIAN_POINT ( 'NONE',  ( 18.11574795581002562, -0.2761699508452428176, -12.69595998167825357 ) ) ;
#50331=VERTEX_POINT ( 'NONE', #43197 ) ;
#50332=( NAMED_UNIT ( * ) SI_UNIT ( $, .STERADIAN. ) SOLID_ANGLE_UNIT ( ) );
#50337=CARTESIAN_POINT ( 'NONE',  ( 18.14814637199130232, 2.302603452852429733, 12.49536313902244622 ) ) ;
#50342=CARTESIAN_POINT ( 'NONE',  ( 12.44006281454390717, -0.6285461057554440067, -12.58436427553342618 ) ) ;
#50344=CARTESIAN_POINT ( 'NONE',  ( 12.31295406811165449, -2.114551508724276108, 12.53308940647968939 ) ) ;
#50350=CARTESIAN_POINT ( 'NONE',  ( 12.57519818727761596, 0.5812897767837151841, 12.68208758371477352 ) ) ;
#50366=CARTESIAN_POINT ( 'NONE',  ( 17.97862686927833309, -0.4596875344175958000, -12.68880368817494642 ) ) ;
#50370=CARTESIAN_POINT ( 'NONE',  ( 17.57587252603351402, -1.875000554927097607, -13.78627161177572269 ) ) ;
#50371=CARTESIAN_POINT ( 'NONE',  ( 4.599999999999999645, -0.7192913403693006469, 12.57945229203838444 ) ) ;
#50379=CARTESIAN_POINT ( 'NONE',  ( 17.55505043854143565, 1.875000000000000000, -13.78631952119025073 ) ) ;
#50387=VECTOR ( 'NONE', #34442, 1000.000000000000114 ) ;
#50390=CARTESIAN_POINT ( 'NONE',  ( 17.55505043854143921, 0.7302158263239199032, -13.98094363220830871 ) ) ;
#50392=CARTESIAN_POINT ( 'NONE',  ( 12.18033843151457063, -2.521515055314785592, 12.44655896212852930 ) ) ;
#50395=CARTESIAN_POINT ( 'NONE',  ( 18.14566850323243230, -2.942004589604671150, 13.68740344564952416 ) ) ;
#50415=CARTESIAN_POINT ( 'NONE',  ( 12.68504826104523175, 3.238474326485677679, 13.62029029943391834 ) ) ;
#50418=CARTESIAN_POINT ( 'NONE',  ( 12.21236377913539961, 0.1994069032837916255, -12.69791261745714905 ) ) ;
#50419=CARTESIAN_POINT ( 'NONE',  ( 12.66324396017929388, -0.6090406077983148148, 13.88203505342131550 ) ) ;
#50424=LINE ( 'NONE', #45189, #45110 ) ;
#50425=DIRECTION ( 'NONE',  ( 0.000000000000000000, 0.000000000000000000, 1.000000000000000000 ) ) ;
#50430=CARTESIAN_POINT ( 'NONE',  ( 12.45041481799818506, 3.107897655637143153, 12.21069225363714494 ) ) ;
#50448=CARTESIAN_POINT ( 'NONE',  ( 12.31588542590557722, 2.889160216979992590, 13.58313038422180696 ) ) ;
#50456=CARTESIAN_POINT ( 'NONE',  ( 18.24702988622816591, 2.264821834935298206, -12.39478563874201633 ) ) ;
#50463=EDGE_LOOP ( 'NONE', ( #31239, #44280, #9222, #35074, #40338 ) ) ;
#50465=CARTESIAN_POINT ( 'NONE',  ( 12.44955560269365158, 0.5141525164327367392, -13.88720023103245360 ) ) ;
#50474=CARTESIAN_POINT ( 'NONE',  ( 18.04669395734977044, 2.113974215446797089, -13.74779306078356456 ) ) ;
#50485=CARTESIAN_POINT ( 'NONE',  ( 17.92070696550175768, -3.007249353073734088, -13.55264287718867244 ) ) ;
#50493=CARTESIAN_POINT ( 'NONE',  ( 18.27918563591884293, -2.436421501371052400, -12.36221688302662791 ) ) ;
#50503=CYLINDRICAL_SURFACE ( 'NONE', #54878, 2.000000000000000444 ) ;
#50507=CARTESIAN_POINT ( 'NONE',  ( 12.08107629042315700, 2.473358331846538860, -13.77980712931822183 ) ) ;
#50510=CARTESIAN_POINT ( 'NONE',  ( 17.65055117253430339, -0.7242550212505970419, 13.98125389334239799 ) ) ;
#50511=CARTESIAN_POINT ( 'NONE',  ( 18.17229989573039717, -2.399660445407139076, 12.47442500975930635 ) ) ;
#50516=CARTESIAN_POINT ( 'NONE',  ( 12.20341915911530961, -2.330389505191049704, 13.70797212925131348 ) ) ;
#50518=EDGE_CURVE ( 'NONE', #37829, #20140, #21354, .T. ) ;
#50519=ADVANCED_FACE ( 'NONE', ( #38118 ), #32543, .T. ) ;
#50527=ADVANCED_FACE ( 'NONE', ( #43724 ), #36545, .T. ) ;
#50528=CARTESIAN_POINT ( 'NONE',  ( 12.80505043854144098, 0.7302158263239095781, 13.98094363220830871 ) ) ;
#50530=CARTESIAN_POINT ( 'NONE',  ( 17.74668184667432769, 0.5949840079737193088, 12.68123264482375490 ) ) ;
#50531=CARTESIAN_POINT ( 'NONE',  ( 12.35320888692065999, -0.4320279633463514068, 12.69011309769952867 ) ) ;
#50535=CARTESIAN_POINT ( 'NONE',  ( 12.15446082642243830, -2.110350925006974077, -12.42276656537216084 ) ) ;
#50541=ADVANCED_FACE ( 'NONE', ( #5610 ), #16429, .F. ) ;
#50545=CARTESIAN_POINT ( 'NONE',  ( 12.29717897459458875, -0.3644117276601275823, -12.69296657371244841 ) ) ;
#50558=ORIENTED_EDGE ( 'NONE', *, *, #68167, .F. ) ;
#50563=CARTESIAN_POINT ( 'NONE',  ( 18.05077945915501303, -0.5329747956505088702, -13.98985355243729423 ) ) ;
#50567=CARTESIAN_POINT ( 'NONE',  ( 4.599999999999999645, 1.875000000000000000, 13.78627172894481667 ) ) ;
#50577=ORIENTED_EDGE ( 'NONE', *, *, #46884, .F. ) ;
#50587=CARTESIAN_POINT ( 'NONE',  ( 12.18004362304668575, -0.009762789003247420577, -13.90000041479088289 ) ) ;
#50588=CARTESIAN_POINT ( 'NONE',  ( 18.03475265876380007, -2.099231872491031936, 12.53598779768162785 ) ) ;
#50593=CARTESIAN_POINT ( 'NONE',  ( 18.18005044575082252, 2.500000006795693785, 13.67340643792831045 ) ) ;
#50611=CARTESIAN_POINT ( 'NONE',  ( 18.08442823429787794, -0.4920215530101185175, 12.59040071882420797 ) ) ;
#50618=CARTESIAN_POINT ( 'NONE',  ( 18.03607885879097594, 1.971554139641144454, 13.86048489721954624 ) ) ;
#50651=CARTESIAN_POINT ( 'NONE',  ( 21.47500033997000202, 7.283063041541000399E-14, -6.705747068735999778E-14 ) ) ;
#50653=CARTESIAN_POINT ( 'NONE',  ( 12.34586232581678900, 2.075512354070471410, -12.54043254740683899 ) ) ;
#50658=B_SPLINE_CURVE_WITH_KNOTS ( 'NONE', 3,
 ( #9948, #52944, #31285, #26030, #47360, #15542, #36871, #10289, #33696 ),
 .UNSPECIFIED., .F., .F.,
 ( 4, 1, 2, 2, 4 ),
 ( 0.000000000000000000, 0.2499999999999983902, 0.3749999999999983347, 0.4999999999999983347, 1.000000000000000000 ),
 .UNSPECIFIED. ) ;
#50663=CARTESIAN_POINT ( 'NONE',  ( 12.22616922475387291, -2.046442494456577332, -12.43271557125384419 ) ) ;
#50668=EDGE_CURVE ( 'NONE', #33164, #21338, #61103, .T. ) ;
#50680=( NAMED_UNIT ( * ) SI_UNIT ( $, .STERADIAN. ) SOLID_ANGLE_UNIT ( ) );
#50682=CARTESIAN_POINT ( 'NONE',  ( 17.83309906212661744, 3.060119824089694962, 13.53852211359576785 ) ) ;
#50684=CARTESIAN_POINT ( 'NONE',  ( 17.76275439675989887, 1.910499210220269362, 12.56953514877129940 ) ) ;
#50689=CARTESIAN_POINT ( 'NONE',  ( 12.19329499274041773, -2.371606608387609505, 12.48058234101797126 ) ) ;
#50696=CARTESIAN_POINT ( 'NONE',  ( 12.21327642329898389, 0.2013262877421457264, 12.69785743964334834 ) ) ;
#50699=CARTESIAN_POINT ( 'NONE',  ( 12.47171258541602512, 1.971212359000195313, 12.55915788719762993 ) ) ;
#50711=EDGE_CURVE ( 'NONE', #48720, #64156, #28686, .T. ) ;
#50713=CARTESIAN_POINT ( 'NONE',  ( 18.08654171825435597, -2.829006819437166254, 13.59815647009357953 ) ) ;
#50724=CARTESIAN_POINT ( 'NONE',  ( 18.14740543753152124, 2.299612738907994114, -13.71393688410719491 ) ) ;
#50726=CARTESIAN_POINT ( 'NONE',  ( 17.81163220004817660, -0.5699871458820113812, 13.88426688812672971 ) ) ;
#50737=CARTESIAN_POINT ( 'NONE',  ( 12.39978108236764598, -2.975905172436775992, 12.32787332407853143 ) ) ;
#50741=CARTESIAN_POINT ( 'NONE',  ( 17.72176632460248769, -3.228945123492078739, 13.62255252064306354 ) ) ;
#50766=CARTESIAN_POINT ( 'NONE',  ( 12.18011073905423736, 2.522020058064990522, 13.66873259811636032 ) ) ;
#50769=CARTESIAN_POINT ( 'NONE',  ( 12.24304070169736747, 0.2736148576388583442, -12.69603606445786959 ) ) ;
#50770=CARTESIAN_POINT ( 'NONE',  ( 12.63955452181609651, 0.7113363331415045732, 13.98191770012929958 ) ) ;
#50784=CARTESIAN_POINT ( 'NONE',  ( 12.78084604758900333, 3.199697762315041771, 12.18695750762853081 ) ) ;
#50791=CARTESIAN_POINT ( 'NONE',  ( 12.18494477640587270, 2.419331844832663503, 12.47000601351364324 ) ) ;
#50793=ORIENTED_EDGE ( 'NONE', *, *, #29393, .F. ) ;
#50803=CARTESIAN_POINT ( 'NONE',  ( 12.72092075291582880, 3.120619064207561077, 13.52200130461806005 ) ) ;
#50807=CARTESIAN_POINT ( 'NONE',  ( 18.13398081625433633, 2.046400819240500546, -12.43272243325428406 ) ) ;
#50810=CARTESIAN_POINT ( 'NONE',  ( 12.26369778066962901, 2.812515541859847534, -13.60219590383643684 ) ) ;
#50815=CARTESIAN_POINT ( 'NONE',  ( 12.75722769875344476, -0.7290248443971383274, -13.98100598729141097 ) ) ;
#50823=CARTESIAN_POINT ( 'NONE',  ( 17.88735652878715499, 1.970265470216408410, -13.77164815731349634 ) ) ;
#50841=CARTESIAN_POINT ( 'NONE',  ( 18.05422494319417481, -1.958382419481337955, -12.44687927882536194 ) ) ;
#50842=AXIS2_PLACEMENT_3D ( 'NONE', #20397, #3286, #57796 ) ;
#50853=CARTESIAN_POINT ( 'NONE',  ( 12.38095956647852880, 3.110256499846526079, -13.65014134263124390 ) ) ;
#50857=CARTESIAN_POINT ( 'NONE',  ( 18.26112155826667305, 0.1662062226620437122, 13.99901824074930978 ) ) ;
#50873=CARTESIAN_POINT ( 'NONE',  ( 12.07990818254330989, 0.1906559481176479942, 14.00000681886699816 ) ) ;
#50875=CARTESIAN_POINT ( 'NONE',  ( 17.55505043854144631, 0.6250000000000001110, 12.67928921589117586 ) ) ;
#50876=CARTESIAN_POINT ( 'NONE',  ( 12.60485626885975030, -0.5921620644301640590, 12.68141136812944758 ) ) ;
#50889=CARTESIAN_POINT ( 'NONE',  ( 12.51625386035102139, 0.6598665579121970604, -12.58271022457859978 ) ) ;
#50906=CARTESIAN_POINT ( 'NONE',  ( 18.16428164030675418, -0.3960277493246738278, -13.99440111282555499 ) ) ;
#50915=EDGE_CURVE ( 'NONE', #11428, #25814, #38542, .T. ) ;
#50917=CARTESIAN_POINT ( 'NONE',  ( 12.18032316970823992, -2.521073842608297255, -13.66891947082361369 ) ) ;
#50926=CARTESIAN_POINT ( 'NONE',  ( 12.80505043854144276, 0.6249999999999994449, 12.67928921589117586 ) ) ;
#50928=CARTESIAN_POINT ( 'NONE',  ( 12.39257741226468745, -0.4700078255514623660, -13.88931146942755390 ) ) ;
#50929=CARTESIAN_POINT ( 'NONE',  ( 18.08682736286122150, -2.829024318083993794, 12.36883279713290484 ) ) ;
#50932=ORIENTED_EDGE ( 'NONE', *, *, #51607, .F. ) ;
#50953=CARTESIAN_POINT ( 'NONE',  ( 17.71955056974169906, -0.7009231686363515124, 12.58048995873113896 ) ) ;
#50959=CARTESIAN_POINT ( 'NONE',  ( 18.23099845246958850, 2.253777188809247711, 13.81740256423587709 ) ) ;
#50972=CARTESIAN_POINT ( 'NONE',  ( 17.91962727382265541, -3.149549635603927200, -13.64113161598087665 ) ) ;
#50984=ORIENTED_EDGE ( 'NONE', *, *, #3173, .F. ) ;
#50994=CARTESIAN_POINT ( 'NONE',  ( 12.26301939624441317, 2.811829068737871307, -12.37346575716765962 ) ) ;
#51004=CARTESIAN_POINT ( 'NONE',  ( 12.44904482565497794, -1.853472941501686400, -12.46293187093603017 ) ) ;
#51010=CARTESIAN_POINT ( 'NONE',  ( 12.27346860450520261, -2.829323760734076210, -13.59803440778111572 ) ) ;
#51020=CARTESIAN_POINT ( 'NONE',  ( 18.16776742079087725, 2.623333169980955670, 13.64647547701603614 ) ) ;
#51024=CARTESIAN_POINT ( 'NONE',  ( 17.91037351677406875, 3.107515944418832277, 12.21078942061118511 ) ) ;
#51027=AXIS2_PLACEMENT_3D ( 'NONE', #43497, #47365, #37896 ) ;
#51030=CARTESIAN_POINT ( 'NONE',  ( 12.18012697958979906, -2.522451323245133548, 12.44635604318887623 ) ) ;
#51036=CARTESIAN_POINT ( 'NONE',  ( 12.29127437512780396, 0.3560396104572040588, 12.69328656575055980 ) ) ;
#51040=CARTESIAN_POINT ( 'NONE',  ( 12.27169925567829623, 2.173540117687664086, 12.52166307684904112 ) ) ;
#51041=EDGE_LOOP ( 'NONE', ( #1042, #57087, #44505, #3617 ) ) ;
#51049=ORIENTED_EDGE ( 'NONE', *, *, #20204, .T. ) ;
#51051=CARTESIAN_POINT ( 'NONE',  ( 18.14735902876271467, -0.1997594609313395053, -12.69789023917851090 ) ) ;
#51059=FACE_OUTER_BOUND ( 'NONE', #21496, .T. ) ;
#51062=EDGE_CURVE ( 'NONE', #37575, #48333, #56668, .T. ) ;
#51078=CARTESIAN_POINT ( 'NONE',  ( 17.93599053679682243, 0.4959091552601219144, -13.88809952003718173 ) ) ;
#51080=CARTESIAN_POINT ( 'NONE',  ( 12.72076653475835428, -3.120601141703879922, 12.28508997180244755 ) ) ;
#51084=CARTESIAN_POINT ( 'NONE',  ( 18.03491643637242348, -3.065379368238255964, 13.66028979695642853 ) ) ;
#51095=CARTESIAN_POINT ( 'NONE',  ( 18.17115522622104606, -0.3798658283128687474, -12.59428767283705319 ) ) ;
#51107=CARTESIAN_POINT ( 'NONE',  ( 12.17639632831536467, 2.882401473261805069, 13.70008095139100135 ) ) ;
#51110=CARTESIAN_POINT ( 'NONE',  ( 12.28050398187715153, -0.3399395272364318932, -12.69387965975802146 ) ) ;
#51117=COLOUR_RGB ( '', 0.09019608, 0.27058824, 0.51372549) ;
#51121=B_SPLINE_CURVE_WITH_KNOTS ( 'NONE', 1,
 ( #27786, #11005 ),
 .UNSPECIFIED., .F., .F.,
 ( 2, 2 ),
 ( 0.000000000000000000, 1.000000000000000000 ),
 .UNSPECIFIED. ) ;
#51124=CARTESIAN_POINT ( 'NONE',  ( 12.75685601902876343, 3.198499228556002105, 12.18727240180921179 ) ) ;
#51140=EDGE_CURVE ( 'NONE', #6955, #48764, #62793, .T. ) ;
#51141=EDGE_CURVE ( 'NONE', #57880, #1963, #40447, .T. ) ;
#51152=CARTESIAN_POINT ( 'NONE',  ( 17.72222400754427696, 1.779821952440179045, -12.47366250980180702 ) ) ;
#51155=CARTESIAN_POINT ( 'NONE',  ( 12.24837323144403278, 2.784344744724901677, -13.60903177733648306 ) ) ;
#51158=ORIENTED_EDGE ( 'NONE', *, *, #63288, .F. ) ;
#51159=CARTESIAN_POINT ( 'NONE',  ( 17.92254446305189575, 3.154612309636608547, -13.64000973911191217 ) ) ;
#51162=CARTESIAN_POINT ( 'NONE',  ( 18.10163077481709237, -2.185641740717685799, -13.73537224937313184 ) ) ;
#51163=B_SPLINE_CURVE_WITH_KNOTS ( 'NONE', 3,
 ( #12729, #7130, #12029, #17631, #50134, #33365, #54327, #44560, #12379, #1200, #39295, #23553, #17273, #29162, #55030, #6426, #28468, #33711, #66197, #49782, #22508 ),
 .UNSPECIFIED., .F., .F.,
 ( 4, 2, 2, 2, 1, 2, 2, 1, 1, 2, 2, 4 ),
 ( 0.000000000000000000, 0.1249999999999764355, 0.1874999999999669154, 0.2499999999999574229, 0.3124999999999479305, 0.3437499999999464873, 0.3749999999999449884, 0.4374999999999377165, 0.4687499999999341083, 0.4843749999999329425, 0.4999999999999318323, 1.000000000000000000 ),
 .UNSPECIFIED. ) ;
#51170=CARTESIAN_POINT ( 'NONE',  ( 18.02597764372132971, 3.073197451853422191, -13.65853278380549263 ) ) ;
#51189=CARTESIAN_POINT ( 'NONE',  ( 17.87014202174174926, -1.960141137139741252, -12.56108054050352685 ) ) ;
#51195=FACE_OUTER_BOUND ( 'NONE', #68454, .T. ) ;
#51200=CARTESIAN_POINT ( 'NONE',  ( 12.33301873031881613, 1.963679441452095720, -13.86160245617593212 ) ) ;
#51202=CARTESIAN_POINT ( 'NONE',  ( 18.18297552798360783, 0.3652063536484332906, 13.99523956222174270 ) ) ;
#51208=CARTESIAN_POINT ( 'NONE',  ( 12.22115613549653546, -2.722964197143763254, 13.62363865713189526 ) ) ;
#51214=LINE ( 'NONE', #62715, #57593 ) ;
#51231=CARTESIAN_POINT ( 'NONE',  ( 12.47306973639847349, 0.6395598188657407590, -12.58375915074078577 ) ) ;
#51238=PRODUCT_CONTEXT ( 'NONE', #21734, 'mechanical' ) ;
#51241=B_SPLINE_CURVE_WITH_KNOTS ( 'NONE', 3,
 ( #34295, #2468, #8747, #23793, #66090, #28707, #30092, #44788, #45127, #3492, #66435, #44448, #18557, #39185, #61203, #29405, #65745, #60509, #12616, #33947, #13658, #55269, #50713, #50024, #2131, #23451, #18209, #2809, #24137, #4175, #36696, #58017, #68838, #9418, #51734, #56982, #15021, #25853, #52769, #47184, #15368, #41591, #25513, #10119, #20956, #20263, #46155, #10455, #31450, #58353, #15710 ),
 .UNSPECIFIED., .F., .F.,
 ( 4, 2, 2, 2, 2, 2, 2, 2, 2, 2, 2, 2, 2, 1, 2, 2, 2, 2, 2, 2, 2, 2, 2, 2, 2, 4 ),
 ( 0.000000000000000000, 0.06261444088629199156, 0.1252288817725839831, 0.1565361022157301107, 0.1878433226588762384, 0.2191505431020223937, 0.2348041533235934453, 0.2504577635451644690, 0.2817649839883067386, 0.2974185942098764301, 0.3130722044314461217, 0.3287258146530158687, 0.3443794248745855602, 0.3600330350961553072, 0.3678598402069396256, 0.3756866453177239440, 0.3913402555392901383, 0.3991670606500741791, 0.4069938657608581645, 0.4226474759824261351, 0.4304742810932104535, 0.4343876836486003645, 0.4383010862039902755, 0.4539546964255526396, 0.4696083066471148926, 0.5009155270902391210 ),
 .UNSPECIFIED. ) ;
#51250=CARTESIAN_POINT ( 'NONE',  ( 18.28003411566973924, -0.02431279293012689191, -13.99999914078080110 ) ) ;
#51257=CARTESIAN_POINT ( 'NONE',  ( 17.63847140750532461, -3.120744938285826109, 12.28504437646398806 ) ) ;
#51263=CARTESIAN_POINT ( 'NONE',  ( 12.43804048104135163, -3.154843637310955629, 13.63995574169148917 ) ) ;
#51265=CARTESIAN_POINT ( 'NONE',  ( 17.91195221639529933, 0.5131987758830273139, -13.88724801698936062 ) ) ;
#51271=CARTESIAN_POINT ( 'NONE',  ( 12.19601928331639051, -0.1418539764880159537, -13.89904537328360945 ) ) ;
#51272=CARTESIAN_POINT ( 'NONE',  ( 18.16486442019682102, -2.361571392960267968, 12.48278654574965607 ) ) ;
#51275=ORIENTED_EDGE ( 'NONE', *, *, #65253, .T. ) ;
#51277=CARTESIAN_POINT ( 'NONE',  ( 12.80505043854144276, -0.6250000000000001110, -12.67928921589118652 ) ) ;
#51289=CARTESIAN_POINT ( 'NONE',  ( 12.80505043854144276, -5.963111948670274387E-16, -25.00000000000000000 ) ) ;
#51294=CARTESIAN_POINT ( 'NONE',  ( 18.15103067362389311, -0.4097539338085443017, 12.59333942654355631 ) ) ;
#51303=DIRECTION ( 'NONE',  ( 1.000000000000000000, 0.000000000000000000, 0.000000000000000000 ) ) ;
#51314=CARTESIAN_POINT ( 'NONE',  ( 17.77834352330038215, -3.212755074437998015, -13.62637949436378015 ) ) ;
#51321=EDGE_CURVE ( 'NONE', #56658, #1963, #25989, .T. ) ;
#51325=ORIENTED_EDGE ( 'NONE', *, *, #14154, .F. ) ;
#51336=CARTESIAN_POINT ( 'NONE',  ( 12.24230779986659101, 2.227307356672650673, -12.51097363402014118 ) ) ;
#51346=CARTESIAN_POINT ( 'NONE',  ( 12.12451730110975134, -2.231694252990107152, -12.40079297172317929 ) ) ;
#51352=CARTESIAN_POINT ( 'NONE',  ( 12.25689739436622716, -2.199570998105317088, -13.73255685804838500 ) ) ;
#51357=ORIENTED_EDGE ( 'NONE', *, *, #43836, .F. ) ;
#51360=CARTESIAN_POINT ( 'NONE',  ( 17.59614113505323729, 3.124999999999999556, 13.52078631348661908 ) ) ;
#51363=CARTESIAN_POINT ( 'NONE',  ( 18.15128053492057703, 2.312280642761794347, 12.49331763295500508 ) ) ;
#51369=CARTESIAN_POINT ( 'NONE',  ( 12.18465059688365848, -2.421662038956231999, 12.46951891513069732 ) ) ;
#51375=CARTESIAN_POINT ( 'NONE',  ( 12.44117949531284317, 0.5082598251325830541, 12.68630931495243352 ) ) ;
#51378=CARTESIAN_POINT ( 'NONE',  ( 12.29407742813162940, 2.139519579705956076, 12.52828553530646793 ) ) ;
#51394=CARTESIAN_POINT ( 'NONE',  ( 17.82925890471818064, -0.5617199691364276326, -12.68327559334252008 ) ) ;
#51418=CARTESIAN_POINT ( 'NONE',  ( 12.21825390183959392, -2.283832253985284666, 12.49935200980254812 ) ) ;
#51422=CARTESIAN_POINT ( 'NONE',  ( 17.85663772380318903, -3.182036958951517835, 13.63358608099387581 ) ) ;
#51424=ORIENTED_EDGE ( 'NONE', *, *, #32363, .T. ) ;
#51434=CARTESIAN_POINT ( 'NONE',  ( 17.93788416347131331, 0.6112845611542863100, -12.58516990776526967 ) ) ;
#51446=CARTESIAN_POINT ( 'NONE',  ( 12.40968101568426007, 3.130119464836095933, 13.64559997174501049 ) ) ;
#51450=CARTESIAN_POINT ( 'NONE',  ( 12.31001894287360265, -0.3816018583990969937, -12.69228475097292375 ) ) ;
#51451=CARTESIAN_POINT ( 'NONE',  ( 12.39267642948476755, -0.6007076874295131930, 13.98710814480368292 ) ) ;
#51460=FACE_OUTER_BOUND ( 'NONE', #31565, .T. ) ;
#51468=CARTESIAN_POINT ( 'NONE',  ( 12.18236035866429390, 2.554391060822402970, 12.43872824571935176 ) ) ;
#51478=CARTESIAN_POINT ( 'NONE',  ( 12.80505043854146940, -2.500000000000000444, -25.00000000000000000 ) ) ;
#51485=CARTESIAN_POINT ( 'NONE',  ( 18.26928656998117972, 2.355301763765361045, -12.37791135143290866 ) ) ;
#51489=CARTESIAN_POINT ( 'NONE',  ( 12.23181585139621674, 2.749296767756840509, -13.61742212736085378 ) ) ;
#51491=DIRECTION ( 'NONE',  ( 0.000000000000000000, 1.000000000000000000, 0.000000000000000000 ) ) ;
#51495=CARTESIAN_POINT ( 'NONE',  ( 12.80505043854143388, 3.124999999999999556, 12.28373071562070074 ) ) ;
#51501=CARTESIAN_POINT ( 'NONE',  ( 18.18506112704242383, 2.156549459697482352, -13.83291014715494427 ) ) ;
#51512=CARTESIAN_POINT ( 'NONE',  ( 5.699994923231000321, 12.50864296698000011, 2.924709704137000266 ) ) ;
#51519=CARTESIAN_POINT ( 'NONE',  ( 17.96242084756264390, -2.025889508701483432, -12.54946620628462917 ) ) ;
#51528=ORIENTED_EDGE ( 'NONE', *, *, #57474, .T. ) ;
#51532=CARTESIAN_POINT ( 'NONE',  ( 12.12494527865623972, 2.264899384641845259, -13.81558393673957141 ) ) ;
#51536=CARTESIAN_POINT ( 'NONE',  ( 18.17483763484055004, -2.416937413759673969, 12.47057468849341078 ) ) ;
#51562=ORIENTED_EDGE ( 'NONE', *, *, #6691, .F. ) ;
#51563=CARTESIAN_POINT ( 'NONE',  ( 12.78440276244763574, -0.6249994333735316987, -12.67928921956170818 ) ) ;
#51564=B_SPLINE_CURVE_WITH_KNOTS ( 'NONE', 3,
 ( #59041, #52764, #64615, #47179, #31790, #16040, #68482, #53108, #42961, #38052, #42286, #4857, #11143, #20952, #59377, #20605, #63588, #26200, #48204, #37034, #21626 ),
 .UNSPECIFIED., .F., .F.,
 ( 4, 2, 2, 2, 1, 2, 2, 1, 1, 2, 2, 4 ),
 ( 0.000000000000000000, 0.1249999999999983902, 0.1875000000000058009, 0.2500000000000132117, 0.3125000000000205946, 0.3437500000000301981, 0.3750000000000398015, 0.4375000000000550671, 0.4687500000000596745, 0.4843750000000524580, 0.5000000000000451861, 1.000000000000000000 ),
 .UNSPECIFIED. ) ;
#51565=CARTESIAN_POINT ( 'NONE',  ( 12.33520056820728072, -2.912263648500925672, -12.34589992753920740 ) ) ;
#51584=CARTESIAN_POINT ( 'NONE',  ( 18.27863135987958287, 0.04720351400547010551, -13.99992551180917211 ) ) ;
#51604=CARTESIAN_POINT ( 'NONE',  ( 12.25867852505488997, 0.3036576181174169831, -13.89554011873102546 ) ) ;
#51606=CARTESIAN_POINT ( 'NONE',  ( 18.17062868725396640, -2.391413364859044766, 12.47623124499065028 ) ) ;
#51607=EDGE_CURVE ( 'NONE', #2983, #31596, #68976, .T. ) ;
#51617=PLANE ( 'NONE',  #19424 ) ;
#51627=CARTESIAN_POINT ( 'NONE',  ( 12.61587921998065021, 3.224448188370961255, -13.62362021573479431 ) ) ;
#51628=CIRCLE ( 'NONE', #39361, 2.000000000000001332 ) ;
#51633=CARTESIAN_POINT ( 'NONE',  ( 18.05961319350868166, 0.5166535389540052314, 12.58940585649086508 ) ) ;
#51637=ORIENTED_EDGE ( 'NONE', *, *, #5284, .T. ) ;
#51649=CARTESIAN_POINT ( 'NONE',  ( 17.55505043854144276, 0.6250000000000001110, -13.88107975066922428 ) ) ;
#51663=CARTESIAN_POINT ( 'NONE',  ( 17.55505043854144631, -0.7192913403693119712, -12.57945229203838267 ) ) ;
#51671=CARTESIAN_POINT ( 'NONE',  ( 12.43829333464978859, 1.993817424706644914, -12.55522976296196980 ) ) ;
#51674=ORIENTED_EDGE ( 'NONE', *, *, #18065, .T. ) ;
#51680=CARTESIAN_POINT ( 'NONE',  ( 12.43906710990146003, -3.006741445058540574, -12.31893827218669557 ) ) ;
#51686=CARTESIAN_POINT ( 'NONE',  ( 12.23404092485631267, -2.245077680571258671, -13.72419654341781126 ) ) ;
#51689=EDGE_CURVE ( 'NONE', #32483, #11912, #66846, .T. ) ;
#51694=CARTESIAN_POINT ( 'NONE',  ( 12.35913878030157598, 0.5835546239762330334, -13.98799446467094221 ) ) ;
#51697=CARTESIAN_POINT ( 'NONE',  ( 18.11601457969558737, 2.775767521728004006, 13.61104273367227258 ) ) ;
#51700=CARTESIAN_POINT ( 'NONE',  ( 18.09708155689161657, 2.811828937043456822, 12.37344130164188627 ) ) ;
#51706=CARTESIAN_POINT ( 'NONE',  ( 12.70142344966306602, -3.116692473072852021, 12.28627407840914643 ) ) ;
#51716=CARTESIAN_POINT ( 'NONE',  ( 12.20137806200446029, 0.1622035078961257260, 12.69861136640059129 ) ) ;
#51724=CARTESIAN_POINT ( 'NONE',  ( 4.599999999999999645, 0.7192913403693119712, -12.57945229203838267 ) ) ;
#51730=CARTESIAN_POINT ( 'NONE',  ( 17.63677106500005465, -0.6210356003259921431, -12.67955509032280403 ) ) ;
#51734=CARTESIAN_POINT ( 'NONE',  ( 18.15002510833730653, -2.691473085186385727, 13.63098399825532070 ) ) ;
#51736=CARTESIAN_POINT ( 'NONE',  ( 12.75695158412492880, -3.246897126047502358, 13.61828421767944164 ) ) ;
#51746=CARTESIAN_POINT ( 'NONE',  ( 18.06968158351558884, -0.3547715225555931884, 13.89390930605073393 ) ) ;
#51761=CARTESIAN_POINT ( 'NONE',  ( 17.79021264935889945, -3.209040350003993236, 13.62725621160039502 ) ) ;
#51773=CARTESIAN_POINT ( 'NONE',  ( 18.16427545049632286, 0.3901114995139649544, -12.59396323349877989 ) ) ;
#51786=CARTESIAN_POINT ( 'NONE',  ( 12.29903578917715379, 3.040996334883330210, 13.66573881806045598 ) ) ;
#51788=ORIENTED_EDGE ( 'NONE', *, *, #64570, .T. ) ;
#51789=CARTESIAN_POINT ( 'NONE',  ( 12.25734197677224202, -0.3012394091496986559, -12.69519438487131069 ) ) ;
#51790=CARTESIAN_POINT ( 'NONE',  ( 12.14438218221665267, -0.3016537271415141164, 13.99676704218776990 ) ) ;
#51807=CARTESIAN_POINT ( 'NONE',  ( 12.19170508189790425, 2.620143503867971901, 12.42276098599301548 ) ) ;
#51824=CARTESIAN_POINT ( 'NONE',  ( 18.21784200350676741, 2.188139590168312498, -12.40855205325248356 ) ) ;
#51829=EDGE_CURVE ( 'NONE', #25486, #7230, #32168, .T. ) ;
#51830=CARTESIAN_POINT ( 'NONE',  ( 12.48673873072914020, 3.044366353191839458, -13.54286685750310504 ) ) ;
#51835=CARTESIAN_POINT ( 'NONE',  ( 12.25981791760051109, 0.4818816852691563124, -13.99171642476390076 ) ) ;
#51843=CARTESIAN_POINT ( 'NONE',  ( 18.20740272079781619, 2.198619098391829230, -13.82629845589066342 ) ) ;
#51847=CARTESIAN_POINT ( 'NONE',  ( 4.600000127571202135, 3.375077994860000042E-14, 13.89999852642010403 ) ) ;
#51857=VECTOR ( 'NONE', #30684, 1000.000000000000227 ) ;
#51860=VERTEX_POINT ( 'NONE', #45641 ) ;
#51862=CARTESIAN_POINT ( 'NONE',  ( 17.88769455523112484, -1.970775861831701947, -12.55923393539036148 ) ) ;
#51870=CYLINDRICAL_SURFACE ( 'NONE', #11773, 0.6250000000000005551 ) ;
#51873=CARTESIAN_POINT ( 'NONE',  ( 18.00570828977289040, 0.5721320424853906239, 13.98830666644471954 ) ) ;
#51879=FACE_OUTER_BOUND ( 'NONE', #64814, .T. ) ;
#51902=DIRECTION ( 'NONE',  ( 0.000000000000000000, 1.000000000000000000, 0.000000000000000000 ) ) ;
#51906=CARTESIAN_POINT ( 'NONE',  ( 12.41256632787946756, -0.4864235087029714633, -12.68745975172791240 ) ) ;
#51907=CARTESIAN_POINT ( 'NONE',  ( 12.24249432806117888, -2.226917153383584758, -12.51101585362955859 ) ) ;
#51913=EDGE_CURVE ( 'NONE', #31596, #27235, #29835, .T. ) ;
#51927=CARTESIAN_POINT ( 'NONE',  ( 7.100000000000000533, 12.03770622561999915, -3.722046322334000124 ) ) ;
#51931=CARTESIAN_POINT ( 'NONE',  ( 17.88880419370420327, -3.028786488652052800, 12.31252201556900339 ) ) ;
#51934=CARTESIAN_POINT ( 'NONE',  ( 12.19254401039981772, -2.624350118461198367, -13.64624664190003500 ) ) ;
#51944=CARTESIAN_POINT ( 'NONE',  ( 12.37622832409308238, 2.954798090471128624, 13.56635979911537859 ) ) ;
#51946=CARTESIAN_POINT ( 'NONE',  ( 17.87083331331565006, -1.960545027353535863, 12.56104967893681845 ) ) ;
#51959=EDGE_CURVE ( 'NONE', #53716, #42472, #24907, .T. ) ;
#51969=CARTESIAN_POINT ( 'NONE',  ( 18.19734990864320778, 0.3336735144251340435, 12.59558214381612551 ) ) ;
#51976=CARTESIAN_POINT ( 'NONE',  ( 17.82352195865853872, 3.196339915866913906, 13.63023968027431465 ) ) ;
#51985=CARTESIAN_POINT ( 'NONE',  ( 17.74460677683594767, -3.176355914694789284, 12.19306589750932623 ) ) ;
#52000=ORIENTED_EDGE ( 'NONE', *, *, #50668, .F. ) ;
#52008=CARTESIAN_POINT ( 'NONE',  ( 12.33224723617686891, 2.090732662878786563, -12.53759506087954456 ) ) ;
#52011=EDGE_CURVE ( 'NONE', #28416, #18264, #48878, .T. ) ;
#52015=CARTESIAN_POINT ( 'NONE',  ( 17.64998052282863839, -0.7146386402724677067, 12.57972080578535312 ) ) ;
#52018=CARTESIAN_POINT ( 'NONE',  ( 12.72250989631414164, -3.119868145445779728, -12.28529260172211224 ) ) ;
#52024=CARTESIAN_POINT ( 'NONE',  ( 21.59999987243000064, 13.89999852641999922, 0.000000000000000000 ) ) ;
#52025=CARTESIAN_POINT ( 'NONE',  ( 12.80505043854146940, -1.875000000000000444, -13.78627172894481667 ) ) ;
#52027=DIRECTION ( 'NONE',  ( 0.000000000000000000, -0.9905022095861402143, 0.1374968101629056305 ) ) ;
#52031=CARTESIAN_POINT ( 'NONE',  ( 12.35923975629391514, -0.5837697427702301933, -13.98798827747872053 ) ) ;
#52033=CARTESIAN_POINT ( 'NONE',  ( 18.03215848269747568, 2.904634633594406434, 13.57923905310747337 ) ) ;
#52037=CARTESIAN_POINT ( 'NONE',  ( 18.15975285618098312, 2.341680162859185010, 12.48703895936063013 ) ) ;
#52044=CARTESIAN_POINT ( 'NONE',  ( 12.66109513597121605, -3.108543426238435714, 12.28874474902926650 ) ) ;
#52053=CARTESIAN_POINT ( 'NONE',  ( 5.606877745312729644, -12.12699005521680817, -3.748526802952889980 ) ) ;
#52074=CARTESIAN_POINT ( 'NONE',  ( 18.15125141007965226, -2.312191647150520613, -13.71145324559126877 ) ) ;
#52085=CARTESIAN_POINT ( 'NONE',  ( 18.14736049945578245, -0.1997550941145084524, 13.89807248760369518 ) ) ;
#52103=EDGE_CURVE ( 'NONE', #11762, #62789, #57798, .T. ) ;
#52106=FILL_AREA_STYLE_COLOUR ( '', #30482 ) ;
#52108=CIRCLE ( 'NONE', #66635, 2.000000000000000444 ) ;
#52113=CARTESIAN_POINT ( 'NONE',  ( 18.23387849499156133, -0.2528603812084161406, -12.59746735456353051 ) ) ;
#52117=ORIENTED_EDGE ( 'NONE', *, *, #52522, .T. ) ;
#52118=AXIS2_PLACEMENT_3D ( 'NONE', #61036, #50206, #65923 ) ;
#52124=CARTESIAN_POINT ( 'NONE',  ( 12.38020518697565286, 1.926193139504584373, 13.86686096623706810 ) ) ;
#52130=CARTESIAN_POINT ( 'NONE',  ( 12.08123665194308138, -0.04806343339258901948, 13.99993753789458850 ) ) ;
#52132=CARTESIAN_POINT ( 'NONE',  ( 12.18657262959521326, -2.104614846739868206, 12.42298765743896816 ) ) ;
#52140=CARTESIAN_POINT ( 'NONE',  ( 12.13061620557590992, 2.744764576889032970, 12.29741386912397338 ) ) ;
#52147=DIRECTION ( 'NONE',  ( -1.000000000000000000, 0.000000000000000000, 0.000000000000000000 ) ) ;
#52160=CARTESIAN_POINT ( 'NONE',  ( 12.64218892536046646, -3.103760129324341754, 13.52669845179788943 ) ) ;
#52164=EDGE_CURVE ( 'NONE', #18264, #16502, #47269, .T. ) ;
#52172=CARTESIAN_POINT ( 'NONE',  ( 17.80580762821592344, 3.072583274995464464, -12.29955455495395711 ) ) ;
#52174=CARTESIAN_POINT ( 'NONE',  ( 18.13957898666327750, 2.721486385479426229, 12.39720401453807419 ) ) ;
#52175=CARTESIAN_POINT ( 'NONE',  ( 12.20205663599317703, 2.664445668530659006, -13.63720455689867350 ) ) ;
#52180=CARTESIAN_POINT ( 'NONE',  ( 12.38296256657291039, 0.5938246120522370219, -13.98740230410798091 ) ) ;
#52189=CARTESIAN_POINT ( 'NONE',  ( 18.21736474454386823, 2.220153890850322664, -13.82285830752081068 ) ) ;
#52207=CARTESIAN_POINT ( 'NONE',  ( 18.07135403277173324, -2.147634186626016017, -12.52670565379013112 ) ) ;
#52218=CARTESIAN_POINT ( 'NONE',  ( 18.26375728754768701, 0.1544074001203936397, 13.99915345895492180 ) ) ;
#52238=CARTESIAN_POINT ( 'NONE',  ( 12.80505043854143388, 3.124999999999999556, 13.52078605991414939 ) ) ;
#52241=CARTESIAN_POINT ( 'NONE',  ( 17.59622528265708041, 3.124999999999999112, -12.28374666422326555 ) ) ;
#52253=CARTESIAN_POINT ( 'NONE',  ( 18.00302879685015967, 3.053770323291399080, 12.22453350001232586 ) ) ;
#52256=CARTESIAN_POINT ( 'NONE',  ( 12.24435292127285635, 0.2761699508452409857, -12.69595998167825357 ) ) ;
#52257=CARTESIAN_POINT ( 'NONE',  ( 12.22445834447965041, -2.731426566108815734, -12.39462880883199603 ) ) ;
#52264=CARTESIAN_POINT ( 'NONE',  ( 17.97862686867181026, 0.4596875349763956398, 12.68880368814833304 ) ) ;
#52284=CARTESIAN_POINT ( 'NONE',  ( 12.17999101424757846, -2.480063841750759668, -13.67763837794374204 ) ) ;
#52289=ORIENTED_EDGE ( 'NONE', *, *, #35285, .F. ) ;
#52291=CARTESIAN_POINT ( 'NONE',  ( 17.71608705221678903, 0.6042412280260501811, -13.88231902342887736 ) ) ;
#52292=CARTESIAN_POINT ( 'NONE',  ( 17.63732991102260783, -0.6196453797482965875, -12.67964297675818308 ) ) ;
#52296=CARTESIAN_POINT ( 'NONE',  ( 12.34730967147302039, 2.925678532231710705, 13.57385403034849425 ) ) ;
#52297=CARTESIAN_POINT ( 'NONE',  ( 17.60707724214346115, -1.877081947552195151, 12.57511531410870020 ) ) ;
#52303=CARTESIAN_POINT ( 'NONE',  ( 12.23000334607946016, 2.254948878044618521, -13.72238900567161579 ) ) ;
#52306=CARTESIAN_POINT ( 'NONE',  ( 17.55505043854147118, -3.125000000000000000, -25.00000000000000000 ) ) ;
#52308=CARTESIAN_POINT ( 'NONE',  ( 18.09811766390441079, 0.3100353841908372599, 13.89536095208713284 ) ) ;
#52314=CARTESIAN_POINT ( 'NONE',  ( 12.47605349747044201, 0.5315089155327396009, 13.88632137824158441 ) ) ;
#52320=CARTESIAN_POINT ( 'NONE',  ( 12.35647036339751637, 1.936369888824708285, -13.86561402904834139 ) ) ;
#52324=CARTESIAN_POINT ( 'NONE',  ( 17.87637886473324755, 0.6448943924266568040, 12.58348668657565916 ) ) ;
#52330=CARTESIAN_POINT ( 'NONE',  ( 17.96944589180082019, 3.117220005880602329, 13.64855254614797886 ) ) ;
#52362=DIRECTION ( 'NONE',  ( -1.000000000000000000, 0.000000000000000000, 0.000000000000000000 ) ) ;
#52370=CARTESIAN_POINT ( 'NONE',  ( 12.24387941792144474, -2.775899267521871217, -12.38300827451277897 ) ) ;
#52374=CARTESIAN_POINT ( 'NONE',  ( 12.72263738247862008, -1.880115814278897846, -13.78550660562619434 ) ) ;
#52377=CARTESIAN_POINT ( 'NONE',  ( 18.22954180134192015, -2.744780546098131158, 12.29741030561552506 ) ) ;
#52380=CARTESIAN_POINT ( 'NONE',  ( 12.43999839845094790, 0.6380582630481954620, -13.98550026811281910 ) ) ;
#52386=CARTESIAN_POINT ( 'NONE',  ( 17.57591570971901618, 3.124999463061048921, 12.28373083832239132 ) ) ;
#52396=CARTESIAN_POINT ( 'NONE',  ( 12.80505043854146940, -3.125000000000000444, 12.28374638332999780 ) ) ;
#52403=CARTESIAN_POINT ( 'NONE',  ( 12.35550214789977552, -0.4343244881883143171, 12.69000555157926868 ) ) ;
#52411=CARTESIAN_POINT ( 'NONE',  ( 17.88807090798125543, 1.970716457409874778, 13.77152834881607113 ) ) ;
#52412=CARTESIAN_POINT ( 'NONE',  ( 12.80505043854146940, -3.199698446519381179, -12.18695736643652516 ) ) ;
#52423=CARTESIAN_POINT ( 'NONE',  ( 18.13009756288984420, -2.254948952832146247, -13.72233930590318884 ) ) ;
#52433=CARTESIAN_POINT ( 'NONE',  ( 18.17506427777800937, -0.08141198786016999589, 13.89969880262531632 ) ) ;
#52435=ORIENTED_EDGE ( 'NONE', *, *, #61237, .F. ) ;
#52440=EDGE_CURVE ( 'NONE', #50331, #1476, #1502, .T. ) ;
#52445=CARTESIAN_POINT ( 'NONE',  ( 12.47072553654362714, 1.841758158201594942, -12.46466843114749068 ) ) ;
#52448=CARTESIAN_POINT ( 'NONE',  ( 17.78989870834646680, -1.827084948615278481, 13.88026577095109815 ) ) ;
#52449=CARTESIAN_POINT ( 'NONE',  ( 18.15002510837776128, 2.691473085059168824, -13.63098399828460927 ) ) ;
#52452=LINE ( 'NONE', #20295, #54833 ) ;
#52461=CARTESIAN_POINT ( 'NONE',  ( 18.20545956023470779, -0.3178346465811165422, -12.59599179195193663 ) ) ;
#52472=CARTESIAN_POINT ( 'NONE',  ( 12.38032181885347960, 3.110191202103290031, 13.65016103957348825 ) ) ;
#52474=CARTESIAN_POINT ( 'NONE',  ( 12.76469316428371847, -0.6250000000000007772, -12.67928922306547257 ) ) ;
#52476=CARTESIAN_POINT ( 'NONE',  ( 12.36383866360284856, -0.5795518042670544379, 13.98800095993141390 ) ) ;
#52479=CARTESIAN_POINT ( 'NONE',  ( 12.58121427537368398, -1.795950320080881069, 12.47134981075813265 ) ) ;
#52486=CARTESIAN_POINT ( 'NONE',  ( 12.18940205905205332, 0.3800566752825982886, 12.59427093624936411 ) ) ;
#52489=CARTESIAN_POINT ( 'NONE',  ( 12.56929374240175612, 1.799893664886381250, 12.47078182885977782 ) ) ;
#52498=CARTESIAN_POINT ( 'NONE',  ( 12.26360295038370651, 2.812350523778595512, 12.37328769146724561 ) ) ;
#52501=CARTESIAN_POINT ( 'NONE',  ( 12.50368198906695127, -0.5476376384638111938, 12.68410501633232279 ) ) ;
#52506=CARTESIAN_POINT ( 'NONE',  ( 12.21987570834416559, -2.720459983100028900, 13.62424277487875202 ) ) ;
#52507=CARTESIAN_POINT ( 'NONE',  ( 12.63953418767183834, 1.875000000000000444, 13.78627077332620665 ) ) ;
#52515=CARTESIAN_POINT ( 'NONE',  ( 18.16584637247983736, 2.632875908479945792, -12.41964751440798054 ) ) ;
#52522=EDGE_CURVE ( 'NONE', #13791, #22723, #11292, .T. ) ;
#52524=CARTESIAN_POINT ( 'NONE',  ( 12.09897931881620181, 0.1662062226620488470, -13.99901824074930978 ) ) ;
#52529=ORIENTED_EDGE ( 'NONE', *, *, #33418, .T. ) ;
#52534=CARTESIAN_POINT ( 'NONE',  ( 18.08710802279906105, 2.021458498708241347, -13.85330284862005890 ) ) ;
#52540=CARTESIAN_POINT ( 'NONE',  ( 12.22418139218991051, 0.2308705899911544235, -13.89742331311149393 ) ) ;
#52541=CARTESIAN_POINT ( 'NONE',  ( 5.500000000000000000, 0.000000000000000000, 0.000000000000000000 ) ) ;
#52551=CARTESIAN_POINT ( 'NONE',  ( 18.13782450322841910, -2.273941707540254153, -12.50136077393157308 ) ) ;
#52560=FACE_OUTER_BOUND ( 'NONE', #843, .T. ) ;
#52586=CARTESIAN_POINT ( 'NONE',  ( 17.94531445437959150, 2.988940031718388290, -12.32413547815658283 ) ) ;
#52596=CARTESIAN_POINT ( 'NONE',  ( 12.18832871607759927, -0.1019009512359513453, -12.69945530929772559 ) ) ;
#52597=CARTESIAN_POINT ( 'NONE',  ( 12.18582115247814990, -2.585797660396002673, -12.43116941335174808 ) ) ;
#52601=ORIENTED_EDGE ( 'NONE', *, *, #9295, .F. ) ;
#52603=CIRCLE ( 'NONE', #15734, 14.00000000000000000 ) ;
#52606=CARTESIAN_POINT ( 'NONE',  ( 17.86534717979584030, 0.5429181308642001547, 12.68438171063677089 ) ) ;
#52622=CARTESIAN_POINT ( 'NONE',  ( 17.98439275848210173, -2.954313498893242684, 12.33404747595917783 ) ) ;
#52627=ORIENTED_EDGE ( 'NONE', *, *, #55803, .T. ) ;
#52635=LINE ( 'NONE', #53333, #63189 ) ;
#52637=CARTESIAN_POINT ( 'NONE',  ( 12.27346860450516708, 2.829323760734074433, 13.59803440778111572 ) ) ;
#52646=CARTESIAN_POINT ( 'NONE',  ( 12.70155625791296572, 1.883284863834661760, -13.78507964965114674 ) ) ;
#52654=CARTESIAN_POINT ( 'NONE',  ( 7.100000000000000533, 13.17499999999999893, 0.000000000000000000 ) ) ;
#52662=ADVANCED_FACE ( 'NONE', ( #51460 ), #69090, .T. ) ;
#52665=CARTESIAN_POINT ( 'NONE',  ( 18.07652645701807970, 0.4998493492226911417, 12.59008424712975227 ) ) ;
#52670=VERTEX_POINT ( 'NONE', #50007 ) ;
#52681=CARTESIAN_POINT ( 'NONE',  ( 12.48426296206727670, -0.6451567829544542221, -12.58347320810648107 ) ) ;
#52682=DIRECTION ( 'NONE',  ( 1.000000000000000000, 0.000000000000000000, 0.000000000000000000 ) ) ;
#52706=CARTESIAN_POINT ( 'NONE',  ( 12.55891702277097011, 3.074517471785632949, -12.29897628258782660 ) ) ;
#52715=CARTESIAN_POINT ( 'NONE',  ( 12.23528344688402036, -2.757674802278839099, -12.38780605717374250 ) ) ;
#52719=CARTESIAN_POINT ( 'NONE',  ( 12.50345261626383220, -3.182071724319532890, -13.63357796689960111 ) ) ;
#52723=CARTESIAN_POINT ( 'NONE',  ( 18.05312913029198896, -3.003720153666145531, 12.23674614497118007 ) ) ;
#52725=ADVANCED_FACE ( 'NONE', ( #58336 ), #62547, .F. ) ;
#52734=CARTESIAN_POINT ( 'NONE',  ( 18.17259031544350023, 2.401600790900606519, 12.47395980848747321 ) ) ;
#52749=CARTESIAN_POINT ( 'NONE',  ( 12.61341903040855783, -0.5949840079737210852, 12.68123264482375490 ) ) ;
#52750=CARTESIAN_POINT ( 'NONE',  ( 5.518321182375771627, -12.20777697081100932, -3.787023466231959734 ) ) ;
#52764=CARTESIAN_POINT ( 'NONE',  ( 5.695116968502542676, -12.04237015855036219, 3.723491068767540657 ) ) ;
#52769=CARTESIAN_POINT ( 'NONE',  ( 18.16582246987730187, -2.632686762925362967, 13.64442020621638818 ) ) ;
#52772=CARTESIAN_POINT ( 'NONE',  ( 18.05358084703149757, -2.122495591609769860, -13.74627451715324078 ) ) ;
#52782=CARTESIAN_POINT ( 'NONE',  ( 18.13610176148302600, -0.2304125752445602970, 13.89743363615726501 ) ) ;
#52792=EDGE_CURVE ( 'NONE', #7236, #33164, #23273, .T. ) ;
#52796=CARTESIAN_POINT ( 'NONE',  ( 12.08118961495425836, 2.529460273524981151, -12.34351656561901400 ) ) ;
#52797=DIRECTION ( 'NONE',  ( 1.000000000000000000, 0.000000000000000000, 0.000000000000000000 ) ) ;
#52798=CARTESIAN_POINT ( 'NONE',  ( 17.55505043854147118, -3.199751711897561801, 12.18694338143115452 ) ) ;
#52799=CARTESIAN_POINT ( 'NONE',  ( 17.88876975676777192, -1.869670916578588526, 13.87459417580158316 ) ) ;
#52800=CARTESIAN_POINT ( 'NONE',  ( 18.16657332772220101, 2.629115783231108949, -13.64522528429649029 ) ) ;
#52808=CARTESIAN_POINT ( 'NONE',  ( 7.100000000000000533, -12.50865771883999855, 2.924687089724999911 ) ) ;
#52812=CARTESIAN_POINT ( 'NONE',  ( 17.88703114068441380, -0.6395598188657377614, -12.58375915074078577 ) ) ;
#52823=CARTESIAN_POINT ( 'NONE',  ( 12.43994760172710023, 1.886699913279277885, 13.87229234465171501 ) ) ;
#52835=CARTESIAN_POINT ( 'NONE',  ( 12.10479047996948943, 0.1866745257715813344, 12.59862229962904046 ) ) ;
#52839=CARTESIAN_POINT ( 'NONE',  ( 12.09642313398529190, 2.633248533341329356, 12.32177498806536953 ) ) ;
#52846=CARTESIAN_POINT ( 'NONE',  ( 12.23179573719470348, 2.749250018103629234, 12.38999654616027790 ) ) ;
#52855=CARTESIAN_POINT ( 'NONE',  ( 12.20884949286986831, -2.312191565065524035, 13.71150332431687424 ) ) ;
#52856=CARTESIAN_POINT ( 'NONE',  ( 12.26374059927404403, 2.812587984009075726, 13.60212386631915571 ) ) ;
#52858=ORIENTED_EDGE ( 'NONE', *, *, #28453, .T. ) ;
#52864=CARTESIAN_POINT ( 'NONE',  ( 17.78683280784126097, 3.080523647204255866, -12.29718062304645798 ) ) ;
#52866=CARTESIAN_POINT ( 'NONE',  ( 18.17813913393023384, 2.550022942068608689, 12.43977370304579644 ) ) ;
#52871=CYLINDRICAL_SURFACE ( 'NONE', #61215, 1.999999999999999556 ) ;
#52873=DIRECTION ( 'NONE',  ( -0.7071069400700297214, 0.7071066223030297859, 2.150916229665089677E-09 ) ) ;
#52878=ORIENTED_EDGE ( 'NONE', *, *, #68898, .T. ) ;
#52902=CARTESIAN_POINT ( 'NONE',  ( 18.05239999627277214, -2.879049404332130191, -12.35514073459315654 ) ) ;
#52911=CARTESIAN_POINT ( 'NONE',  ( 17.55505043854147118, -1.760910691117812954, -12.47634535983622861 ) ) ;
#52913=AXIS2_PLACEMENT_3D ( 'NONE', #35470, #56792, #61684 ) ;
#52922=CARTESIAN_POINT ( 'NONE',  ( 12.34854013679586160, -2.926988005537949800, 13.57357535316058694 ) ) ;
#52944=CARTESIAN_POINT ( 'NONE',  ( 5.534341696747668848, 12.89488364838971712, -2.703816490859269894 ) ) ;
#52947=CARTESIAN_POINT ( 'NONE',  ( 12.35550214789977908, 0.4343244881883154274, -12.69000555157927757 ) ) ;
#52948=CARTESIAN_POINT ( 'NONE',  ( 12.21857308197977687, -2.283092344262311002, -12.49946922047021225 ) ) ;
#52953=FACE_OUTER_BOUND ( 'NONE', #27115, .T. ) ;
#52956=CARTESIAN_POINT ( 'NONE',  ( 17.55505043854143565, 1.875000000000000000, 13.78627172894481667 ) ) ;
#52957=CARTESIAN_POINT ( 'NONE',  ( 18.17506407532043866, 0.08141364314609686459, 12.69967032936880713 ) ) ;
#52964=CARTESIAN_POINT ( 'NONE',  ( 18.05225003025148922, 2.879247418710621176, -13.58568546892325557 ) ) ;
#52984=CARTESIAN_POINT ( 'NONE',  ( 18.17506427775392197, 0.08141198804361876595, -13.89969880262316337 ) ) ;
#52989=DIRECTION ( 'NONE',  ( -0.000000000000000000, -0.000000000000000000, 1.000000000000000000 ) ) ;
#52997=AXIS2_PLACEMENT_3D ( 'NONE', #67743, #62506, #15653 ) ;
#53002=CARTESIAN_POINT ( 'NONE',  ( 17.57569743819256658, -0.6249994633519876386, 13.88107975068473365 ) ) ;
#53005=CARTESIAN_POINT ( 'NONE',  ( 12.41700012676155218, 0.4899485149124510608, 13.88837626668677316 ) ) ;
#53008=CARTESIAN_POINT ( 'NONE',  ( 18.09811766381520215, -0.3100353843471406190, -13.89536095208329236 ) ) ;
#53017=CARTESIAN_POINT ( 'NONE',  ( 18.13088395572279410, 0.4376617689587105064, 12.59240970319242869 ) ) ;
#53026=B_SPLINE_CURVE_WITH_KNOTS ( 'NONE', 3,
 ( #17734, #66300, #35194, #18077, #34159, #51263, #66649, #45339, #18768, #39399, #8269, #40097, #3359, #39055, #13529, #60376, #29266, #2337 ),
 .UNSPECIFIED., .F., .F.,
 ( 4, 2, 2, 2, 2, 2, 2, 2, 4 ),
 ( 0.000000000000000000, 0.06250000000000112410, 0.1250000000000022482, 0.2500000000000026090, 0.5000000000000021094, 0.7500000000000015543, 0.8750000000000019984, 0.9375000000000009992, 1.000000000000000000 ),
 .UNSPECIFIED. ) ;
#53037=VERTEX_POINT ( 'NONE', #24384 ) ;
#53065=CARTESIAN_POINT ( 'NONE',  ( 12.18425839594608995, -2.573099938722084534, -12.43423733299712985 ) ) ;
#53069=PLANE ( 'NONE',  #33072 ) ;
#53070=CARTESIAN_POINT ( 'NONE',  ( 12.16922513814163054, -2.166987123599049436, -13.83127908232058267 ) ) ;
#53073=CARTESIAN_POINT ( 'NONE',  ( 18.20778913885557415, -2.166651812353031392, 12.41232206190563048 ) ) ;
#53074=VERTEX_POINT ( 'NONE', #29302 ) ;
#53075=EDGE_LOOP ( 'NONE', ( #28911, #19409, #35799, #21850 ) ) ;
#53082=CARTESIAN_POINT ( 'NONE',  ( 18.14748133480223302, 2.299853946629115686, -12.49599191558583655 ) ) ;
#53087=CARTESIAN_POINT ( 'NONE',  ( 12.39876276414171485, -2.975035832937171776, 12.32812070139215521 ) ) ;
#53088=CYLINDRICAL_SURFACE ( 'NONE', #18111, 14.00000000000000000 ) ;
#53099=ORIENTED_EDGE ( 'NONE', *, *, #25252, .T. ) ;
#53102=CARTESIAN_POINT ( 'NONE',  ( 17.71877800696617200, 1.896477791912290378, 13.78304299653506781 ) ) ;
#53108=CARTESIAN_POINT ( 'NONE',  ( 5.647168941336192738, -12.08810193142197242, 3.737902345523164360 ) ) ;
#53116=CARTESIAN_POINT ( 'NONE',  ( 18.06560877808663079, -2.138932497554039802, -13.74340275081395291 ) ) ;
#53126=CARTESIAN_POINT ( 'NONE',  ( 18.18005043824477696, -1.062925945863725942E-10, 13.90000000153292881 ) ) ;
#53138=CARTESIAN_POINT ( 'NONE',  ( 12.35083548769875250, 1.919332845685024935, -12.45296032288162813 ) ) ;
#53141=CARTESIAN_POINT ( 'NONE',  ( 18.17602379430283932, 2.571655014618306812, -13.65800652342106325 ) ) ;
#53153=CARTESIAN_POINT ( 'NONE',  ( 17.88507951091366621, 0.5311517451680620727, -12.68505220952107493 ) ) ;
#53157=ORIENTED_EDGE ( 'NONE', *, *, #42775, .T. ) ;
#53163=CARTESIAN_POINT ( 'NONE',  ( 18.24542859620200019, 2.700577031380341886, 12.30719352326003779 ) ) ;
#53164=CARTESIAN_POINT ( 'NONE',  ( 12.48191940168456604, 1.864230036291395720, 13.87532606992096795 ) ) ;
#53166=CARTESIAN_POINT ( 'NONE',  ( 12.38151466856633220, -0.4597251445480311505, -12.68880184500082819 ) ) ;
#53169=CARTESIAN_POINT ( 'NONE',  ( 12.38926598778393995, -1.890730539229764862, 12.45733450583996671 ) ) ;
#53175=CARTESIAN_POINT ( 'NONE',  ( 12.17126533935444499, 0.3494793053307373998, 12.59515668824706580 ) ) ;
#53181=CARTESIAN_POINT ( 'NONE',  ( 12.11850681454232515, 2.712075317534401897, 12.30466467946555831 ) ) ;
#53190=CARTESIAN_POINT ( 'NONE',  ( 12.20125275681506238, 2.661451430635814575, 12.41248063365286924 ) ) ;
#53195=CARTESIAN_POINT ( 'NONE',  ( 17.78895972989507257, 0.6824382159868358499, -12.58151825845973271 ) ) ;
#53197=CARTESIAN_POINT ( 'NONE',  ( 12.43942356506269142, -3.006998533878517676, 13.55276137517231838 ) ) ;
#53205=CARTESIAN_POINT ( 'NONE',  ( 18.08682736286118597, 2.829024318083993794, -12.36883279713289951 ) ) ;
#53208=CARTESIAN_POINT ( 'NONE',  ( 18.17603698666708212, 2.571536872321186440, 12.43461505415530866 ) ) ;
#53231=CARTESIAN_POINT ( 'NONE',  ( 12.55587196706169095, 0.5732793990000022433, -13.88408420575383850 ) ) ;
#53241=CARTESIAN_POINT ( 'NONE',  ( 17.55505043854147118, -3.125000000000000000, -12.28373071562069896 ) ) ;
#53243=CARTESIAN_POINT ( 'NONE',  ( 17.72046959778183961, -1.874999999999999556, -12.57541560742024345 ) ) ;
#53244=CARTESIAN_POINT ( 'NONE',  ( 12.20137680394560142, -0.1621987986621315492, 13.89873133405097327 ) ) ;
#53256=EDGE_CURVE ( 'NONE', #66718, #63209, #15491, .T. ) ;
#53265=CARTESIAN_POINT ( 'NONE',  ( 12.32889761174919485, -2.904977411726858527, 13.57918629439492442 ) ) ;
#53280=CARTESIAN_POINT ( 'NONE',  ( 17.75789140671455968, 3.091531401869214157, -12.29387995131248346 ) ) ;
#53288=CARTESIAN_POINT ( 'NONE',  ( 17.74468889437551766, 1.784327658738282363, 12.47302143557446996 ) ) ;
#53290=CARTESIAN_POINT ( 'NONE',  ( 12.24897804304629290, 0.2853680816562786937, -12.69568625917504257 ) ) ;
#53306=CARTESIAN_POINT ( 'NONE',  ( 17.99129208686611392, 2.947687251868547520, -13.56825406139790680 ) ) ;
#53313=CARTESIAN_POINT ( 'NONE',  ( 17.55505043854147118, -1.787797342887044172, -13.88538010501570774 ) ) ;
#53324=ORIENTED_EDGE ( 'NONE', *, *, #7337, .T. ) ;
#53330=CARTESIAN_POINT ( 'NONE',  ( 18.14038165173105099, 0.2193642558646157759, -13.89767506191630098 ) ) ;
#53333=CARTESIAN_POINT ( 'NONE',  ( 21.47500033997000202, -1.509903313490000218E-14, 12.72499970925004398 ) ) ;
#53343=CARTESIAN_POINT ( 'NONE',  ( 12.43812277102952635, 1.993632728549933786, -13.76791003216515286 ) ) ;
#53346=CARTESIAN_POINT ( 'NONE',  ( 18.12459203954894349, 0.2581888431706754750, 13.89679013629345228 ) ) ;
#53347=CARTESIAN_POINT ( 'NONE',  ( 18.00676300520316886, 0.4321619634324096459, 13.89096157872187298 ) ) ;
#53353=CARTESIAN_POINT ( 'NONE',  ( 18.05194946914436471, -0.3792369706354827286, -13.89303997535758661 ) ) ;
#53361=CARTESIAN_POINT ( 'NONE',  ( 18.11564574962621066, -0.2765170649790819057, 12.69595318831093778 ) ) ;
#53377=CARTESIAN_POINT ( 'NONE',  ( 12.61757266016683232, -0.6952251598378732522, -12.58080715426406293 ) ) ;
#53380=CARTESIAN_POINT ( 'NONE',  ( 17.87828936854284478, 3.124432504806127220, -12.20647160316251245 ) ) ;
#53389=ORIENTED_EDGE ( 'NONE', *, *, #24000, .T. ) ;
#53399=CARTESIAN_POINT ( 'NONE',  ( 5.500000000000000000, -11.06886219213000011, 1.536526853569999851 ) ) ;
#53402=CARTESIAN_POINT ( 'NONE',  ( 12.76336819523226929, 3.123957167202322971, -12.28406425424631365 ) ) ;
#53415=CARTESIAN_POINT ( 'NONE',  ( 12.27409806343529652, -3.015283977741793020, -13.67143535301651447 ) ) ;
#53416=AXIS2_PLACEMENT_3D ( 'NONE', #57645, #25840, #14670 ) ;
#53419=CARTESIAN_POINT ( 'NONE',  ( 18.03569330394761039, -3.019535577993367692, 12.23285103262380424 ) ) ;
#53441=CARTESIAN_POINT ( 'NONE',  ( 12.60374982967590185, -0.5917829749564905706, 12.68143435689271215 ) ) ;
#53443=DIRECTION ( 'NONE',  ( -1.000000000000000000, 0.000000000000000000, 0.000000000000000000 ) ) ;
#53448=CARTESIAN_POINT ( 'NONE',  ( 17.77689708618907005, 3.084393760937525375, 13.53193451522998103 ) ) ;
#53463=VECTOR ( 'NONE', #6150, 1000.000000000000000 ) ;
#53464=CARTESIAN_POINT ( 'NONE',  ( 17.57587588171171689, -3.124999410540973521, -13.52078618842887181 ) ) ;
#53482=CARTESIAN_POINT ( 'NONE',  ( 12.68566995881735870, 1.770266656024989116, -12.47502217142794478 ) ) ;
#53486=CARTESIAN_POINT ( 'NONE',  ( 18.16762906240600017, 2.624018810214213460, -13.64637396502920019 ) ) ;
#53491=CARTESIAN_POINT ( 'NONE',  ( 12.39015342239249762, -3.070413439580835568, -12.22017215029075032 ) ) ;
#53499=CARTESIAN_POINT ( 'NONE',  ( 17.56702613447739481, -0.7192913015564690316, -12.57945229205062354 ) ) ;
#53510=CARTESIAN_POINT ( 'NONE',  ( 18.22068658462131197, 2.765866853816869142, 12.29268492208001540 ) ) ;
#53514=CARTESIAN_POINT ( 'NONE',  ( 12.80505043854146940, -1.845938772038641318, 13.81933890150171074 ) ) ;
#53517=CARTESIAN_POINT ( 'NONE',  ( 12.20599951553718832, -2.074681531931807488, 12.42802467457380367 ) ) ;
#53525=CARTESIAN_POINT ( 'NONE',  ( 12.54953071380263196, 0.6732419856523105262, 12.58200148172923960 ) ) ;
#53528=CARTESIAN_POINT ( 'NONE',  ( 12.80505043854143388, 1.760910691117812510, 12.47634535983623394 ) ) ;
#53536=CARTESIAN_POINT ( 'NONE',  ( 12.22445834451951541, 2.731426566208313922, 12.39462880880582318 ) ) ;
#53540=CARTESIAN_POINT ( 'NONE',  ( 12.54858945031608997, 0.5700410258791628326, 12.68277524907516884 ) ) ;
#53541=EDGE_CURVE ( 'NONE', #62494, #24573, #23096, .T. ) ;
#53545=CARTESIAN_POINT ( 'NONE',  ( 12.18118526251765665, -2.542711865659281756, 13.66432766657963960 ) ) ;
#53546=CARTESIAN_POINT ( 'NONE',  ( 12.22105292102199137, 2.722876829147647282, 13.62360956004511792 ) ) ;
#53553=CARTESIAN_POINT ( 'NONE',  ( 18.02645743154359081, 2.910866584900387188, -12.34632125423082982 ) ) ;
#53576=CARTESIAN_POINT ( 'NONE',  ( 12.47664075733698219, 0.5322329922976065664, -13.88628950328449285 ) ) ;
#53588=CARTESIAN_POINT ( 'NONE',  ( 18.14695621644404611, -2.700933560328190985, -12.40248159148175944 ) ) ;
#53591=FACE_OUTER_BOUND ( 'NONE', #6020, .T. ) ;
#53592=CARTESIAN_POINT ( 'NONE',  ( 12.39257741226468390, 0.4700078255514595904, 13.88931146942756811 ) ) ;
#53604=CARTESIAN_POINT ( 'NONE',  ( 17.55505043854144276, 0.6250000000000001110, -13.88107975066922428 ) ) ;
#53606=CARTESIAN_POINT ( 'NONE',  ( 18.20361801365685750, -2.140066979970441263, 13.83614404522478480 ) ) ;
#53616=ADVANCED_FACE ( 'NONE', ( #43744 ), #65041, .T. ) ;
#53619=CARTESIAN_POINT ( 'NONE',  ( 5.700000000000000178, -13.04986661130000059, 1.811520473896000016 ) ) ;
#53621=CARTESIAN_POINT ( 'NONE',  ( 18.07108758010737048, 2.852736468701840611, -12.36237742790534533 ) ) ;
#53624=B_SPLINE_CURVE_WITH_KNOTS ( 'NONE', 3,
 ( #9974, #30619, #3353, #4027 ),
 .UNSPECIFIED., .F., .F.,
 ( 4, 4 ),
 ( 0.000000000000000000, 1.000000000000000000 ),
 .UNSPECIFIED. ) ;
#53631=DIRECTION ( 'NONE',  ( 0.000000000000000000, -0.9553735099700838562, 0.2954005017724949944 ) ) ;
#53633=CARTESIAN_POINT ( 'NONE',  ( 12.47441792805236815, 0.5304820368560160260, -12.68508456201359991 ) ) ;
#53641=CARTESIAN_POINT ( 'NONE',  ( 18.11727294764897067, 0.2737714783216526060, 12.69604447593775198 ) ) ;
#53647=CARTESIAN_POINT ( 'NONE',  ( 17.75779383521792099, 3.091556742956585779, -13.53003950643005204 ) ) ;
#53653=ORIENTED_EDGE ( 'NONE', *, *, #59426, .F. ) ;
#53661=CARTESIAN_POINT ( 'NONE',  ( 7.100000000000000533, -12.50865771883999855, 2.924687089724999911 ) ) ;
#53672=CARTESIAN_POINT ( 'NONE',  ( 18.06968158350326092, 0.3547715225740352696, -13.89390930605025787 ) ) ;
#53684=CIRCLE ( 'NONE', #35816, 12.59999999999999964 ) ;
#53686=CARTESIAN_POINT ( 'NONE',  ( 12.52680909801648390, 3.059742249080376286, -13.53867541207075220 ) ) ;
#53689=CARTESIAN_POINT ( 'NONE',  ( 18.17477505917495151, 0.08167545936615694391, 13.89968205666727386 ) ) ;
#53691=VERTEX_POINT ( 'NONE', #30089 ) ;
#53692=CARTESIAN_POINT ( 'NONE',  ( 12.34511315269135778, 0.4233056299066624839, 13.89132630015666514 ) ) ;
#53695=CARTESIAN_POINT ( 'NONE',  ( 18.06844887846742154, -0.3566139488127487156, -13.89384732036045023 ) ) ;
#53701=EDGE_CURVE ( 'NONE', #32730, #65648, #37484, .T. ) ;
#53703=CARTESIAN_POINT ( 'NONE',  ( 18.17180462559269571, 0.1017072266180434337, 12.69945743039634856 ) ) ;
#53716=VERTEX_POINT ( 'NONE', #30758 ) ;
#53719=AXIS2_PLACEMENT_3D ( 'NONE', #24724, #29297, #13218 ) ;
#53720=CARTESIAN_POINT ( 'NONE',  ( 17.57925688241711626, 3.199751027636638323, -12.18694352263475444 ) ) ;
#53735=CARTESIAN_POINT ( 'NONE',  ( 17.74610569661007631, -0.5951713840684283996, -13.88284414672551392 ) ) ;
#53751=CARTESIAN_POINT ( 'NONE',  ( 12.23381074371948429, -2.246196888878375209, -12.50707970526073609 ) ) ;
#53755=CARTESIAN_POINT ( 'NONE',  ( 12.21346991607045496, -2.095738610141145486, -13.84225324474580354 ) ) ;
#53758=CARTESIAN_POINT ( 'NONE',  ( 18.26928656998121525, -2.355301763765359713, 12.37791135143290866 ) ) ;
#53788=CARTESIAN_POINT ( 'NONE',  ( 18.17997055489863811, 2.522561811188517300, 13.66861645680632797 ) ) ;
#53799=CARTESIAN_POINT ( 'NONE',  ( 18.26224557552280103, -2.355566563843558558, -13.80042983216602437 ) ) ;
#53829=CARTESIAN_POINT ( 'NONE',  ( 12.56995090575623308, -3.160862399908569209, -12.19708787818173867 ) ) ;
#53837=CARTESIAN_POINT ( 'NONE',  ( 17.69686089611048985, 0.6090396975623089126, -12.68033511803396252 ) ) ;
#53848=CARTESIAN_POINT ( 'NONE',  ( 18.00922683609308095, 1.919385048924809656, 12.45295227646844616 ) ) ;
#53849=CARTESIAN_POINT ( 'NONE',  ( 12.53635786351535053, 1.839692799137174095, 13.87860051966028152 ) ) ;
#53852=CARTESIAN_POINT ( 'NONE',  ( 12.80505043854146940, -1.787816316115923287, 13.88537766212463076 ) ) ;
#53854=CARTESIAN_POINT ( 'NONE',  ( 12.51946955736931422, -3.141640009352832941, 12.20205326030422199 ) ) ;
#53860=CARTESIAN_POINT ( 'NONE',  ( 12.13986395842897537, 0.2863297863804566412, 12.59675086341328409 ) ) ;
#53863=CARTESIAN_POINT ( 'NONE',  ( 12.76350962112086407, 3.123958135104669243, 12.28404825260450117 ) ) ;
#53870=CARTESIAN_POINT ( 'NONE',  ( 12.30934879320328079, 2.881204795976714639, 12.35454860660065890 ) ) ;
#53874=CARTESIAN_POINT ( 'NONE',  ( 12.31001894270039720, 0.3816018581758214845, 12.69228475098156395 ) ) ;
#53876=CARTESIAN_POINT ( 'NONE',  ( 18.00096484323668022, 0.5748214922193798371, -12.58705572532864991 ) ) ;
#53878=CARTESIAN_POINT ( 'NONE',  ( 12.08107629042319253, -2.473358331846541525, 13.77980712931821827 ) ) ;
#53881=EDGE_LOOP ( 'NONE', ( #52529, #2176, #17094, #65153 ) ) ;
#53898=EDGE_CURVE ( 'NONE', #19784, #47809, #21545, .T. ) ;
#53904=CARTESIAN_POINT ( 'NONE',  ( 18.05294241905986041, -2.122066809870763571, 13.74638883949612023 ) ) ;
#53913=CARTESIAN_POINT ( 'NONE',  ( 12.32101708576682064, 0.3953980351523287418, -13.89243073565737241 ) ) ;
#53923=CARTESIAN_POINT ( 'NONE',  ( 18.12468263438044147, -2.757387671472311119, -12.38786642819431982 ) ) ;
#53928=CARTESIAN_POINT ( 'NONE',  ( 17.55505043854147118, -1.875000000000000000, -12.57541666120755863 ) ) ;
#53929=CARTESIAN_POINT ( 'NONE',  ( 12.24422661137779400, -0.2766185922798731212, 13.89631150889696798 ) ) ;
#53941=DIRECTION ( 'NONE',  ( -0.000000000000000000, -0.000000000000000000, 1.000000000000000000 ) ) ;
#53967=ORIENTED_EDGE ( 'NONE', *, *, #53256, .T. ) ;
#53968=CARTESIAN_POINT ( 'NONE',  ( 12.78441639972301758, 0.6247443594537122058, -12.67930618256806419 ) ) ;
#53972=CARTESIAN_POINT ( 'NONE',  ( 12.07911454975265642, 2.296549521726467091, 12.39040777275211624 ) ) ;
#53973=ORIENTED_EDGE ( 'NONE', *, *, #18087, .F. ) ;
#53979=CARTESIAN_POINT ( 'NONE',  ( 18.05193840056092114, 0.3791517837227010856, 12.69238281682775416 ) ) ;
#53987=CARTESIAN_POINT ( 'NONE',  ( 17.93750432894411517, 2.994741171281513736, -13.55599983589036484 ) ) ;
#54008=EDGE_CURVE ( 'NONE', #21149, #7230, #39712, .T. ) ;
#54018=CARTESIAN_POINT ( 'NONE',  ( 12.70875935989986338, 1.793877008111237403, -13.88459618876652968 ) ) ;
#54021=CARTESIAN_POINT ( 'NONE',  ( 18.12461517476719308, -0.2575405707509137443, 13.89679341043304994 ) ) ;
#54026=CARTESIAN_POINT ( 'NONE',  ( 12.20957190031489503, -0.1900921648596720082, 13.89825464817906564 ) ) ;
#54028=CARTESIAN_POINT ( 'NONE',  ( 12.53086501631639393, -0.5620205155227050442, -13.88470856849332513 ) ) ;
#54030=CARTESIAN_POINT ( 'NONE',  ( 17.96218347282713879, -0.4743995195315680591, -13.88910611340119772 ) ) ;
#54040=CARTESIAN_POINT ( 'NONE',  ( 18.15913468976203404, 0.1616215023347959134, 12.69863621249087871 ) ) ;
#54059=CARTESIAN_POINT ( 'NONE',  ( 18.03569330394757131, 3.019535577993371689, -12.23285103262380957 ) ) ;
#54075=CARTESIAN_POINT ( 'NONE',  ( 17.55505043854144276, -0.6250000000000001110, -13.88107975066922428 ) ) ;
#54084=CARTESIAN_POINT ( 'NONE',  ( 18.18506112704245581, -2.156549459697490345, 13.83291014715494072 ) ) ;
#54087=CARTESIAN_POINT ( 'NONE',  ( 18.00086602813224701, 0.5750310236279777554, 12.58704914195693192 ) ) ;
#54090=CARTESIAN_POINT ( 'NONE',  ( 12.22206196700521375, -2.274492675301823752, -12.50124639636504220 ) ) ;
#54092=CARTESIAN_POINT ( 'NONE',  ( 7.100000000000000533, 0.000000000000000000, 0.000000000000000000 ) ) ;
#54094=CARTESIAN_POINT ( 'NONE',  ( 17.55505043854144276, 0.000000000000000000, -25.00000000000000000 ) ) ;
#54095=CARTESIAN_POINT ( 'NONE',  ( 12.15443728026463965, -2.840296387118483867, -13.70885984368922372 ) ) ;
#54098=CARTESIAN_POINT ( 'NONE',  ( 12.43699713708037891, -3.107380776419843560, 12.21088077983946363 ) ) ;
#54099=B_SPLINE_CURVE_WITH_KNOTS ( 'NONE', 1,
 ( #11900, #11548 ),
 .UNSPECIFIED., .F., .F.,
 ( 2, 2 ),
 ( 0.000000000000000000, 1.000000000000000000 ),
 .UNSPECIFIED. ) ;
#54100=CARTESIAN_POINT ( 'NONE',  ( 17.93748940951491022, -2.994360127459124943, 12.32254798267195106 ) ) ;
#54130=CARTESIAN_POINT ( 'NONE',  ( 18.17537806675982637, 2.421014888063410808, 13.68986186821173767 ) ) ;
#54137=FACE_OUTER_BOUND ( 'NONE', #62339, .T. ) ;
#54141=CARTESIAN_POINT ( 'NONE',  ( 18.17327101506966969, -2.135860178445234236, -13.83613041148202605 ) ) ;
#54158=PRODUCT_DEFINITION_FORMATION_WITH_SPECIFIED_SOURCE ( 'ANY', '', #46133, .NOT_KNOWN. ) ;
#54161=CARTESIAN_POINT ( 'NONE',  ( 12.29866314003339589, 2.995318252715385654, -12.23879431495722514 ) ) ;
#54169=CARTESIAN_POINT ( 'NONE',  ( 12.40985643288215812, -3.083578315866618347, -12.21685683184791138 ) ) ;
#54178=CARTESIAN_POINT ( 'NONE',  ( 17.67403227923241005, -0.7096370184368607781, -12.58000072970462924 ) ) ;
#54187=CARTESIAN_POINT ( 'NONE',  ( 18.22966818124860211, 2.744306698987324822, 12.29751612260396954 ) ) ;
#54188=CARTESIAN_POINT ( 'NONE',  ( 12.54752909501214297, 1.835309592424127834, 13.87918066653183224 ) ) ;
#54193=CARTESIAN_POINT ( 'NONE',  ( 12.75668783919150151, -3.198551280946745567, 12.18725874734143844 ) ) ;
#54199=CARTESIAN_POINT ( 'NONE',  ( 12.25943167926923749, -0.4738025322793273930, 12.59109159930368627 ) ) ;
#54202=CARTESIAN_POINT ( 'NONE',  ( 12.18551697106545717, 2.583096739011645493, 12.43182067874258578 ) ) ;
#54206=CARTESIAN_POINT ( 'NONE',  ( 18.17069881803083220, -0.3800566752825981776, 12.59427093624936234 ) ) ;
#54212=CARTESIAN_POINT ( 'NONE',  ( 18.00675905399072363, -0.4321659192889827916, 12.69010673283423429 ) ) ;
#54219=CARTESIAN_POINT ( 'NONE',  ( 17.65223863466379228, -0.7192245859875955327, -12.57945610904468658 ) ) ;
#54221=CARTESIAN_POINT ( 'NONE',  ( 12.17076609166790746, -2.871707895891081108, 13.70231394784453371 ) ) ;
#54228=CARTESIAN_POINT ( 'NONE',  ( 7.100000000000000533, -12.03770622561999915, 3.722046322334000124 ) ) ;
#54231=CARTESIAN_POINT ( 'NONE',  ( 17.78721996965301955, 1.919630126996079600, -12.56804012644223612 ) ) ;
#54236=CARTESIAN_POINT ( 'NONE',  ( 12.80505043854144276, -0.6250000000000001110, 12.67928921589117586 ) ) ;
#54239=CARTESIAN_POINT ( 'NONE',  ( 5.599958567364899942, -11.06886219213000011, 1.536526853569999851 ) ) ;
#54245=CARTESIAN_POINT ( 'NONE',  ( 17.96105691736160637, -2.975276276409919873, 13.56109295189183150 ) ) ;
#54253=CARTESIAN_POINT ( 'NONE',  ( 12.07956470885932987, -2.330212498096153606, -13.80606232674627520 ) ) ;
#54267=CARTESIAN_POINT ( 'NONE',  ( 18.01300802853351968, -2.925445001331292705, -12.34219835790438502 ) ) ;
#54271=CARTESIAN_POINT ( 'NONE',  ( 12.49912319420860030, 3.045104416349984522, 13.54255671968480357 ) ) ;
#54274=CARTESIAN_POINT ( 'NONE',  ( 12.78440343889028874, 0.6249994633519863063, 13.88107975068473365 ) ) ;
#54303=CARTESIAN_POINT ( 'NONE',  ( 5.700000000000000178, -13.04986661130000059, -1.811520473896000016 ) ) ;
#54319=CARTESIAN_POINT ( 'NONE',  ( 12.75601868328677213, 3.199663661910121526, 12.18696649917219332 ) ) ;
#54327=CARTESIAN_POINT ( 'NONE',  ( 5.655092287088755221, 12.08052032219111815, -3.735600122825968317 ) ) ;
#54330=CARTESIAN_POINT ( 'NONE',  ( 17.84291783703835677, 3.054853729147657848, -13.53999333998545573 ) ) ;
#54332=DIRECTION ( 'NONE',  ( 1.000000000000000000, 0.000000000000000000, 0.000000000000000000 ) ) ;
#54343=CARTESIAN_POINT ( 'NONE',  ( 17.86920599196271198, -3.040695425050457867, -13.54374392799785198 ) ) ;
#54362=FACE_OUTER_BOUND ( 'NONE', #38218, .T. ) ;
#54365=CARTESIAN_POINT ( 'NONE',  ( 12.20418674196358388, 2.672312675674151095, -13.63540648336421413 ) ) ;
#54368=CARTESIAN_POINT ( 'NONE',  ( 18.14493363608988474, -0.4251989115648892592, 13.99355557726514654 ) ) ;
#54374=CARTESIAN_POINT ( 'NONE',  ( 12.20071588506785254, -0.1606973241710302203, 13.89876784138693289 ) ) ;
#54375=CARTESIAN_POINT ( 'NONE',  ( 12.29146891699357091, -0.3563501258530247240, -13.89385640120244325 ) ) ;
#54376=DIRECTION ( 'NONE',  ( 0.000000000000000000, -1.000000000000000000, -0.000000000000000000 ) ) ;
#54377=CARTESIAN_POINT ( 'NONE',  ( 17.55505043854144276, 0.6250000000000001110, -25.00000000000000000 ) ) ;
#54388=CARTESIAN_POINT ( 'NONE',  ( 18.02507753857511474, -0.4124490627810481480, 12.69099791225215235 ) ) ;
#54390=CARTESIAN_POINT ( 'NONE',  ( 18.02583793287565683, -2.911580782555497127, -12.34610277261805855 ) ) ;
#54405=CARTESIAN_POINT ( 'NONE',  ( 12.10479047996948232, -0.1866745257715890227, -12.59862229962904223 ) ) ;
#54407=CARTESIAN_POINT ( 'NONE',  ( 17.79586754331421972, 3.158948767300548965, -12.19758365745370021 ) ) ;
#54408=CARTESIAN_POINT ( 'NONE',  ( 5.569720047906554505, 12.16229356903371794, 3.760137167885124754 ) ) ;
#54416=AXIS2_PLACEMENT_3D ( 'NONE', #22394, #16456, #32216 ) ;
#54421=CARTESIAN_POINT ( 'NONE',  ( 12.75601781082312947, 1.760880198315114553, -12.47634966360018005 ) ) ;
#54423=CARTESIAN_POINT ( 'NONE',  ( 17.78863088638136247, 0.6916885356983994981, -13.98290438115173906 ) ) ;
#54438=CARTESIAN_POINT ( 'NONE',  ( 12.51634965191645499, -1.945578265428328457, -12.56358890505709880 ) ) ;
#54440=DIRECTION ( 'NONE',  ( -0.000000000000000000, 0.6194815870790952861, 0.7850111867164476509 ) ) ;
#54441=EDGE_CURVE ( 'NONE', #32174, #6933, #37949, .T. ) ;
#54442=DIRECTION ( 'NONE',  ( 1.000000000000000000, 0.000000000000000000, 0.000000000000000000 ) ) ;
#54443=CARTESIAN_POINT ( 'NONE',  ( 12.11816748453751913, -2.752694035764604141, -13.72673318081622718 ) ) ;
#54446=CARTESIAN_POINT ( 'NONE',  ( 12.08055032392415207, -2.669683454855332094, 12.31540075205091966 ) ) ;
#54447=CARTESIAN_POINT ( 'NONE',  ( 18.08807463888095057, -1.992345594299827161, 12.44148860874184592 ) ) ;
#54456=AXIS2_PLACEMENT_3D ( 'NONE', #27148, #31704, #21202 ) ;
#54460=VERTEX_POINT ( 'NONE', #52654 ) ;
#54464=FACE_OUTER_BOUND ( 'NONE', #28220, .T. ) ;
#54469=EDGE_CURVE ( 'NONE', #24573, #35849, #32415, .T. ) ;
#54478=CARTESIAN_POINT ( 'NONE',  ( 18.09841665128858779, 2.190490658128017021, 13.73421521058127759 ) ) ;
#54490=CARTESIAN_POINT ( 'NONE',  ( 18.23381869303825553, -2.775531333002572598, -13.72213247881302856 ) ) ;
#54513=CARTESIAN_POINT ( 'NONE',  ( 12.36094932703097093, 3.049537035394463746, -12.22540636754321319 ) ) ;
#54523=CARTESIAN_POINT ( 'NONE',  ( 12.75685601902880073, -3.198499228556006990, -12.18727240180921179 ) ) ;
#54532=CARTESIAN_POINT ( 'NONE',  ( 17.86819591275963148, -0.5409888710114163501, -12.68448745112149645 ) ) ;
#54533=CARTESIAN_POINT ( 'NONE',  ( 12.18822406274264658, 2.601257609780446067, -12.42743042557257915 ) ) ;
#54540=DIRECTION ( 'NONE',  ( 0.000000000000000000, -1.000000000000000000, 0.000000000000000000 ) ) ;
#54543=CARTESIAN_POINT ( 'NONE',  ( 17.98055108453612760, 1.897673117161885248, 12.45627908894455338 ) ) ;
#54549=CARTESIAN_POINT ( 'NONE',  ( 12.11326330726104139, -2.264210275637939418, 12.39489744172470687 ) ) ;
#54556=CARTESIAN_POINT ( 'NONE',  ( 12.80505043854144276, -0.7192913403693028673, 12.57945229203838444 ) ) ;
#54559=AXIS2_PLACEMENT_3D ( 'NONE', #35404, #3569, #24903 ) ;
#54560=CARTESIAN_POINT ( 'NONE',  ( 12.66194203315988709, 3.108482559131307443, 12.28874639354599196 ) ) ;
#54564=CARTESIAN_POINT ( 'NONE',  ( 18.24150829797649109, -0.2316996085785957560, 12.59787430930301433 ) ) ;
#54578=CARTESIAN_POINT ( 'NONE',  ( 12.23619509270001160, -2.970722878206530471, 13.68118758531137757 ) ) ;
#54588=CARTESIAN_POINT ( 'NONE',  ( 17.98541303540591940, 2.046657644932490250, -12.54573712159720777 ) ) ;
#54600=CARTESIAN_POINT ( 'NONE',  ( 18.17895306041987880, -2.542296241241987165, 13.66441818551904852 ) ) ;
#54602=ORIENTED_EDGE ( 'NONE', *, *, #66716, .T. ) ;
#54617=ORIENTED_EDGE ( 'NONE', *, *, #65099, .T. ) ;
#54618=CARTESIAN_POINT ( 'NONE',  ( 4.600000207916515649, 0.000000000000000000, -9.325873406851000657E-14 ) ) ;
#54621=PLANE ( 'NONE',  #62644 ) ;
#54624=CARTESIAN_POINT ( 'NONE',  ( 12.57340716663134295, 1.919420395509098043, 13.77954053360031850 ) ) ;
#54626=CARTESIAN_POINT ( 'NONE',  ( 17.63816080826980226, -1.880463790428644533, 12.57456020225082050 ) ) ;
#54628=CARTESIAN_POINT ( 'NONE',  ( 12.42411034028606309, 0.4959091552601215813, 13.88809952003718173 ) ) ;
#54632=ADVANCED_FACE ( 'NONE', ( #51879 ), #42188, .F. ) ;
#54644=CARTESIAN_POINT ( 'NONE',  ( 17.74431590772262979, -1.811500042934492072, 13.88231098337033131 ) ) ;
#54671=CARTESIAN_POINT ( 'NONE',  ( 12.61270316626370125, 1.780234759031155134, 12.47365767676520854 ) ) ;
#54674=CARTESIAN_POINT ( 'NONE',  ( 12.11457335221577303, -0.2229649748661372555, -13.99822903660538564 ) ) ;
#54683=CARTESIAN_POINT ( 'NONE',  ( 18.12605992003768307, 2.245077608621426357, -13.72424617901693544 ) ) ;
#54690=CARTESIAN_POINT ( 'NONE',  ( 18.18005043855006875, 0.04052604707540623935, -12.70000016496744522 ) ) ;
#54693=ORIENTED_EDGE ( 'NONE', *, *, #30875, .T. ) ;
#54697=CARTESIAN_POINT ( 'NONE',  ( 18.16759718505687005, -2.624144390823405892, -13.64629239165651953 ) ) ;
#54704=CARTESIAN_POINT ( 'NONE',  ( 18.08635919897133704, -2.970004615628412559, -12.24496439055023522 ) ) ;
#54707=PLANE ( 'NONE',  #12864 ) ;
#54716=CARTESIAN_POINT ( 'NONE',  ( 12.19422188688372266, 2.632730885462788883, -13.64441700900758292 ) ) ;
#54720=CARTESIAN_POINT ( 'NONE',  ( 18.26152657770007082, -0.1657344298535245175, 13.99903850390422910 ) ) ;
#54726=CARTESIAN_POINT ( 'NONE',  ( 12.21279768065092952, -0.1999278271778355542, 13.89806912752932710 ) ) ;
#54727=CARTESIAN_POINT ( 'NONE',  ( 12.46489557886510191, -0.5244061151917449592, -13.88668399598972947 ) ) ;
#54729=CARTESIAN_POINT ( 'NONE',  ( 4.599999651764306030, -13.27499965161999818, 2.617290972024999914E-09 ) ) ;
#54739=CARTESIAN_POINT ( 'NONE',  ( 17.98240372392063335, -0.4561785182478259038, 12.68897339690746762 ) ) ;
#54741=CARTESIAN_POINT ( 'NONE',  ( 18.11161644829667949, -2.784507902030457505, -12.38071508487800010 ) ) ;
#54749=CARTESIAN_POINT ( 'NONE',  ( 12.80505043854143388, 3.124999999999999556, -25.00000000000000000 ) ) ;
#54752=CARTESIAN_POINT ( 'NONE',  ( 12.15464131684816884, 0.3178346465811170418, -12.59599179195193486 ) ) ;
#54767=AXIS2_PLACEMENT_3D ( 'NONE', #37853, #59177, #36475 ) ;
#54769=CARTESIAN_POINT ( 'NONE',  ( 18.17477505917495151, -0.08167545936615620839, -13.89968205666727386 ) ) ;
#54780=CARTESIAN_POINT ( 'NONE',  ( 12.27940634383494789, -2.838250353068023646, -13.59582428665004450 ) ) ;
#54786=CARTESIAN_POINT ( 'NONE',  ( 12.42127013197883656, -2.006280959398177632, -12.55298695860706992 ) ) ;
#54790=CARTESIAN_POINT ( 'NONE',  ( 12.80505043854146940, -1.787797342887048169, -13.88538010501570952 ) ) ;
#54793=CARTESIAN_POINT ( 'NONE',  ( 17.87931509819279441, -1.836668601340719187, 12.46541920085823918 ) ) ;
#54825=CARTESIAN_POINT ( 'NONE',  ( 18.17186084707618576, 2.602861751209118779, 13.65107289232777177 ) ) ;
#54833=VECTOR ( 'NONE', #62929, 1000.000000000000000 ) ;
#54834=DIRECTION ( 'NONE',  ( -1.000000000000000000, -0.000000000000000000, -0.000000000000000000 ) ) ;
#54838=PLANE ( 'NONE',  #14945 ) ;
#54839=CARTESIAN_POINT ( 'NONE',  ( 18.27904986288418243, -2.473365887482168901, -13.77980577478706969 ) ) ;
#54859=CARTESIAN_POINT ( 'NONE',  ( 12.80505043854143388, 3.199751711897557804, -12.18694338143115630 ) ) ;
#54870=CARTESIAN_POINT ( 'NONE',  ( 12.51412939328312390, -3.139365204187050118, -12.20263940233110311 ) ) ;
#54876=CARTESIAN_POINT ( 'NONE',  ( 12.64146116164748435, -3.103558470340185949, -13.52669597090169340 ) ) ;
#54877=CARTESIAN_POINT ( 'NONE',  ( 17.83205770179218774, -0.5603556898929438201, -12.68335562943301476 ) ) ;
#54878=AXIS2_PLACEMENT_3D ( 'NONE', #19370, #3965, #35124 ) ;
#54879=CARTESIAN_POINT ( 'NONE',  ( 12.19252377751849536, 2.624242476089503118, -12.42177825695367943 ) ) ;
#54884=FACE_OUTER_BOUND ( 'NONE', #26746, .T. ) ;
#54888=CARTESIAN_POINT ( 'NONE',  ( 17.88769455523108931, 1.970775861831701947, 12.55923393539035970 ) ) ;
#54895=CARTESIAN_POINT ( 'NONE',  ( 12.17614882354827621, -2.839252809666454880, 12.27595571488803827 ) ) ;
#54898=DIRECTION ( 'NONE',  ( 0.7071058580587948894, 0.7071077043130949979, -4.007479631938970195E-09 ) ) ;
#54901=CARTESIAN_POINT ( 'NONE',  ( 12.47306973639847882, -0.6395598188657312111, 12.58375915074078577 ) ) ;
#54904=CARTESIAN_POINT ( 'NONE',  ( 12.34719455185577885, 2.925915912524184925, 12.34207449233261933 ) ) ;
#54905=EDGE_LOOP ( 'NONE', ( #44681, #32592, #29981, #32513 ) ) ;
#54923=CARTESIAN_POINT ( 'NONE',  ( 12.08891106753600830, -2.402099963521321602, 13.79240636836165024 ) ) ;
#54942=CARTESIAN_POINT ( 'NONE',  ( 17.55505043854144276, -0.7302158263239199032, -13.98094363220830871 ) ) ;
#54948=CARTESIAN_POINT ( 'NONE',  ( 18.17181771166727344, -2.603111764601558686, 13.65106951237197386 ) ) ;
#54966=CARTESIAN_POINT ( 'NONE',  ( 17.65158693965129899, -1.792693047833532116, -13.88475221912021418 ) ) ;
#54971=CARTESIAN_POINT ( 'NONE',  ( 12.72263738247858456, 1.880115814278896957, 13.78550660562620145 ) ) ;
#54975=CARTESIAN_POINT ( 'NONE',  ( 12.76431688221209981, 0.6240105542978634512, -12.67935574133243470 ) ) ;
#54976=CARTESIAN_POINT ( 'NONE',  ( 12.37769783401832768, -0.4561791668615506889, 13.88992602861185333 ) ) ;
#54986=AXIS2_PLACEMENT_3D ( 'NONE', #57553, #41825, #42180 ) ;
#54997=DIRECTION ( 'NONE',  ( 0.7071068219128313626, 0.000000000000000000, 0.7071067404602613404 ) ) ;
#55013=FACE_OUTER_BOUND ( 'NONE', #34517, .T. ) ;
#55017=CARTESIAN_POINT ( 'NONE',  ( 12.75354487906747458, 0.6229596466635303198, -12.67942438339646749 ) ) ;
#55021=DIRECTION ( 'NONE',  ( 0.000000000000000000, -0.7198977633594747516, -0.6940801180771756229 ) ) ;
#55024=CARTESIAN_POINT ( 'NONE',  ( 12.80505043854144276, 0.6249999999999995559, -13.88107975066922428 ) ) ;
#55030=CARTESIAN_POINT ( 'NONE',  ( 5.604756202879674909, 12.12903653622838007, -3.749090042450943461 ) ) ;
#55033=CARTESIAN_POINT ( 'NONE',  ( 17.57920827036996059, 3.248109283636066102, -13.61799489948997888 ) ) ;
#55044=CARTESIAN_POINT ( 'NONE',  ( 18.16596415355668981, -2.632031932216792658, -13.64451525700246393 ) ) ;
#55049=ORIENTED_EDGE ( 'NONE', *, *, #7820, .T. ) ;
#55051=CARTESIAN_POINT ( 'NONE',  ( 18.25561427624399613, -2.667326636134559337, -12.31445830791194140 ) ) ;
#55063=CARTESIAN_POINT ( 'NONE',  ( 12.20145977811404414, 2.662504703663703065, -13.63765425733092229 ) ) ;
#55067=CARTESIAN_POINT ( 'NONE',  ( 17.88507584039978937, 0.5311540453515649629, 13.88634387573209139 ) ) ;
#55068=CARTESIAN_POINT ( 'NONE',  ( 17.77470470800434654, 0.5852235852771162650, 13.88341353704861270 ) ) ;
#55072=CARTESIAN_POINT ( 'NONE',  ( 12.55587196711313602, -0.5732793990213274071, 13.88408420575303559 ) ) ;
#55073=CARTESIAN_POINT ( 'NONE',  ( 12.60487368088291582, -0.5921679929136640652, -13.88301795523049087 ) ) ;
#55084=CARTESIAN_POINT ( 'NONE',  ( 17.57568447735987149, 0.6247443594537129830, 12.67930618256805886 ) ) ;
#55086=CARTESIAN_POINT ( 'NONE',  ( 18.08152692720914345, -2.836954189429314432, -12.36664858736754447 ) ) ;
#55101=CARTESIAN_POINT ( 'NONE',  ( 12.25170120909045934, 0.4648927885597781695, -12.59142395508372836 ) ) ;
#55116=ADVANCED_FACE ( 'NONE', ( #14590, #9325, #67706, #56893 ), #47094, .T. ) ;
#55119=CARTESIAN_POINT ( 'NONE',  ( 18.14706097348721414, -0.2014071429975138050, -13.89805485625563364 ) ) ;
#55123=DIRECTION ( 'NONE',  ( 0.000000000000000000, -0.7507612787780010288, -0.6605736161001442008 ) ) ;
#55125=CARTESIAN_POINT ( 'NONE',  ( 18.17055204340471875, -2.609142802259613703, 12.42550174405653962 ) ) ;
#55130=FACE_OUTER_BOUND ( 'NONE', #29530, .T. ) ;
#55140=CARTESIAN_POINT ( 'NONE',  ( 17.88706890093973811, -3.029615921040858861, 12.31227368058699412 ) ) ;
#55143=ORIENTED_EDGE ( 'NONE', *, *, #19532, .F. ) ;
#55170=CARTESIAN_POINT ( 'NONE',  ( 18.27121482242686312, 2.402104771923904369, 13.79240553248645540 ) ) ;
#55173=ORIENTED_EDGE ( 'NONE', *, *, #15611, .F. ) ;
#55181=CARTESIAN_POINT ( 'NONE',  ( 18.16514092158340432, -2.912582788079554064, -13.69368340938387973 ) ) ;
#55202=ORIENTED_EDGE ( 'NONE', *, *, #60012, .T. ) ;
#55203=B_SPLINE_SURFACE_WITH_KNOTS ( 'NONE', 1, 3, ( 
 ( #38677, #53720, #48477, #22587, #37632, #5817, #43580, #6156, #7807, #55709, #59301, #58617, #54407, #584, #32063, #27497, #10716, #53380, #27156, #16309, #17349, #43928, #37978, #48822, #21893, #26816, #64881, #43230, #59998, #54059, #236, #12109, #21213, #69107, #65234, #11404, #16994, #32743, #34393, #42543, #64194, #58966, #38322, #32404, #11070, #33091, #59652, #11749, #6508, #49159, #8840, #24578, #9514, #57073, #2899, #9174, #30512, #61632, #14777, #30179, #51485, #67903, #18646, #50456, #24229, #29500, #3581, #45901, #51824, #56044, #67211, #45568, #45221, #66526, #50807, #66873, #19677, #18985, #13748, #13410, #34732, #40311, #61293, #3922, #24916, #56393, #35080, #46248, #8496, #20020, #3249, #41345, #29844, #25259, #62657, #67554, #46598, #36096, #51152, #40998, #57411, #2557, #56744, #23885, #39980, #62323, #8154, #14437 ),
 ( #19324, #40648, #61982, #14092, #35758, #35418, #58792, #48302, #408, #26649, #46936, #42719, #62989, #9867, #52864, #52172, #30856, #47965, #41684, #10898, #21723, #43058, #64, #68238, #64023, #15118, #31211, #4965, #42033, #64361, #15464, #10211, #53553, #68582, #36790, #53205, #37130, #37814, #16485, #21049, #20360, #16144, #31545, #36437, #58449, #57755, #52515, #58111, #47281, #59135, #5644, #26298, #10551, #47626, #4614, #21386, #68936, #4273, #15802, #25948, #25608, #20705, #63336, #26986, #42381, #31894, #63687, #5307, #37466, #32244, #28722, #38502, #43759, #48652, #44466, #1450, #11238, #59827, #1106, #38862, #54588, #39549, #17883, #32918, #39202, #60524, #22418, #44803, #60183, #12289, #50039, #754, #32575, #54231, #59475, #33617, #6683, #12633, #16825, #28028, #6330, #5989, #27328, #11575, #27680, #49688, #48994, #65053 ) ),
 .UNSPECIFIED., .F., .F., .F.,
 ( 2, 2 ),
 ( 4, 2, 2, 2, 2, 2, 2, 2, 2, 2, 2, 2, 2, 2, 2, 2, 2, 2, 2, 2, 2, 2, 2, 2, 2, 2, 2, 2, 2, 2, 2, 2, 2, 2, 2, 2, 2, 2, 2, 2, 2, 2, 2, 2, 2, 2, 2, 2, 2, 2, 2, 2, 2, 4 ),
 ( 0.000000000000000000, 1.000000000000000000 ),
 ( 0.000000000000000000, 7.157214214794704388E-05, 0.0001431442842958940878, 0.0001789303553698675894, 0.0002147164264438411181, 0.0002326094619808278825, 0.0002505024975178146468, 0.0002862885685917881755, 0.0003220746396657616500, 0.0003578607107397351788, 0.0003936467818137087075, 0.0004294328528876822362, 0.0004652189239616557649, 0.0004831119594986425293, 0.0005010049950356292936, 0.0005725771371835763511, 0.0006441492793315233001, 0.0007157214214794703575, 0.0007872935636274174150, 0.0008588657057753644724, 0.0008946517768493380011, 0.0009304378479233115298, 0.0009662239189972850585, 0.001002009990071258587, 0.001037796061145232224, 0.001073582132219205645, 0.001145154274367152702, 0.001180940345441126339, 0.001216726416515099760, 0.001252512487589073180, 0.001288298558663046600, 0.001359870700810993658, 0.001395656771884967295, 0.001431442842958940715, 0.001467228914032914135, 0.001503014985106887772, 0.001574587127254834830, 0.001646159269402781887, 0.001681945340476755524, 0.001717731411550728945, 0.001753517482624702365, 0.001789303553698676002, 0.001860875695846623060, 0.001896661766920596480, 0.001932447837994570117, 0.001968233909068543754, 0.002004019980142517175, 0.002039806051216491029, 0.002075592122290464449, 0.002147164264438411289, 0.002182950335512384710, 0.002218736406586358130, 0.002254522477660331550, 0.002290308548734305404 ),
 .UNSPECIFIED. ) ;
#55207=CARTESIAN_POINT ( 'NONE',  ( 12.21409778435354809, 2.897922531322544515, -12.26223633105722044 ) ) ;
#55213=DIRECTION ( 'NONE',  ( -1.000000000000000000, 0.000000000000000000, 0.000000000000000000 ) ) ;
#55215=B_SPLINE_SURFACE_WITH_KNOTS ( 'NONE', 1, 3, ( 
 ( #16277, #53002, #22208, #43545, #549, #20840, #37945, #58240, #5098, #201, #37602, #27125, #59267, #10685, #11370, #42852, #47414, #63474, #27462, #42512, #58933, #10345, #32711, #59617, #21861, #54021, #37263, #43198, #26434, #68719, #21181, #64845, #896, #21520, #32374, #26785, #47764, #64500, #6123, #32033, #63819, #11037, #16956, #42174, #53689, #64164, #11713, #33052, #4745, #15933, #26087, #15596, #5448, #53346, #48441, #18358, #50171, #40033, #23942, #27820, #28507, #49468, #49820, #1933, #28154, #1579, #22897, #44595, #44249, #34095, #65545, #55067, #60312, #18700, #12768, #23253, #12420, #6819, #55415, #60999, #33403, #29198, #7508, #55763, #34449, #2273 ),
 ( #23591, #18016, #61345, #50510, #17668, #65888, #39334, #43892, #44934, #60654, #66239, #13120, #38992, #13465, #1238, #7168, #28864, #22550, #39680, #7865, #54368, #33751, #2611, #45275, #66581, #6472, #65194, #49125, #17314, #38638, #59960, #12071, #54720, #8206, #67261, #29895, #41731, #57456, #24967, #36145, #57118, #46644, #3630, #35805, #14142, #8890, #9219, #52218, #50857, #24284, #67951, #45618, #3295, #56444, #20067, #34786, #51202, #14486, #24631, #14822, #25653, #46299, #2951, #20406, #41394, #45950, #40362, #51873, #4318, #63035, #67599, #9565, #46985, #30905, #66924, #3969, #62370, #19034, #19377, #40699, #62027, #8548, #19725, #68286, #62701, #56095 ) ),
 .UNSPECIFIED., .F., .F., .F.,
 ( 2, 2 ),
 ( 4, 2, 2, 2, 2, 2, 2, 2, 2, 2, 2, 2, 2, 2, 2, 2, 2, 2, 2, 2, 2, 2, 2, 2, 2, 2, 2, 2, 2, 2, 2, 2, 2, 2, 2, 2, 2, 2, 2, 2, 2, 2, 4 ),
 ( 0.000000000000000000, 1.000000000000000000 ),
 ( 0.000000000000000000, 7.083094307561030529E-05, 0.0001416618861512206106, 0.0002124928292268309159, 0.0002833237723024412211, 0.0003541547153780515264, 0.0004249856584536618317, 0.0004958166015292721912, 0.0005666475446048824423, 0.0006374784876804926934, 0.0007083094307561030529, 0.0007791403738317134123, 0.0008145558453695185379, 0.0008499713169073236634, 0.0008853867884451287890, 0.0009208022599829340229, 0.0009916332030585443824, 0.001027048674596349508, 0.001062464146134154633, 0.001097879617671959759, 0.001133295089209764885, 0.001204126032285375136, 0.001239541503823180261, 0.001274956975360985387, 0.001310372446898790512, 0.001345787918436595638, 0.001416618861512206106, 0.001487449804587816574, 0.001522865276125621699, 0.001558280747663426825, 0.001629111690739037076, 0.001699942633814647327, 0.001735358105352452452, 0.001770773576890257578, 0.001806189048428062920, 0.001841604519965868046, 0.001912435463041478514, 0.001983266406117088765, 0.002018681877654893674, 0.002054097349192699016, 0.002124928292268309267, 0.002195759235343919518, 0.002266590178419529769 ),
 .UNSPECIFIED. ) ;
#55216=CARTESIAN_POINT ( 'NONE',  ( 12.28024471298230047, -1.983745382141950397, -12.44286253672009757 ) ) ;
#55222=CARTESIAN_POINT ( 'NONE',  ( 12.35432851685907707, -2.933105360581562682, -13.57195094675648228 ) ) ;
#55223=CARTESIAN_POINT ( 'NONE',  ( 18.11801110581809127, -0.2715269968477674323, -12.69609476950841831 ) ) ;
#55230=CARTESIAN_POINT ( 'NONE',  ( 4.599999999999999645, 0.000000000000000000, 0.000000000000000000 ) ) ;
#55234=CARTESIAN_POINT ( 'NONE',  ( 17.86124198984730782, 1.955044089803213536, 12.56196094884553105 ) ) ;
#55242=CARTESIAN_POINT ( 'NONE',  ( 12.08521996405951171, -2.390121770085883668, 12.37125191860131501 ) ) ;
#55249=CARTESIAN_POINT ( 'NONE',  ( 12.61664271790067282, -0.6949735217938508569, 12.58082105808780682 ) ) ;
#55253=CARTESIAN_POINT ( 'NONE',  ( 12.18778960455903082, 2.401422506651157196, 12.47398279053984460 ) ) ;
#55261=CARTESIAN_POINT ( 'NONE',  ( 17.77470270346956482, -0.5852243768284137726, 12.68184418015406223 ) ) ;
#55268=DIRECTION ( 'NONE',  ( 0.000000000000000000, 0.9553735099700839672, 0.2954005017724949389 ) ) ;
#55269=CARTESIAN_POINT ( 'NONE',  ( 18.08128123659606246, -2.837338021487807893, 13.59610410466120278 ) ) ;
#55272=CARTESIAN_POINT ( 'NONE',  ( 12.15817878876227809, -2.188143349582273078, 13.82794795582454306 ) ) ;
#55276=VERTEX_POINT ( 'NONE', #67365 ) ;
#55279=CARTESIAN_POINT ( 'NONE',  ( 18.11654246898725518, 2.224740281524702823, -13.72801203775192036 ) ) ;
#55293=CARTESIAN_POINT ( 'NONE',  ( 12.29679984375326285, -2.863892094194480986, 12.35932590994786295 ) ) ;
#55297=CARTESIAN_POINT ( 'NONE',  ( 18.09820959019767628, -2.190632709185573290, 13.73422630893085916 ) ) ;
#55304=CARTESIAN_POINT ( 'NONE',  ( 12.61333915124458116, -3.228660600416717319, -13.62267210747915058 ) ) ;
#55316=ADVANCED_FACE ( 'NONE', ( #37622 ), #22212, .T. ) ;
#55317=CARTESIAN_POINT ( 'NONE',  ( 12.58303802678790362, 1.915668549203846993, 13.78011653961192096 ) ) ;
#55323=CARTESIAN_POINT ( 'NONE',  ( 12.08466087602983841, 0.08309727575450238934, 13.99975851644561864 ) ) ;
#55328=DIRECTION ( 'NONE',  ( 1.000000000000000000, 0.000000000000000000, 0.000000000000000000 ) ) ;
#55331=DIRECTION ( 'NONE',  ( -1.000000000000000000, 0.000000000000000000, 0.000000000000000000 ) ) ;
#55349=FACE_OUTER_BOUND ( 'NONE', #13496, .T. ) ;
#55361=VECTOR ( 'NONE', #6666, 1000.000000000000000 ) ;
#55364=CARTESIAN_POINT ( 'NONE',  ( 12.18203530712867177, 2.449198598598032461, -13.68410320367736155 ) ) ;
#55367=ORIENTED_EDGE ( 'NONE', *, *, #5087, .T. ) ;
#55369=CARTESIAN_POINT ( 'NONE',  ( 12.08123665194307073, 0.04806343339260338993, -13.99993753789457962 ) ) ;
#55376=AXIS2_PLACEMENT_3D ( 'NONE', #41665, #52147, #10194 ) ;
#55377=CARTESIAN_POINT ( 'NONE',  ( 18.01376003089016109, 2.074995895013257652, -13.75447352907418974 ) ) ;
#55397=CARTESIAN_POINT ( 'NONE',  ( 18.27481983568693380, -2.390134998303168778, -12.37124935920179070 ) ) ;
#55412=CARTESIAN_POINT ( 'NONE',  ( 12.21285350005639536, 2.096151405059777151, -13.84220188050173839 ) ) ;
#55415=CARTESIAN_POINT ( 'NONE',  ( 17.74610569661007631, 0.5951713840684285106, 13.88284414672552991 ) ) ;
#55417=CARTESIAN_POINT ( 'NONE',  ( 17.69618303683414240, 0.6091729397312527494, 13.88202727520882540 ) ) ;
#55419=ORIENTED_EDGE ( 'NONE', *, *, #30844, .F. ) ;
#55422=CARTESIAN_POINT ( 'NONE',  ( 12.21427240548824500, -2.704226675393127888, 13.62802533672049954 ) ) ;
#55434=CARTESIAN_POINT ( 'NONE',  ( 17.86819591275964214, 0.5409888710114112431, 12.68448745112149467 ) ) ;
#55436=CARTESIAN_POINT ( 'NONE',  ( 18.13163533201626620, -2.741228481684170770, -12.39208274280229993 ) ) ;
#55448=CARTESIAN_POINT ( 'NONE',  ( 12.17712767754845693, -0.3597466176220747713, -12.59486741915706531 ) ) ;
#55453=ORIENTED_EDGE ( 'NONE', *, *, #57884, .T. ) ;
#55464=CARTESIAN_POINT ( 'NONE',  ( 12.80505043854146940, -3.207098164520926886, -13.58558594083658910 ) ) ;
#55466=CARTESIAN_POINT ( 'NONE',  ( 18.23388030753893219, 0.2566959043864865397, -13.99765098363215365 ) ) ;
#55471=AXIS2_PLACEMENT_3D ( 'NONE', #25952, #11850, #44029 ) ;
#55488=CARTESIAN_POINT ( 'NONE',  ( 18.02779610229251617, -1.934613261143892426, 12.45059556317631611 ) ) ;
#55519=CARTESIAN_POINT ( 'NONE',  ( 18.28009623694099162, 2.497067955185368948, 13.77553007214568659 ) ) ;
#55533=CARTESIAN_POINT ( 'NONE',  ( 18.05265757431624962, -3.049509720595951823, -13.66384965554843767 ) ) ;
#55555=CARTESIAN_POINT ( 'NONE',  ( 12.76350981947226515, 1.876041592482996290, -12.57528602315340827 ) ) ;
#55563=CARTESIAN_POINT ( 'NONE',  ( 18.20121223417782730, 0.3818843736423395696, 13.99543728850611757 ) ) ;
#55565=CARTESIAN_POINT ( 'NONE',  ( 12.08198123077154840, -2.425144973324802944, -12.36441727636090349 ) ) ;
#55572=CARTESIAN_POINT ( 'NONE',  ( 12.24414859480286921, -2.775896286417997239, -13.61101139974199548 ) ) ;
#55573=CARTESIAN_POINT ( 'NONE',  ( 18.17177216100527914, 0.1019009512359512898, -12.69945530929772559 ) ) ;
#55584=CARTESIAN_POINT ( 'NONE',  ( 18.14141836411847208, 2.283433982113741045, 12.49938471124204931 ) ) ;
#55588=CARTESIAN_POINT ( 'NONE',  ( 5.700000000000000178, -12.50865771883999855, -2.924687089723999822 ) ) ;
#55589=CARTESIAN_POINT ( 'NONE',  ( 12.71012035428156928, -0.7146386402780370295, -12.57972080578504404 ) ) ;
#55591=CARTESIAN_POINT ( 'NONE',  ( 12.80505043854146940, -1.875000000000000444, 12.57545641911172396 ) ) ;
#55598=CARTESIAN_POINT ( 'NONE',  ( 12.09164653790448440, -0.1286734328892388535, 12.59934825840596595 ) ) ;
#55601=B_SPLINE_CURVE_WITH_KNOTS ( 'NONE', 3,
 ( #62383, #66937, #7878, #45289 ),
 .UNSPECIFIED., .F., .F.,
 ( 4, 4 ),
 ( 0.000000000000000000, 1.000000000000000000 ),
 .UNSPECIFIED. ) ;
#55602=CARTESIAN_POINT ( 'NONE',  ( 12.22206196700517822, 2.274492675301821976, 12.50124639636504931 ) ) ;
#55609=CARTESIAN_POINT ( 'NONE',  ( 18.01482197265775653, -0.4234835428822800174, 12.69049809666515394 ) ) ;
#55614=CARTESIAN_POINT ( 'NONE',  ( 17.96364285837030650, -0.4729642813570114068, -12.68814481174042363 ) ) ;
#55628=CARTESIAN_POINT ( 'NONE',  ( 17.77476912165378664, -0.5854932480584860155, 13.88340087527186384 ) ) ;
#55641=CARTESIAN_POINT ( 'NONE',  ( 12.20883946518622132, -2.687526094403444255, 12.40592204487990990 ) ) ;
#55645=CARTESIAN_POINT ( 'NONE',  ( 17.95040605897959196, -3.130086699081792379, 13.64560748759991071 ) ) ;
#55669=CARTESIAN_POINT ( 'NONE',  ( 12.70873338277715980, 3.242082958893194089, 13.61943113270052663 ) ) ;
#55674=CARTESIAN_POINT ( 'NONE',  ( 12.80505043854144098, 0.7302158263239096891, 13.98094363220831227 ) ) ;
#55684=VECTOR ( 'NONE', #2510, 1000.000000000000000 ) ;
#55687=CARTESIAN_POINT ( 'NONE',  ( 12.80505043854143388, 3.199698446519374517, 12.18695736643652694 ) ) ;
#55703=CARTESIAN_POINT ( 'NONE',  ( 12.49122810691469709, 3.040889930145693754, 13.54369178477972468 ) ) ;
#55709=CARTESIAN_POINT ( 'NONE',  ( 17.77301286688677706, 3.166510366255908870, -12.19562279494696178 ) ) ;
#55720=CARTESIAN_POINT ( 'NONE',  ( 12.61399518047280210, 0.5951713840684276224, -13.88284414672551392 ) ) ;
#55728=CARTESIAN_POINT ( 'NONE',  ( 17.78669369145615420, 1.919420387948956419, -13.77958849407365527 ) ) ;
#55735=CARTESIAN_POINT ( 'NONE',  ( 17.69617877290574626, 0.6091736731973926844, -12.68032649603847339 ) ) ;
#55736=DIRECTION ( 'NONE',  ( 0.000000000000000000, -0.6556630511404241135, 0.7550536162215433222 ) ) ;
#55739=CARTESIAN_POINT ( 'NONE',  ( 17.94485468265261119, -2.989306481691796691, -13.55738131292138426 ) ) ;
#55749=CARTESIAN_POINT ( 'NONE',  ( 18.23116755655862065, -2.220104646260180559, -12.40287289761280398 ) ) ;
#55759=CARTESIAN_POINT ( 'NONE',  ( 12.08002994951551123, 2.497059486053646360, -13.77553160571068425 ) ) ;
#55763=CARTESIAN_POINT ( 'NONE',  ( 17.59617041303008378, 0.6239795106976183670, 13.88114172264461210 ) ) ;
#55764=CARTESIAN_POINT ( 'NONE',  ( 18.14129716923323699, -2.282346377875212884, 12.49966253006511430 ) ) ;
#55769=CARTESIAN_POINT ( 'NONE',  ( 12.20100803716184679, -2.660536040162761573, 13.63809770095273066 ) ) ;
#55781=CARTESIAN_POINT ( 'NONE',  ( 17.81530815050373917, -3.068584091768072231, -12.30073186569158850 ) ) ;
#55786=CARTESIAN_POINT ( 'NONE',  ( 12.78422835261028112, -1.875000554926937291, 13.78631940402569001 ) ) ;
#55790=CYLINDRICAL_SURFACE ( 'NONE', #33165, 13.17499999999999893 ) ;
#55795=CARTESIAN_POINT ( 'NONE',  ( 12.41154142318500675, 0.6042324041877048524, -12.58550538354983672 ) ) ;
#55803=EDGE_CURVE ( 'NONE', #18846, #46748, #22235, .T. ) ;
#55811=ORIENTED_EDGE ( 'NONE', *, *, #47373, .F. ) ;
#55814=CARTESIAN_POINT ( 'NONE',  ( 17.97798355280614402, 0.5935699150349397213, -13.98741755999924941 ) ) ;
#55815=ORIENTED_EDGE ( 'NONE', *, *, #43986, .F. ) ;
#55823=CARTESIAN_POINT ( 'NONE',  ( 12.72092075291392987, -3.120619064207171611, -13.52200130461745431 ) ) ;
#55833=CARTESIAN_POINT ( 'NONE',  ( 12.54664124763764121, -0.5694488842926265226, -13.88429844810376323 ) ) ;
#55834=CARTESIAN_POINT ( 'NONE',  ( 18.17157907633054137, -2.603049611614717040, 12.42699283961531265 ) ) ;
#55858=CARTESIAN_POINT ( 'NONE',  ( 18.00565376249822336, -0.5635217852606937416, 12.58739276154098086 ) ) ;
#55864=CARTESIAN_POINT ( 'NONE',  ( 18.14518304970620477, 2.942254210842375262, 13.68733852372544568 ) ) ;
#55901=CARTESIAN_POINT ( 'NONE',  ( 12.19329499274038398, 2.371606608387608617, -12.48058234101797126 ) ) ;
#55904=ADVANCED_FACE ( 'NONE', ( #51059 ), #19235, .F. ) ;
#55909=CARTESIAN_POINT ( 'NONE',  ( 17.74534446683163225, -0.7110419930699923841, 13.98197980709423760 ) ) ;
#55911=CARTESIAN_POINT ( 'NONE',  ( 12.12640605329509391, -2.733942857944761329, -12.29982446443561628 ) ) ;
#55917=CARTESIAN_POINT ( 'NONE',  ( 12.52635726938502003, -3.059519608057332807, -13.53867825407381176 ) ) ;
#55918=CARTESIAN_POINT ( 'NONE',  ( 18.15913468976204825, -0.1616215023347997159, -12.69863621249089825 ) ) ;
#55925=CARTESIAN_POINT ( 'NONE',  ( 18.16706615774980449, 2.626761370952298336, 13.64570327794280757 ) ) ;
#55929=CARTESIAN_POINT ( 'NONE',  ( 17.85706045311519929, 3.134356930968896116, 12.20392612899626528 ) ) ;
#55930=CARTESIAN_POINT ( 'NONE',  ( 17.55505043854143565, 3.125000000000000000, -12.28374638332999602 ) ) ;
#55935=CARTESIAN_POINT ( 'NONE',  ( 12.26151780194103935, -2.191289199348898986, 12.51818198400761339 ) ) ;
#55940=CARTESIAN_POINT ( 'NONE',  ( 12.19636936301369978, 0.1422617729927580787, 12.69893308522357245 ) ) ;
#55943=CARTESIAN_POINT ( 'NONE',  ( 12.49819407809062177, 1.955416873541953038, 12.56189665940130773 ) ) ;
#55954=CARTESIAN_POINT ( 'NONE',  ( 18.13610002190272752, -0.2304169715717201972, -12.69719098617233222 ) ) ;
#55960=CARTESIAN_POINT ( 'NONE',  ( 7.100000000000000533, 13.04986661130000059, 1.811520473896000016 ) ) ;
#55963=AXIS2_PLACEMENT_3D ( 'NONE', #58187, #21128, #53631 ) ;
#55969=CARTESIAN_POINT ( 'NONE',  ( 17.55505043854144276, -0.6250000000000001110, 13.88107975066923316 ) ) ;
#55978=CARTESIAN_POINT ( 'NONE',  ( 4.599999999999999645, -12.59999999999999964, 1.543054966925665076E-15 ) ) ;
#55982=EDGE_CURVE ( 'NONE', #58563, #48158, #66791, .T. ) ;
#55986=CARTESIAN_POINT ( 'NONE',  ( 17.92131488010602069, -1.993461139475334321, 13.76793304563129361 ) ) ;
#55988=VERTEX_POINT ( 'NONE', #55960 ) ;
#55998=CARTESIAN_POINT ( 'NONE',  ( 17.55505043854144276, 0.7192913403693124152, -12.57945229203838267 ) ) ;
#56007=CARTESIAN_POINT ( 'NONE',  ( 12.43878596651942026, 1.993461161472736887, 13.76788477248720177 ) ) ;
#56010=CARTESIAN_POINT ( 'NONE',  ( 12.18006440151454939, -0.02055073170813858166, -12.69999918148730700 ) ) ;
#56011=CARTESIAN_POINT ( 'NONE',  ( 12.39285819377765918, -0.4699225802676950670, 13.88930950616751936 ) ) ;
#56044=CARTESIAN_POINT ( 'NONE',  ( 18.20778913885554218, 2.166651812353023843, -12.41232206190563225 ) ) ;
#56052=CARTESIAN_POINT ( 'NONE',  ( 12.48353988083097477, -0.6549277419692678404, -13.98467727287826889 ) ) ;
#56061=CARTESIAN_POINT ( 'NONE',  ( 17.92131488010598517, 1.993461139475334321, -13.76793304563128828 ) ) ;
#56071=EDGE_LOOP ( 'NONE', ( #43240, #26700, #65383, #24814 ) ) ;
#56074=CARTESIAN_POINT ( 'NONE',  ( 18.15919096721063042, -2.338588349689834534, 13.70638546470246233 ) ) ;
#56081=CARTESIAN_POINT ( 'NONE',  ( 18.04847759739545410, -3.007479059277872402, -12.23581163759356194 ) ) ;
#56085=DIRECTION ( 'NONE',  ( 0.000000000000000000, -0.000000000000000000, 1.000000000000000000 ) ) ;
#56088=ORIENTED_EDGE ( 'NONE', *, *, #63340, .F. ) ;
#56092=CARTESIAN_POINT ( 'NONE',  ( 12.39066945341150117, 3.117187738603023561, -13.64855991556033921 ) ) ;
#56095=CARTESIAN_POINT ( 'NONE',  ( 17.55505043854144276, 0.7302158263239096891, 13.98094363220831049 ) ) ;
#56103=CARTESIAN_POINT ( 'NONE',  ( 12.19167018792508550, -2.619965297397002679, 13.64728369052816248 ) ) ;
#56114=CARTESIAN_POINT ( 'NONE',  ( 17.65762099059919521, 0.6166112555940438389, 12.67984200623734381 ) ) ;
#56115=CARTESIAN_POINT ( 'NONE',  ( 12.18006440151460801, 0.02055073179308012851, 12.69999918148658935 ) ) ;
#56125=EDGE_CURVE ( 'NONE', #68711, #42806, #18562, .T. ) ;
#56126=DIRECTION ( 'NONE',  ( 0.9999999998973936322, -8.065200975671946287E-06, 1.183914378896991529E-05 ) ) ;
#56131=CARTESIAN_POINT ( 'NONE',  ( 12.44955242156041919, -0.5141503178158092213, -12.68598964581897626 ) ) ;
#56139=DIRECTION ( 'NONE',  ( 1.000000000000000000, 0.000000000000000000, 0.000000000000000000 ) ) ;
#56140=FACE_OUTER_BOUND ( 'NONE', #3020, .T. ) ;
#56142=ORIENTED_EDGE ( 'NONE', *, *, #35285, .T. ) ;
#56148=CARTESIAN_POINT ( 'NONE',  ( 18.22055847946776197, 0.2899337805559810688, -13.99700184298317396 ) ) ;
#56157=CARTESIAN_POINT ( 'NONE',  ( 12.34838569212906556, -2.927120983245214969, -13.57349088381706181 ) ) ;
#56171=CARTESIAN_POINT ( 'NONE',  ( 12.52788616429851842, -0.5605600754933547369, -13.88478672247768664 ) ) ;
#56172=CARTESIAN_POINT ( 'NONE',  ( 17.96249544862753922, -2.025954803622692424, 12.54949280001589074 ) ) ;
#56198=CARTESIAN_POINT ( 'NONE',  ( 17.84362596415753188, -0.6599616342124031698, 12.58270523616455705 ) ) ;
#56202=VERTEX_POINT ( 'NONE', #58358 ) ;
#56204=CIRCLE ( 'NONE', #35012, 1.999999999999999556 ) ;
#56205=CARTESIAN_POINT ( 'NONE',  ( 18.10325613414704193, 2.040025360435026691, 13.85057320474804854 ) ) ;
#56216=CARTESIAN_POINT ( 'NONE',  ( 17.60315097558334330, -3.246934396132596046, -13.61827533163850923 ) ) ;
#56241=CARTESIAN_POINT ( 'NONE',  ( 12.37479069268420950, 2.046560891103777813, -12.54575476380192711 ) ) ;
#56249=ORIENTED_EDGE ( 'NONE', *, *, #30204, .F. ) ;
#56250=CARTESIAN_POINT ( 'NONE',  ( 12.41832178632831507, -1.871654022356046276, -12.46021467525213566 ) ) ;
#56257=CARTESIAN_POINT ( 'NONE',  ( 17.65762099059918810, -0.6166112555940442830, -12.67984200623736513 ) ) ;
#56260=CARTESIAN_POINT ( 'NONE',  ( 17.79016990201544246, -3.160912468841198475, 12.19707490278732642 ) ) ;
#56265=CARTESIAN_POINT ( 'NONE',  ( 17.88831561175062745, 3.029094439802118011, 13.54684341221733668 ) ) ;
#56268=CARTESIAN_POINT ( 'NONE',  ( 17.57591033989425000, 1.875000590519982246, 12.57541652832150803 ) ) ;
#56275=EDGE_CURVE ( 'NONE', #10401, #60760, #58022, .T. ) ;
#56277=CARTESIAN_POINT ( 'NONE',  ( 12.70216005901007783, -1.883184384472673445, 12.57411343304723772 ) ) ;
#56283=CARTESIAN_POINT ( 'NONE',  ( 12.64343166449435962, 0.6040886362899380302, 12.68065483099174884 ) ) ;
#56287=CARTESIAN_POINT ( 'NONE',  ( 12.34565325027254978, 2.076107717502758465, 12.54027567175044844 ) ) ;
#56288=ORIENTED_EDGE ( 'NONE', *, *, #52440, .T. ) ;
#56295=FACE_OUTER_BOUND ( 'NONE', #68265, .T. ) ;
#56305=FACE_BOUND ( 'NONE', #51041, .T. ) ;
#56308=ORIENTED_EDGE ( 'NONE', *, *, #51062, .F. ) ;
#56310=DIRECTION ( 'NONE',  ( 1.000000000000000000, 0.000000000000000000, 0.000000000000000000 ) ) ;
#56312=CIRCLE ( 'NONE', #58540, 12.59999999999999964 ) ;
#56313=CARTESIAN_POINT ( 'NONE',  ( 17.91195221636559864, -0.5131987759028846519, 13.88724801698877620 ) ) ;
#56325=CARTESIAN_POINT ( 'NONE',  ( 12.80505043854143388, 1.875000000000000000, -12.57545641911172751 ) ) ;
#56327=CARTESIAN_POINT ( 'NONE',  ( 12.22109980847048050, -2.722998852016973892, 12.39684006590273668 ) ) ;
#56330=CARTESIAN_POINT ( 'NONE',  ( 17.75752317324811003, -1.908613644657472408, 13.78124409819558771 ) ) ;
#56342=CARTESIAN_POINT ( 'NONE',  ( 18.20009441896382540, -0.3284204639250697944, -12.59572022474404562 ) ) ;
#56351=DIRECTION ( 'NONE',  ( 1.000000000000000000, 0.000000000000000000, 0.000000000000000000 ) ) ;
#56353=CARTESIAN_POINT ( 'NONE',  ( 12.08884934673719869, 2.402320636441721557, 13.79236805980801428 ) ) ;
#56356=CARTESIAN_POINT ( 'NONE',  ( 12.41269347218823604, 0.4865065284325135186, -12.68745508180288262 ) ) ;
#56358=CARTESIAN_POINT ( 'NONE',  ( 12.13954239761513243, 0.2899337805559719650, 13.99700184298317041 ) ) ;
#56379=CARTESIAN_POINT ( 'NONE',  ( 12.18024789519070872, 2.481080537771255035, 12.45595244966267501 ) ) ;
#56393=CARTESIAN_POINT ( 'NONE',  ( 17.95182328287549822, 1.877974217481243269, -12.45926392518878068 ) ) ;
#56402=CARTESIAN_POINT ( 'NONE',  ( 18.27946005101762950, 2.709881966519577468, -13.73658560568436293 ) ) ;
#56411=CARTESIAN_POINT ( 'NONE',  ( 18.27871553590497911, 2.567375067704834812, -13.76260043498214003 ) ) ;
#56430=CARTESIAN_POINT ( 'NONE',  ( 18.14814637199133429, -2.302603452852429733, -12.49536313902244089 ) ) ;
#56441=CARTESIAN_POINT ( 'NONE',  ( 12.08961158949548675, 2.638129719752015045, -13.74921199938403937 ) ) ;
#56444=CARTESIAN_POINT ( 'NONE',  ( 18.21571869486622930, 0.3016537271415110077, 13.99676704218776990 ) ) ;
#56447=ORIENTED_EDGE ( 'NONE', *, *, #49083, .F. ) ;
#56450=CARTESIAN_POINT ( 'NONE',  ( 12.21068878739219343, -2.693668765267103637, 13.63048043076724625 ) ) ;
#56465=FACE_OUTER_BOUND ( 'NONE', #42457, .T. ) ;
#56475=CARTESIAN_POINT ( 'NONE',  ( 12.61664271790066927, 0.6949735217938437515, -12.58082105808780504 ) ) ;
#56479=DIRECTION ( 'NONE',  ( 0.000000000000000000, -1.000000000000000000, 0.000000000000000000 ) ) ;
#56492=CARTESIAN_POINT ( 'NONE',  ( 18.26112155826667660, -0.1662062226620539818, -13.99901824074930445 ) ) ;
#56497=CARTESIAN_POINT ( 'NONE',  ( 17.55505043854147118, -3.248109929747637903, 13.61799478206225444 ) ) ;
#56498=CARTESIAN_POINT ( 'NONE',  ( 5.700000000000000178, -13.04986661130000059, 1.811520473896000016 ) ) ;
#56499=CARTESIAN_POINT ( 'NONE',  ( 18.11618405628967210, -2.775422336763186504, 12.38314678678514369 ) ) ;
#56508=CARTESIAN_POINT ( 'NONE',  ( 17.83817875635889294, 0.5572864142399046594, -13.88496202738553187 ) ) ;
#56513=CARTESIAN_POINT ( 'NONE',  ( 12.21985227486504400, -0.2197089332467947187, -13.89766776387045866 ) ) ;
#56514=CARTESIAN_POINT ( 'NONE',  ( 18.15589597092050056, -2.672372730248489425, 12.40976522372663737 ) ) ;
#56528=B_SPLINE_CURVE_WITH_KNOTS ( 'NONE', 3,
 ( #8375, #34951, #29717, #35636, #68110, #3794, #41216, #51020, #61848, #9047, #55925, #8029, #40867, #30725, #14310, #25130, #30387, #20228, #25473, #13289, #46463, #51697, #13626, #46805, #35963, #29367, #13964, #62190, #56607, #35293, #52033, #8714, #67763, #57278, #3120, #67087, #62527, #56265, #45776, #50682, #4136, #67424, #2777, #24104, #51360, #24792 ),
 .UNSPECIFIED., .F., .F.,
 ( 4, 2, 2, 2, 2, 1, 2, 2, 2, 1, 2, 2, 2, 2, 2, 2, 1, 2, 2, 1, 2, 2, 2, 2, 4 ),
 ( 0.4988098180370147405, 0.5301342044097088202, 0.5457963975960562486, 0.5614585907824035660, 0.5653741390789909227, 0.5692896873755783904, 0.5771207839687497732, 0.5927829771550930937, 0.6006140737482646985, 0.6084451703414361923, 0.6241073635277791798, 0.6397695567141222783, 0.6554317499004652658, 0.6710939430868083644, 0.6867561362731513519, 0.7024183294594943394, 0.7180805226458374380, 0.7494049090185229689, 0.7650671022048658454, 0.7807292953912086109, 0.8120536817638945859, 0.8433780681365805609, 0.8747024545092665360, 0.9373512272546333790, 1.000000000000000000 ),
 .UNSPECIFIED. ) ;
#56546=CARTESIAN_POINT ( 'NONE',  ( 18.20591985607867258, 2.840417715854210101, 13.70884684492145489 ) ) ;
#56550=VECTOR ( 'NONE', #52362, 1000.000000000000000 ) ;
#56559=CARTESIAN_POINT ( 'NONE',  ( 18.14518304970624030, -2.942254210842380147, -13.68733852372544391 ) ) ;
#56563=ORIENTED_EDGE ( 'NONE', *, *, #42718, .T. ) ;
#56578=EDGE_CURVE ( 'NONE', #22839, #55276, #33893, .T. ) ;
#56582=DIRECTION ( 'NONE',  ( 1.000000000000000000, 0.000000000000000000, 0.000000000000000000 ) ) ;
#56584=CARTESIAN_POINT ( 'NONE',  ( 12.37974467178318072, 2.958002365504007525, -12.33299351980446446 ) ) ;
#56593=CARTESIAN_POINT ( 'NONE',  ( 12.30575661439783275, -1.958493781132636391, -12.44686177741867006 ) ) ;
#56599=CARTESIAN_POINT ( 'NONE',  ( 12.20320247475637743, -2.331154411892201850, -13.70777421733260049 ) ) ;
#56602=CARTESIAN_POINT ( 'NONE',  ( 4.699999740790659963, -13.17499974068000057, 1.948180898180000060E-09 ) ) ;
#56607=CARTESIAN_POINT ( 'NONE',  ( 18.06394506374553899, 2.862992422144976068, 13.58968849268369894 ) ) ;
#56612=CARTESIAN_POINT ( 'NONE',  ( 18.14695621644401058, 2.700933560328190541, 12.40248159148175766 ) ) ;
#56618=CARTESIAN_POINT ( 'NONE',  ( 12.18117696241649206, -2.542707536216995745, 12.44156325543625208 ) ) ;
#56626=CARTESIAN_POINT ( 'NONE',  ( 12.18528753443599477, -0.08139242733401307051, 12.69965452654166960 ) ) ;
#56630=CARTESIAN_POINT ( 'NONE',  ( 12.19523649643094920, 2.361571219431552571, 12.48275271858022961 ) ) ;
#56641=CARTESIAN_POINT ( 'NONE',  ( 17.81164675510670037, -0.5699806461405237945, -12.68277882560511749 ) ) ;
#56646=CARTESIAN_POINT ( 'NONE',  ( 12.39066945341153492, -3.117187738603024894, 13.64855991556033743 ) ) ;
#56658=VERTEX_POINT ( 'NONE', #12454 ) ;
#56668=CIRCLE ( 'NONE', #44450, 12.79999953825000425 ) ;
#56677=CARTESIAN_POINT ( 'NONE',  ( 17.57920827037000322, -3.248109283636080757, 13.61799489948998065 ) ) ;
#56688=CARTESIAN_POINT ( 'NONE',  ( 18.12277215905345429, 0.4475098806653864392, -12.59205372277267898 ) ) ;
#56692=CARTESIAN_POINT ( 'NONE',  ( 4.599999999999999645, -3.125000000000000000, 13.52084414783465682 ) ) ;
#56693=ORIENTED_EDGE ( 'NONE', *, *, #10391, .F. ) ;
#56700=CARTESIAN_POINT ( 'NONE',  ( 12.23477282158792612, 2.066986176408053044, 13.84657559728969822 ) ) ;
#56703=CARTESIAN_POINT ( 'NONE',  ( 12.46489138717631029, 0.5244033891532404734, -12.68542455842735706 ) ) ;
#56711=VECTOR ( 'NONE', #18234, 1000.000000000000000 ) ;
#56719=CARTESIAN_POINT ( 'NONE',  ( 12.53614341883831251, 3.148504814753053882, 12.20028441070642700 ) ) ;
#56727=CARTESIAN_POINT ( 'NONE',  ( 17.55505043854143565, 1.875000000000000000, 12.57541666120756041 ) ) ;
#56744=CARTESIAN_POINT ( 'NONE',  ( 17.63949335857236633, 1.765638956106261537, -12.47567715783345577 ) ) ;
#56752=CARTESIAN_POINT ( 'NONE',  ( 12.27567203567526910, 0.4994936913945444146, -13.99109680828866686 ) ) ;
#56756=CARTESIAN_POINT ( 'NONE',  ( 18.17992876607663177, 2.487411392565050505, 12.45448399074147972 ) ) ;
#56761=CARTESIAN_POINT ( 'NONE',  ( 18.26192063240346286, 2.355523948311720073, -13.80042196861913339 ) ) ;
#56781=CARTESIAN_POINT ( 'NONE',  ( 17.67527538783546959, -3.190136231796161237, -12.18946489087518970 ) ) ;
#56789=CIRCLE ( 'NONE', #5425, 2.000000000000001332 ) ;
#56791=CARTESIAN_POINT ( 'NONE',  ( 12.22680470609049230, 2.076949241994379136, -13.84509419021260435 ) ) ;
#56792=DIRECTION ( 'NONE',  ( -1.000000000000000000, 0.000000000000000000, 0.000000000000000000 ) ) ;
#56794=CARTESIAN_POINT ( 'NONE',  ( 18.14748133481813852, -2.299853946675995520, 12.49599191557683930 ) ) ;
#56800=CARTESIAN_POINT ( 'NONE',  ( 12.20625471196118816, -2.679103183993202464, 13.63384013638393100 ) ) ;
#56814=CARTESIAN_POINT ( 'NONE',  ( 18.18003600477294057, -2.504879791492763630, -12.45042248974575294 ) ) ;
#56822=CARTESIAN_POINT ( 'NONE',  ( 12.44180168752028770, 0.6226057762474821455, -12.58460959628226128 ) ) ;
#56823=CARTESIAN_POINT ( 'NONE',  ( 12.24831336539215521, -2.784226791605522777, -12.38079107515907396 ) ) ;
#56842=CARTESIAN_POINT ( 'NONE',  ( 18.26152657770008148, 0.1657344298535251004, -13.99903850390423798 ) ) ;
#56857=CARTESIAN_POINT ( 'NONE',  ( 17.96365918282847218, 0.4729502186230333249, -13.88916975806286658 ) ) ;
#56861=CARTESIAN_POINT ( 'NONE',  ( 12.80505043854144276, 0.6878608935795343937, 12.61273126665598276 ) ) ;
#56862=CARTESIAN_POINT ( 'NONE',  ( 12.21303990359567848, 0.2014071429975201610, -13.89805485625563186 ) ) ;
#56863=CARTESIAN_POINT ( 'NONE',  ( 18.17995611468272443, -2.522932803854498918, 12.44624262618111921 ) ) ;
#56864=VERTEX_POINT ( 'NONE', #35838 ) ;
#56885=CARTESIAN_POINT ( 'NONE',  ( 17.67403227923241360, 0.7096370184368610001, 12.58000072970462924 ) ) ;
#56893=FACE_OUTER_BOUND ( 'NONE', #62073, .T. ) ;
#56895=ORIENTED_EDGE ( 'NONE', *, *, #39733, .F. ) ;
#56917=CARTESIAN_POINT ( 'NONE',  ( 12.80505043854146940, -1.816864895258029522, -13.85234397965874464 ) ) ;
#56924=CARTESIAN_POINT ( 'NONE',  ( 12.18833199825126101, 2.603395164171333764, -12.42692484756187810 ) ) ;
#56934=CARTESIAN_POINT ( 'NONE',  ( 12.78418764580521660, -3.124999405572221445, -12.28373085793387531 ) ) ;
#56941=CARTESIAN_POINT ( 'NONE',  ( 12.66207816929887819, -1.891226320509243664, -13.78383611977690570 ) ) ;
#56944=CARTESIAN_POINT ( 'NONE',  ( 17.57925688241715179, -3.199751027636643208, 12.18694352263475089 ) ) ;
#56946=ORIENTED_EDGE ( 'NONE', *, *, #4804, .T. ) ;
#56949=CARTESIAN_POINT ( 'NONE',  ( 17.55505043854147118, -3.125000000000000000, 13.52084414783465860 ) ) ;
#56952=CARTESIAN_POINT ( 'NONE',  ( 18.11597065765684533, 2.775858272760586054, 12.38300578299705812 ) ) ;
#56957=CARTESIAN_POINT ( 'NONE',  ( 12.43829333464982234, -1.993817424706645802, 12.55522976296197157 ) ) ;
#56963=CARTESIAN_POINT ( 'NONE',  ( 12.51941477301789796, 0.5560043133243441904, 12.68361349193353860 ) ) ;
#56982=CARTESIAN_POINT ( 'NONE',  ( 18.15114771535201754, -2.688105180961021468, 13.63176637561060645 ) ) ;
#56984=CARTESIAN_POINT ( 'NONE',  ( 12.36183802548528377, -3.095880799707801057, 13.65340897264974629 ) ) ;
#56994=CARTESIAN_POINT ( 'NONE',  ( 18.09779443563016343, -0.3101119056630274873, 13.89534721487939528 ) ) ;
#57010=CARTESIAN_POINT ( 'NONE',  ( 18.20564091649233163, -2.840274733304995358, 13.70886432971491331 ) ) ;
#57017=CONICAL_SURFACE ( 'NONE', #14594, 13.22499948080999843, 0.7853981240402999608 ) ;
#57023=CARTESIAN_POINT ( 'NONE',  ( 18.27543972223746493, -0.08185661189467333121, -12.59973963693671983 ) ) ;
#57032=CARTESIAN_POINT ( 'NONE',  ( 17.77886761546797345, 1.796012712130039324, 12.47134082573985658 ) ) ;
#57033=CARTESIAN_POINT ( 'NONE',  ( 12.08002314427566759, 2.496413253464124793, 13.77564875264238253 ) ) ;
#57036=CARTESIAN_POINT ( 'NONE',  ( 12.33488707444048949, 0.4118223548554933444, -12.69101228721791763 ) ) ;
#57037=CARTESIAN_POINT ( 'NONE',  ( 12.09634358953520206, -0.1544074001203955548, 13.99915345895492180 ) ) ;
#57039=CARTESIAN_POINT ( 'NONE',  ( 12.80505043854143388, 3.199698446519374517, 12.18695736643652694 ) ) ;
#57051=VECTOR ( 'NONE', #25585, 1000.000000000000000 ) ;
#57069=ORIENTED_EDGE ( 'NONE', *, *, #64655, .T. ) ;
#57073=CARTESIAN_POINT ( 'NONE',  ( 18.28026264019197811, 2.471821293434738553, -12.35517058147370584 ) ) ;
#57075=CARTESIAN_POINT ( 'NONE',  ( 4.700001368028300597, 0.000000000000000000, 0.000000000000000000 ) ) ;
#57077=CARTESIAN_POINT ( 'NONE',  ( 12.18408897593520201, 2.571470745536066804, -13.65804488217700552 ) ) ;
#57081=CARTESIAN_POINT ( 'NONE',  ( 12.42222097287479343, 0.6205713442106896016, -13.98624562867392385 ) ) ;
#57084=CARTESIAN_POINT ( 'NONE',  ( 18.18005043835058743, 2.498838836751009040, 12.45183430367551303 ) ) ;
#57086=DIRECTION ( 'NONE',  ( 0.000000000000000000, 0.9905022095861402143, -0.1374968101629056305 ) ) ;
#57087=ORIENTED_EDGE ( 'NONE', *, *, #353, .T. ) ;
#57089=CARTESIAN_POINT ( 'NONE',  ( 18.28005242394217689, 2.496404808517244334, -13.77565028140658931 ) ) ;
#57093=ADVANCED_FACE ( 'NONE', ( #63769 ), #47681, .T. ) ;
#57108=CARTESIAN_POINT ( 'NONE',  ( 17.69826591161636031, -1.891282299241872522, -12.57273691359005596 ) ) ;
#57118=CARTESIAN_POINT ( 'NONE',  ( 18.28005834358922499, -0.01140630886273579121, 14.00000041621361291 ) ) ;
#57121=CARTESIAN_POINT ( 'NONE',  ( 17.72043029666332004, -1.875000000000000444, 12.57545629021522871 ) ) ;
#57125=VERTEX_POINT ( 'NONE', #840 ) ;
#57135=DIRECTION ( 'NONE',  ( 1.000000000000000000, 0.000000000000000000, 0.000000000000000000 ) ) ;
#57154=CARTESIAN_POINT ( 'NONE',  ( 12.42881362571445614, -0.4990964484179726823, -12.68679736436867778 ) ) ;
#57155=CARTESIAN_POINT ( 'NONE',  ( 12.19170508189248991, -2.620143503840312249, -12.42276098599978340 ) ) ;
#57172=CARTESIAN_POINT ( 'NONE',  ( 17.81056431323685985, -0.6834693007276704257, -13.98330741474946137 ) ) ;
#57179=CARTESIAN_POINT ( 'NONE',  ( 18.05168367659330642, -2.879595443346424588, 12.35500515152848955 ) ) ;
#57182=CARTESIAN_POINT ( 'NONE',  ( 12.19240574124822807, -2.623658933770948387, -13.64640170901807714 ) ) ;
#57185=LINE ( 'NONE', #67664, #44187 ) ;
#57186=CARTESIAN_POINT ( 'NONE',  ( 4.599999999999999645, -0.6250000000000001110, -13.88107975066922428 ) ) ;
#57192=CARTESIAN_POINT ( 'NONE',  ( 12.21299871467824971, -0.2005085131878081850, -13.89805835524348865 ) ) ;
#57193=CARTESIAN_POINT ( 'NONE',  ( 17.81575242098906742, -1.931873426913545355, 12.56596755615858818 ) ) ;
#57216=CARTESIAN_POINT ( 'NONE',  ( 18.20808481425076408, 0.3124912280145324961, 12.59612551846059958 ) ) ;
#57247=CARTESIAN_POINT ( 'NONE',  ( 12.80505043854144276, 0.6249999999999994449, -25.00000000000000000 ) ) ;
#57254=CARTESIAN_POINT ( 'NONE',  ( 12.24870215512120275, 2.784965704346237025, -12.38061966815949866 ) ) ;
#57263=CARTESIAN_POINT ( 'NONE',  ( 12.34719455185581261, -2.925915912524184925, -12.34207449233261755 ) ) ;
#57269=CARTESIAN_POINT ( 'NONE',  ( 12.26189125119393175, -2.190632771808445511, -13.73417700668423436 ) ) ;
#57275=CARTESIAN_POINT ( 'NONE',  ( 12.80505043854143388, 3.125000000000000000, 13.52078605991414939 ) ) ;
#57278=CARTESIAN_POINT ( 'NONE',  ( 17.98396147896337638, 2.954720660945521438, 13.56638041066990574 ) ) ;
#57281=CARTESIAN_POINT ( 'NONE',  ( 18.14016391943232520, 2.719929439268204074, 12.39760446975600594 ) ) ;
#57287=CARTESIAN_POINT ( 'NONE',  ( 12.37974467178321625, -2.958002365504007969, 12.33299351980446268 ) ) ;
#57288=EDGE_CURVE ( 'NONE', #40006, #28416, #44882, .T. ) ;
#57298=CARTESIAN_POINT ( 'NONE',  ( 12.34869027095183824, 0.4275228316712915144, 12.69032453495386292 ) ) ;
#57311=CIRCLE ( 'NONE', #37203, 14.00000000000000000 ) ;
#57320=CARTESIAN_POINT ( 'NONE',  ( 17.94528078231818924, -2.988314720655957490, -13.55762497744564499 ) ) ;
#57354=CARTESIAN_POINT ( 'NONE',  ( 18.27048529734874549, -0.1170514037749927627, -12.59946170170351465 ) ) ;
#57355=CARTESIAN_POINT ( 'NONE',  ( 12.39978108233925269, 2.975905172412623756, -12.32787332408411984 ) ) ;
#57366=CARTESIAN_POINT ( 'NONE',  ( 17.84632148815558139, 1.821395309707476429, 12.46765979085770937 ) ) ;
#57367=CARTESIAN_POINT ( 'NONE',  ( 12.43989325004533164, 3.148871498663009305, 13.64128470488402378 ) ) ;
#57370=CARTESIAN_POINT ( 'NONE',  ( 12.64261153907313506, -0.6049396497490575619, -12.68060203380715834 ) ) ;
#57371=CARTESIAN_POINT ( 'NONE',  ( 12.35439258730998446, -0.5721320424853859610, 13.98830666644471954 ) ) ;
#57374=CARTESIAN_POINT ( 'NONE',  ( 12.21279934347913176, -2.064970636307561502, 12.42964156345203541 ) ) ;
#57383=CARTESIAN_POINT ( 'NONE',  ( 12.15399652902987171, 2.797872959086249445, 12.28545279959702796 ) ) ;
#57395=EDGE_CURVE ( 'NONE', #52670, #19784, #64565, .T. ) ;
#57401=CARTESIAN_POINT ( 'NONE',  ( 12.58320380180961884, -3.084393765090618356, 13.53199207997351117 ) ) ;
#57402=CARTESIAN_POINT ( 'NONE',  ( 12.21849864558328136, 2.283168037611178036, 13.71702792529043258 ) ) ;
#57411=CARTESIAN_POINT ( 'NONE',  ( 17.67525416028801644, 1.770698066894638156, -12.47496018400917173 ) ) ;
#57414=CARTESIAN_POINT ( 'NONE',  ( 18.06413707770591515, 2.862722769414956847, 12.35962335206644802 ) ) ;
#57422=CARTESIAN_POINT ( 'NONE',  ( 18.10184514648642207, 2.186078922847817019, 12.51950284167777383 ) ) ;
#57425=VERTEX_POINT ( 'NONE', #14780 ) ;
#57426=CARTESIAN_POINT ( 'NONE',  ( 17.97988082628305762, 1.926206752467414463, -13.86685907515736638 ) ) ;
#57445=CARTESIAN_POINT ( 'NONE',  ( 18.06549347002472317, -2.139198186095363940, -12.52833527917196754 ) ) ;
#57449=EDGE_LOOP ( 'NONE', ( #61290, #45600, #22201, #61855 ) ) ;
#57454=LINE ( 'NONE', #57806, #48383 ) ;
#57456=CARTESIAN_POINT ( 'NONE',  ( 18.27776594916668174, -0.05915529127692874256, 13.99988012777929214 ) ) ;
#57474=EDGE_CURVE ( 'NONE', #3060, #2983, #30911, .T. ) ;
#57486=( GEOMETRIC_REPRESENTATION_CONTEXT ( 3 ) GLOBAL_UNCERTAINTY_ASSIGNED_CONTEXT ( ( #46497 ) ) GLOBAL_UNIT_ASSIGNED_CONTEXT ( ( #17480, #28314, #50332 ) ) REPRESENTATION_CONTEXT ( 'NONE', 'WORKASPACE' ) );
#57490=CARTESIAN_POINT ( 'NONE',  ( 12.20981273398931499, 0.1908418880314473598, -12.69807545005480875 ) ) ;
#57491=CARTESIAN_POINT ( 'NONE',  ( 12.72293129229483988, -3.125000000000000444, -12.28373127578713842 ) ) ;
#57498=CARTESIAN_POINT ( 'NONE',  ( 17.94287612696653156, 0.4902485962002651187, 12.68726381691200800 ) ) ;
#57507=AXIS2_PLACEMENT_3D ( 'NONE', #64149, #17303, #52027 ) ;
#57508=CARTESIAN_POINT ( 'NONE',  ( 17.74252317112528132, -0.7057854747025560371, -13.98219993205038847 ) ) ;
#57509=EDGE_CURVE ( 'NONE', #38751, #26914, #58758, .T. ) ;
#57522=CARTESIAN_POINT ( 'NONE',  ( 12.18008396645310398, -2.512642877105788930, -13.67072295643538560 ) ) ;
#57530=CARTESIAN_POINT ( 'NONE',  ( 17.57568447735986794, -0.6247443594537128719, -12.67930618256806419 ) ) ;
#57534=CARTESIAN_POINT ( 'NONE',  ( 12.58300520725473426, 3.084588251740255860, 13.53188417542246746 ) ) ;
#57543=CARTESIAN_POINT ( 'NONE',  ( 12.26168426244253240, 2.190490593926006646, -13.73426451135290449 ) ) ;
#57545=B_SPLINE_CURVE_WITH_KNOTS ( 'NONE', 3,
 ( #11471, #59033, #11136, #42278 ),
 .UNSPECIFIED., .F., .F.,
 ( 4, 4 ),
 ( 0.000000000000000000, 1.000000000000000000 ),
 .UNSPECIFIED. ) ;
#57549=CARTESIAN_POINT ( 'NONE',  ( 18.04535492090956694, 0.3877560770473448826, 13.89272419024897154 ) ) ;
#57553=CARTESIAN_POINT ( 'NONE',  ( 4.599999999999999645, 0.000000000000000000, 0.000000000000000000 ) ) ;
#57563=CARTESIAN_POINT ( 'NONE',  ( 17.55505043854144631, 0.7192913403693016461, 12.57945229203838444 ) ) ;
#57570=CARTESIAN_POINT ( 'NONE',  ( 17.87779404330688138, 3.171907921506167849, 13.63594617280360310 ) ) ;
#57571=DIRECTION ( 'NONE',  ( 0.000000000000000000, 1.000000000000000000, 0.000000000000000000 ) ) ;
#57593=VECTOR ( 'NONE', #45633, 1000.000000000000114 ) ;
#57609=ORIENTED_EDGE ( 'NONE', *, *, #57826, .F. ) ;
#57610=CARTESIAN_POINT ( 'NONE',  ( 12.58288255545466683, -3.084271795211693590, -12.29604036100132625 ) ) ;
#57616=CARTESIAN_POINT ( 'NONE',  ( 12.29504137777690609, -2.138585174375769782, -13.74345269122309254 ) ) ;
#57629=CARTESIAN_POINT ( 'NONE',  ( 17.87019584817731754, 3.039826384816739502, 12.30925258946623835 ) ) ;
#57635=CARTESIAN_POINT ( 'NONE',  ( 12.21993702172676954, -2.719929609653446434, 12.39763114037444680 ) ) ;
#57642=CARTESIAN_POINT ( 'NONE',  ( 12.49190496432325226, -0.5409888710114151289, 12.68448745112149467 ) ) ;
#57643=CARTESIAN_POINT ( 'NONE',  ( 5.557969180995212533, -12.17302321295568213, -3.765215263422377223 ) ) ;
#57644=CARTESIAN_POINT ( 'NONE',  ( 7.100000000000000533, 0.000000000000000000, 0.000000000000000000 ) ) ;
#57645=CARTESIAN_POINT ( 'NONE',  ( 17.55505043854144276, -0.6250000000000001110, -25.00000000000000000 ) ) ;
#57647=VERTEX_POINT ( 'NONE', #40163 ) ;
#57663=CARTESIAN_POINT ( 'NONE',  ( 17.92197813837935527, -1.993632751867237207, -13.76786175838294923 ) ) ;
#57672=CARTESIAN_POINT ( 'NONE',  ( 17.91802112668279179, -0.5089014838709605693, 13.88746088750631635 ) ) ;
#57675=CARTESIAN_POINT ( 'NONE',  ( 4.600000207916445483, -13.27499874714999883, 0.000000000000000000 ) ) ;
#57683=DIRECTION ( 'NONE',  ( 0.000000000000000000, 1.000000000000000000, 0.000000000000000000 ) ) ;
#57684=EDGE_CURVE ( 'NONE', #35474, #2919, #33884, .T. ) ;
#57687=CARTESIAN_POINT ( 'NONE',  ( 18.21736474454390375, -2.220153890850323553, 13.82285830752080713 ) ) ;
#57688=CARTESIAN_POINT ( 'NONE',  ( 18.09696660044057026, 2.811537062192479119, -13.60243477576679538 ) ) ;
#57700=CARTESIAN_POINT ( 'NONE',  ( 18.24552617758597606, -0.2196334679052314443, -12.59809060309703277 ) ) ;
#57712=CARTESIAN_POINT ( 'NONE',  ( 17.65082925870466113, 1.766819657443030600, 12.47551016841904215 ) ) ;
#57713=CARTESIAN_POINT ( 'NONE',  ( 12.16922513814159679, 2.166987123599053433, 13.83127908232058267 ) ) ;
#57716=CARTESIAN_POINT ( 'NONE',  ( 12.53103059986594481, -0.5618114787718360148, -12.68327018738675172 ) ) ;
#57717=CARTESIAN_POINT ( 'NONE',  ( 12.33591485593543347, -0.5568603909045801714, 13.98892293345219962 ) ) ;
#57725=FACE_OUTER_BOUND ( 'NONE', #16433, .T. ) ;
#57728=CARTESIAN_POINT ( 'NONE',  ( 12.53569427112573820, 1.812281311417180740, 12.46898785302652257 ) ) ;
#57735=CARTESIAN_POINT ( 'NONE',  ( 12.25843860535923469, 2.803243370102336929, 12.37572767901811588 ) ) ;
#57736=CARTESIAN_POINT ( 'NONE',  ( 5.500000000000000000, -12.65263727151999795, -3.063503113339999917 ) ) ;
#57739=CARTESIAN_POINT ( 'NONE',  ( 12.24748280284102542, -0.2825744477460949144, 12.69577188568745285 ) ) ;
#57746=CARTESIAN_POINT ( 'NONE',  ( 12.20418674196361764, -2.672312675674152427, 13.63540648336421945 ) ) ;
#57747=CARTESIAN_POINT ( 'NONE',  ( 12.18008396645303826, 2.512642877094447780, 13.67072295643779078 ) ) ;
#57752=VECTOR ( 'NONE', #48557, 1000.000000000000000 ) ;
#57755=CARTESIAN_POINT ( 'NONE',  ( 18.16360624365136189, 2.642789843301108998, -12.41718366361782699 ) ) ;
#57757=CARTESIAN_POINT ( 'NONE',  ( 17.63951772021993492, 3.120582521217798444, 12.28507980727042614 ) ) ;
#57763=CARTESIAN_POINT ( 'NONE',  ( 12.61757770595761308, 0.7057854747025396058, -13.98219993205039025 ) ) ;
#57766=CARTESIAN_POINT ( 'NONE',  ( 18.18005044575085449, -2.500000006795658702, -13.67340643792831401 ) ) ;
#57775=CARTESIAN_POINT ( 'NONE',  ( 17.92019487611647932, 3.148838011673610993, -13.64129243465967711 ) ) ;
#57781=CARTESIAN_POINT ( 'NONE',  ( 12.18394749351824480, -0.08111026479008709433, -13.89976203980642566 ) ) ;
#57793=CARTESIAN_POINT ( 'NONE',  ( 18.08809746899279602, -2.173637705205955672, -12.52162896472547260 ) ) ;
#57796=DIRECTION ( 'NONE',  ( 0.000000000000000000, -0.9553735099700838562, 0.2954005017724949944 ) ) ;
#57797=B_SPLINE_CURVE_WITH_KNOTS ( 'NONE', 3,
 ( #52808, #47570, #68874, #20992 ),
 .UNSPECIFIED., .F., .F.,
 ( 4, 4 ),
 ( 0.000000000000000000, 1.000000000000000000 ),
 .UNSPECIFIED. ) ;
#57798=CIRCLE ( 'NONE', #20980, 13.89999852641999922 ) ;
#57806=CARTESIAN_POINT ( 'NONE',  ( 4.599999999999999645, 1.787797342887044394, 13.88538010501570952 ) ) ;
#57815=CARTESIAN_POINT ( 'NONE',  ( 12.42225203013928514, -3.001455243171148535, 13.55441486463508660 ) ) ;
#57826=EDGE_CURVE ( 'NONE', #53716, #24573, #46773, .T. ) ;
#57830=CARTESIAN_POINT ( 'NONE',  ( 18.13624123201584837, 2.730018939185353322, -12.39502206882475299 ) ) ;
#57837=B_SPLINE_CURVE_WITH_KNOTS ( 'NONE', 3,
 ( #6132, #16964, #26791, #15938, #42858, #21186, #10351, #42517, #16283, #53008, #37608, #53695, #27829, #53353, #27469, #11046, #63826, #26442, #59627, #48796, #207, #59274, #54030, #31687, #37954, #32380, #21527, #22218, #64507, #5788, #5455, #11377, #905, #16628, #32718, #49134, #58591, #1246, #43554, #5105, #63483, #27131 ),
 .UNSPECIFIED., .F., .F.,
 ( 4, 2, 2, 2, 2, 2, 2, 2, 2, 2, 2, 2, 2, 1, 2, 2, 2, 2, 2, 1, 2, 4 ),
 ( 0.4997863768984587285, 0.5623130797861424224, 0.6248397826738261163, 0.6404714583957457075, 0.6561031341176652987, 0.6873664855615019276, 0.7029981612834201865, 0.7186298370053385565, 0.7264456748662961871, 0.7342615127272538178, 0.7498931884491690791, 0.7811565398929997128, 0.7889723777539620064, 0.7967882156149244111, 0.8124198913368532171, 0.8280515670587820232, 0.8436832427807109402, 0.8749465942245686634, 0.8905782699464975805, 0.9062099456684264975, 0.9374732971122843317, 1.000000000000000000 ),
 .UNSPECIFIED. ) ;
#57844=CARTESIAN_POINT ( 'NONE',  ( 12.29653175235436002, 0.3639343692979905565, -12.69299665021505419 ) ) ;
#57845=CARTESIAN_POINT ( 'NONE',  ( 12.20125275665228060, -2.661451430028674459, -12.41248063380501421 ) ) ;
#57868=B_SPLINE_CURVE_WITH_KNOTS ( 'NONE', 3,
 ( #15204, #67642, #8587, #62408, #35844, #9259, #31296, #20107, #35170, #41436, #36186, #52606, #30600, #40743, #67303, #24670, #57498, #42126, #9607, #30949, #26045, #52264, #4360, #26738, #58535, #11326, #5402, #53979, #10300, #36882, #48055, #10642, #1196, #16913, #53641, #64802, #16577, #6082, #32330, #64455, #42809, #501, #52957, #32667, #63776, #37902 ),
 .UNSPECIFIED., .F., .F.,
 ( 4, 2, 2, 2, 2, 2, 2, 2, 2, 2, 2, 2, 2, 2, 1, 2, 2, 2, 2, 2, 1, 2, 2, 4 ),
 ( 0.000000000000000000, 0.06247329711059514817, 0.09370994566589528618, 0.1249465942211954311, 0.1405649184988454758, 0.1561832427764955067, 0.1874198913317954851, 0.2030382156094475421, 0.2186565398870995436, 0.2264657020259255582, 0.2342748641647515728, 0.2498931884424035743, 0.2811298369977103806, 0.2889389991365332588, 0.2967481612753561371, 0.3123664855530020046, 0.3279848098306478166, 0.3436031341082936841, 0.3748397826635854746, 0.3904581069412313421, 0.4060764312188773206, 0.4373130797741676679, 0.4685497283294579596, 0.4997863768847483068 ),
 .UNSPECIFIED. ) ;
#57876=CARTESIAN_POINT ( 'NONE',  ( 12.21849864557798249, -2.283168037624248470, -13.71702792528834358 ) ) ;
#57878=ORIENTED_EDGE ( 'NONE', *, *, #33147, .F. ) ;
#57880=VERTEX_POINT ( 'NONE', #68765 ) ;
#57884=EDGE_CURVE ( 'NONE', #37829, #48911, #4509, .T. ) ;
#57888=CARTESIAN_POINT ( 'NONE',  ( 12.47278092208622802, 3.029458323191938529, 13.54674174801983710 ) ) ;
#57911=CARTESIAN_POINT ( 'NONE',  ( 12.15832103308141399, 2.898357473917167138, -13.69738840704374816 ) ) ;
#57916=ADVANCED_FACE ( 'NONE', ( #4792 ), #21564, .F. ) ;
#57917=CARTESIAN_POINT ( 'NONE',  ( 18.27776587948807219, 0.05827135643915087176, 12.59987075990256677 ) ) ;
#57925=EDGE_CURVE ( 'NONE', #18184, #64966, #34642, .T. ) ;
#57951=CARTESIAN_POINT ( 'NONE',  ( 18.14710216240463581, 0.2005085131878108773, -13.89805835524348865 ) ) ;
#57960=ORIENTED_EDGE ( 'NONE', *, *, #49648, .F. ) ;
#57965=CARTESIAN_POINT ( 'NONE',  ( 12.20420485406511979, -2.672372548754605504, -12.40973746665996380 ) ) ;
#57970=CARTESIAN_POINT ( 'NONE',  ( 12.55438499206309011, -1.927376109800346571, -13.77831414012769429 ) ) ;
#57974=CARTESIAN_POINT ( 'NONE',  ( 18.17205452211572947, -2.859046691836187648, 12.27135926524918297 ) ) ;
#57983=CARTESIAN_POINT ( 'NONE',  ( 17.98035626696890432, 2.958002308262752234, 12.33297292539930723 ) ) ;
#57986=CARTESIAN_POINT ( 'NONE',  ( 17.74710428552098662, -3.180431966555338441, -12.19205794678746990 ) ) ;
#57997=CARTESIAN_POINT ( 'NONE',  ( 12.27392562293324829, -0.3300695133819704918, 12.69424233780835287 ) ) ;
#58008=FACE_OUTER_BOUND ( 'NONE', #21575, .T. ) ;
#58017=CARTESIAN_POINT ( 'NONE',  ( 18.13950502211732640, -2.721680756027779147, 13.62394404485162624 ) ) ;
#58020=CARTESIAN_POINT ( 'NONE',  ( 18.03429950922811287, -2.098690172523155262, -13.75037901049766376 ) ) ;
#58022=LINE ( 'NONE', #68492, #40000 ) ;
#58031=CARTESIAN_POINT ( 'NONE',  ( 17.97864539831671493, -0.4596704778279275261, 13.88977177192326096 ) ) ;
#58042=CARTESIAN_POINT ( 'NONE',  ( 12.32338852522665107, 1.942342658536874378, -12.44939237451325909 ) ) ;
#58044=DIRECTION ( 'NONE',  ( -0.000000000000000000, -0.000000000000000000, 1.000000000000000000 ) ) ;
#58045=CARTESIAN_POINT ( 'NONE',  ( 18.27898184041761453, -2.472823623527009129, 13.77990254017906935 ) ) ;
#58050=ORIENTED_EDGE ( 'NONE', *, *, #18421, .F. ) ;
#58058=CARTESIAN_POINT ( 'NONE',  ( 17.97798751929653704, -0.5846869236304562678, -12.58643362292763612 ) ) ;
#58069=CARTESIAN_POINT ( 'NONE',  ( 12.75695018768100830, 1.789009927756595175, 13.88522413357867080 ) ) ;
#58073=CARTESIAN_POINT ( 'NONE',  ( 12.11831821888145555, -0.2353130933619223264, 13.99804086085458721 ) ) ;
#58074=ORIENTED_EDGE ( 'NONE', *, *, #1228, .T. ) ;
#58075=CARTESIAN_POINT ( 'NONE',  ( 12.80505043854146940, -1.760845406083394016, 12.47635457398814829 ) ) ;
#58084=CARTESIAN_POINT ( 'NONE',  ( 12.18809860077013596, 2.859021363400007232, 12.27136516364851460 ) ) ;
#58095=CARTESIAN_POINT ( 'NONE',  ( 12.34378620388170233, 0.4226185367035117935, 12.69055435919257313 ) ) ;
#58100=CARTESIAN_POINT ( 'NONE',  ( 12.20145977811407434, -2.662504703663703509, 13.63765425733092052 ) ) ;
#58111=CARTESIAN_POINT ( 'NONE',  ( 18.16983287387825996, 2.613005487247105130, -12.42455217891717467 ) ) ;
#58113=CARTESIAN_POINT ( 'NONE',  ( 18.15011306039755823, 2.691200174448529658, 12.40496142756183673 ) ) ;
#58114=CARTESIAN_POINT ( 'NONE',  ( 18.27929200418771671, 2.710634889609412124, 13.73643850023514013 ) ) ;
#58119=DIRECTION ( 'NONE',  ( 1.000000000000000000, 0.000000000000000000, 0.000000000000000000 ) ) ;
#58134=CARTESIAN_POINT ( 'NONE',  ( 12.29062815658215513, 0.3550741888481653286, -13.89389891668081134 ) ) ;
#58151=DIRECTION ( 'NONE',  ( -1.000000000000000000, 0.000000000000000000, 0.000000000000000000 ) ) ;
#58155=AXIS2_PLACEMENT_3D ( 'NONE', #7851, #23926, #29541 ) ;
#58179=CARTESIAN_POINT ( 'NONE',  ( 17.81528574998282721, 3.068593513703687936, -12.30074760041392068 ) ) ;
#58187=CARTESIAN_POINT ( 'NONE',  ( 5.699999545467999695, 0.000000000000000000, 0.000000000000000000 ) ) ;
#58190=CARTESIAN_POINT ( 'NONE',  ( 12.20096618732086213, 0.1616215023347943314, -12.69863621249090002 ) ) ;
#58193=PLANE ( 'NONE',  #33483 ) ;
#58208=CARTESIAN_POINT ( 'NONE',  ( 17.87597250029675777, -0.6552116771452581867, -13.98466387211990281 ) ) ;
#58211=CIRCLE ( 'NONE', #37010, 13.27499874714999883 ) ;
#58213=CARTESIAN_POINT ( 'NONE',  ( 12.80505043854146940, -3.125000000000000000, -12.28373071562070074 ) ) ;
#58220=DIRECTION ( 'NONE',  ( 0.000000000000000000, 0.6884191022827191864, -0.7253131321107147977 ) ) ;
#58221=EDGE_LOOP ( 'NONE', ( #64530, #16639, #23767, #61728 ) ) ;
#58225=AXIS2_PLACEMENT_3D ( 'NONE', #57186, #58220, #40766 ) ;
#58226=DIRECTION ( 'NONE',  ( -0.000000000000000000, -0.000000000000000000, 1.000000000000000000 ) ) ;
#58238=CARTESIAN_POINT ( 'NONE',  ( 12.24735473125024576, 2.217676833728435160, -13.72929951782216484 ) ) ;
#58240=CARTESIAN_POINT ( 'NONE',  ( 17.75641289383300148, -0.5920240553917509585, 13.88302649426328372 ) ) ;
#58243=CARTESIAN_POINT ( 'NONE',  ( 12.29580333567063377, 0.3624858757096150463, 13.89364165471758739 ) ) ;
#58256=CARTESIAN_POINT ( 'NONE',  ( 17.84384701673185702, 0.6598665579121832936, 12.58271022457860688 ) ) ;
#58262=CARTESIAN_POINT ( 'NONE',  ( 17.99827832423966711, 3.095912246742684282, 13.65340184222058184 ) ) ;
#58272=CARTESIAN_POINT ( 'NONE',  ( 18.00435067849408810, -1.907656978620086763, 12.45493970930050764 ) ) ;
#58278=CARTESIAN_POINT ( 'NONE',  ( 5.699994923231000321, 12.50864296698000011, 2.924709704137000266 ) ) ;
#58292=CARTESIAN_POINT ( 'NONE',  ( 12.78418516728948973, 3.124999463064650040, -12.28374650604039964 ) ) ;
#58302=CARTESIAN_POINT ( 'NONE',  ( 12.76350962112090137, -3.123958135104670575, -12.28404825260450473 ) ) ;
#58307=CARTESIAN_POINT ( 'NONE',  ( 12.12605828839494038, -2.774939115234953846, -13.72225238672861281 ) ) ;
#58312=CARTESIAN_POINT ( 'NONE',  ( 17.82398025068296832, -3.148553868299628800, 12.20027175159510513 ) ) ;
#58321=CARTESIAN_POINT ( 'NONE',  ( 18.05707515698803078, 2.118723117023476821, -12.53248177915881278 ) ) ;
#58324=CARTESIAN_POINT ( 'NONE',  ( 17.92325670915549907, -1.853371315644311901, -12.46300045701685910 ) ) ;
#58325=VERTEX_POINT ( 'NONE', #25701 ) ;
#58327=CARTESIAN_POINT ( 'NONE',  ( 12.35410221487145499, -2.932869452542228306, 12.34012701440640214 ) ) ;
#58333=CARTESIAN_POINT ( 'NONE',  ( 12.37008254743958524, -0.4489258298041881590, 12.68932177688764362 ) ) ;
#58335=DIRECTION ( 'NONE',  ( 0.000000000000000000, 0.9553735099700838562, 0.2954005017724949944 ) ) ;
#58336=FACE_OUTER_BOUND ( 'NONE', #30597, .T. ) ;
#58353=CARTESIAN_POINT ( 'NONE',  ( 18.18005043852540581, -2.520325007585945354, 13.66916896904711898 ) ) ;
#58356=CARTESIAN_POINT ( 'NONE',  ( 18.02623320712471511, -2.911124530445448055, -13.57757619639374624 ) ) ;
#58358=CARTESIAN_POINT ( 'NONE',  ( 7.100000000000000533, 12.03770622561999915, 3.722046322334000124 ) ) ;
#58366=CARTESIAN_POINT ( 'NONE',  ( 18.02961597941495953, -0.4069473555476081916, 13.89198745891521192 ) ) ;
#58375=FACE_OUTER_BOUND ( 'NONE', #59188, .T. ) ;
#58378=CARTESIAN_POINT ( 'NONE',  ( 17.82373361328025041, -1.839709763185445546, 13.87859827090101383 ) ) ;
#58379=CARTESIAN_POINT ( 'NONE',  ( 18.05125194750646855, 2.880159330030322096, -13.58544989776502554 ) ) ;
#58392=CARTESIAN_POINT ( 'NONE',  ( 17.63678281077947219, 0.6199686954221031998, -12.67962180225518942 ) ) ;
#58393=CARTESIAN_POINT ( 'NONE',  ( 12.23606560776517860, 2.758669204905062067, -12.38755309841745422 ) ) ;
#58403=CARTESIAN_POINT ( 'NONE',  ( 17.55505043854143565, 1.760910691117812066, 12.47634535983623039 ) ) ;
#58409=CARTESIAN_POINT ( 'NONE',  ( 12.30583355256791300, -1.958333444515658606, 12.44688698484233669 ) ) ;
#58415=CARTESIAN_POINT ( 'NONE',  ( 12.68688152457048268, 0.7100593550699842993, 12.57997761080729759 ) ) ;
#58419=CARTESIAN_POINT ( 'NONE',  ( 12.08482599452294437, 2.564444806221811479, 12.33627826672299044 ) ) ;
#58427=CARTESIAN_POINT ( 'NONE',  ( 18.12841930325617668, -0.2489729014350941239, 12.69672092237004257 ) ) ;
#58438=CARTESIAN_POINT ( 'NONE',  ( 12.17997927555901505, -2.482106649064418136, 13.67725710540907613 ) ) ;
#58439=CARTESIAN_POINT ( 'NONE',  ( 12.19551626499556463, 2.360211740085632393, 13.70208339271400355 ) ) ;
#58446=AXIS2_PLACEMENT_3D ( 'NONE', #36330, #31779, #64259 ) ;
#58449=CARTESIAN_POINT ( 'NONE',  ( 18.15862102414876489, 2.662578152609974769, -12.41223253473083332 ) ) ;
#58451=CARTESIAN_POINT ( 'NONE',  ( 17.71871529296970493, 3.104542143063796722, 12.28994062198843906 ) ) ;
#58462=VECTOR ( 'NONE', #35840, 1000.000000000000000 ) ;
#58463=ORIENTED_EDGE ( 'NONE', *, *, #28754, .F. ) ;
#58468=CONICAL_SURFACE ( 'NONE', #2681, 12.69999976913000062, 0.7853981453603698926 ) ;
#58473=CARTESIAN_POINT ( 'NONE',  ( 12.25734203442973502, 0.3012395218291776811, -13.89560941714155540 ) ) ;
#58478=ADVANCED_FACE ( 'NONE', ( #37227 ), #22513, .T. ) ;
#58483=ORIENTED_EDGE ( 'NONE', *, *, #49648, .T. ) ;
#58487=CARTESIAN_POINT ( 'NONE',  ( 18.18005043835062295, -2.498838836691497534, -12.45183430368941835 ) ) ;
#58488=CARTESIAN_POINT ( 'NONE',  ( 12.20096535489426870, 0.1616183441363953921, 13.89875400931294536 ) ) ;
#58489=ORIENTED_EDGE ( 'NONE', *, *, #51913, .T. ) ;
#58515=CARTESIAN_POINT ( 'NONE',  ( 5.679181292414646087, -13.00268187323304225, -2.124261077943678355 ) ) ;
#58517=EDGE_CURVE ( 'NONE', #5374, #24349, #16587, .T. ) ;
#58518=CARTESIAN_POINT ( 'NONE',  ( 18.01273579184442752, 2.926031893962671049, -12.34206213438296551 ) ) ;
#58527=CARTESIAN_POINT ( 'NONE',  ( 12.21327642329898389, -0.2013262877421473085, -12.69785743964336078 ) ) ;
#58535=CARTESIAN_POINT ( 'NONE',  ( 18.02962380328376213, 0.4069377568334723860, 12.69123026945923627 ) ) ;
#58540=AXIS2_PLACEMENT_3D ( 'NONE', #8902, #30242, #46313 ) ;
#58547=CARTESIAN_POINT ( 'NONE',  ( 17.71954595323150627, -0.7115697451012072960, -13.98190580764195801 ) ) ;
#58551=CARTESIAN_POINT ( 'NONE',  ( 12.80505043854146940, -3.174798964346249530, -12.21921514949791820 ) ) ;
#58557=CARTESIAN_POINT ( 'NONE',  ( 4.599999999999999645, 0.7192913403693119712, -12.57945229203838267 ) ) ;
#58561=AXIS2_PLACEMENT_3D ( 'NONE', #42049, #36808, #10228 ) ;
#58563=VERTEX_POINT ( 'NONE', #59579 ) ;
#58565=CARTESIAN_POINT ( 'NONE',  ( 18.09779443567301271, 0.3101119055885873110, -13.89534721488124447 ) ) ;
#58567=AXIS2_PLACEMENT_3D ( 'NONE', #34748, #14789, #57086 ) ;
#58579=VECTOR ( 'NONE', #17376, 1000.000000000000000 ) ;
#58581=CARTESIAN_POINT ( 'NONE',  ( 12.21197387330458461, 2.302545343651722920, -13.71336076199744802 ) ) ;
#58586=CARTESIAN_POINT ( 'NONE',  ( 18.16002775360864518, 0.1622926919634330167, 13.89880504291887320 ) ) ;
#58591=CARTESIAN_POINT ( 'NONE',  ( 17.75497764268494549, -0.5922531181022384628, -13.88301284246451139 ) ) ;
#58599=CARTESIAN_POINT ( 'NONE',  ( 18.11105811251409037, -0.2856309244984046591, 12.69568149856437067 ) ) ;
#58615=CARTESIAN_POINT ( 'NONE',  ( 12.50564389185356973, -0.6551943188411786245, -12.58295456804122914 ) ) ;
#58617=CARTESIAN_POINT ( 'NONE',  ( 17.79016990201540693, 3.160912468841193590, -12.19707490278732820 ) ) ;
#58618=CARTESIAN_POINT ( 'NONE',  ( 5.606877745311565242, 12.12699005521752049, 3.748526802953684012 ) ) ;
#58636=CARTESIAN_POINT ( 'NONE',  ( 12.39876276414167933, 2.975035832937170888, -12.32812070139215166 ) ) ;
#58650=CARTESIAN_POINT ( 'NONE',  ( 12.38986377076840206, -2.032719501308457577, -12.54823268863294849 ) ) ;
#58654=CARTESIAN_POINT ( 'NONE',  ( 12.48191940168460157, -1.864230036291391057, -13.87532606992096618 ) ) ;
#58657=CARTESIAN_POINT ( 'NONE',  ( 17.92000013766230637, -3.102113379644124702, 12.21216327800867774 ) ) ;
#58680=CARTESIAN_POINT ( 'NONE',  ( 5.569720047903312654, -12.16229356903719250, -3.760137167885687415 ) ) ;
#58686=CARTESIAN_POINT ( 'NONE',  ( 17.80546914520760993, 3.072731260628056127, 13.53510445278182672 ) ) ;
#58701=CARTESIAN_POINT ( 'NONE',  ( 17.88684482918182184, -3.030051203688146622, -13.54658895838268151 ) ) ;
#58717=CIRCLE ( 'NONE', #34179, 2.000000000000000444 ) ;
#58721=CARTESIAN_POINT ( 'NONE',  ( 12.08853825830067841, 2.367028970089855910, -12.37569070051500830 ) ) ;
#58724=CARTESIAN_POINT ( 'NONE',  ( 18.11145169124867138, 2.784830482480015412, -13.60891328693460522 ) ) ;
#58725=EDGE_CURVE ( 'NONE', #38787, #65648, #28121, .T. ) ;
#58736=CARTESIAN_POINT ( 'NONE',  ( 17.65692019170432303, 0.6169782284476039713, -12.67981870385671428 ) ) ;
#58746=CARTESIAN_POINT ( 'NONE',  ( 17.99911394258097630, 3.049496102151219912, 12.22541657636149282 ) ) ;
#58747=CARTESIAN_POINT ( 'NONE',  ( 7.100000000000000533, 13.94845324556000143, -4.312847325879000770 ) ) ;
#58752=CARTESIAN_POINT ( 'NONE',  ( 12.23408645687635143, -2.036599147259928078, 12.43432143783615551 ) ) ;
#58758=B_SPLINE_CURVE_WITH_KNOTS ( 'NONE', 3,
 ( #9870, #27595, #15467, #36442, #64640, #1715, #36794, #60103, #58114, #48921, #41687, #31548, #1029, #26302, #49258, #22341, #47630, #33188 ),
 .UNSPECIFIED., .F., .F.,
 ( 4, 2, 2, 2, 2, 2, 2, 2, 4 ),
 ( 0.000000000000000000, 0.06250000000000024980, 0.1250000000000004996, 0.2500000000000009992, 0.4999999999999992228, 0.7499999999999974465, 0.8749999999999965583, 0.9374999999999983347, 1.000000000000000000 ),
 .UNSPECIFIED. ) ;
#58763=CARTESIAN_POINT ( 'NONE',  ( 12.10796728133592026, 2.678710578830982847, 12.31197141455839272 ) ) ;
#58771=CARTESIAN_POINT ( 'NONE',  ( 12.34829947334116262, 2.926730327392950137, 12.34183739587882300 ) ) ;
#58773=ORIENTED_EDGE ( 'NONE', *, *, #33418, .F. ) ;
#58774=CARTESIAN_POINT ( 'NONE',  ( 12.23478131640822753, 0.2564338549407608747, 12.69653134296957120 ) ) ;
#58780=CARTESIAN_POINT ( 'NONE',  ( 12.52680909801651765, -3.059742249080376286, 13.53867541207075220 ) ) ;
#58781=CARTESIAN_POINT ( 'NONE',  ( 12.18999301580459793, 2.611634498301437013, 13.64910281353442656 ) ) ;
#58792=CARTESIAN_POINT ( 'NONE',  ( 17.69815883927265787, 3.108482560213371215, -12.28876257455221221 ) ) ;
#58795=CARTESIAN_POINT ( 'NONE',  ( 18.02583793286699176, 2.911580782565375891, 12.34610277261516309 ) ) ;
#58815=DIRECTION ( 'NONE',  ( 1.000000000000000000, 0.000000000000000000, 0.000000000000000000 ) ) ;
#58816=CARTESIAN_POINT ( 'NONE',  ( 12.28049946582619434, 0.3399327003773965905, -13.89440849576309667 ) ) ;
#58820=VERTEX_POINT ( 'NONE', #45919 ) ;
#58826=CARTESIAN_POINT ( 'NONE',  ( 17.98409414022582453, -2.954502725563342480, -12.33397020297173796 ) ) ;
#58832=CARTESIAN_POINT ( 'NONE',  ( 12.19409625758322413, -0.1321590433901052575, 13.89915950722681970 ) ) ;
#58843=ORIENTED_EDGE ( 'NONE', *, *, #62690, .T. ) ;
#58861=B_SPLINE_CURVE_WITH_KNOTS ( 'NONE', 3,
 ( #24722, #29989, #14579, #51627, #15606, #10010, #46738, #57911, #31006, #68382, #25402, #52320, #35896, #30654, #25752, #26098, #46046, #67353 ),
 .UNSPECIFIED., .F., .F.,
 ( 4, 2, 2, 2, 2, 2, 2, 2, 4 ),
 ( 0.000000000000000000, 0.06249999999999873712, 0.1249999999999974742, 0.2499999999999972800, 0.4999999999999987788, 0.7500000000000002220, 0.8750000000000001110, 0.9375000000000000000, 1.000000000000000000 ),
 .UNSPECIFIED. ) ;
#58866=CARTESIAN_POINT ( 'NONE',  ( 18.17608830303050027, 2.571081552045474616, -12.43475473545199073 ) ) ;
#58876=CARTESIAN_POINT ( 'NONE',  ( 12.23161381921988600, -0.2487950381773050834, -12.69672507751632828 ) ) ;
#58887=EDGE_CURVE ( 'NONE', #41143, #59809, #1059, .T. ) ;
#58898=( GEOMETRIC_REPRESENTATION_CONTEXT ( 3 ) GLOBAL_UNCERTAINTY_ASSIGNED_CONTEXT ( ( #5211 ) ) GLOBAL_UNIT_ASSIGNED_CONTEXT ( ( #29365, #66055, #50680 ) ) REPRESENTATION_CONTEXT ( 'NONE', 'WORKASPACE' ) );
#58909=DIRECTION ( 'NONE',  ( -1.000000000000000000, 0.000000000000000000, 0.000000000000000000 ) ) ;
#58914=EDGE_LOOP ( 'NONE', ( #17946, #60444, #66115, #60956 ) ) ;
#58916=CARTESIAN_POINT ( 'NONE',  ( 17.77886761546800187, -1.796012712130053313, -12.47134082573985658 ) ) ;
#58926=CARTESIAN_POINT ( 'NONE',  ( 17.55505043854147118, -1.875000000000000000, -12.57541666120755863 ) ) ;
#58933=CARTESIAN_POINT ( 'NONE',  ( 18.06357043707759402, -0.3639325664385105186, 13.89360161040563035 ) ) ;
#58934=CARTESIAN_POINT ( 'NONE',  ( 18.06407613809071577, 0.3627976897793646627, 13.89363072199764204 ) ) ;
#58936=CARTESIAN_POINT ( 'NONE',  ( 12.38194801265183109, 0.4608083867824496749, 13.88973595540270978 ) ) ;
#58939=CARTESIAN_POINT ( 'NONE',  ( 7.100000000000000533, -13.04986661130000059, -1.811520473896000016 ) ) ;
#58947=CARTESIAN_POINT ( 'NONE',  ( 18.13994946422174337, -0.2205037192104046251, 12.69742880170239019 ) ) ;
#58950=CARTESIAN_POINT ( 'NONE',  ( 7.100000000000000533, 0.000000000000000000, 0.000000000000000000 ) ) ;
#58961=DIRECTION ( 'NONE',  ( -1.000000000000000000, 0.000000000000000000, 0.000000000000000000 ) ) ;
#58966=CARTESIAN_POINT ( 'NONE',  ( 18.24165222613598303, 2.712088604378295909, -12.30466175173926935 ) ) ;
#58984=CARTESIAN_POINT ( 'NONE',  ( 17.55505043854143921, 0.6250000000000002220, -13.88107975066922428 ) ) ;
#58989=CARTESIAN_POINT ( 'NONE',  ( 12.48990506108388665, 3.039826403548175460, -12.30927084193774235 ) ) ;
#59002=CARTESIAN_POINT ( 'NONE',  ( 12.63921101284457293, -1.806754227364050669, -13.88292698645336465 ) ) ;
#59007=CARTESIAN_POINT ( 'NONE',  ( 17.79586754331425524, -3.158948767300545413, 12.19758365745370021 ) ) ;
#59029=CARTESIAN_POINT ( 'NONE',  ( 12.44044950778751080, -0.5080407711865464471, 12.68632595416892883 ) ) ;
#59033=CARTESIAN_POINT ( 'NONE',  ( 6.633333333537346554, 12.50865282024215297, -2.924692170536358660 ) ) ;
#59035=EDGE_CURVE ( 'NONE', #32586, #37575, #51163, .T. ) ;
#59036=EDGE_CURVE ( 'NONE', #28970, #12254, #28823, .T. ) ;
#59037=CARTESIAN_POINT ( 'NONE',  ( 18.17246482408070918, 2.400822122662769509, 13.69396077230720721 ) ) ;
#59041=CARTESIAN_POINT ( 'NONE',  ( 5.699999545467999695, -12.03770622561999915, 3.722046322334000124 ) ) ;
#59049=CARTESIAN_POINT ( 'NONE',  ( 17.65774109649150958, -3.116847231231422377, -13.52303903038508004 ) ) ;
#59068=CARTESIAN_POINT ( 'NONE',  ( 12.20599951553714924, 2.074681531931801715, -12.42802467457380899 ) ) ;
#59072=CARTESIAN_POINT ( 'NONE',  ( 18.17219575274162935, 2.599291946997700276, -13.65190342897701470 ) ) ;
#59083=CARTESIAN_POINT ( 'NONE',  ( 17.57569811463524445, 0.6249994333735308105, -12.67928921956171173 ) ) ;
#59084=CARTESIAN_POINT ( 'NONE',  ( 12.63924565014722923, 1.874999999999999556, -12.57545536278438902 ) ) ;
#59092=CARTESIAN_POINT ( 'NONE',  ( 18.23533704695767810, 2.231030541001932210, 12.40091240268597872 ) ) ;
#59100=CARTESIAN_POINT ( 'NONE',  ( 12.28182936075429943, -2.978585426876346087, 12.24287970063667252 ) ) ;
#59105=CARTESIAN_POINT ( 'NONE',  ( 12.47371306568759408, 0.6398865404514789690, 12.58374251866278826 ) ) ;
#59108=CARTESIAN_POINT ( 'NONE',  ( 12.26287255281685695, 2.811570894161414813, 12.37351047967075424 ) ) ;
#59116=CARTESIAN_POINT ( 'NONE',  ( 12.80505043854146940, -1.875000000000000444, -13.78627172894481667 ) ) ;
#59120=ADVANCED_FACE ( 'NONE', ( #67567 ), #24244, .F. ) ;
#59121=CARTESIAN_POINT ( 'NONE',  ( 12.31508698957360615, 0.3880315155551694595, 12.69202109204528739 ) ) ;
#59125=CARTESIAN_POINT ( 'NONE',  ( 12.61514273204572589, -1.812907417374193031, 13.88212581052982486 ) ) ;
#59135=CARTESIAN_POINT ( 'NONE',  ( 18.17458387927298702, 2.583096938294931810, -12.43185036011799482 ) ) ;
#59142=PLANE ( 'NONE',  #68970 ) ;
#59148=CARTESIAN_POINT ( 'NONE',  ( 18.05225003025152120, -2.879247418710622508, 13.58568546892325912 ) ) ;
#59158=CARTESIAN_POINT ( 'NONE',  ( 12.20957190034697248, 0.1900921649601574615, -13.89825464817679901 ) ) ;
#59163=LINE ( 'NONE', #13362, #55684 ) ;
#59171=CARTESIAN_POINT ( 'NONE',  ( 17.80592519432568821, -3.072462716380374381, -12.29957259991316931 ) ) ;
#59177=DIRECTION ( 'NONE',  ( -1.000000000000000000, 0.000000000000000000, 0.000000000000000000 ) ) ;
#59179=CARTESIAN_POINT ( 'NONE',  ( 12.19004662364084091, 0.1118032413084496662, 13.89939982891986148 ) ) ;
#59188=EDGE_LOOP ( 'NONE', ( #34658, #4749, #55811, #2414 ) ) ;
#59191=CARTESIAN_POINT ( 'NONE',  ( 17.92262925323456102, -1.881361389426406960, 13.87306285016402363 ) ) ;
#59220=CARTESIAN_POINT ( 'NONE',  ( 12.43656315537375612, 1.853531805833888324, 12.46297683056294048 ) ) ;
#59230=FACE_OUTER_BOUND ( 'NONE', #7160, .T. ) ;
#59249=FACE_OUTER_BOUND ( 'NONE', #65438, .T. ) ;
#59264=CARTESIAN_POINT ( 'NONE',  ( 12.78089888617682846, 1.787816964400945619, -13.88537754411822434 ) ) ;
#59267=CARTESIAN_POINT ( 'NONE',  ( 17.88582179699705677, -0.5306878043354128494, 13.88636785578044730 ) ) ;
#59271=CARTESIAN_POINT ( 'NONE',  ( 12.78475456301477386, 0.6249999999999994449, 13.88107975066923494 ) ) ;
#59274=CARTESIAN_POINT ( 'NONE',  ( 17.97806348698183854, -0.4608880372975631690, -13.88973238275042021 ) ) ;
#59283=CARTESIAN_POINT ( 'NONE',  ( 18.17005379958825273, 0.1118057330073154582, 12.69934308675516377 ) ) ;
#59298=CARTESIAN_POINT ( 'NONE',  ( 12.39267273778989242, -0.5917181940048676925, -12.58609996267492903 ) ) ;
#59301=CARTESIAN_POINT ( 'NONE',  ( 17.77874050697764829, 3.164693776342188070, -12.19609433843463009 ) ) ;
#59317=CARTESIAN_POINT ( 'NONE',  ( 12.43699713721653310, 3.107380776471872608, -12.21088077982606102 ) ) ;
#59320=CARTESIAN_POINT ( 'NONE',  ( 18.15598102061104768, -0.1720826668005526749, -13.89857125525884207 ) ) ;
#59322=DIRECTION ( 'NONE',  ( -1.000000000000000000, 0.000000000000000000, 0.000000000000000000 ) ) ;
#59332=B_SPLINE_CURVE_WITH_KNOTS ( 'NONE', 3,
 ( #18926, #67148, #25193, #13687, #46527, #67835, #9446, #19956, #15047, #19261, #41280, #62927, #36373, #8092, #42650, #32173, #10148, #11172, #58379, #37403, #689, #37745, #21657, #57688, #4893, #58724, #5578, #31148, #26581, #9798, #10829, #31478, #63960, #36727, #52449, #31824, #26921, #4544, #10486, #52800, #16754, #42990, #64299, #53486, #26233, #59072, #340, #53141, #47563, #27263, #25884 ),
 .UNSPECIFIED., .F., .F.,
 ( 4, 2, 2, 2, 2, 2, 2, 2, 2, 2, 2, 2, 2, 1, 2, 2, 2, 2, 2, 2, 2, 2, 2, 2, 2, 4 ),
 ( 0.000000000000000000, 0.06261444088627614313, 0.1252288817725522863, 0.1565361022156903370, 0.1878433226588283878, 0.2191505431019664663, 0.2348041533235355194, 0.2504577635451045725, 0.2817649839882465646, 0.2974185942098189206, 0.3130722044313913321, 0.3287258146529636327, 0.3443794248745360442, 0.3600330350961084003, 0.3678598402068946061, 0.3756866453176807563, 0.3913402555392500592, 0.3991670606500349328, 0.4069938657608198618, 0.4226474759823886096, 0.4304742810931723174, 0.4343876836485654480, 0.4383010862039585231, 0.4539546964255286032, 0.4696083066470986278, 0.5009155270902381218 ),
 .UNSPECIFIED. ) ;
#59335=CARTESIAN_POINT ( 'NONE',  ( 12.18490839767386014, -2.421563015655832984, -12.46949130182972354 ) ) ;
#59339=CARTESIAN_POINT ( 'NONE',  ( 12.35155033006833136, -1.948172666216914983, -13.86379038907994854 ) ) ;
#59341=CARTESIAN_POINT ( 'NONE',  ( 12.35552214746119049, -1.907986453762815060, 12.45488571128362665 ) ) ;
#59343=CARTESIAN_POINT ( 'NONE',  ( 17.81282484970914126, -3.152868460668823758, 12.19915726504404851 ) ) ;
#59345=EDGE_LOOP ( 'NONE', ( #21421, #58463, #59942, #53967 ) ) ;
#59355=VECTOR ( 'NONE', #19242, 1000.000000000000000 ) ;
#59373=CARTESIAN_POINT ( 'NONE',  ( 18.08802622730387100, 2.172927601657333341, 13.73737356033239188 ) ) ;
#59377=CARTESIAN_POINT ( 'NONE',  ( 5.604756202875922355, -12.12903653623212108, 3.749090042451754812 ) ) ;
#59384=CARTESIAN_POINT ( 'NONE',  ( 17.98066499537654650, -1.926393605117494578, -13.86683778668631106 ) ) ;
#59386=EDGE_CURVE ( 'NONE', #4266, #38087, #25271, .T. ) ;
#59403=EDGE_LOOP ( 'NONE', ( #26831, #46772, #55173, #64280 ) ) ;
#59405=CARTESIAN_POINT ( 'NONE',  ( 12.12616169587827741, 2.733465040722955486, -12.29993066094647958 ) ) ;
#59408=AXIS2_PLACEMENT_3D ( 'NONE', #60923, #38913, #18623 ) ;
#59423=CARTESIAN_POINT ( 'NONE',  ( 17.75589797987078100, 0.5919389804100245733, -12.68142457171642690 ) ) ;
#59424=CARTESIAN_POINT ( 'NONE',  ( 12.18798377887743278, 2.400256349710756076, -12.47427327511915962 ) ) ;
#59426=EDGE_CURVE ( 'NONE', #20309, #9109, #53624, .T. ) ;
#59433=CARTESIAN_POINT ( 'NONE',  ( 18.28006803703874183, 2.506146490485266387, 12.34827083869106978 ) ) ;
#59439=CARTESIAN_POINT ( 'NONE',  ( 12.70853553880221298, -3.193755089013870840, 12.18851650745940418 ) ) ;
#59440=B_SPLINE_CURVE_WITH_KNOTS ( 'NONE', 3,
 ( #14645, #9044, #67760, #9378, #30384, #52380, #51694, #46461, #41214, #35961, #19887, #52031, #62524, #62861, #4133, #31074 ),
 .UNSPECIFIED., .F., .F.,
 ( 4, 2, 2, 2, 2, 2, 2, 4 ),
 ( 0.000000000000000000, 0.06250000000000113798, 0.1250000000000022760, 0.2500000000000024980, 0.5000000000000011102, 0.7499999999999997780, 0.8749999999999998890, 1.000000000000000000 ),
 .UNSPECIFIED. ) ;
#59448=CARTESIAN_POINT ( 'NONE',  ( 12.33572460179970953, -0.5483668826291607790, 12.58806376549905082 ) ) ;
#59451=CARTESIAN_POINT ( 'NONE',  ( 12.75673482301074735, 1.762409409947518046, 12.47613375359912169 ) ) ;
#59458=CARTESIAN_POINT ( 'NONE',  ( 17.89454609201841251, -0.5248351044085231010, 12.68540052859852452 ) ) ;
#59462=CARTESIAN_POINT ( 'NONE',  ( 12.40638932693400420, 0.4813547430073586986, 12.68771948605883892 ) ) ;
#59466=CARTESIAN_POINT ( 'NONE',  ( 12.70875935989989713, -1.793877008111231186, 13.88459618876652790 ) ) ;
#59475=CARTESIAN_POINT ( 'NONE',  ( 17.77761373051709981, 1.915879702936831519, -12.56867159344775153 ) ) ;
#59493=CARTESIAN_POINT ( 'NONE',  ( 17.96968152693882104, -2.032227188856706945, 13.76161273592455281 ) ) ;
#59506=ORIENTED_EDGE ( 'NONE', *, *, #35989, .T. ) ;
#59521=CARTESIAN_POINT ( 'NONE',  ( 12.52635726938498628, 3.059519608057332363, 13.53867825407380998 ) ) ;
#59524=CARTESIAN_POINT ( 'NONE',  ( 12.21299871467824971, 0.2005085131878075189, 13.89805835524349931 ) ) ;
#59534=ORIENTED_EDGE ( 'NONE', *, *, #61446, .F. ) ;
#59552=CARTESIAN_POINT ( 'NONE',  ( 5.660639679273599789, -12.98305834912500956, -2.241106595026677528 ) ) ;
#59579=CARTESIAN_POINT ( 'NONE',  ( 12.80505043854146940, -1.875000000000000444, 12.57545641911172396 ) ) ;
#59588=VERTEX_POINT ( 'NONE', #53661 ) ;
#59597=ADVANCED_FACE ( 'NONE', ( #5754 ), #17644, .F. ) ;
#59600=CARTESIAN_POINT ( 'NONE',  ( 17.74439936569998366, -1.785463535057947970, -12.47285731025142930 ) ) ;
#59613=CARTESIAN_POINT ( 'NONE',  ( 12.18472282150162478, 2.421014800242781373, -13.68991273180144574 ) ) ;
#59617=CARTESIAN_POINT ( 'NONE',  ( 18.11117642456259347, -0.2854033456632683041, 13.89606078824648172 ) ) ;
#59618=AXIS2_PLACEMENT_3D ( 'NONE', #7778, #55328, #7425 ) ;
#59619=CARTESIAN_POINT ( 'NONE',  ( 17.90980351667704085, 0.5146449799214740661, 13.88717540043435861 ) ) ;
#59623=CARTESIAN_POINT ( 'NONE',  ( 12.31853810497323920, -0.3923498216886506240, 13.89254714538524027 ) ) ;
#59624=CIRCLE ( 'NONE', #62951, 14.00000000000000000 ) ;
#59627=CARTESIAN_POINT ( 'NONE',  ( 18.02496672418951107, -0.4121037243925090299, -13.89177745834417088 ) ) ;
#59635=CARTESIAN_POINT ( 'NONE',  ( 17.74611058647004214, -0.5951698179256270649, 12.68122092285040559 ) ) ;
#59650=CARTESIAN_POINT ( 'NONE',  ( 12.09898038912532847, -0.1637242582067878482, -12.59894148523290980 ) ) ;
#59652=CARTESIAN_POINT ( 'NONE',  ( 18.26373780016885107, 2.633255345072546216, -12.32177353326231461 ) ) ;
#59653=CARTESIAN_POINT ( 'NONE',  ( 5.600889858812243105, 12.13276343987783257, 3.750125071915198838 ) ) ;
#59657=ADVANCED_FACE ( 'NONE', ( #40005 ), #44064, .T. ) ;
#59669=CARTESIAN_POINT ( 'NONE',  ( 17.67410956179875470, 0.7206971133477627633, -13.98143832535762776 ) ) ;
#59670=ORIENTED_EDGE ( 'NONE', *, *, #23183, .T. ) ;
#59684=CARTESIAN_POINT ( 'NONE',  ( 12.18947222198080205, -2.391413182808839633, -12.47619792628429813 ) ) ;
#59688=CARTESIAN_POINT ( 'NONE',  ( 12.29903578917718932, -3.040996334883329766, -13.66573881806045421 ) ) ;
#59690=CARTESIAN_POINT ( 'NONE',  ( 12.80505043854146940, -1.760845406083394016, 12.47635457398814829 ) ) ;
#59691=CARTESIAN_POINT ( 'NONE',  ( 18.05438665931233189, -1.958444820271050046, 12.44686948166836160 ) ) ;
#59708=B_SPLINE_CURVE_WITH_KNOTS ( 'NONE', 3,
 ( #54942, #44810, #44472, #60189, #12294, #24159, #65765, #18579, #23120, #12638, #33624, #7043, #17891, #28378, #8086, #50390 ),
 .UNSPECIFIED., .F., .F.,
 ( 4, 2, 2, 2, 2, 2, 2, 4 ),
 ( 0.000000000000000000, 0.06250000000000123512, 0.1250000000000024702, 0.2500000000000007216, 0.5000000000000004441, 0.7500000000000002220, 0.8750000000000002220, 1.000000000000000000 ),
 .UNSPECIFIED. ) ;
#59720=CARTESIAN_POINT ( 'NONE',  ( 18.09690629521215044, 2.811641957965460570, 13.60235445620235595 ) ) ;
#59732=CARTESIAN_POINT ( 'NONE',  ( 18.02709866344915923, -1.963667282347026921, -13.86160417883469975 ) ) ;
#59753=CARTESIAN_POINT ( 'NONE',  ( 12.28182936075425857, 2.978585426876357189, -12.24287970063667075 ) ) ;
#59771=CARTESIAN_POINT ( 'NONE',  ( 17.93599305328152482, -0.4959072410923969776, -12.68697406334525546 ) ) ;
#59772=CARTESIAN_POINT ( 'NONE',  ( 12.19311196912284778, 2.627115699720651065, -12.42106741852103191 ) ) ;
#59775=ORIENTED_EDGE ( 'NONE', *, *, #59963, .F. ) ;
#59780=CARTESIAN_POINT ( 'NONE',  ( 18.10215020711899214, 2.952580169587743164, 12.24917755118608831 ) ) ;
#59788=CARTESIAN_POINT ( 'NONE',  ( 12.30724456330684546, -3.003488097433224535, 12.23679193692684741 ) ) ;
#59794=CARTESIAN_POINT ( 'NONE',  ( 12.48372201234963086, -0.6448943924266594685, 12.58348668657566094 ) ) ;
#59799=CARTESIAN_POINT ( 'NONE',  ( 12.74469048821893402, 1.763307075768890453, 12.47600695802491266 ) ) ;
#59800=VERTEX_POINT ( 'NONE', #25633 ) ;
#59803=CARTESIAN_POINT ( 'NONE',  ( 17.88638781139528788, -0.6398865404514794131, 12.58374251866278826 ) ) ;
#59808=CARTESIAN_POINT ( 'NONE',  ( 17.55505043854144276, 0.6250000000000001110, -25.00000000000000000 ) ) ;
#59809=VERTEX_POINT ( 'NONE', #62681 ) ;
#59815=CARTESIAN_POINT ( 'NONE',  ( 12.21285350005642911, -2.096151405059779815, 13.84220188050174016 ) ) ;
#59827=CARTESIAN_POINT ( 'NONE',  ( 18.01444767332560204, 2.076107767824256989, -12.54031350746514129 ) ) ;
#59839=CARTESIAN_POINT ( 'NONE',  ( 17.71863970650579745, -3.103558472751648090, 13.52675378075879209 ) ) ;
#59848=CARTESIAN_POINT ( 'NONE',  ( 12.15646017001375512, -2.140061664339810932, -13.83614491991404272 ) ) ;
#59850=CARTESIAN_POINT ( 'NONE',  ( 17.85445698522930869, 0.6551943188411784025, -12.58295456804123091 ) ) ;
#59856=CIRCLE ( 'NONE', #37539, 12.84999890301999947 ) ;
#59864=CARTESIAN_POINT ( 'NONE',  ( 12.25689739436619341, 2.199570998105316200, 13.73255685804838500 ) ) ;
#59868=FACE_OUTER_BOUND ( 'NONE', #32455, .T. ) ;
#59875=CARTESIAN_POINT ( 'NONE',  ( 5.599999772733800008, -6.661338147750999827E-14, 12.69999976912998108 ) ) ;
#59910=CARTESIAN_POINT ( 'NONE',  ( 12.48799821678961308, 1.955167389914997722, -13.77408040568415615 ) ) ;
#59912=CARTESIAN_POINT ( 'NONE',  ( 12.61551017423881405, 3.176304576345524211, 12.19307927065969999 ) ) ;
#59915=CARTESIAN_POINT ( 'NONE',  ( 12.17676779642099660, -0.3651687365794661910, -13.99525266148724256 ) ) ;
#59923=CARTESIAN_POINT ( 'NONE',  ( 17.67504841906447055, 3.238437383711908701, -13.62029908313572157 ) ) ;
#59942=ORIENTED_EDGE ( 'NONE', *, *, #6691, .T. ) ;
#59944=CARTESIAN_POINT ( 'NONE',  ( 18.24314268136838990, -2.253095180823014854, -12.39692251310592574 ) ) ;
#59957=CARTESIAN_POINT ( 'NONE',  ( 12.18763606713061520, 2.400822034753086864, -13.69401148367744092 ) ) ;
#59960=CARTESIAN_POINT ( 'NONE',  ( 18.24552752486709650, -0.2229649748661350905, 13.99822903660538564 ) ) ;
#59963=EDGE_CURVE ( 'NONE', #38087, #64166, #42406, .T. ) ;
#59968=CARTESIAN_POINT ( 'NONE',  ( 12.29893553472659029, -0.3669576693511948928, 13.89348614079305655 ) ) ;
#59969=CARTESIAN_POINT ( 'NONE',  ( 12.76431812847650704, -0.6240106079411803508, -13.88114051191588594 ) ) ;
#59979=CARTESIAN_POINT ( 'NONE',  ( 17.69686089611048985, -0.6090396975623083575, 12.68033511803395363 ) ) ;
#59981=CARTESIAN_POINT ( 'NONE',  ( 17.99291067209890826, -2.946084426705714687, -12.33636513593941508 ) ) ;
#59995=VERTEX_POINT ( 'NONE', #7405 ) ;
#59996=CARTESIAN_POINT ( 'NONE',  ( 12.27567264278500048, -0.4920215530101137436, -12.59040071882420264 ) ) ;
#59998=CARTESIAN_POINT ( 'NONE',  ( 18.01279894578400942, 3.038334268486855283, -12.22818629355008468 ) ) ;
#60012=EDGE_CURVE ( 'NONE', #20309, #64166, #44829, .T. ) ;
#60013=CARTESIAN_POINT ( 'NONE',  ( 12.61298032294660310, 3.180483649502660271, -12.19204447434304051 ) ) ;
#60015=CARTESIAN_POINT ( 'NONE',  ( 17.96724268330523344, -0.4699225802676937902, -13.88930950616751225 ) ) ;
#60030=CARTESIAN_POINT ( 'NONE',  ( 12.21847001913372388, -2.284010606415768585, -12.49926433191011732 ) ) ;
#60038=CARTESIAN_POINT ( 'NONE',  ( 17.55505043854147118, -1.760845406083394682, 12.47635457398815184 ) ) ;
#60043=VECTOR ( 'NONE', #31901, 1000.000000000000000 ) ;
#60061=CARTESIAN_POINT ( 'NONE',  ( 12.80505043854144276, -0.6878608935795413881, -12.61273126665598454 ) ) ;
#60075=CARTESIAN_POINT ( 'NONE',  ( 18.12600850643434569, 2.245563876552335358, 13.72409254399188150 ) ) ;
#60086=CARTESIAN_POINT ( 'NONE',  ( 18.21732822554151809, -2.220719680094997095, -13.82275391900495798 ) ) ;
#60090=ORIENTED_EDGE ( 'NONE', *, *, #61873, .F. ) ;
#60098=ORIENTED_EDGE ( 'NONE', *, *, #4156, .T. ) ;
#60103=CARTESIAN_POINT ( 'NONE',  ( 18.20180239426969138, 2.898381337229589683, 13.69738341128404002 ) ) ;
#60104=ORIENTED_EDGE ( 'NONE', *, *, #37727, .F. ) ;
#60109=CARTESIAN_POINT ( 'NONE',  ( 12.56948062052969206, 3.161141996800560516, -12.19701735778311935 ) ) ;
#60124=CARTESIAN_POINT ( 'NONE',  ( 12.18524896721729966, -2.583003884521777760, -13.65547336762760544 ) ) ;
#60125=CARTESIAN_POINT ( 'NONE',  ( 18.14682445378390341, 0.2013262877421451713, -12.69785743964336078 ) ) ;
#60126=CARTESIAN_POINT ( 'NONE',  ( 12.19004578040465070, 2.611920287575038024, -12.42482035883542046 ) ) ;
#60134=CARTESIAN_POINT ( 'NONE',  ( 18.13206058706447621, 2.916601882134809642, 12.25780480496326241 ) ) ;
#60143=CARTESIAN_POINT ( 'NONE',  ( 12.09872039853184589, -2.644866564252636554, 12.31930286224045368 ) ) ;
#60149=CARTESIAN_POINT ( 'NONE',  ( 12.54926746055851616, -0.6731412448965049533, 12.58200685883812930 ) ) ;
#60154=CARTESIAN_POINT ( 'NONE',  ( 12.72250989631410789, 3.119868145445779284, 12.28529260172211757 ) ) ;
#60169=DIRECTION ( 'NONE',  ( -0.7071069400699796503, -0.7071066223030796349, -2.150925218129939376E-09 ) ) ;
#60172=CARTESIAN_POINT ( 'NONE',  ( 12.08142877465145659, -2.567860614650635753, 13.76250926564159016 ) ) ;
#60182=DIRECTION ( 'NONE',  ( -1.000000000000000000, 0.000000000000000000, 0.000000000000000000 ) ) ;
#60183=CARTESIAN_POINT ( 'NONE',  ( 17.86190681601106078, 1.955416883085901558, -12.56193573862143786 ) ) ;
#60189=CARTESIAN_POINT ( 'NONE',  ( 17.74278521991431390, -0.7069209314805200428, -13.98214394338238087 ) ) ;
#60190=FACE_OUTER_BOUND ( 'NONE', #65083, .T. ) ;
#60191=CARTESIAN_POINT ( 'NONE',  ( 12.19252377756937911, -2.624242476340350461, 12.42177825689173432 ) ) ;
#60196=CARTESIAN_POINT ( 'NONE',  ( 18.12879638218882761, -2.748081584522202636, 13.61770999214558309 ) ) ;
#60203=CARTESIAN_POINT ( 'NONE',  ( 21.59999953993000332, 12.84999890301999947, 0.000000000000000000 ) ) ;
#60218=CARTESIAN_POINT ( 'NONE',  ( 12.23404092485628247, 2.245077680571258671, 13.72419654341781126 ) ) ;
#60223=CARTESIAN_POINT ( 'NONE',  ( 12.18894359730774113, 0.3856318793704044401, 13.99470184309725873 ) ) ;
#60264=CARTESIAN_POINT ( 'NONE',  ( 12.19576242957160872, 2.360357254155278639, -13.70208745183198928 ) ) ;
#60266=CARTESIAN_POINT ( 'NONE',  ( 5.694051799045005247, 13.02176618969100552, 2.006311319538786719 ) ) ;
#60269=CARTESIAN_POINT ( 'NONE',  ( 12.54917863858677762, -0.6836428945794239542, -13.98330131869062321 ) ) ;
#60277=CARTESIAN_POINT ( 'NONE',  ( 18.17485192111303860, 2.583003800953513007, -13.65552556266986528 ) ) ;
#60289=CARTESIAN_POINT ( 'NONE',  ( 18.12469242183976093, -2.757364536338188898, -13.61544764698360943 ) ) ;
#60296=CARTESIAN_POINT ( 'NONE',  ( 18.24677884388065863, -2.264233918701653803, -12.39489312188808512 ) ) ;
#60302=PLANE ( 'NONE',  #48193 ) ;
#60303=EDGE_CURVE ( 'NONE', #31596, #59588, #41898, .T. ) ;
#60309=CARTESIAN_POINT ( 'NONE',  ( 12.17997927555898308, 2.482106649064417692, -13.67725710540907436 ) ) ;
#60312=CARTESIAN_POINT ( 'NONE',  ( 17.86760510161943571, 0.5416168188285641616, 13.88579828294358798 ) ) ;
#60313=CARTESIAN_POINT ( 'NONE',  ( 17.75497764282780366, 0.5922531180535276496, 13.88301284246674783 ) ) ;
#60317=CARTESIAN_POINT ( 'NONE',  ( 12.42592716720131030, -0.4969868314062168002, 13.88804154507259447 ) ) ;
#60318=CARTESIAN_POINT ( 'NONE',  ( 12.23477845766454308, -0.2559490220536964067, -13.89683205629668628 ) ) ;
#60331=CARTESIAN_POINT ( 'NONE',  ( 17.88568294903051381, 0.5304820368560144717, 12.68508456201358747 ) ) ;
#60333=CARTESIAN_POINT ( 'NONE',  ( 17.63951772023416709, -3.120582521214973148, -12.28507980727128057 ) ) ;
#60344=CARTESIAN_POINT ( 'NONE',  ( 12.09634453438820501, -0.1521017209118943059, -12.59908727444664045 ) ) ;
#60353=CARTESIAN_POINT ( 'NONE',  ( 12.80505043854143388, 1.875000000000000000, 12.57541666120756041 ) ) ;
#60361=CARTESIAN_POINT ( 'NONE',  ( 17.78490373093669774, -0.5812901181791690908, -13.88363587338389493 ) ) ;
#60362=ADVANCED_FACE ( 'NONE', ( #2597 ), #54707, .F. ) ;
#60376=CARTESIAN_POINT ( 'NONE',  ( 12.70851731081069502, -1.792711832340346145, 13.88474979353782501 ) ) ;
#60385=CARTESIAN_POINT ( 'NONE',  ( 17.84275129854003694, -3.054939169952809230, 12.30480372676524681 ) ) ;
#60418=CARTESIAN_POINT ( 'NONE',  ( 18.05368493555551268, 1.987806113122528640, 13.85816345346370504 ) ) ;
#60429=CARTESIAN_POINT ( 'NONE',  ( 17.71791196170131144, -3.103760126671077035, -13.52664063941736217 ) ) ;
#60444=ORIENTED_EDGE ( 'NONE', *, *, #56275, .F. ) ;
#60453=CARTESIAN_POINT ( 'NONE',  ( 12.32471554566191685, 3.019419751198737956, -12.23287256106958054 ) ) ;
#60461=CARTESIAN_POINT ( 'NONE',  ( 12.09642313398532742, -2.633248533341327580, -12.32177498806537130 ) ) ;
#60467=FACE_OUTER_BOUND ( 'NONE', #66906, .T. ) ;
#60468=CARTESIAN_POINT ( 'NONE',  ( 18.12848705786299419, 0.2487950381773061104, -12.69672507751632828 ) ) ;
#60470=CARTESIAN_POINT ( 'NONE',  ( 12.19400419508993139, 2.631361540197885152, -12.42001554614283165 ) ) ;
#60473=ORIENTED_EDGE ( 'NONE', *, *, #38938, .F. ) ;
#60479=CARTESIAN_POINT ( 'NONE',  ( 18.08264632488620194, 2.164896798301381153, 12.52334278189866623 ) ) ;
#60485=CARTESIAN_POINT ( 'NONE',  ( 12.29441019255336975, -2.991168332544440034, 12.23980925793768293 ) ) ;
#60491=CARTESIAN_POINT ( 'NONE',  ( 12.28357442006480937, -0.4998493492226937507, 12.59008424712975227 ) ) ;
#60494=CARTESIAN_POINT ( 'NONE',  ( 12.68485691281874672, 1.770762539963691484, 12.47495103249912596 ) ) ;
#60500=CARTESIAN_POINT ( 'NONE',  ( 17.97807132104770744, -0.4608801940066536984, 12.68876176373188258 ) ) ;
#60508=DIRECTION ( 'NONE',  ( 1.000000000000000000, -4.332706595949694629E-15, 1.401268137124204108E-14 ) ) ;
#60509=CARTESIAN_POINT ( 'NONE',  ( 18.04486049889702670, -2.888348857472848863, 13.58339007193440828 ) ) ;
#60511=CARTESIAN_POINT ( 'NONE',  ( 12.80505043854146940, -1.787816316115923732, 13.88537766212463431 ) ) ;
#60524=CARTESIAN_POINT ( 'NONE',  ( 17.89701680218574609, 1.976751596789643850, -12.55823001632907143 ) ) ;
#60531=LINE ( 'NONE', #55978, #47198 ) ;
#60536=DIRECTION ( 'NONE',  ( 0.000000000000000000, 0.000000000000000000, 1.000000000000000000 ) ) ;
#60540=CARTESIAN_POINT ( 'NONE',  ( 18.09702113181633365, -2.811936484508641865, 13.60234957393456590 ) ) ;
#60543=CYLINDRICAL_SURFACE ( 'NONE', #3371, 0.6250000000000005551 ) ;
#60554=EDGE_CURVE ( 'NONE', #57425, #29163, #64188, .T. ) ;
#60558=DIRECTION ( 'NONE',  ( 1.000000000000000000, 0.000000000000000000, 0.000000000000000000 ) ) ;
#60562=CARTESIAN_POINT ( 'NONE',  ( 12.39818000720378599, 2.025460462753591706, 13.76267819017275507 ) ) ;
#60566=CARTESIAN_POINT ( 'NONE',  ( 12.41655229043184860, -0.4896942981276220519, 13.88839019180477052 ) ) ;
#60569=DIRECTION ( 'NONE',  ( 0.000000000000000000, 0.9586234969520801563, 0.2846769943134941361 ) ) ;
#60606=CARTESIAN_POINT ( 'NONE',  ( 12.18501279888951316, 2.418803504819920125, -13.69036126157237732 ) ) ;
#60610=CARTESIAN_POINT ( 'NONE',  ( 18.20361801367284826, 2.140066979998675123, -13.83614404522070096 ) ) ;
#60612=CARTESIAN_POINT ( 'NONE',  ( 12.61664971283087233, -0.7055305429986125088, -13.98221279804358019 ) ) ;
#60613=EDGE_CURVE ( 'NONE', #55988, #54460, #29650, .T. ) ;
#60621=CARTESIAN_POINT ( 'NONE',  ( 17.85663772380316061, 3.182036958951508954, -13.63358608099387403 ) ) ;
#60628=CARTESIAN_POINT ( 'NONE',  ( 17.94896820972214613, 0.4852478460479964784, -12.68752000237319066 ) ) ;
#60629=DIRECTION ( 'NONE',  ( -1.000000000000000000, 0.000000000000000000, 0.000000000000000000 ) ) ;
#60632=CARTESIAN_POINT ( 'NONE',  ( 18.17228756843369197, -2.598712620565390097, -13.65197972922593017 ) ) ;
#60635=ADVANCED_FACE ( 'NONE', ( #32956 ), #48340, .F. ) ;
#60640=CARTESIAN_POINT ( 'NONE',  ( 18.18564075751668341, -2.124969003714949345, -12.41952547471440660 ) ) ;
#60650=CARTESIAN_POINT ( 'NONE',  ( 12.43942356506265590, 3.006998533878516788, -13.55276137517231838 ) ) ;
#60654=CARTESIAN_POINT ( 'NONE',  ( 17.85480509960783380, -0.6653129401483779404, 13.98418548573915743 ) ) ;
#60655=CARTESIAN_POINT ( 'NONE',  ( 17.81146176625148314, 0.5702785222608648397, 13.88425216382746541 ) ) ;
#60660=CARTESIAN_POINT ( 'NONE',  ( 12.21236231058155042, 0.1994024997942437372, 13.89809293279921754 ) ) ;
#60661=CARTESIAN_POINT ( 'NONE',  ( 12.18001976712855772, -2.492954602552174048, 13.67495394281278642 ) ) ;
#60670=CARTESIAN_POINT ( 'NONE',  ( 12.35913878034446611, -0.5835546240207333257, 13.98799446466930263 ) ) ;
#60674=CARTESIAN_POINT ( 'NONE',  ( 12.76431688229904537, -0.6240105543035401325, 12.67935574133242582 ) ) ;
#60675=CARTESIAN_POINT ( 'NONE',  ( 18.07102077504177728, -2.852831731489053446, -12.36232801722093555 ) ) ;
#60680=CARTESIAN_POINT ( 'NONE',  ( 12.47202999840593129, -1.970716439074158943, 13.77157652140723876 ) ) ;
#60685=ORIENTED_EDGE ( 'NONE', *, *, #60613, .F. ) ;
#60686=CARTESIAN_POINT ( 'NONE',  ( 12.10431270533525350, 0.1860047152749561838, -12.59864695008082869 ) ) ;
#60704=CARTESIAN_POINT ( 'NONE',  ( 18.22962728801297416, 0.2678304234474076506, -13.99744223245316199 ) ) ;
#60713=CARTESIAN_POINT ( 'NONE',  ( 12.76382664775976750, -3.125000000000000444, -13.52078629068866533 ) ) ;
#60717=DIRECTION ( 'NONE',  ( -0.000000000000000000, 0.6884191022827191864, 0.7253131321107147977 ) ) ;
#60718=ORIENTED_EDGE ( 'NONE', *, *, #4039, .T. ) ;
#60727=CARTESIAN_POINT ( 'NONE',  ( 17.76260332629192717, -3.089553855563651918, 12.29447117690774149 ) ) ;
#60732=CARTESIAN_POINT ( 'NONE',  ( 18.14737500098294376, 2.299536442365951228, 13.71390152310211974 ) ) ;
#60757=CARTESIAN_POINT ( 'NONE',  ( 17.57587588171168136, 3.124999410540973521, 13.52078618842886115 ) ) ;
#60760=VERTEX_POINT ( 'NONE', #1483 ) ;
#60776=EDGE_CURVE ( 'NONE', #35849, #21130, #64251, .T. ) ;
#60793=DIRECTION ( 'NONE',  ( 0.000000000000000000, 0.000000000000000000, 1.000000000000000000 ) ) ;
#60795=CARTESIAN_POINT ( 'NONE',  ( 12.41914228198395698, 3.089530644545721128, -12.21535262842080805 ) ) ;
#60801=ORIENTED_EDGE ( 'NONE', *, *, #42317, .T. ) ;
#60806=CARTESIAN_POINT ( 'NONE',  ( 12.53569427112577372, -1.812281311417189178, -12.46898785302652080 ) ) ;
#60812=CARTESIAN_POINT ( 'NONE',  ( 12.70159504149946805, -3.116720374454505116, -13.52307403002092556 ) ) ;
#60813=CARTESIAN_POINT ( 'NONE',  ( 18.17001854112162462, 0.1120021961262575583, -12.69934078656688925 ) ) ;
#60818=CIRCLE ( 'NONE', #64139, 2.000000000000000444 ) ;
#60824=CARTESIAN_POINT ( 'NONE',  ( 18.12635565526706216, 2.245741716918843167, 12.50718761097852472 ) ) ;
#60831=CARTESIAN_POINT ( 'NONE',  ( 12.48995884033426762, -1.960141145868676382, 12.56111957647684463 ) ) ;
#60837=CARTESIAN_POINT ( 'NONE',  ( 12.78111495345091875, -0.7189971323193962149, 12.57946912511938109 ) ) ;
#60843=ORIENTED_EDGE ( 'NONE', *, *, #8050, .T. ) ;
#60851=ORIENTED_EDGE ( 'NONE', *, *, #26608, .T. ) ;
#60853=CARTESIAN_POINT ( 'NONE',  ( 17.86534717991289156, -0.5429181307973055537, -12.68438171064090980 ) ) ;
#60880=CARTESIAN_POINT ( 'NONE',  ( 12.18136627099996439, -2.541785745019590426, 12.44176459540337376 ) ) ;
#60884=CARTESIAN_POINT ( 'NONE',  ( 18.26121249471884411, -2.684743402744603991, 13.74018592865772703 ) ) ;
#60906=CARTESIAN_POINT ( 'NONE',  ( 12.80505043854143388, 1.874999999999999556, 13.78627172894481667 ) ) ;
#60910=CARTESIAN_POINT ( 'NONE',  ( 12.44955560269364803, -0.5141525164327368502, 13.88720023103246248 ) ) ;
#60915=FACE_OUTER_BOUND ( 'NONE', #17910, .T. ) ;
#60923=CARTESIAN_POINT ( 'NONE',  ( 17.55505043854147118, -2.500000000000000000, -25.00000000000000000 ) ) ;
#60929=CARTESIAN_POINT ( 'NONE',  ( 12.57114114720731557, 0.6824382159985146190, 12.58151825845911809 ) ) ;
#60934=LINE ( 'NONE', #33679, #28421 ) ;
#60956=ORIENTED_EDGE ( 'NONE', *, *, #51959, .F. ) ;
#60958=CARTESIAN_POINT ( 'NONE',  ( 12.40062321164033499, 0.4766231184928879094, -13.88900205690511136 ) ) ;
#60966=CARTESIAN_POINT ( 'NONE',  ( 18.09820959019764075, 2.190632709185573734, -13.73422630893085561 ) ) ;
#60974=CARTESIAN_POINT ( 'NONE',  ( 17.72088406261400451, 1.806772466812846867, -13.88292461265716327 ) ) ;
#60975=CARTESIAN_POINT ( 'NONE',  ( 18.09811783085399028, 0.3100350603811417027, -12.69492243000556364 ) ) ;
#60980=CARTESIAN_POINT ( 'NONE',  ( 18.16281717209332314, -2.646070499629755268, -13.64134067086682656 ) ) ;
#60984=ORIENTED_EDGE ( 'NONE', *, *, #18087, .T. ) ;
#60986=CARTESIAN_POINT ( 'NONE',  ( 18.24542859620203572, -2.700577031380342330, -12.30719352326003779 ) ) ;
#60996=CARTESIAN_POINT ( 'NONE',  ( 12.44048633593776643, 3.149516123668032908, -13.64113935299650926 ) ) ;
#60999=CARTESIAN_POINT ( 'NONE',  ( 17.71666486338982338, 0.6040897852209331509, 13.88232707694115398 ) ) ;
#61006=CARTESIAN_POINT ( 'NONE',  ( 12.26246717652413309, -0.3103928945121602334, 13.89533876751213448 ) ) ;
#61010=CARTESIAN_POINT ( 'NONE',  ( 12.26191093051546588, -2.190091418679299906, 13.73433605229447707 ) ) ;
#61018=CONICAL_SURFACE ( 'NONE', #62104, 12.72499970924999957, 0.7853981386146715593 ) ;
#61019=CARTESIAN_POINT ( 'NONE',  ( 12.15760927739264297, 0.3803681712231598011, 13.99548972734121577 ) ) ;
#61021=CARTESIAN_POINT ( 'NONE',  ( 17.81340500845573871, 0.5691963043021754931, 12.68282590392938047 ) ) ;
#61022=CARTESIAN_POINT ( 'NONE',  ( 12.80505043854144276, -0.6250000000000001110, 12.67928921589117586 ) ) ;
#61035=CARTESIAN_POINT ( 'NONE',  ( 12.30048768357419853, 0.5166535389540172218, -12.58940585649086863 ) ) ;
#61036=CARTESIAN_POINT ( 'NONE',  ( 4.699998537092440642, 0.000000000000000000, 0.000000000000000000 ) ) ;
#61043=CARTESIAN_POINT ( 'NONE',  ( 5.500000000000000000, 12.65263727151999795, 3.063503113339999917 ) ) ;
#61054=CARTESIAN_POINT ( 'NONE',  ( 18.18297552798362560, -0.3652063536484516648, -13.99523956222174448 ) ) ;
#61057=FACE_OUTER_BOUND ( 'NONE', #18702, .T. ) ;
#61076=CARTESIAN_POINT ( 'NONE',  ( 12.33448524795695711, -0.4118363585311515807, -13.89180007025484720 ) ) ;
#61077=CARTESIAN_POINT ( 'NONE',  ( 18.02812495262685744, -2.091428156338118960, 12.53745402072848592 ) ) ;
#61100=CARTESIAN_POINT ( 'NONE',  ( 18.25531039711339432, -0.1866745257715827222, 12.59862229962904046 ) ) ;
#61103=CIRCLE ( 'NONE', #32065, 14.00000000000000000 ) ;
#61107=CARTESIAN_POINT ( 'NONE',  ( 18.18357137170425020, 2.882057337525661289, 13.70014066609292058 ) ) ;
#61133=VERTEX_POINT ( 'NONE', #37195 ) ;
#61143=CARTESIAN_POINT ( 'NONE',  ( 12.36741688735892986, 2.053674487412246563, -12.54445365011033786 ) ) ;
#61153=CARTESIAN_POINT ( 'NONE',  ( 12.10480575880364107, -2.667436721895846130, -12.31441907085211973 ) ) ;
#61160=CARTESIAN_POINT ( 'NONE',  ( 12.19342855462631370, -2.370970601743436212, -13.69993124892199354 ) ) ;
#61161=CARTESIAN_POINT ( 'NONE',  ( 18.17602447836047475, 0.07155418421575511501, -12.69973420405193032 ) ) ;
#61170=CARTESIAN_POINT ( 'NONE',  ( 17.96242084756261193, 2.025889508701483877, 12.54946620628462206 ) ) ;
#61178=CARTESIAN_POINT ( 'NONE',  ( 12.64184255386822464, -1.896331190223615515, 12.57194050387411899 ) ) ;
#61185=CARTESIAN_POINT ( 'NONE',  ( 12.72331806630341156, 0.6199686954221025337, 12.67962180225517876 ) ) ;
#61188=CARTESIAN_POINT ( 'NONE',  ( 12.23381074371944877, 2.246196888878373432, 12.50707970526073254 ) ) ;
#61201=CARTESIAN_POINT ( 'NONE',  ( 18.10291658814850990, -0.3009529450547471785, -12.69520353502832677 ) ) ;
#61203=CARTESIAN_POINT ( 'NONE',  ( 17.99250848601378650, -2.946479007108954828, 13.56856542436122659 ) ) ;
#61207=CARTESIAN_POINT ( 'NONE',  ( 12.68593947922895460, -3.238585582162124776, 13.62026383368923454 ) ) ;
#61208=CARTESIAN_POINT ( 'NONE',  ( 4.599999999999999645, 0.000000000000000000, 0.000000000000000000 ) ) ;
#61215=AXIS2_PLACEMENT_3D ( 'NONE', #8848, #41007, #32249 ) ;
#61220=FACE_OUTER_BOUND ( 'NONE', #34698, .T. ) ;
#61228=CARTESIAN_POINT ( 'NONE',  ( 12.21592886434220482, -2.708773148185487756, 12.40049785804586691 ) ) ;
#61231=CARTESIAN_POINT ( 'NONE',  ( 17.71798387292789556, -1.896258650311507310, 13.78312406285442293 ) ) ;
#61237=EDGE_CURVE ( 'NONE', #34497, #65244, #20059, .T. ) ;
#61253=CARTESIAN_POINT ( 'NONE',  ( 12.18091821863271207, 2.461361028094612546, 13.68154568029715890 ) ) ;
#61257=CARTESIAN_POINT ( 'NONE',  ( 12.23478064045376534, 0.2559538865055897561, -12.69653251249011205 ) ) ;
#61258=CARTESIAN_POINT ( 'NONE',  ( 12.72332061973729012, -0.6199690124688027604, 13.88138352397878705 ) ) ;
#61271=CARTESIAN_POINT ( 'NONE',  ( 12.36135608140797615, 3.049327969019413498, 12.22544940668144875 ) ) ;
#61274=CARTESIAN_POINT ( 'NONE',  ( 12.15762345757557661, -0.3746922850240320679, 12.59513687151645200 ) ) ;
#61290=ORIENTED_EDGE ( 'NONE', *, *, #14445, .T. ) ;
#61292=CARTESIAN_POINT ( 'NONE',  ( 4.650000881942629505, 3.375077994860000042E-14, 1.048050535245999973E-13 ) ) ;
#61293=CARTESIAN_POINT ( 'NONE',  ( 18.02779610229248064, 1.934613261143887319, -12.45059556317631788 ) ) ;
#61297=CARTESIAN_POINT ( 'NONE',  ( 12.21068878750229381, 2.693668765628876027, -13.63048043068445381 ) ) ;
#61303=CARTESIAN_POINT ( 'NONE',  ( 12.38211732427673439, -0.5935699150349511566, -13.98741755999924941 ) ) ;
#61310=CARTESIAN_POINT ( 'NONE',  ( 18.18010564875746837, 2.481546250174181623, -13.67737493447379293 ) ) ;
#61324=LINE ( 'NONE', #51512, #42894 ) ;
#61325=CARTESIAN_POINT ( 'NONE',  ( 18.12577783848301038, -2.244501219366055622, 13.72435250368118531 ) ) ;
#61332=CARTESIAN_POINT ( 'NONE',  ( 18.16391642019722141, -2.089583161048361948, -12.42552483951006614 ) ) ;
#61338=ORIENTED_EDGE ( 'NONE', *, *, #62690, .F. ) ;
#61342=CARTESIAN_POINT ( 'NONE',  ( 12.11838997910883720, 2.753273141185786255, -13.72661716423428935 ) ) ;
#61345=CARTESIAN_POINT ( 'NONE',  ( 17.60287317832943543, -0.7290248443971262260, 13.98100598729141097 ) ) ;
#61352=CARTESIAN_POINT ( 'NONE',  ( 12.48799821679275546, -1.955167389913696763, 13.77408040568291803 ) ) ;
#61364=CARTESIAN_POINT ( 'NONE',  ( 12.18504239631809405, 0.08143391461294853528, 12.69966978410897518 ) ) ;
#61365=EDGE_CURVE ( 'NONE', #11513, #31652, #40993, .T. ) ;
#61366=DIRECTION ( 'NONE',  ( 0.000000000000000000, 0.9553735099700839672, 0.2954005017724949389 ) ) ;
#61375=B_SPLINE_SURFACE_WITH_KNOTS ( 'NONE', 1, 3, ( 
 ( #42835, #26770, #11355, #16940, #15912, #11698, #59600, #6454, #58916, #37582, #184, #27804, #22534, #43873, #65179, #5081, #21502, #69060, #21166, #42494, #63803, #37246, #64144, #16259, #32356, #17999, #23237, #50841, #44917, #34082, #44581, #38978, #66221, #23925, #65527, #61332, #18344, #39663, #39318, #60640, #33735, #13101, #34433, #55749, #50156, #59944, #60296, #7849, #29540, #12751, #6802, #29184, #55397, #50493, #45260, #12404, #2938, #2594, #12055, #66565, #55051, #60986, #28139, #23574, #18684, #7154, #40017, #28489, #24267, #33388, #49807, #1917, #13451, #65873, #34772, #54704, #49453, #7493, #28848, #45604, #56081, #2260, #8190, #17298, #38623, #1562, #22884, #44235, #17655, #14129, #19023, #8534, #9905, #3619, #35456, #20395, #67590, #30894, #66908, #56781, #46632, #25297, #25642, #35793 ),
 ( #46972, #62689, #3958, #3285, #13786, #57108, #30548, #24954, #46286, #36131, #24615, #67938, #20054, #41721, #8879, #9206, #29882, #45938, #51189, #51862, #67249, #30214, #14812, #19364, #40349, #51519, #15152, #63022, #62357, #36473, #31244, #9553, #41382, #57445, #52207, #25988, #19714, #57793, #40687, #4308, #35118, #68275, #61670, #52551, #4648, #56430, #62016, #41034, #14475, #16177, #37503, #63721, #11272, #15500, #42753, #47316, #42068, #99, #64056, #5683, #43450, #64746, #53588, #11612, #27024, #68974, #53923, #10589, #4998, #444, #48001, #16519, #52902, #36828, #68621, #54267, #16860, #21087, #21759, #58826, #31928, #10935, #6024, #43096, #48338, #26336, #63376, #32277, #64398, #5341, #26685, #37848, #47659, #59171, #32613, #791, #15834, #27364, #10245, #42414, #31583, #48687, #37164, #53241 ) ),
 .UNSPECIFIED., .F., .F., .F.,
 ( 2, 2 ),
 ( 4, 2, 2, 2, 2, 2, 2, 2, 2, 2, 2, 2, 2, 2, 2, 2, 2, 2, 2, 2, 2, 2, 2, 2, 2, 2, 2, 2, 2, 2, 2, 2, 2, 2, 2, 2, 2, 2, 2, 2, 2, 2, 2, 2, 2, 2, 2, 2, 2, 2, 2, 4 ),
 ( 0.000000000000000000, 1.000000000000000000 ),
 ( 0.000000000000000000, 7.157017711320847928E-05, 0.0001431403542264169586, 0.0002147105313396254378, 0.0002326030756179275644, 0.0002504956198962296639, 0.0002862807084528339171, 0.0003220657970094381703, 0.0003578508855660424235, 0.0003936359741226466225, 0.0004294210626792508757, 0.0004652061512358551289, 0.0005009912397924593279, 0.0005367763283490635268, 0.0005725614169056678342, 0.0006441315940188763406, 0.0006799166825754805396, 0.0007157017711320848470, 0.0007335943154103870007, 0.0007514868596886890460, 0.0007872719482452932450, 0.0008588421253585017514, 0.0008946272139151059503, 0.0009304123024717102577, 0.0009661973910283144567, 0.001001982479584918656, 0.001073552656698127054, 0.001145122833811335668, 0.001216693010924544283, 0.001288263188037752681, 0.001359833365150961079, 0.001395618453707565387, 0.001431403542264169694, 0.001467188630820774001, 0.001502973719377378092, 0.001574543896490586490, 0.001646114073603795105, 0.001681899162160399412, 0.001717684250717003503, 0.001735576794995305656, 0.001753469339273607593, 0.001789254427830211901, 0.001860824604943420515, 0.001896609693500024823, 0.001932394782056628913, 0.001968179870613233004, 0.001986072414891535375, 0.002003964959169837311, 0.002075535136283045493, 0.002147105313396254107, 0.002218675490509462722, 0.002290245667622671337 ),
 .UNSPECIFIED. ) ;
#61379=CARTESIAN_POINT ( 'NONE',  ( 12.45211143562937117, 0.6284163952874691761, -12.58432055988357767 ) ) ;
#61384=ORIENTED_EDGE ( 'NONE', *, *, #26917, .F. ) ;
#61387=CARTESIAN_POINT ( 'NONE',  ( 17.55505043854143565, 2.500000000000000000, -25.00000000000000000 ) ) ;
#61392=ORIENTED_EDGE ( 'NONE', *, *, #47801, .F. ) ;
#61395=CARTESIAN_POINT ( 'NONE',  ( 18.03319344185666040, -0.5490318484135096044, -13.98923259457975732 ) ) ;
#61407=EDGE_CURVE ( 'NONE', #9344, #67932, #38845, .T. ) ;
#61408=CARTESIAN_POINT ( 'NONE',  ( 12.36816014208256043, -2.947033975326387445, -13.56836638442085530 ) ) ;
#61419=CARTESIAN_POINT ( 'NONE',  ( 12.33502240264713379, 0.4124479947379849909, -13.89177559470775236 ) ) ;
#61420=CARTESIAN_POINT ( 'NONE',  ( 18.08840168032791951, -2.173540213500963159, 12.52169971385178471 ) ) ;
#61426=CARTESIAN_POINT ( 'NONE',  ( 18.16413073598318917, 2.358269131826202791, 13.70246680370518710 ) ) ;
#61443=CARTESIAN_POINT ( 'NONE',  ( 17.85445698522930869, -0.6551943188411679664, 12.58295456804123091 ) ) ;
#61446=EDGE_CURVE ( 'NONE', #12771, #21149, #10652, .T. ) ;
#61450=CARTESIAN_POINT ( 'NONE',  ( 18.14726809210091218, 2.096144380837180243, 13.84220294531915485 ) ) ;
#61484=CARTESIAN_POINT ( 'NONE',  ( 12.18012697958976709, 2.522451323245131771, -12.44635604318887445 ) ) ;
#61489=ORIENTED_EDGE ( 'NONE', *, *, #19877, .F. ) ;
#61494=CARTESIAN_POINT ( 'NONE',  ( 12.35979995375152463, -1.912019040637401135, -12.45409236230133843 ) ) ;
#61502=DIRECTION ( 'NONE',  ( -0.000000000000000000, -0.000000000000000000, 1.000000000000000000 ) ) ;
#61504=CARTESIAN_POINT ( 'NONE',  ( 17.77301286688680904, -3.166510366255906650, 12.19562279494696178 ) ) ;
#61514=CARTESIAN_POINT ( 'NONE',  ( 17.72206310054079381, 3.180756431682058682, 12.19191584669666462 ) ) ;
#61520=CARTESIAN_POINT ( 'NONE',  ( 12.41357648242118294, -2.012680472106853191, 12.55187634341709035 ) ) ;
#61525=CARTESIAN_POINT ( 'NONE',  ( 12.24904276456879160, 0.2856309244984035489, 12.69568149856437067 ) ) ;
#61528=CARTESIAN_POINT ( 'NONE',  ( 12.66096866354269856, 1.891485216129971114, 12.57270334283925450 ) ) ;
#61540=CARTESIAN_POINT ( 'NONE',  ( 17.95718847876655033, -0.4784641821339099543, -12.68786700121472855 ) ) ;
#61545=FACE_OUTER_BOUND ( 'NONE', #25698, .T. ) ;
#61553=CARTESIAN_POINT ( 'NONE',  ( 17.83817875645617690, -0.5572864141904814161, 13.88496202738737217 ) ) ;
#61567=CARTESIAN_POINT ( 'NONE',  ( 12.19239630168272726, -2.623612345332759777, 12.42193400450689289 ) ) ;
#61571=CARTESIAN_POINT ( 'NONE',  ( 17.97976423439218507, -3.110159202364634723, 13.65016833014880682 ) ) ;
#61582=CARTESIAN_POINT ( 'NONE',  ( 18.23353331006402911, 0.2537702651956263988, -12.59744904646397679 ) ) ;
#61593=CARTESIAN_POINT ( 'NONE',  ( 12.47114117431408076, 3.166196762519381647, 13.63727363649663538 ) ) ;
#61596=CARTESIAN_POINT ( 'NONE',  ( 12.23478131644321998, -0.2564338550251593074, -12.69653134296677699 ) ) ;
#61597=CARTESIAN_POINT ( 'NONE',  ( 12.78109991897669673, 0.7302151993337113733, 13.98094363222392467 ) ) ;
#61615=CARTESIAN_POINT ( 'NONE',  ( 12.18199593246769119, 2.449686698290863163, 12.46314100316935480 ) ) ;
#61632=CARTESIAN_POINT ( 'NONE',  ( 18.27597346048318627, 2.401680171065123659, -12.36899652916222436 ) ) ;
#61639=CARTESIAN_POINT ( 'NONE',  ( 5.500000000000000000, -12.87590651766999983, 2.791353855799999728 ) ) ;
#61640=CARTESIAN_POINT ( 'NONE',  ( 12.32690743522622334, 0.5490318484135059407, -13.98923259457975732 ) ) ;
#61652=CARTESIAN_POINT ( 'NONE',  ( 18.24190944330472419, 2.752675741764504025, -13.72673684790926529 ) ) ;
#61668=ORIENTED_EDGE ( 'NONE', *, *, #19134, .T. ) ;
#61670=CARTESIAN_POINT ( 'NONE',  ( 18.12635565526709769, -2.245741716918843611, -12.50718761097852116 ) ) ;
#61680=CARTESIAN_POINT ( 'NONE',  ( 12.18685148345900338, 2.135865664097131855, -13.83612956354243906 ) ) ;
#61684=DIRECTION ( 'NONE',  ( 0.000000000000000000, 0.000000000000000000, -1.000000000000000000 ) ) ;
#61690=CARTESIAN_POINT ( 'NONE',  ( 12.18127175124231165, -2.459544125572825646, 13.68195797703611305 ) ) ;
#61699=CARTESIAN_POINT ( 'NONE',  ( 12.61731565720671000, -0.7069209314891412577, 13.98214394338193678 ) ) ;
#61704=CARTESIAN_POINT ( 'NONE',  ( 18.15028814309356520, 0.1908418880314464161, 12.69807545005479810 ) ) ;
#61709=VECTOR ( 'NONE', #21331, 1000.000000000000000 ) ;
#61712=DIRECTION ( 'NONE',  ( 0.000000000000000000, -0.7198977633594747516, 0.6940801180771756229 ) ) ;
#61714=CARTESIAN_POINT ( 'NONE',  ( 12.63954751664500797, 0.7006927685645021331, -12.58050281163331796 ) ) ;
#61728=ORIENTED_EDGE ( 'NONE', *, *, #65217, .T. ) ;
#61731=CARTESIAN_POINT ( 'NONE',  ( 18.05115593671926888, 0.5330308249010425881, -13.98985951701901520 ) ) ;
#61738=CARTESIAN_POINT ( 'NONE',  ( 18.10321044368077281, -2.800384070978154671, 12.37651499848969650 ) ) ;
#61754=CARTESIAN_POINT ( 'NONE',  ( 12.18532581790793401, 0.08167545936615711044, -13.89968205666727386 ) ) ;
#61755=CARTESIAN_POINT ( 'NONE',  ( 18.17899100331062101, -2.462234907104897896, 12.46031481527572282 ) ) ;
#61781=CARTESIAN_POINT ( 'NONE',  ( 17.99623368854100036, -0.5708113556792879795, 12.58706429964239071 ) ) ;
#61790=CARTESIAN_POINT ( 'NONE',  ( 18.23517937092938368, 2.264898893658550794, 13.81558401759068744 ) ) ;
#61823=CARTESIAN_POINT ( 'NONE',  ( 12.21195445704740656, 2.302603597045699946, -12.49539791649142906 ) ) ;
#61831=CARTESIAN_POINT ( 'NONE',  ( 12.08482599452297812, -2.564444806221819473, -12.33627826672298866 ) ) ;
#61838=CARTESIAN_POINT ( 'NONE',  ( 12.43878596651945401, -1.993461161472737775, -13.76788477248720355 ) ) ;
#61843=CARTESIAN_POINT ( 'NONE',  ( 17.74426251268377186, -3.174930969421385196, 12.19343357469032085 ) ) ;
#61848=CARTESIAN_POINT ( 'NONE',  ( 18.16782992319337708, 2.622990445277169513, 13.64655204326457927 ) ) ;
#61851=CARTESIAN_POINT ( 'NONE',  ( 18.06549347002469474, 2.139198186095363052, 12.52833527917195866 ) ) ;
#61855=ORIENTED_EDGE ( 'NONE', *, *, #59036, .F. ) ;
#61856=CARTESIAN_POINT ( 'NONE',  ( 12.66183496498647365, -1.891282299343450601, 12.57277654391869248 ) ) ;
#61862=CARTESIAN_POINT ( 'NONE',  ( 12.18829625149018803, -0.1017072266180455709, 12.69945743039634856 ) ) ;
#61866=CARTESIAN_POINT ( 'NONE',  ( 12.69127452969527603, 1.885356761727419173, 12.57371515106196114 ) ) ;
#61873=EDGE_CURVE ( 'NONE', #45267, #6955, #49150, .T. ) ;
#61887=CARTESIAN_POINT ( 'NONE',  ( 12.58176516051273630, -3.212719125873755299, 13.62638797003613966 ) ) ;
#61889=DIRECTION ( 'NONE',  ( 1.000000000000000000, 0.000000000000000000, -0.000000000000000000 ) ) ;
#61902=LINE ( 'NONE', #8423, #48682 ) ;
#61909=CARTESIAN_POINT ( 'NONE',  ( 12.18517285595739175, -2.419552247691227453, 12.46997200859748389 ) ) ;
#61913=CARTESIAN_POINT ( 'NONE',  ( 17.57587346436487152, -1.875000586273749992, 13.78631940097168673 ) ) ;
#61915=ORIENTED_EDGE ( 'NONE', *, *, #68001, .T. ) ;
#61925=CARTESIAN_POINT ( 'NONE',  ( 18.24182894713847602, -0.2307628456012796592, -12.59789151516662997 ) ) ;
#61929=CARTESIAN_POINT ( 'NONE',  ( 12.80505043854146940, -1.875000000000000444, 12.57545641911172396 ) ) ;
#61938=CARTESIAN_POINT ( 'NONE',  ( 12.15443728026460946, 2.840296387118482091, 13.70885984368922017 ) ) ;
#61941=CARTESIAN_POINT ( 'NONE',  ( 12.29893172089695952, -0.3669524142237010622, -12.69287054297889483 ) ) ;
#61947=DIRECTION ( 'NONE',  ( 0.000000000000000000, -0.7506664619968553831, 0.6606813625592322659 ) ) ;
#61974=CARTESIAN_POINT ( 'NONE',  ( 12.54566616138316526, 3.068981097031269201, 13.53612220331575600 ) ) ;
#61982=CARTESIAN_POINT ( 'NONE',  ( 17.59659125555221948, 3.123958135111998491, -12.28406395290800468 ) ) ;
#61985=CARTESIAN_POINT ( 'NONE',  ( 12.18008982747168112, 2.511713771612850810, -13.67097129483465068 ) ) ;
#61993=CARTESIAN_POINT ( 'NONE',  ( 18.16429560769915952, 2.358968865796700065, 12.48332026670510864 ) ) ;
#61996=ORIENTED_EDGE ( 'NONE', *, *, #54008, .F. ) ;
#61998=CARTESIAN_POINT ( 'NONE',  ( 18.18368263331577594, 2.882378207881307386, -13.70008584495759152 ) ) ;
#61999=ORIENTED_EDGE ( 'NONE', *, *, #65166, .F. ) ;
#62008=ORIENTED_EDGE ( 'NONE', *, *, #48044, .F. ) ;
#62016=CARTESIAN_POINT ( 'NONE',  ( 18.15128053492060900, -2.312280642761794791, -12.49331763295500863 ) ) ;
#62019=CARTESIAN_POINT ( 'NONE',  ( 17.55505043854144276, 0.6250000000000001110, 13.88107975066923316 ) ) ;
#62025=CARTESIAN_POINT ( 'NONE',  ( 12.09788000779844630, 2.355563551342471751, -13.80043034480240216 ) ) ;
#62027=CARTESIAN_POINT ( 'NONE',  ( 17.71954595323150627, 0.7115697451011995245, 13.98190580764195978 ) ) ;
#62060=CARTESIAN_POINT ( 'NONE',  ( 12.37769715316224506, -0.4561785182478235723, -12.68897339690747295 ) ) ;
#62061=CARTESIAN_POINT ( 'NONE',  ( 12.19116924868947471, -2.617374923999068681, -12.42344294665103988 ) ) ;
#62073=EDGE_LOOP ( 'NONE', ( #40298, #9568, #66869, #1860, #16989, #47377 ) ) ;
#62076=CARTESIAN_POINT ( 'NONE',  ( 18.00570828977290461, -0.5721320424853957309, -13.98830666644471599 ) ) ;
#62079=DIRECTION ( 'NONE',  ( -1.000000000000000000, 0.000000000000000000, 0.000000000000000000 ) ) ;
#62090=CARTESIAN_POINT ( 'NONE',  ( 17.95719809541170520, 0.4784561393452470557, -13.88891570267007403 ) ) ;
#62092=DIRECTION ( 'NONE',  ( 1.000000000000000000, 0.000000000000000000, 0.000000000000000000 ) ) ;
#62097=CARTESIAN_POINT ( 'NONE',  ( 12.42411034028606309, -0.4959091552601235242, -13.88809952003718173 ) ) ;
#62098=CARTESIAN_POINT ( 'NONE',  ( 18.15862102414880042, -2.662578152609975213, 12.41223253473083155 ) ) ;
#62104=AXIS2_PLACEMENT_3D ( 'NONE', #35749, #2894, #24220 ) ;
#62110=CARTESIAN_POINT ( 'NONE',  ( 18.18005043824376443, -1.329523415562850021E-10, -12.70000000088146486 ) ) ;
#62111=VERTEX_POINT ( 'NONE', #61043 ) ;
#62123=CARTESIAN_POINT ( 'NONE',  ( 18.26152580467099540, 0.1632583333441799678, 12.59896334813831764 ) ) ;
#62129=CARTESIAN_POINT ( 'NONE',  ( 17.81237950545464699, 3.200707792931475559, 13.62921448194399154 ) ) ;
#62132=ORIENTED_EDGE ( 'NONE', *, *, #8835, .T. ) ;
#62142=CARTESIAN_POINT ( 'NONE',  ( 17.74396022931449934, -3.223333129201646052, -13.62388254889262029 ) ) ;
#62163=CARTESIAN_POINT ( 'NONE',  ( 12.44669855353769350, 1.987833209345827967, -12.55628527126821226 ) ) ;
#62166=EDGE_LOOP ( 'NONE', ( #49232, #15908, #40704 ) ) ;
#62171=CARTESIAN_POINT ( 'NONE',  ( 12.55429323164601207, -3.072583267488711023, -12.29953727834259958 ) ) ;
#62178=CARTESIAN_POINT ( 'NONE',  ( 12.30715842069481702, -2.122066859011513262, -13.74633992746440292 ) ) ;
#62185=B_SPLINE_CURVE_WITH_KNOTS ( 'NONE', 3,
 ( #21729, #16149, #32924, #37136, #64368, #68943, #63692, #43063, #16491, #27334, #65058, #17179, #5994, #42386, #15807, #48658 ),
 .UNSPECIFIED., .F., .F.,
 ( 4, 2, 2, 2, 2, 2, 2, 4 ),
 ( 0.000000000000000000, 0.06249999999999930611, 0.1249999999999986122, 0.2499999999999994449, 0.4999999999999997780, 0.7500000000000001110, 0.8750000000000000000, 1.000000000000000000 ),
 .UNSPECIFIED. ) ;
#62190=CARTESIAN_POINT ( 'NONE',  ( 18.07078568656085338, 2.853178104762410072, 13.59212922196301143 ) ) ;
#62199=CARTESIAN_POINT ( 'NONE',  ( 12.52605318029424275, -1.940633248599432203, 12.56447441435821943 ) ) ;
#62206=CARTESIAN_POINT ( 'NONE',  ( 12.18127380957210271, -0.04040257046694565451, 12.69991905489010442 ) ) ;
#62210=VECTOR ( 'NONE', #41357, 1000.000000000000000 ) ;
#62211=CARTESIAN_POINT ( 'NONE',  ( 12.24247500090512553, 2.227530134987963706, 12.51087939115179104 ) ) ;
#62222=CARTESIAN_POINT ( 'NONE',  ( 18.06139130775558854, -0.3666439886896704636, -12.69288249682903569 ) ) ;
#62229=CARTESIAN_POINT ( 'NONE',  ( 12.57032717430624480, -3.208883835765893533, 13.62729181966624026 ) ) ;
#62254=CARTESIAN_POINT ( 'NONE',  ( 18.18368263331580437, -2.882378207881296284, 13.70008584495759152 ) ) ;
#62256=VERTEX_POINT ( 'NONE', #16883 ) ;
#62266=CARTESIAN_POINT ( 'NONE',  ( 18.26112048795755172, 0.1637242582067865437, -12.59894148523290802 ) ) ;
#62270=EDGE_CURVE ( 'NONE', #23992, #4182, #28365, .T. ) ;
#62278=CARTESIAN_POINT ( 'NONE',  ( 17.74439936569994813, 1.785463535057948636, 12.47285731025143463 ) ) ;
#62280=CARTESIAN_POINT ( 'NONE',  ( 12.30654613137381759, 1.987682873648402015, 13.85818111229403016 ) ) ;
#62283=CARTESIAN_POINT ( 'NONE',  ( 12.33180295249681713, 0.4082649242943290346, -12.69116688078651833 ) ) ;
#62285=CARTESIAN_POINT ( 'NONE',  ( 12.30932141792787959, -0.5329747956504982120, 13.98985355243729245 ) ) ;
#62286=ORIENTED_EDGE ( 'NONE', *, *, #47801, .T. ) ;
#62295=DIRECTION ( 'NONE',  ( 0.000000000000000000, 1.000000000000000000, 0.000000000000000000 ) ) ;
#62314=EDGE_CURVE ( 'NONE', #24123, #59800, #41955, .T. ) ;
#62315=CARTESIAN_POINT ( 'NONE',  ( 12.76382664777360354, 3.124999999999999112, 13.52078629068864757 ) ) ;
#62323=CARTESIAN_POINT ( 'NONE',  ( 17.57923549477748537, 1.761145725279485541, -12.47631219955854043 ) ) ;
#62326=CARTESIAN_POINT ( 'NONE',  ( 12.20440283767314327, 2.672818874493718244, -13.63528575822274469 ) ) ;
#62330=CARTESIAN_POINT ( 'NONE',  ( 12.08616987952486532, 0.09542514088230683034, -13.99967976774382272 ) ) ;
#62338=CARTESIAN_POINT ( 'NONE',  ( 18.16658511877954751, 2.125673232124648759, -13.83768827471936724 ) ) ;
#62339=EDGE_LOOP ( 'NONE', ( #14977, #1936, #36423, #57878 ) ) ;
#62343=CARTESIAN_POINT ( 'NONE',  ( 12.80505043854144276, -0.7192913403693027563, 12.57945229203838267 ) ) ;
#62357=CARTESIAN_POINT ( 'NONE',  ( 17.99268395210761540, -2.053674450599853873, -12.54441556206896990 ) ) ;
#62368=CARTESIAN_POINT ( 'NONE',  ( 12.63927634677108713, 3.229167277941579872, -13.62249984660984303 ) ) ;
#62370=CARTESIAN_POINT ( 'NONE',  ( 17.81056431323685629, 0.6834693007276584353, 13.98330741474946315 ) ) ;
#62383=CARTESIAN_POINT ( 'NONE',  ( 12.80505043854143388, 3.124999999999999556, 12.28373071562070074 ) ) ;
#62390=CARTESIAN_POINT ( 'NONE',  ( 18.17998003037035204, -2.509683781248572387, -12.44929946634871953 ) ) ;
#62400=CARTESIAN_POINT ( 'NONE',  ( 12.78111495345091697, 0.7189971323193988795, -12.57946912511938109 ) ) ;
#62401=CARTESIAN_POINT ( 'NONE',  ( 12.19222608800083663, -2.622765415629520813, -12.42211422045274105 ) ) ;
#62408=CARTESIAN_POINT ( 'NONE',  ( 17.69809845384140701, 0.6087666915464966522, 12.68035271361765126 ) ) ;
#62410=CARTESIAN_POINT ( 'NONE',  ( 17.55505043854143565, 3.199698446519375850, 12.18695736643652694 ) ) ;
#62428=CARTESIAN_POINT ( 'NONE',  ( 12.19551626500196839, -2.360211740052808427, -13.70208339272018350 ) ) ;
#62436=CARTESIAN_POINT ( 'NONE',  ( 17.55505043854143565, 2.500000000000000000, -25.00000000000000000 ) ) ;
#62438=CARTESIAN_POINT ( 'NONE',  ( 12.37030616679614070, 0.4491394412341185860, -13.89023495843588840 ) ) ;
#62439=CARTESIAN_POINT ( 'NONE',  ( 17.88838831427751686, -1.971212373206994384, 12.55919681887186456 ) ) ;
#62440=ORIENTED_EDGE ( 'NONE', *, *, #13666, .T. ) ;
#62461=CARTESIAN_POINT ( 'NONE',  ( -17.56123417799999942, 13.94845324556000143, 4.312847325879000770 ) ) ;
#62463=CARTESIAN_POINT ( 'NONE',  ( 17.72055336043788287, 0.7006927685644959158, 12.58050281163332151 ) ) ;
#62469=CARTESIAN_POINT ( 'NONE',  ( 17.67416556365684244, 3.238622530711260605, 13.62025504818856625 ) ) ;
#62471=ORIENTED_EDGE ( 'NONE', *, *, #51689, .F. ) ;
#62479=CARTESIAN_POINT ( 'NONE',  ( 18.27937482164658789, -2.670364552392027857, 12.31525491564956809 ) ) ;
#62494=VERTEX_POINT ( 'NONE', #67531 ) ;
#62499=CARTESIAN_POINT ( 'NONE',  ( 12.48995884033423032, 1.960141145868676382, -12.56111957647685351 ) ) ;
#62505=CIRCLE ( 'NONE', #7822, 13.17499999999999893 ) ;
#62506=DIRECTION ( 'NONE',  ( -1.000000000000000000, 0.000000000000000000, 0.000000000000000000 ) ) ;
#62512=CARTESIAN_POINT ( 'NONE',  ( 12.63789105315733075, -1.779885672808168895, -12.47365341745800649 ) ) ;
#62518=CARTESIAN_POINT ( 'NONE',  ( 12.37528356179629441, -2.046093867836326297, -13.75926687192407094 ) ) ;
#62522=VERTEX_POINT ( 'NONE', #38798 ) ;
#62524=CARTESIAN_POINT ( 'NONE',  ( 12.43971800581059739, -0.6379138416578148396, -13.98550699733554303 ) ) ;
#62527=CARTESIAN_POINT ( 'NONE',  ( 17.92070696553032505, 3.007249353054399332, 13.55264287719425376 ) ) ;
#62531=CARTESIAN_POINT ( 'NONE',  ( 17.89623257347365382, 3.023758741516315407, 12.31397229722846731 ) ) ;
#62543=CARTESIAN_POINT ( 'NONE',  ( 12.70318068537855893, 0.6169782284476045264, 12.67981870385669652 ) ) ;
#62545=CARTESIAN_POINT ( 'NONE',  ( 5.656849040861676059, -12.07883750123030708, -3.735095616319062284 ) ) ;
#62547=PLANE ( 'NONE',  #53416 ) ;
#62552=CARTESIAN_POINT ( 'NONE',  ( 17.55505043854147118, -3.125000000000000000, 12.28374638332999780 ) ) ;
#62566=CARTESIAN_POINT ( 'NONE',  ( 18.01266241223994768, -2.926178784092879681, -13.57373383468747186 ) ) ;
#62587=CARTESIAN_POINT ( 'NONE',  ( 18.00853468083869302, -1.948185427393968716, 13.86378859567400568 ) ) ;
#62599=CARTESIAN_POINT ( 'NONE',  ( 18.28005836700934239, -0.01123479547583286324, -12.60000044989513590 ) ) ;
#62604=AXIS2_PLACEMENT_3D ( 'NONE', #19756, #40387, #61712 ) ;
#62612=CARTESIAN_POINT ( 'NONE',  ( 12.11707904423852966, 2.286486548259629714, 13.81204227851268840 ) ) ;
#62615=CARTESIAN_POINT ( 'NONE',  ( 12.42340696030921521, 0.4949990735619317905, -12.68701406540670540 ) ) ;
#62616=CARTESIAN_POINT ( 'NONE',  ( 12.30074708396108996, -0.5247499651446895230, 13.99016470477802265 ) ) ;
#62618=CARTESIAN_POINT ( 'NONE',  ( 12.53584957871194128, -1.812149883874480505, 12.46900695079345489 ) ) ;
#62623=FACE_OUTER_BOUND ( 'NONE', #30447, .T. ) ;
#62625=CARTESIAN_POINT ( 'NONE',  ( 12.21223476585295487, 2.065380716993680199, 12.42958554107382163 ) ) ;
#62633=CARTESIAN_POINT ( 'NONE',  ( 12.80505043854143388, 1.875000000000000000, 12.57541666120756041 ) ) ;
#62644=AXIS2_PLACEMENT_3D ( 'NONE', #43449, #12319, #60558 ) ;
#62645=DIRECTION ( 'NONE',  ( 1.000000000000000000, 0.000000000000000000, 0.000000000000000000 ) ) ;
#62646=CARTESIAN_POINT ( 'NONE',  ( 12.29043182814385560, -2.854820394136933004, 13.59177665069740470 ) ) ;
#62647=CARTESIAN_POINT ( 'NONE',  ( 12.18947262544869048, 2.391368178646923415, 13.69585133611195005 ) ) ;
#62657=CARTESIAN_POINT ( 'NONE',  ( 17.81328364446394019, 1.807903055951886273, -12.46962321666120665 ) ) ;
#62660=CARTESIAN_POINT ( 'NONE',  ( 12.32889761174196863, 2.904977411718398184, -13.57918629439654978 ) ) ;
#62664=CARTESIAN_POINT ( 'NONE',  ( 12.33591485593542281, 0.5568603909045817257, -13.98892293345220139 ) ) ;
#62667=CARTESIAN_POINT ( 'NONE',  ( 18.15926133226627925, 2.338854968114922883, 12.48766092794227589 ) ) ;
#62673=CARTESIAN_POINT ( 'NONE',  ( 18.19085350567997139, 2.166991405623370337, -13.83127841112310996 ) ) ;
#62681=CARTESIAN_POINT ( 'NONE',  ( 12.80505043854143388, 1.875000000000000000, 12.57541666120756041 ) ) ;
#62682=ORIENTED_EDGE ( 'NONE', *, *, #39147, .T. ) ;
#62689=CARTESIAN_POINT ( 'NONE',  ( 17.57591033989428908, -1.875000590519982246, -12.57541652832150447 ) ) ;
#62690=EDGE_CURVE ( 'NONE', #58563, #16266, #29018, .T. ) ;
#62701=CARTESIAN_POINT ( 'NONE',  ( 17.57900089668073917, 0.7302151644511168938, 13.98094363559787823 ) ) ;
#62709=CARTESIAN_POINT ( 'NONE',  ( 12.64149076266971328, -3.109019952252448871, 13.52530492583600541 ) ) ;
#62715=CARTESIAN_POINT ( 'NONE',  ( 21.59999946634000167, -13.89999946622000060, -2.316958215196000280E-09 ) ) ;
#62721=CARTESIAN_POINT ( 'NONE',  ( 18.18005043873318982, -2.501166356684528580, -12.45128845098599335 ) ) ;
#62722=DIRECTION ( 'NONE',  ( 1.000000000000000000, 0.000000000000000000, 0.000000000000000000 ) ) ;
#62734=CARTESIAN_POINT ( 'NONE',  ( 12.40062372901866894, -0.4766234715920634746, -12.68796191786314154 ) ) ;
#62735=CARTESIAN_POINT ( 'NONE',  ( 12.18124154974851336, -2.460017072494863122, -12.46078795777972736 ) ) ;
#62760=CARTESIAN_POINT ( 'NONE',  ( 18.12484680923011382, -2.757022365768678096, 12.38798834872858556 ) ) ;
#62761=ORIENTED_EDGE ( 'NONE', *, *, #11992, .T. ) ;
#62763=CARTESIAN_POINT ( 'NONE',  ( 12.21587634999234595, -2.708625115319929666, -13.62694294269819117 ) ) ;
#62769=CARTESIAN_POINT ( 'NONE',  ( 17.55505043854144276, 0.6250000000000001110, -13.88107975066922428 ) ) ;
#62770=CARTESIAN_POINT ( 'NONE',  ( 17.59627748481874221, -0.6237239846186468650, -12.67937377942301502 ) ) ;
#62775=CARTESIAN_POINT ( 'NONE',  ( 12.33367687689867687, 2.910531109056639032, 13.57771726184491357 ) ) ;
#62783=CARTESIAN_POINT ( 'NONE',  ( 12.54469325725303541, 1.931433442391065070, -13.77773667378076361 ) ) ;
#62787=LINE ( 'NONE', #14228, #32804 ) ;
#62789=VERTEX_POINT ( 'NONE', #52024 ) ;
#62793=LINE ( 'NONE', #25400, #7546 ) ;
#62798=DIRECTION ( 'NONE',  ( 0.000000000000000000, -0.9553735099700839672, -0.2954005017724949389 ) ) ;
#62802=CARTESIAN_POINT ( 'NONE',  ( 17.90798944145350902, 0.6284163952874703973, 12.58432055988358123 ) ) ;
#62809=ADVANCED_FACE ( 'NONE', ( #42577 ), #53069, .T. ) ;
#62810=CARTESIAN_POINT ( 'NONE',  ( 17.77834352330034307, 3.212755074437993130, 13.62637949436378015 ) ) ;
#62822=VERTEX_POINT ( 'NONE', #26501 ) ;
#62849=CARTESIAN_POINT ( 'NONE',  ( 12.78086743291011551, -1.761210985583074207, -12.47630298729255216 ) ) ;
#62855=CARTESIAN_POINT ( 'NONE',  ( 12.40968101568429383, -3.130119464836099485, -13.64559997174500872 ) ) ;
#62861=CARTESIAN_POINT ( 'NONE',  ( 12.61475641025121774, -0.7110419930699988234, -13.98197980709423760 ) ) ;
#62867=CARTESIAN_POINT ( 'NONE',  ( 17.69900574642232272, 3.108543425041114805, 12.28872856983837458 ) ) ;
#62873=CARTESIAN_POINT ( 'NONE',  ( 12.42229329081243705, -2.994506204212080469, 12.32251488760203628 ) ) ;
#62881=CARTESIAN_POINT ( 'NONE',  ( 12.54669586862715214, -0.5691963043021777136, 12.68282590392938047 ) ) ;
#62903=CARTESIAN_POINT ( 'NONE',  ( 17.99238080566778564, -2.053374525523686156, -13.75805324639250493 ) ) ;
#62907=ORIENTED_EDGE ( 'NONE', *, *, #4656, .T. ) ;
#62912=CARTESIAN_POINT ( 'NONE',  ( 18.07980642413443917, -0.3396162601792407920, 13.89441893193904676 ) ) ;
#62924=DIRECTION ( 'NONE',  ( 1.000000000000000000, 0.000000000000000000, 0.000000000000000000 ) ) ;
#62926=CARTESIAN_POINT ( 'NONE',  ( 17.77845184731634021, -1.823244735605234812, 13.88077056497939843 ) ) ;
#62927=CARTESIAN_POINT ( 'NONE',  ( 17.96066850193498965, 2.975608638399078743, -13.56100830560624360 ) ) ;
#62929=DIRECTION ( 'NONE',  ( 1.000000000000000000, 0.000000000000000000, 1.649474208015000260E-14 ) ) ;
#62937=CARTESIAN_POINT ( 'NONE',  ( 18.25578817174764978, -0.1860047152749900456, -12.59864695008083046 ) ) ;
#62940=CARTESIAN_POINT ( 'NONE',  ( 12.80505043854146940, -1.836948468694464820, 12.54242247073720051 ) ) ;
#62947=CARTESIAN_POINT ( 'NONE',  ( 12.22832816813797585, 2.961039467707558437, 13.68329631872641095 ) ) ;
#62950=CARTESIAN_POINT ( 'NONE',  ( 12.44244977473554492, -0.5091670849982490310, -12.68626057781829175 ) ) ;
#62951=AXIS2_PLACEMENT_3D ( 'NONE', #57075, #3583, #13412 ) ;
#62952=CARTESIAN_POINT ( 'NONE',  ( 12.17712534909926880, -0.3652063536484373985, 13.99523956222174270 ) ) ;
#62954=CARTESIAN_POINT ( 'NONE',  ( 12.75685216135446964, -1.762044409276920076, 12.47618552084819399 ) ) ;
#62959=CARTESIAN_POINT ( 'NONE',  ( 12.75734966356159994, 0.7181168112306464124, 12.57951960855070261 ) ) ;
#62962=CARTESIAN_POINT ( 'NONE',  ( 12.41832178632828310, 1.871654022356042502, 12.46021467525213744 ) ) ;
#62975=CARTESIAN_POINT ( 'NONE',  ( 12.38195926916771583, -0.4608195502960515388, 12.68876479730130313 ) ) ;
#62979=CARTESIAN_POINT ( 'NONE',  ( 21.59999987243000064, -1.749711486808999826E-13, -3.819167204710999825E-14 ) ) ;
#62980=CARTESIAN_POINT ( 'NONE',  ( 12.39110436774228141, -2.968713941934962630, 13.56281002627122945 ) ) ;
#62981=CARTESIAN_POINT ( 'NONE',  ( 12.28991563249832808, 2.854049639532288296, 13.59191281879116708 ) ) ;
#62989=CARTESIAN_POINT ( 'NONE',  ( 17.76260332629189165, 3.089553855563651918, -12.29447117690774505 ) ) ;
#62992=CARTESIAN_POINT ( 'NONE',  ( 18.17985377383957157, 2.516953534566725104, 12.44759707711947883 ) ) ;
#62997=CARTESIAN_POINT ( 'NONE',  ( 12.39267642948476222, 0.6007076874295218527, -13.98710814480368114 ) ) ;
#62999=FACE_OUTER_BOUND ( 'NONE', #47135, .T. ) ;
#63006=CARTESIAN_POINT ( 'NONE',  ( 18.25313429507006546, 2.320711718358090536, -13.80631856085854992 ) ) ;
#63012=CARTESIAN_POINT ( 'NONE',  ( 17.55505043854147118, -1.875000000000000000, -25.00000000000000000 ) ) ;
#63018=AXIS2_PLACEMENT_3D ( 'NONE', #34996, #56310, #2141 ) ;
#63022=CARTESIAN_POINT ( 'NONE',  ( 17.98531014845341858, -2.046560857067137640, -12.54571659797611360 ) ) ;
#63035=CARTESIAN_POINT ( 'NONE',  ( 17.97713831050996447, 0.5938246120522454596, 13.98740230410797558 ) ) ;
#63047=AXIS2_PLACEMENT_3D ( 'NONE', #25799, #10060, #25110 ) ;
#63055=CARTESIAN_POINT ( 'NONE',  ( 21.59999946634000167, 13.89999946622000060, 2.316962009661000178E-09 ) ) ;
#63064=ADVANCED_FACE ( 'NONE', ( #968 ), #48859, .F. ) ;
#63069=EDGE_LOOP ( 'NONE', ( #39199, #13702, #64381, #24371 ) ) ;
#63070=CARTESIAN_POINT ( 'NONE',  ( 12.58454787187813650, 0.5848996845204771367, -12.68186405703079167 ) ) ;
#63071=CARTESIAN_POINT ( 'NONE',  ( 12.19364288166475063, -2.630035214363327434, -12.42031982033429038 ) ) ;
#63086=ORIENTED_EDGE ( 'NONE', *, *, #42614, .T. ) ;
#63090=CARTESIAN_POINT ( 'NONE',  ( 17.57900089668074273, -0.7302151644511190032, -13.98094363559787290 ) ) ;
#63096=CARTESIAN_POINT ( 'NONE',  ( 17.94531445438002848, -2.988940031718063217, 12.32413547815666277 ) ) ;
#63099=CARTESIAN_POINT ( 'NONE',  ( 12.21323965719961180, -2.701097326009253230, -13.62869820424139178 ) ) ;
#63108=CARTESIAN_POINT ( 'NONE',  ( 12.80505043854146940, -2.500000000000000444, -25.00000000000000000 ) ) ;
#63112=CARTESIAN_POINT ( 'NONE',  ( 12.39904396558114463, 2.975276281382167376, 13.56103672317924769 ) ) ;
#63129=CARTESIAN_POINT ( 'NONE',  ( 12.46489557882766341, 0.5244061151666827847, 13.88668399599068870 ) ) ;
#63142=CARTESIAN_POINT ( 'NONE',  ( 18.03335409833309555, 0.5406785836137698587, 12.58839662496522749 ) ) ;
#63148=CARTESIAN_POINT ( 'NONE',  ( 17.74396022931447092, 3.223333129201660707, 13.62388254889261496 ) ) ;
#63156=CARTESIAN_POINT ( 'NONE',  ( 17.65323508305261768, -1.760912828005723130, 12.47634505842160735 ) ) ;
#63168=CARTESIAN_POINT ( 'NONE',  ( 5.700000000000000178, 12.50865771883999855, -2.924687089724999911 ) ) ;
#63174=CARTESIAN_POINT ( 'NONE',  ( 18.12876426765905791, 0.2481576080865483258, -13.89702325994032783 ) ) ;
#63182=VERTEX_POINT ( 'NONE', #24354 ) ;
#63188=CARTESIAN_POINT ( 'NONE',  ( 12.20147980349672601, -2.662577969174665604, -12.41220455913370380 ) ) ;
#63189=VECTOR ( 'NONE', #47058, 1000.000000000000114 ) ;
#63193=CARTESIAN_POINT ( 'NONE',  ( 12.21194158638448002, -2.301857635319168427, -13.71345735897203610 ) ) ;
#63197=CARTESIAN_POINT ( 'NONE',  ( 18.27387565520749391, -2.575953525795620092, 12.33388021351436947 ) ) ;
#63206=CARTESIAN_POINT ( 'NONE',  ( 17.77739983953768643, 3.084473828682777974, 12.29598274197195806 ) ) ;
#63208=CARTESIAN_POINT ( 'NONE',  ( 18.27948916824812287, -2.669673601445818889, -12.31540264490818615 ) ) ;
#63209=VERTEX_POINT ( 'NONE', #23661 ) ;
#63212=CARTESIAN_POINT ( 'NONE',  ( 12.58270105247236970, -3.084473834238325107, 12.29599965897949865 ) ) ;
#63246=CARTESIAN_POINT ( 'NONE',  ( 18.15591411656202325, -2.672312740310635260, -13.63535347231577077 ) ) ;
#63250=ORIENTED_EDGE ( 'NONE', *, *, #30844, .T. ) ;
#63256=CARTESIAN_POINT ( 'NONE',  ( 18.01649462512370903, -0.4224288469488072795, 13.89137824130979126 ) ) ;
#63266=CARTESIAN_POINT ( 'NONE',  ( 12.56405804856026442, 1.801709437036786099, -12.47051912880706404 ) ) ;
#63271=CARTESIAN_POINT ( 'NONE',  ( 18.26447107791332058, -2.367226376531796461, 13.79841952404521166 ) ) ;
#63282=CARTESIAN_POINT ( 'NONE',  ( 17.94855945389787877, -0.6042324041877072949, -12.58550538354983672 ) ) ;
#63288=EDGE_CURVE ( 'NONE', #32586, #31711, #58717, .T. ) ;
#63295=CARTESIAN_POINT ( 'NONE',  ( 12.51429325950072169, 1.848987300417678226, 13.87736530974562754 ) ) ;
#63298=CARTESIAN_POINT ( 'NONE',  ( 12.47664625021882046, -0.5322368320764085947, -12.68499235032976102 ) ) ;
#63299=CARTESIAN_POINT ( 'NONE',  ( 12.38296256657291394, -0.5938246120522429061, 13.98740230410797558 ) ) ;
#63301=CARTESIAN_POINT ( 'NONE',  ( 12.43945954148919064, -1.858853511423144145, 12.46213071393705007 ) ) ;
#63307=CARTESIAN_POINT ( 'NONE',  ( 12.30074667651850184, 0.5168989769797244227, 12.58939571008426839 ) ) ;
#63310=CARTESIAN_POINT ( 'NONE',  ( 12.27207149905416550, 1.992391748285591513, 12.44148121715491584 ) ) ;
#63317=CARTESIAN_POINT ( 'NONE',  ( 18.14887404799286230, -0.1995702674007985011, 12.69797248607370754 ) ) ;
#63321=CARTESIAN_POINT ( 'NONE',  ( 12.49508659866806859, 0.5431048945666756556, 12.68437082640543245 ) ) ;
#63326=CARTESIAN_POINT ( 'NONE',  ( 12.26319456176233125, -2.811641923064096993, 13.60240885908115516 ) ) ;
#63327=CARTESIAN_POINT ( 'NONE',  ( 12.24918480870364945, 2.785872542152070697, 13.60860763679485075 ) ) ;
#63336=CARTESIAN_POINT ( 'NONE',  ( 18.16006747845239744, 2.341920795209952555, -12.48703680160761209 ) ) ;
#63338=CARTESIAN_POINT ( 'NONE',  ( 18.15919311622385024, 2.661142131363571028, 12.41257606650292011 ) ) ;
#63340=EDGE_CURVE ( 'NONE', #40048, #59800, #52635, .T. ) ;
#63348=CARTESIAN_POINT ( 'NONE',  ( -17.56123417799999942, 11.06886219213000011, 1.536526853569999851 ) ) ;
#63362=CARTESIAN_POINT ( 'NONE',  ( 12.40639171139639885, 0.4813567170340031232, -13.88878047999878440 ) ) ;
#63376=CARTESIAN_POINT ( 'NONE',  ( 17.88765289689609972, -3.029249243711964468, -12.31236272700674839 ) ) ;
#63380=CARTESIAN_POINT ( 'NONE',  ( 18.17882542849182315, -2.459571230369202333, -12.46089164812839378 ) ) ;
#63384=DIRECTION ( 'NONE',  ( 1.000000000000000000, 0.000000000000000000, 0.000000000000000000 ) ) ;
#63394=EDGE_LOOP ( 'NONE', ( #4022, #62132, #51275, #15895 ) ) ;
#63411=CARTESIAN_POINT ( 'NONE',  ( 18.17920460086783407, 2.538974944925445509, -12.44245230915264955 ) ) ;
#63421=ADVANCED_FACE ( 'NONE', ( #31667 ), #41123, .F. ) ;
#63422=CARTESIAN_POINT ( 'NONE',  ( 12.18107318252211613, -0.04114048977874555646, -12.69993211551499535 ) ) ;
#63423=CARTESIAN_POINT ( 'NONE',  ( 12.26360295036286452, -2.812350523742413788, -12.37328769147676155 ) ) ;
#63425=VECTOR ( 'NONE', #2202, 1000.000000000000114 ) ;
#63430=ADVANCED_FACE ( 'NONE', ( #14895 ), #20823, .F. ) ;
#63470=CARTESIAN_POINT ( 'NONE',  ( 12.34612353109747573, 2.075598726024749929, -13.75436385846648157 ) ) ;
#63474=CARTESIAN_POINT ( 'NONE',  ( 18.01189197849806334, -0.4270206790917105422, 13.89118144889039286 ) ) ;
#63483=CARTESIAN_POINT ( 'NONE',  ( 17.59542397721386209, -0.6249999999999998890, -13.88107975724990695 ) ) ;
#63491=CARTESIAN_POINT ( 'NONE',  ( 18.24552617758596540, 0.2196334679052291683, 12.59809060309703277 ) ) ;
#63498=CARTESIAN_POINT ( 'NONE',  ( 17.78978190923676550, 3.208919636066285719, 13.62728338959921359 ) ) ;
#63512=CARTESIAN_POINT ( 'NONE',  ( 5.695281798973955034, 12.04221271193345189, 3.723442287067866729 ) ) ;
#63542=FACE_OUTER_BOUND ( 'NONE', #33789, .T. ) ;
#63546=CARTESIAN_POINT ( 'NONE',  ( 12.22009801487426550, -2.720357631080354999, -12.39749406087475947 ) ) ;
#63550=CARTESIAN_POINT ( 'NONE',  ( 12.22752497338540145, -2.076440593937393775, -13.84516123709150826 ) ) ;
#63553=CARTESIAN_POINT ( 'NONE',  ( 18.25703273071139421, -2.298329627318190571, 12.38863175403534989 ) ) ;
#63558=CARTESIAN_POINT ( 'NONE',  ( 12.80505043854144276, -0.6250000000000001110, -13.88107975066922428 ) ) ;
#63562=CARTESIAN_POINT ( 'NONE',  ( 17.55505043854143565, 1.875000000000000000, -12.57545641911172751 ) ) ;
#63576=CARTESIAN_POINT ( 'NONE',  ( 12.66237550623657171, -0.6088395004560435142, 12.68034807294329269 ) ) ;
#63583=CARTESIAN_POINT ( 'NONE',  ( 17.69888641710118549, 1.891428316105117746, 13.78380564104364936 ) ) ;
#63588=CARTESIAN_POINT ( 'NONE',  ( 5.601974509046187656, -12.13172069192463987, 3.749825701181730420 ) ) ;
#63595=CARTESIAN_POINT ( 'NONE',  ( 18.14022514731439628, -2.720460039646586115, -13.62418930002215589 ) ) ;
#63608=CARTESIAN_POINT ( 'NONE',  ( 18.10291897062741029, -0.3009486141072659215, 13.89561788111045182 ) ) ;
#63622=CARTESIAN_POINT ( 'NONE',  ( 18.24299778933912819, -2.286486205740230204, 13.81204233372298340 ) ) ;
#63628=ORIENTED_EDGE ( 'NONE', *, *, #66295, .T. ) ;
#63630=DIRECTION ( 'NONE',  ( 0.000000000000000000, -0.7198977633595244896, -0.6940801180771239975 ) ) ;
#63634=CARTESIAN_POINT ( 'NONE',  ( 18.05961319350869232, -0.5166535389540217738, -12.58940585649086508 ) ) ;
#63656=CARTESIAN_POINT ( 'NONE',  ( 12.71024088650322525, 0.7135009822674867053, 12.57978225961208807 ) ) ;
#63659=CARTESIAN_POINT ( 'NONE',  ( 12.08628615590296995, 2.575951425301598263, 12.33388065128748323 ) ) ;
#63668=ORIENTED_EDGE ( 'NONE', *, *, #29465, .F. ) ;
#63676=CARTESIAN_POINT ( 'NONE',  ( 12.34743845434969067, -2.926178772989072030, 13.57378949252271028 ) ) ;
#63677=CARTESIAN_POINT ( 'NONE',  ( 12.18524893064656744, 2.418966797248156553, 13.69026124204055783 ) ) ;
#63687=CARTESIAN_POINT ( 'NONE',  ( 18.13803896488298761, 2.274492816832913267, -12.50128160305151859 ) ) ;
#63689=CARTESIAN_POINT ( 'NONE',  ( 17.99291067209865957, 2.946084426705852355, 12.33636513593942752 ) ) ;
#63692=CARTESIAN_POINT ( 'NONE',  ( 12.35624619795302515, 1.936672541213169119, 13.86556857871777027 ) ) ;
#63699=ORIENTED_EDGE ( 'NONE', *, *, #51829, .F. ) ;
#63712=CARTESIAN_POINT ( 'NONE',  ( 12.27345183613374147, 0.3288514423020141852, -13.89476819318362999 ) ) ;
#63721=CARTESIAN_POINT ( 'NONE',  ( 18.17259031544353931, -2.401600790900606963, -12.47395980848748742 ) ) ;
#63723=CARTESIAN_POINT ( 'NONE',  ( 18.14123990137488818, -2.282196115462137520, -12.49965818828723840 ) ) ;
#63725=CARTESIAN_POINT ( 'NONE',  ( 12.34820889858482040, 0.4270206790917077111, 13.89118144889039286 ) ) ;
#63755=CARTESIAN_POINT ( 'NONE',  ( 18.16572637360205889, 2.633126309616273808, -12.41957822412274837 ) ) ;
#63767=CARTESIAN_POINT ( 'NONE',  ( 12.18829625149018447, 0.1017072266180437112, -12.69945743039636099 ) ) ;
#63769=FACE_OUTER_BOUND ( 'NONE', #21777, .T. ) ;
#63776=CARTESIAN_POINT ( 'NONE',  ( 18.18005043853714398, 0.02024571650141320303, 12.69999991888671076 ) ) ;
#63782=CARTESIAN_POINT ( 'NONE',  ( 17.88731995174120826, 3.029458325253038264, -13.54679862780130151 ) ) ;
#63783=ORIENTED_EDGE ( 'NONE', *, *, #57474, .F. ) ;
#63803=CARTESIAN_POINT ( 'NONE',  ( 17.95101261602637166, -1.877525629946219965, -12.45933154191684444 ) ) ;
#63819=CARTESIAN_POINT ( 'NONE',  ( 18.18005725403618911, -0.009762789003249691330, 13.90000041479089532 ) ) ;
#63820=CARTESIAN_POINT ( 'NONE',  ( 18.01482774839357859, 0.4234772792570224986, 13.89131919812331439 ) ) ;
#63822=ADVANCED_FACE ( 'NONE', ( #48606 ), #26942, .F. ) ;
#63826=CARTESIAN_POINT ( 'NONE',  ( 18.03351232765111334, -0.4021407113407378109, -13.89217057782752818 ) ) ;
#63835=CARTESIAN_POINT ( 'NONE',  ( 17.91054845552245922, -0.5141503178158091103, 12.68598964581896738 ) ) ;
#63855=ORIENTED_EDGE ( 'NONE', *, *, #57288, .T. ) ;
#63874=ORIENTED_EDGE ( 'NONE', *, *, #66995, .F. ) ;
#63883=CARTESIAN_POINT ( 'NONE',  ( 12.79462099885205184, -1.875000035136121568, -12.57541665307954659 ) ) ;
#63887=CARTESIAN_POINT ( 'NONE',  ( 12.18844676753248457, -2.902714632704707309, -13.69578956119810620 ) ) ;
#63890=CARTESIAN_POINT ( 'NONE',  ( 18.13398081625437541, -2.046400819240521418, 12.43272243325427873 ) ) ;
#63900=CARTESIAN_POINT ( 'NONE',  ( 18.17891623993478944, 2.457256301271274257, -12.46146663851731340 ) ) ;
#63915=CARTESIAN_POINT ( 'NONE',  ( 12.40045920100465082, -0.4764818960106725343, 12.68796903437992540 ) ) ;
#63923=CARTESIAN_POINT ( 'NONE',  ( 17.84240044433949990, 3.055120806185297244, 13.53986419860029145 ) ) ;
#63932=CARTESIAN_POINT ( 'NONE',  ( 5.600023899775999681, 13.94845324556000143, 4.312847325879000770 ) ) ;
#63937=CARTESIAN_POINT ( 'NONE',  ( 18.09690629521218241, -2.811641957965457905, -13.60235445620236128 ) ) ;
#63946=CIRCLE ( 'NONE', #33829, 2.000000000000000444 ) ;
#63947=CARTESIAN_POINT ( 'NONE',  ( 18.15698508547025369, -0.1703860850750339440, 13.89862588397355658 ) ) ;
#63957=CARTESIAN_POINT ( 'NONE',  ( 12.10652924560087307, 2.286704390305608570, -12.39076728011198725 ) ) ;
#63960=CARTESIAN_POINT ( 'NONE',  ( 18.14470825313953739, 2.707255376642708100, -13.62731588235574698 ) ) ;
#63970=CARTESIAN_POINT ( 'NONE',  ( 17.94350157889105901, 0.4896501542853345379, -12.68729270499358108 ) ) ;
#63979=CARTESIAN_POINT ( 'NONE',  ( 17.98022888730379165, 3.063516777430822735, 12.22190850126833972 ) ) ;
#63980=DIRECTION ( 'NONE',  ( 1.000000000000000000, 0.000000000000000000, 0.000000000000000000 ) ) ;
#63988=CARTESIAN_POINT ( 'NONE',  ( 12.36031510016529822, -1.911905511008638259, 12.45410252665035600 ) ) ;
#63991=DIRECTION ( 'NONE',  ( 1.000000000000000000, 0.000000000000000000, 0.000000000000000000 ) ) ;
#63994=CARTESIAN_POINT ( 'NONE',  ( 12.35444711458465505, 0.5635217852606908551, 12.58739276154098086 ) ) ;
#63997=FACE_OUTER_BOUND ( 'NONE', #17334, .T. ) ;
#63998=CARTESIAN_POINT ( 'NONE',  ( 12.43868857148325269, 1.859375588728223505, 12.46205283878464876 ) ) ;
#64004=ADVANCED_FACE ( 'NONE', ( #54884 ), #2432, .F. ) ;
#64007=CARTESIAN_POINT ( 'NONE',  ( 12.33520056822022148, 2.912263648515628134, 12.34589992753487664 ) ) ;
#64010=CARTESIAN_POINT ( 'NONE',  ( 12.26246716466153863, 0.3103928898581689300, 12.69489813901718911 ) ) ;
#64012=CARTESIAN_POINT ( 'NONE',  ( 17.55505043854144631, -0.7192913403693119712, -12.57945229203838267 ) ) ;
#64014=CARTESIAN_POINT ( 'NONE',  ( 12.51770044094180534, -3.055120810438262335, 13.53992139506082459 ) ) ;
#64015=CARTESIAN_POINT ( 'NONE',  ( 12.18032316971016193, 2.521073842666304632, 13.66891947081129111 ) ) ;
#64023=CARTESIAN_POINT ( 'NONE',  ( 17.92103372721321364, 3.006741473881710647, -12.31895748915804489 ) ) ;
#64037=ORIENTED_EDGE ( 'NONE', *, *, #36325, .F. ) ;
#64046=CARTESIAN_POINT ( 'NONE',  ( 12.38151006065648296, 0.4597209100133001214, -13.88976952606943271 ) ) ;
#64056=CARTESIAN_POINT ( 'NONE',  ( 18.17176891181421539, -2.603394967838110308, -12.42689558795375326 ) ) ;
#64079=CARTESIAN_POINT ( 'NONE',  ( 18.28051081950330570, -2.330210462394771476, 13.80606256597843995 ) ) ;
#64097=CARTESIAN_POINT ( 'NONE',  ( 18.13004437684510961, 2.745098799910168808, -12.39110308483444634 ) ) ;
#64099=CIRCLE ( 'NONE', #33989, 12.59999999999999964 ) ;
#64104=CARTESIAN_POINT ( 'NONE',  ( 12.80505043854146940, -1.760845406083394016, 12.47635457398814829 ) ) ;
#64107=CARTESIAN_POINT ( 'NONE',  ( 12.19004707749462924, 0.1118057330073172623, -12.69934308675517620 ) ) ;
#64110=DIRECTION ( 'NONE',  ( 0.000000000000000000, 0.000000000000000000, -1.000000000000000000 ) ) ;
#64139=AXIS2_PLACEMENT_3D ( 'NONE', #23852, #32963, #49377 ) ;
#64144=CARTESIAN_POINT ( 'NONE',  ( 17.98055108453616668, -1.897673117161889467, -12.45627908894455338 ) ) ;
#64149=CARTESIAN_POINT ( 'NONE',  ( 7.100000000000000533, -11.06886219213000011, 1.536526853569999851 ) ) ;
#64156=VERTEX_POINT ( 'NONE', #19890 ) ;
#64164=CARTESIAN_POINT ( 'NONE',  ( 18.17177275037307638, 0.1018973686818568924, 13.89950237059086291 ) ) ;
#64166=VERTEX_POINT ( 'NONE', #56949 ) ;
#64167=CARTESIAN_POINT ( 'NONE',  ( 12.76431812838242230, 0.6240106079350378199, 13.88114051191589660 ) ) ;
#64174=EDGE_CURVE ( 'NONE', #6106, #31059, #56528, .T. ) ;
#64178=CARTESIAN_POINT ( 'NONE',  ( 18.17607568152034148, 0.07112609253419145683, 12.69973757146476245 ) ) ;
#64188=CIRCLE ( 'NONE', #50842, 12.60000000000000142 ) ;
#64194=CARTESIAN_POINT ( 'NONE',  ( 18.23375231277518083, 2.733957939387004821, -12.29982111303847958 ) ) ;
#64195=CARTESIAN_POINT ( 'NONE',  ( 5.598857209342392949, 12.13471601159925406, 3.750691118698490811 ) ) ;
#64197=ORIENTED_EDGE ( 'NONE', *, *, #11001, .T. ) ;
#64202=ORIENTED_EDGE ( 'NONE', *, *, #30875, .F. ) ;
#64208=CARTESIAN_POINT ( 'NONE',  ( 17.81345962944524075, 0.5694488842926277439, -13.88429844810376323 ) ) ;
#64209=EDGE_CURVE ( 'NONE', #44214, #16046, #30058, .T. ) ;
#64210=EDGE_CURVE ( 'NONE', #42806, #35474, #48103, .T. ) ;
#64220=LINE ( 'NONE', #64908, #58579 ) ;
#64222=DIRECTION ( 'NONE',  ( 0.000000000000000000, 1.000000000000000000, 0.000000000000000000 ) ) ;
#64225=CARTESIAN_POINT ( 'NONE',  ( 12.80505043854146940, -1.874999999999999778, -12.57541666120756396 ) ) ;
#64229=CARTESIAN_POINT ( 'NONE',  ( 12.58164121395691559, -1.823227133926378585, -13.88077287699123197 ) ) ;
#64232=CARTESIAN_POINT ( 'NONE',  ( 17.87828936854287676, -3.124432504806129440, 12.20647160316251068 ) ) ;
#64235=EDGE_CURVE ( 'NONE', #68711, #2919, #552, .T. ) ;
#64237=B_SPLINE_CURVE_WITH_KNOTS ( 'NONE', 1,
 ( #40022, #62019 ),
 .UNSPECIFIED., .F., .F.,
 ( 2, 2 ),
 ( 0.000000000000000000, 1.000000000000000000 ),
 .UNSPECIFIED. ) ;
#64251=B_SPLINE_CURVE_WITH_KNOTS ( 'NONE', 3,
 ( #11969, #22800, #34695, #23844 ),
 .UNSPECIFIED., .F., .F.,
 ( 4, 4 ),
 ( 0.000000000000000000, 1.000000000000000000 ),
 .UNSPECIFIED. ) ;
#64259=DIRECTION ( 'NONE',  ( 0.000000000000000000, 0.7198977633594745296, -0.6940801180771756229 ) ) ;
#64264=CARTESIAN_POINT ( 'NONE',  ( 18.13779378220191063, 2.273859756726421377, 13.71877938508613326 ) ) ;
#64276=CARTESIAN_POINT ( 'NONE',  ( 18.20194470744738524, -2.188139888162251800, -13.82794850388582475 ) ) ;
#64280=ORIENTED_EDGE ( 'NONE', *, *, #53898, .F. ) ;
#64296=CARTESIAN_POINT ( 'NONE',  ( 12.23408645687631591, 2.036599147259922749, -12.43432143783615729 ) ) ;
#64299=CARTESIAN_POINT ( 'NONE',  ( 18.16777246613359154, 2.623276685346445980, -13.64654026446401502 ) ) ;
#64304=CARTESIAN_POINT ( 'NONE',  ( 12.35197574246973673, -3.042005152232414744, -12.22727356655694209 ) ) ;
#64310=CARTESIAN_POINT ( 'NONE',  ( 17.99694387276892726, -0.5707228546307235861, -12.58707662888203771 ) ) ;
#64311=CARTESIAN_POINT ( 'NONE',  ( 12.31573549167064030, 2.888971355165489197, -12.35241121502826545 ) ) ;
#64318=CARTESIAN_POINT ( 'NONE',  ( 18.02766945781917585, 1.934589073148402116, 12.45059934707292726 ) ) ;
#64321=CARTESIAN_POINT ( 'NONE',  ( 12.39828795418346274, -0.4745523467757941094, -12.68806523616956206 ) ) ;
#64324=CARTESIAN_POINT ( 'NONE',  ( 12.07980306947244031, -2.459616342362513919, 12.35762317364248020 ) ) ;
#64328=CARTESIAN_POINT ( 'NONE',  ( 4.599999999999999645, -1.760845406083394682, 12.47635457398814829 ) ) ;
#64333=CARTESIAN_POINT ( 'NONE',  ( 12.64055030734119001, 0.7009231686363525116, 12.58048995873113896 ) ) ;
#64337=CARTESIAN_POINT ( 'NONE',  ( 12.55429323164597299, 3.072583267488710579, 12.29953727834259603 ) ) ;
#64348=CARTESIAN_POINT ( 'NONE',  ( 12.29893172067548690, 0.3669524139187689271, 12.69287054299043227 ) ) ;
#64351=CARTESIAN_POINT ( 'NONE',  ( 18.27937482164660565, 2.670364552387198387, -12.31525491565053798 ) ) ;
#64352=CARTESIAN_POINT ( 'NONE',  ( 12.25686392147160220, -2.040034559784666968, 13.85057184956195542 ) ) ;
#64361=CARTESIAN_POINT ( 'NONE',  ( 17.96930180488788409, 2.968443477542578979, -12.33001868694669589 ) ) ;
#64368=CARTESIAN_POINT ( 'NONE',  ( 12.56925896342638183, 1.825837054105086787, 13.88044190432479041 ) ) ;
#64381=ORIENTED_EDGE ( 'NONE', *, *, #26355, .F. ) ;
#64387=CARTESIAN_POINT ( 'NONE',  ( 12.18504202264279712, 0.08143095636433357598, -13.89969831568923020 ) ) ;
#64397=CARTESIAN_POINT ( 'NONE',  ( 18.20180239440930947, -2.898381337075406794, -13.69738341131825266 ) ) ;
#64398=CARTESIAN_POINT ( 'NONE',  ( 17.86131849338084265, -3.044913046804099466, -12.30775201372483885 ) ) ;
#64403=CARTESIAN_POINT ( 'NONE',  ( 17.88333207268022917, -1.943312949537261636, -12.56472734206913522 ) ) ;
#64404=CARTESIAN_POINT ( 'NONE',  ( 12.64263601961789263, 0.6038715862870271955, 13.88233985103439494 ) ) ;
#64433=CARTESIAN_POINT ( 'NONE',  ( 5.694051797832758055, -13.02176618664603502, -2.006311339876389432 ) ) ;
#64436=CARTESIAN_POINT ( 'NONE',  ( 17.77858768906835962, 3.083996659899494563, -12.29614209097632838 ) ) ;
#64443=CARTESIAN_POINT ( 'NONE',  ( 12.22352039041727245, 0.2292434675627110230, -12.69722039463305840 ) ) ;
#64453=ADVANCED_FACE ( 'NONE', ( #9995 ), #43300, .T. ) ;
#64455=CARTESIAN_POINT ( 'NONE',  ( 18.15698397290777777, 0.1703900906530151915, 12.69849596186095297 ) ) ;
#64462=CARTESIAN_POINT ( 'NONE',  ( 18.15894044208799230, 2.662322226546016246, -13.63771003692132311 ) ) ;
#64469=CARTESIAN_POINT ( 'NONE',  ( 18.17614054500835508, 0.08113966114449443212, -12.69973816841072178 ) ) ;
#64475=CARTESIAN_POINT ( 'NONE',  ( 7.100000000000000533, 11.06886219213000011, -1.536526853569999851 ) ) ;
#64493=EDGE_LOOP ( 'NONE', ( #17799, #4663, #26015, #13566 ) ) ;
#64497=CARTESIAN_POINT ( 'NONE',  ( 12.64218892536043093, 3.103760129324341310, -13.52669845179790364 ) ) ;
#64500=CARTESIAN_POINT ( 'NONE',  ( 18.17808105194527002, -0.05063168410658782509, 13.89988098555966012 ) ) ;
#64501=CARTESIAN_POINT ( 'NONE',  ( 17.86525158951534209, 0.5426919696039526064, 13.88574006265539396 ) ) ;
#64504=CARTESIAN_POINT ( 'NONE',  ( 12.27274360194281755, 0.3282986408611026641, 13.89479914613944267 ) ) ;
#64505=CARTESIAN_POINT ( 'NONE',  ( 12.58523710839113008, -0.5851630251701737118, -13.88341719038490929 ) ) ;
#64507=CARTESIAN_POINT ( 'NONE',  ( 17.89454199023491299, -0.5248377731598605767, -13.88666204733997134 ) ) ;
#64517=CARTESIAN_POINT ( 'NONE',  ( 17.83159136582988680, -0.5605836838512557874, 12.68334204399184273 ) ) ;
#64520=DIRECTION ( 'NONE',  ( 0.000000000000000000, -0.9905022095861402143, -0.1374968101629056305 ) ) ;
#64530=ORIENTED_EDGE ( 'NONE', *, *, #23750, .T. ) ;
#64532=CARTESIAN_POINT ( 'NONE',  ( 12.42221671361157043, -0.6112845611542921942, -12.58516990776527500 ) ) ;
#64536=CARTESIAN_POINT ( 'NONE',  ( 5.630370665535105346, 12.10426712533993232, 3.742487578857858654 ) ) ;
#64551=CARTESIAN_POINT ( 'NONE',  ( 12.56879673640925077, 1.798456840536528434, -12.47100214317278954 ) ) ;
#64553=CARTESIAN_POINT ( 'NONE',  ( 18.17001922193490415, -0.1119984579798035534, -13.89939774083725688 ) ) ;
#64565=B_SPLINE_CURVE_WITH_KNOTS ( 'NONE', 3,
 ( #39631, #1189, #44549, #59910, #22498, #7120, #43842, #17263, #38586, #12018, #17966, #6766, #28105, #65842, #49418, #60264, #12369, #28458, #60606, #55364, #67557, #3252, #3925, #61985, #24581, #30182, #25263, #57077, #46939, #30861, #24921, #35085, #41349, #35761, #8158, #19681, #19327, #14441, #20363, #52175, #62326, #34736, #61297, #9519, #40652, #45904, #29504, #46601, #51489, #13417, #14096, #51155, #41002, #50810, #45571, #9177, #13751, #20023, #62660, #67216, #25611, #30517, #67906, #51830, #68242, #4276, #24232 ),
 .UNSPECIFIED., .F., .F.,
 ( 4, 2, 2, 2, 2, 2, 2, 2, 2, 2, 2, 2, 2, 2, 1, 1, 1, 2, 2, 2, 2, 2, 2, 2, 2, 2, 2, 2, 2, 2, 2, 2, 2, 2, 4 ),
 ( 0.000000000000000000, 0.1249999999998060995, 0.2499999999996121991, 0.3124999999995152766, 0.3437499999994663713, 0.3749999999994174660, 0.4062499999993685607, 0.4218749999993443023, 0.4374999999993200994, 0.4687499999992710831, 0.4843749999992468247, 0.4999999999992225108, 0.5156249999991983080, 0.5312499999991739941, 0.5468749999991497912, 0.5546874999991379118, 0.5585937499991319166, 0.5605468749991289190, 0.5624999999991259214, 0.5781249999991577848, 0.5859374999991732169, 0.5898437499991809885, 0.5937499999991886490, 0.6093749999992187361, 0.6171874999992340571, 0.6249999999992492672, 0.6406249999992801314, 0.6562499999993109956, 0.6718749999993418598, 0.6874999999993726130, 0.7187499999994347855, 0.7343749999994649835, 0.7499999999994952926, 0.8749999999997475353, 1.000000000000000000 ),
 .UNSPECIFIED. ) ;
#64569=CARTESIAN_POINT ( 'NONE',  ( 12.32534826942435835, -2.099231811413891258, -12.53595023114330687 ) ) ;
#64570=EDGE_CURVE ( 'NONE', #26914, #46748, #57454, .T. ) ;
#64575=CARTESIAN_POINT ( 'NONE',  ( 12.18713711904778130, -2.135907760014724488, -13.83611243771405874 ) ) ;
#64578=CARTESIAN_POINT ( 'NONE',  ( 12.43681290826173225, -1.853313662595208688, 12.46300903944178984 ) ) ;
#64579=CARTESIAN_POINT ( 'NONE',  ( 18.01279894578404495, -3.038334268486861944, 12.22818629355008468 ) ) ;
#64587=CARTESIAN_POINT ( 'NONE',  ( 12.80505043854143388, 1.875000000000000000, -25.00000000000000000 ) ) ;
#64611=CARTESIAN_POINT ( 'NONE',  ( 18.17891560871126799, 2.542711950176887559, 13.66427582110434003 ) ) ;
#64615=CARTESIAN_POINT ( 'NONE',  ( 5.685751648550910531, -12.05129647863330966, 3.726325695169322660 ) ) ;
#64623=CARTESIAN_POINT ( 'NONE',  ( 17.79045811871164773, -1.826948899878886534, -13.88028486463507249 ) ) ;
#64640=CARTESIAN_POINT ( 'NONE',  ( 17.79074592073776628, 3.210128306652872521, 13.62701119232196234 ) ) ;
#64643=B_SPLINE_SURFACE_WITH_KNOTS ( 'NONE', 1, 3, ( 
 ( #55998, #13358, #2507, #45169, #8102, #22788, #29446, #45514, #1819, #17197, #6708, #38528, #59850, #28048, #49357, #44136, #51434, #46194, #30800, #30461, #18938, #3871, #19969, #41631, #3531, #24525, #29793, #66825, #24866, #56688, #25205, #40262, #25554, #51773, #46540, #46880, #68187, #8787, #31159, #41292, #14040, #67505, #61582, #4557, #14723, #4216, #30131, #62266, #20305, #3198, #14386, #40600, #35706, #67846, #15061, #62599, #36384, #35367, #36038, #57023, #13698, #57354, #35027, #9458, #62937, #57700, #61925, #52113, #19623, #9810, #40944, #9123, #52461, #56342, #25897, #8446, #51095, #45850, #67159, #19271, #68879, #11185, #47226, #63634, #26933, #26246, #36738, #64310, #58058, #63282, #32865, #32520, #37079, #52812, #16428, #64662, #6276, #41977, #16766, #37757, #351, #38097, #15751, #26593, #54178, #702, #48247, #16085, #21333, #15412, #53499, #37415 ),
 ( #68529, #59083, #47914, #58392, #58736, #53837, #43004, #20651, #59423, #10842, #20996, #31837, #5934, #42662, #42332, #10497, #53153, #32184, #5255, #21668, #11, #63970, #5589, #11521, #27276, #48599, #22014, #43361, #10160, #31490, #47574, #4905, #28664, #44747, #22707, #33906, #45087, #23410, #66047, #18169, #60468, #13279, #2425, #60125, #1735, #23054, #17114, #39491, #44404, #60813, #55573, #49280, #61161, #43703, #28307, #12576, #64999, #49630, #12926, #34605, #38800, #1391, #7674, #17475, #55918, #38448, #12232, #44051, #34253, #29020, #27619, #55223, #50327, #33557, #65356, #48945, #23751, #17827, #66394, #49977, #18517, #65704, #2092, #6980, #39143, #39839, #1053, #59771, #11872, #22365, #33212, #54532, #6632, #27970, #54877, #7323, #18858, #36909, #26419, #47746, #4728, #24097, #20820, #40185, #56257, #52292, #19190, #69061, #62770, #57530, #31665, #45769 ) ),
 .UNSPECIFIED., .F., .F., .F.,
 ( 2, 2 ),
 ( 4, 2, 2, 2, 2, 2, 2, 2, 2, 2, 2, 2, 2, 2, 2, 2, 2, 2, 2, 2, 2, 2, 2, 2, 2, 2, 2, 2, 2, 2, 2, 2, 2, 2, 2, 2, 2, 2, 2, 2, 2, 2, 2, 2, 2, 2, 2, 2, 2, 2, 2, 2, 2, 2, 2, 4 ),
 ( 0.000000000000000000, 1.000000000000000000 ),
 ( 0.000000000000000000, 7.083325941644366664E-05, 0.0001416665188328873333, 0.0002124997782493309999, 0.0002479164079575528197, 0.0002833330376657746666, 0.0003187496673739965134, 0.0003541662970822183603, 0.0004249995564986619998, 0.0004604161862068838467, 0.0004781245010609947430, 0.0004958328159151056394, 0.0005312494456233274320, 0.0005666660753315493331, 0.0006374993347479930269, 0.0006729159644562148195, 0.0007083325941644367206, 0.0007437492238726585133, 0.0007791658535808803059, 0.0008145824832891022070, 0.0008499991129973239997, 0.0008854157427055457923, 0.0009208323724137676934, 0.0009562490021219894861, 0.0009916656318302112787, 0.001027082261538433180, 0.001062498891246654864, 0.001133332150663098666, 0.001168748780371320567, 0.001204165410079542468, 0.001239582039787764153, 0.001274998669495986054, 0.001345831928912429639, 0.001381248558620651540, 0.001416665188328873441, 0.001452081818037095125, 0.001469790132891206184, 0.001487498447745317027, 0.001558331707161760612, 0.001629164966578204414, 0.001664581596286426098, 0.001699998225994647999, 0.001735414855702869900, 0.001770831485411091585, 0.001841664744827535387, 0.001877081374535757071, 0.001912498004243978972, 0.001947914633952200873, 0.001983331263660422557, 0.002018747893368644242, 0.002054164523076866360, 0.002124997782493309728, 0.002160414412201531846, 0.002195831041909753530, 0.002231247671617975215, 0.002266664301326197332 ),
 .UNSPECIFIED. ) ;
#64645=CARTESIAN_POINT ( 'NONE',  ( 12.09524978539961104, 2.332501710336875256, -12.38222815831571566 ) ) ;
#64655=EDGE_CURVE ( 'NONE', #52670, #15133, #50424, .T. ) ;
#64662=CARTESIAN_POINT ( 'NONE',  ( 17.85474174040770023, -0.6550687562476319448, -12.58296113213902423 ) ) ;
#64663=CARTESIAN_POINT ( 'NONE',  ( 12.19822292018694654, 2.649955819899461495, -12.41539170542472093 ) ) ;
#64671=CARTESIAN_POINT ( 'NONE',  ( 18.24176189833872996, 2.711585165818143128, 12.30477270241628318 ) ) ;
#64672=CARTESIAN_POINT ( 'NONE',  ( 12.50340631570014693, 1.853896141579338019, 13.87671057111554340 ) ) ;
#64673=B_SPLINE_CURVE_WITH_KNOTS ( 'NONE', 3,
 ( #52412, #20600, #4504, #25845, #47173, #68476, #23964, #13488, #1955, #18723, #50535, #34121, #65913, #50196, #2637, #34473 ),
 .UNSPECIFIED., .F., .F.,
 ( 4, 2, 2, 2, 2, 2, 2, 4 ),
 ( 0.000000000000000000, 0.06249999999999995837, 0.1249999999999999167, 0.2499999999999998335, 0.5000000000000005551, 0.7500000000000012212, 0.8750000000000006661, 1.000000000000000000 ),
 .UNSPECIFIED. ) ;
#64678=CARTESIAN_POINT ( 'NONE',  ( 12.12616169587831294, -2.733465040722951933, 12.29993066094647958 ) ) ;
#64683=CARTESIAN_POINT ( 'NONE',  ( 12.08006680260082888, 0.02395120399003008299, 12.59999907117300033 ) ) ;
#64685=ADVANCED_FACE ( 'NONE', ( #60915 ), #45872, .T. ) ;
#64688=CARTESIAN_POINT ( 'NONE',  ( 12.49051143973448497, 3.040180064579588670, 12.30914836342242680 ) ) ;
#64695=CARTESIAN_POINT ( 'NONE',  ( 18.11245859366771072, -0.2828884610821091883, 12.69576253191529069 ) ) ;
#64698=CARTESIAN_POINT ( 'NONE',  ( 12.53103060003192226, 0.5618114788522101666, 12.68327018738109402 ) ) ;
#64702=CARTESIAN_POINT ( 'NONE',  ( 12.80505043854146940, -3.125000000000000444, 13.52084414783465860 ) ) ;
#64706=DIRECTION ( 'NONE',  ( -0.000000000000000000, -0.000000000000000000, 1.000000000000000000 ) ) ;
#64711=ADVANCED_FACE ( 'NONE', ( #2528 ), #66303, .T. ) ;
#64720=FACE_OUTER_BOUND ( 'NONE', #4487, .T. ) ;
#64725=CARTESIAN_POINT ( 'NONE',  ( 18.01376003089018596, -2.074995895013258096, 13.75447352907418619 ) ) ;
#64734=CARTESIAN_POINT ( 'NONE',  ( 12.20062805326818278, -0.1603563348589100157, -13.89877286452650829 ) ) ;
#64736=B_SPLINE_CURVE_WITH_KNOTS ( 'NONE', 3,
 ( #4404, #5100, #15597, #58586, #36576, #31338, #11038, #26089, #47415, #52308, #10346, #47765, #58934, #32034, #57549, #25743, #47073, #68374, #31682, #63820, #53347, #26786, #48101, #65546, #28865, #33752, #1934, #59619, #1239, #17669, #64501, #16621, #1581, #60655, #44251, #55068, #60313, #50172, #55417, #21863, #7170, #38993 ),
 .UNSPECIFIED., .F., .F.,
 ( 4, 2, 2, 2, 2, 2, 2, 2, 2, 2, 2, 2, 2, 1, 2, 2, 2, 2, 2, 1, 2, 4 ),
 ( 0.4997863768984585620, 0.5623130797861395358, 0.6248397826738204541, 0.6404714583957415996, 0.6561031341176628562, 0.6873664855615074787, 0.7029981612834298454, 0.7186298370053522122, 0.7264456748663133956, 0.7342615127272744679, 0.7498931884491969457, 0.7811565398930446769, 0.7889723777540051941, 0.7967882156149656003, 0.8124198913368909647, 0.8280515670588164401, 0.8436832427807419155, 0.8749465942245924222, 0.8905782699465176755, 0.9062099456684430399, 0.9374732971122935465, 1.000000000000000000 ),
 .UNSPECIFIED. ) ;
#64745=CARTESIAN_POINT ( 'NONE',  ( 17.60475804966761970, -1.787836225788245414, -13.88537509868912956 ) ) ;
#64746=CARTESIAN_POINT ( 'NONE',  ( 18.15011669908946601, -2.691369836981456931, -12.40492163541245141 ) ) ;
#64749=CARTESIAN_POINT ( 'NONE',  ( 12.70159504149943430, 3.116720374454505116, 13.52307403002092379 ) ) ;
#64750=CARTESIAN_POINT ( 'NONE',  ( 17.55505043854147118, -1.874999999999999556, 12.57545641911173107 ) ) ;
#64752=CARTESIAN_POINT ( 'NONE',  ( 12.24428838907443229, 0.2761834754990887264, 13.89631168292872587 ) ) ;
#64762=ADVANCED_FACE ( 'NONE', ( #13719 ), #14062, .T. ) ;
#64769=EDGE_CURVE ( 'NONE', #2919, #34701, #67282, .T. ) ;
#64797=CARTESIAN_POINT ( 'NONE',  ( 12.35578833720754055, 1.907710147573941972, 12.45493153469542236 ) ) ;
#64802=CARTESIAN_POINT ( 'NONE',  ( 18.12548766255678601, 0.2560639957353438301, 12.69654133872496793 ) ) ;
#64808=CARTESIAN_POINT ( 'NONE',  ( 17.96105691736157084, 2.975276276409919873, -13.56109295189183328 ) ) ;
#64814=EDGE_LOOP ( 'NONE', ( #49408, #42813, #6811, #24872 ) ) ;
#64830=CARTESIAN_POINT ( 'NONE',  ( 18.08681467613411442, 0.3285836819253546426, -13.89477675118497935 ) ) ;
#64832=CIRCLE ( 'NONE', #58155, 1.800000000000000266 ) ;
#64839=DIRECTION ( 'NONE',  ( 0.000000000000000000, 0.000000000000000000, 1.000000000000000000 ) ) ;
#64842=CARTESIAN_POINT ( 'NONE',  ( 12.55463174185018715, 3.072731264995192113, -13.53516186994626658 ) ) ;
#64845=CARTESIAN_POINT ( 'NONE',  ( 18.15913552218862037, -0.1616183441363965301, 13.89875400931294536 ) ) ;
#64850=CARTESIAN_POINT ( 'NONE',  ( 12.20062805325453148, 0.1603563348074356076, 13.89877286452765404 ) ) ;
#64855=DIRECTION ( 'NONE',  ( 0.000000000000000000, 1.000000000000000000, 0.000000000000000000 ) ) ;
#64863=CARTESIAN_POINT ( 'NONE',  ( 17.94350157889105901, -0.4896501542853345379, 12.68729270499356510 ) ) ;
#64878=CARTESIAN_POINT ( 'NONE',  ( 12.17126533935443611, -0.3494793053307434505, -12.59515668824706580 ) ) ;
#64880=VECTOR ( 'NONE', #27022, 1000.000000000000000 ) ;
#64881=CARTESIAN_POINT ( 'NONE',  ( 17.99878237954352400, 3.049368882785695067, -12.22543920180491739 ) ) ;
#64891=CARTESIAN_POINT ( 'NONE',  ( 18.05677685611890126, -2.118334401119843946, -13.74715678131696883 ) ) ;
#64897=CARTESIAN_POINT ( 'NONE',  ( 18.16408159376649678, 0.1418539764880162590, -13.89904537328360945 ) ) ;
#64907=ORIENTED_EDGE ( 'NONE', *, *, #8445, .F. ) ;
#64908=CARTESIAN_POINT ( 'NONE',  ( 4.599999999999999645, 3.248147246781390329, 13.61798588129781251 ) ) ;
#64912=CARTESIAN_POINT ( 'NONE',  ( 12.33197597414245728, -2.091428098900829369, -12.53741636228080836 ) ) ;
#64916=CARTESIAN_POINT ( 'NONE',  ( 12.20666462242727590, -2.105579624229079183, -13.84076000201158152 ) ) ;
#64919=CARTESIAN_POINT ( 'NONE',  ( 17.91108626730883202, -1.853415294216375298, 12.46294044425349767 ) ) ;
#64945=ORIENTED_EDGE ( 'NONE', *, *, #54441, .F. ) ;
#64948=CARTESIAN_POINT ( 'NONE',  ( 17.96899650538950155, 2.968713945236787222, 13.56275387600714311 ) ) ;
#64962=CARTESIAN_POINT ( 'NONE',  ( 18.25201697487001340, -2.719281809836145314, -13.73337690942506129 ) ) ;
#64966=VERTEX_POINT ( 'NONE', #41808 ) ;
#64982=CARTESIAN_POINT ( 'NONE',  ( 12.25024874575444933, 2.943737818075150336, -12.25130580795035407 ) ) ;
#64990=CARTESIAN_POINT ( 'NONE',  ( 12.80505043854146940, -3.199698446519381179, -12.18695736643652516 ) ) ;
#64999=CARTESIAN_POINT ( 'NONE',  ( 18.17981518646734784, -0.01996654564806030208, -12.69998441237379971 ) ) ;
#65000=CARTESIAN_POINT ( 'NONE',  ( 12.25748074640750751, 2.187380181871708018, -12.51928400913670814 ) ) ;
#65007=CARTESIAN_POINT ( 'NONE',  ( 17.99974802964002762, 1.911958328522579187, 12.45409441785080773 ) ) ;
#65014=ORIENTED_EDGE ( 'NONE', *, *, #65753, .T. ) ;
#65015=CARTESIAN_POINT ( 'NONE',  ( 12.14218285455822333, -2.187615620731410804, 12.40865911928243825 ) ) ;
#65019=APPLICATION_CONTEXT ( 'automotive_design' ) ;
#65022=ADVANCED_FACE ( 'NONE', ( #10332 ), #298, .T. ) ;
#65024=CARTESIAN_POINT ( 'NONE',  ( 12.53820945512841689, -0.6689034848678564460, 12.58223305319197394 ) ) ;
#65027=CARTESIAN_POINT ( 'NONE',  ( 12.54493252275448079, 3.068391087487184254, 12.30078773432381034 ) ) ;
#65040=EDGE_CURVE ( 'NONE', #16477, #12411, #48258, .T. ) ;
#65041=PLANE ( 'NONE',  #42296 ) ;
#65044=CARTESIAN_POINT ( 'NONE',  ( 12.32403884885184198, -1.971565993173706621, 13.86048321094706814 ) ) ;
#65053=CARTESIAN_POINT ( 'NONE',  ( 17.55505043854143565, 1.874999999999999556, -12.57545641911173107 ) ) ;
#65056=FACE_OUTER_BOUND ( 'NONE', #37321, .T. ) ;
#65058=CARTESIAN_POINT ( 'NONE',  ( 12.15689047918783849, 2.896806234391597012, 13.69773071443709256 ) ) ;
#65067=CARTESIAN_POINT ( 'NONE',  ( 18.02642401515176829, -2.910531091912870849, 13.57777274349195729 ) ) ;
#65081=ORIENTED_EDGE ( 'NONE', *, *, #4738, .F. ) ;
#65083=EDGE_LOOP ( 'NONE', ( #35718, #29248, #50577, #21162 ) ) ;
#65087=CARTESIAN_POINT ( 'NONE',  ( 17.55505043854147118, -3.248147246781390329, -13.61798588129781074 ) ) ;
#65093=CARTESIAN_POINT ( 'NONE',  ( 12.43888651633844056, 3.006915248264996343, 13.55273156457843697 ) ) ;
#65096=CARTESIAN_POINT ( 'NONE',  ( 12.18528724423033438, 0.08139021474669518030, 13.89968437038781524 ) ) ;
#65099=EDGE_CURVE ( 'NONE', #7987, #7389, #429, .T. ) ;
#65115=AXIS2_PLACEMENT_3D ( 'NONE', #42322, #41964, #20638 ) ;
#65128=CARTESIAN_POINT ( 'NONE',  ( 5.667284888080160066, -12.98956018065501894, -2.203076788700562005 ) ) ;
#65140=CARTESIAN_POINT ( 'NONE',  ( 12.61341903040855783, 0.5949840079737199749, -12.68123264482376555 ) ) ;
#65153=ORIENTED_EDGE ( 'NONE', *, *, #49334, .F. ) ;
#65163=CARTESIAN_POINT ( 'NONE',  ( 17.82373361328021488, 1.839709763185447988, -13.87859827090101028 ) ) ;
#65166=EDGE_CURVE ( 'NONE', #24800, #38239, #32266, .T. ) ;
#65173=ORIENTED_EDGE ( 'NONE', *, *, #26072, .F. ) ;
#65179=CARTESIAN_POINT ( 'NONE',  ( 17.85722199349619643, -1.826245811740498270, -12.46695042358089012 ) ) ;
#65191=CARTESIAN_POINT ( 'NONE',  ( 12.43914160838490623, 1.887194142572508282, -13.87222517180307868 ) ) ;
#65194=CARTESIAN_POINT ( 'NONE',  ( 18.22055847946775131, -0.2899337805559755732, 13.99700184298317041 ) ) ;
#65200=CARTESIAN_POINT ( 'NONE',  ( 12.32101708573729226, -0.3953980351163901563, 13.89243073565879172 ) ) ;
#65203=CARTESIAN_POINT ( 'NONE',  ( 12.33180813479863502, -0.4082709497318060543, -13.89192968283203200 ) ) ;
#65214=CARTESIAN_POINT ( 'NONE',  ( 17.59617179617751503, -0.6239794389693676946, 12.67935706666152740 ) ) ;
#65217=EDGE_CURVE ( 'NONE', #34701, #42176, #1748, .T. ) ;
#65218=CARTESIAN_POINT ( 'NONE',  ( 17.92143259511168552, -3.006721712955584991, -12.31894844866650551 ) ) ;
#65232=CARTESIAN_POINT ( 'NONE',  ( 12.08233499759479912, 0.05827135643914355123, -12.59987075990256855 ) ) ;
#65234=CARTESIAN_POINT ( 'NONE',  ( 18.14576286523417892, 2.898275280820967748, -12.26215340014708488 ) ) ;
#65243=CARTESIAN_POINT ( 'NONE',  ( 12.80505043854143388, 1.836970230372604318, 12.54239289408378255 ) ) ;
#65244=VERTEX_POINT ( 'NONE', #55930 ) ;
#65248=DIRECTION ( 'NONE',  ( -0.000000000000000000, -0.000000000000000000, 1.000000000000000000 ) ) ;
#65250=CARTESIAN_POINT ( 'NONE',  ( 18.11587426570509862, -0.2766185922798718999, -13.89631150889695732 ) ) ;
#65253=EDGE_CURVE ( 'NONE', #47064, #62822, #44416, .T. ) ;
#65256=CARTESIAN_POINT ( 'NONE',  ( 4.600000127571202135, 3.375077994860000042E-14, 1.048050535245999973E-13 ) ) ;
#65262=CARTESIAN_POINT ( 'NONE',  ( 12.54566616139125834, -3.068981097034638950, -13.53612220331446281 ) ) ;
#65267=CARTESIAN_POINT ( 'NONE',  ( 12.69127452969531156, -1.885356761727419839, -12.57371515106196114 ) ) ;
#65273=FACE_OUTER_BOUND ( 'NONE', #16154, .T. ) ;
#65274=CARTESIAN_POINT ( 'NONE',  ( 17.74533816909192296, -1.785653880132711535, 12.47283005504979059 ) ) ;
#65288=EDGE_LOOP ( 'NONE', ( #38642, #3086, #13297, #47119 ) ) ;
#65291=FACE_BOUND ( 'NONE', #21813, .T. ) ;
#65292=CARTESIAN_POINT ( 'NONE',  ( 12.80505043854144276, -0.6564304467897706941, -12.64601024127358286 ) ) ;
#65305=CARTESIAN_POINT ( 'NONE',  ( 18.11617320663394892, 2.776000138870930556, 13.61099849375432491 ) ) ;
#65316=CARTESIAN_POINT ( 'NONE',  ( 17.65134488495972676, -1.793858269351544132, -13.88459860980089644 ) ) ;
#65322=DIRECTION ( 'NONE',  ( -1.000000000000000000, 0.000000000000000000, 0.000000000000000000 ) ) ;
#65338=CARTESIAN_POINT ( 'NONE',  ( 12.11828080172247724, 2.711598415135494378, -12.30476978351483375 ) ) ;
#65348=CARTESIAN_POINT ( 'NONE',  ( 12.63902032760546668, -3.180686373181428106, -12.19193352998605029 ) ) ;
#65356=CARTESIAN_POINT ( 'NONE',  ( 18.10875687686965563, -0.2899325138666228319, -12.69554708236672980 ) ) ;
#65357=CARTESIAN_POINT ( 'NONE',  ( 12.21825390184417159, 2.283832253973942183, -12.49935200980489114 ) ) ;
#65366=CARTESIAN_POINT ( 'NONE',  ( 18.04847759739541857, 3.007479059277873734, 12.23581163759356194 ) ) ;
#65370=CARTESIAN_POINT ( 'NONE',  ( 12.43982406840033050, 0.6284010951863483463, -12.58437167746805940 ) ) ;
#65372=CARTESIAN_POINT ( 'NONE',  ( 12.09524978539964479, -2.332501710336877920, 12.38222815831571566 ) ) ;
#65378=CARTESIAN_POINT ( 'NONE',  ( 12.09634453438821566, 0.1521017209118858404, 12.59908727444664045 ) ) ;
#65382=CARTESIAN_POINT ( 'NONE',  ( 12.44743307598044879, 3.012678875451596738, 12.31720924913609849 ) ) ;
#65383=ORIENTED_EDGE ( 'NONE', *, *, #40361, .F. ) ;
#65395=DIRECTION ( 'NONE',  ( -1.000000000000000000, 0.000000000000000000, 0.000000000000000000 ) ) ;
#65400=CARTESIAN_POINT ( 'NONE',  ( 12.68500746440623317, -1.797494983113976152, 13.88412888179957427 ) ) ;
#65402=CARTESIAN_POINT ( 'NONE',  ( 12.80505043854143388, 1.787797342887042840, 13.88538010501570774 ) ) ;
#65419=ADVANCED_FACE ( 'NONE', ( #19894 ), #58468, .F. ) ;
#65420=CARTESIAN_POINT ( 'NONE',  ( 12.21329150903074101, -2.701250043963952852, 12.40242623241618958 ) ) ;
#65425=CARTESIAN_POINT ( 'NONE',  ( 18.17249645628719534, -2.401006805677767808, 13.69397427989632909 ) ) ;
#65438=EDGE_LOOP ( 'NONE', ( #48808, #29534, #62471, #67037, #13859 ) ) ;
#65441=VECTOR ( 'NONE', #23797, 1000.000000000000000 ) ;
#65445=CARTESIAN_POINT ( 'NONE',  ( 17.60412247569231425, -3.248108758003541485, -13.61799506159942474 ) ) ;
#65450=CARTESIAN_POINT ( 'NONE',  ( 12.66207816929884444, 1.891226320509242553, 13.78383611977690570 ) ) ;
#65453=CARTESIAN_POINT ( 'NONE',  ( 12.25919481816070267, 0.4811670829680709249, 13.99174107639406017 ) ) ;
#65495=CARTESIAN_POINT ( 'NONE',  ( 5.700000000000000178, -11.06886219213000011, -1.536526853569999851 ) ) ;
#65498=CARTESIAN_POINT ( 'NONE',  ( 12.66324396017929388, 0.6090406077983142596, -13.88203505342130661 ) ) ;
#65505=EDGE_LOOP ( 'NONE', ( #12151, #51357, #52435, #68391 ) ) ;
#65508=CARTESIAN_POINT ( 'NONE',  ( 18.14140153244917286, 2.282676164818131515, -13.71717056020690606 ) ) ;
#65515=CARTESIAN_POINT ( 'NONE',  ( 17.89454609197015600, 0.5248351044407618682, -12.68540052859646217 ) ) ;
#65519=CARTESIAN_POINT ( 'NONE',  ( 18.17514039570439977, -2.578830837888117067, -13.65637626283699113 ) ) ;
#65527=CARTESIAN_POINT ( 'NONE',  ( 18.15405049586277997, -2.074720874654904623, -12.42801810613654823 ) ) ;
#65541=VECTOR ( 'NONE', #29231, 1000.000000000000000 ) ;
#65542=CARTESIAN_POINT ( 'NONE',  ( 12.21305109721488869, 2.701423549395648216, -13.62869161905334359 ) ) ;
#65545=CARTESIAN_POINT ( 'NONE',  ( 17.91054527438922861, 0.5141525164327357400, 13.88720023103246248 ) ) ;
#65546=CARTESIAN_POINT ( 'NONE',  ( 17.94896392900171733, 0.4852513397891488056, 13.88859817538062558 ) ) ;
#65552=CARTESIAN_POINT ( 'NONE',  ( 12.19590749973210286, -0.1412517843910542081, 13.89905214520371679 ) ) ;
#65553=CARTESIAN_POINT ( 'NONE',  ( 12.24303834290234505, -0.2736100115472018257, -13.89637849652428514 ) ) ;
#65565=CARTESIAN_POINT ( 'NONE',  ( 17.75635104740699077, 0.5917829749564882391, 12.68143435689271037 ) ) ;
#65573=CARTESIAN_POINT ( 'NONE',  ( 12.60210251410538618, -1.908512130997220835, 13.78126077419328510 ) ) ;
#65578=DIRECTION ( 'NONE',  ( 0.000000000000000000, 1.000000000000000000, 0.000000000000000000 ) ) ;
#65581=CARTESIAN_POINT ( 'NONE',  ( 12.30074667651849474, -0.5168989769797315281, -12.58939571008426839 ) ) ;
#65598=CARTESIAN_POINT ( 'NONE',  ( 17.91891929415153228, -0.5082612142235584107, -13.88749228919889767 ) ) ;
#65600=DIRECTION ( 'NONE',  ( -0.000000000000000000, -0.000000000000000000, 1.000000000000000000 ) ) ;
#65605=CARTESIAN_POINT ( 'NONE',  ( 18.17230637739242383, -2.598591657424966783, 12.42808133540079574 ) ) ;
#65619=CARTESIAN_POINT ( 'NONE',  ( 17.80580762821595897, -3.072583274995464464, 12.29955455495395888 ) ) ;
#65648=VERTEX_POINT ( 'NONE', #62110 ) ;
#65653=CARTESIAN_POINT ( 'NONE',  ( 17.85704948507091672, 1.853727412078925330, 13.87673533860537667 ) ) ;
#65664=CARTESIAN_POINT ( 'NONE',  ( 17.81289281796191304, -1.835117743393744671, -13.87920855489149474 ) ) ;
#65688=CARTESIAN_POINT ( 'NONE',  ( 12.70853553880217568, 3.193755089013868620, -12.18851650745940240 ) ) ;
#65694=CARTESIAN_POINT ( 'NONE',  ( 18.28019269455628404, -0.1906559479456389483, 14.00000681886698928 ) ) ;
#65696=CARTESIAN_POINT ( 'NONE',  ( 12.25813800312572432, -2.953224329521601188, -12.24903309118795214 ) ) ;
#65703=CARTESIAN_POINT ( 'NONE',  ( 12.29585337184159499, -2.862976231886636302, -13.58970269765488403 ) ) ;
#65704=CARTESIAN_POINT ( 'NONE',  ( 18.01167108103433279, -0.4268810874232039088, -12.69034564040270396 ) ) ;
#65715=CARTESIAN_POINT ( 'NONE',  ( 17.97018005872493518, 2.032669421145251842, 12.54824173908127527 ) ) ;
#65719=CARTESIAN_POINT ( 'NONE',  ( 12.61731147763009631, -0.6963438834283414147, -12.58074676375338896 ) ) ;
#65721=CARTESIAN_POINT ( 'NONE',  ( 12.11689977649202099, -2.253070615825701228, 12.39692697851452330 ) ) ;
#65726=CARTESIAN_POINT ( 'NONE',  ( 12.08965323865565011, 0.1172743548790619733, 12.59945959730644027 ) ) ;
#65730=CARTESIAN_POINT ( 'NONE',  ( 12.63789105315729877, 1.779885672808162678, 12.47365341745800471 ) ) ;
#65745=CARTESIAN_POINT ( 'NONE',  ( 18.02549019388837337, -2.911978589119716077, 13.57741733930972217 ) ) ;
#65747=CARTESIAN_POINT ( 'NONE',  ( 12.11838997910887628, -2.753273141185784478, 13.72661716423429112 ) ) ;
#65753=EDGE_CURVE ( 'NONE', #12380, #62494, #64736, .T. ) ;
#65755=CARTESIAN_POINT ( 'NONE',  ( 17.87143624835593059, 1.954798354056923371, -13.77413458888036679 ) ) ;
#65759=FACE_OUTER_BOUND ( 'NONE', #22176, .T. ) ;
#65765=CARTESIAN_POINT ( 'NONE',  ( 18.00096209670562786, -0.5835546240610994806, -13.98799446466780694 ) ) ;
#65768=ORIENTED_EDGE ( 'NONE', *, *, #21703, .F. ) ;
#65770=ORIENTED_EDGE ( 'NONE', *, *, #61365, .F. ) ;
#65771=CARTESIAN_POINT ( 'NONE',  ( 18.12605992003771505, -2.245077608621426357, 13.72424617901693189 ) ) ;
#65773=ORIENTED_EDGE ( 'NONE', *, *, #32996, .F. ) ;
#65789=CARTESIAN_POINT ( 'NONE',  ( 18.20500217910819885, -2.141655701387318977, -13.83591107703642997 ) ) ;
#65793=CARTESIAN_POINT ( 'NONE',  ( 12.44718984625868430, 1.987489649616605236, 13.76884489496294961 ) ) ;
#65794=B_SPLINE_SURFACE_WITH_KNOTS ( 'NONE', 1, 3, ( 
 ( #10444, #46831, #10106, #31784, #31440, #63583, #53102, #36336, #31106, #3818, #5202, #25156, #52411, #46489, #67795, #41240, #35990, #38748, #21965, #32137, #12179, #11473, #33161, #43304, #32473, #59373, #54478, #17063, #6924, #60075, #32813, #64264, #5884, #38395, #16718, #16379, #37709, #59037, #54130, #11138, #1000, #53788, #64611, #27225, #54825, #48895, #38047, #48548, #42956, #22312, #27919, #304, #65305, #43654, #59720, #652, #27567, #33509, #11822, #6579, #49229, #6227, #28258, #17420, #64948, #1338, #22653, #43998, #49576, #21283, #42615, #63923, #16034, #37364, #58686, #10790, #53448, #5545, #26885, #48200, #21621, #12874, #23358, #29658, #60757, #8652 ),
 ( #24043, #34200, #40460, #23699, #18118, #34890, #39093, #66338, #1686, #65653, #45034, #18462, #29306, #67028, #19139, #7972, #50618, #60418, #18809, #2038, #45378, #56205, #40136, #30000, #61450, #7273, #12523, #23003, #44352, #66688, #33854, #50959, #61790, #13906, #13568, #17775, #8312, #55170, #49927, #39787, #55519, #39437, #44697, #3057, #28613, #7621, #2719, #65993, #28967, #24390, #50274, #2376, #56546, #45719, #61107, #13227, #35234, #34554, #55864, #46060, #68743, #68393, #4425, #20860, #67705, #30668, #58262, #4767, #52330, #20169, #25416, #19488, #57570, #41497, #42198, #51976, #62129, #63498, #62810, #63148, #4080, #62469, #14927, #15275, #47093, #36948 ) ),
 .UNSPECIFIED., .F., .F., .F.,
 ( 2, 2 ),
 ( 4, 2, 2, 2, 2, 2, 2, 2, 2, 2, 2, 2, 2, 2, 2, 2, 2, 2, 2, 2, 2, 2, 2, 2, 2, 2, 2, 2, 2, 2, 2, 2, 2, 2, 2, 2, 2, 2, 2, 2, 2, 2, 4 ),
 ( 0.000000000000000000, 1.000000000000000000 ),
 ( 0.000000000000000000, 7.142680049747104757E-05, 0.0001428536009949420951, 0.0002142804014924131427, 0.0002857072019898841903, 0.0003571340024873552108, 0.0004285608029848262854, 0.0004999876034822973601, 0.0005357010037310328161, 0.0005714144039797683806, 0.0006071278042285039450, 0.0006428412044772394010, 0.0007142680049747104215, 0.0007856948054721815504, 0.0008214082057209171148, 0.0008571216059696525709, 0.0008928350062183880269, 0.0009285484064671235913, 0.0009999752069645947202, 0.001071402007462065632, 0.001142828807959536761, 0.001214255608457007890, 0.001285682408954478802, 0.001321395809203214367, 0.001357109209451949714, 0.001428536009949420843, 0.001499962810446891972, 0.001535676210695627536, 0.001571389610944363101, 0.001607103011193098665, 0.001642816411441834230, 0.001714243211939305142, 0.001785670012436776054, 0.001821383412685511618, 0.001857096812934247183, 0.001928523613431718312, 0.001964237013680454093, 0.001999950413929189440, 0.002035663814177924788, 0.002071377214426660569, 0.002142804014924131265, 0.002214230815421602393, 0.002285657615919073522 ),
 .UNSPECIFIED. ) ;
#65798=CARTESIAN_POINT ( 'NONE',  ( 12.11827043973743301, 0.2342631834278612046, 13.99804438501501203 ) ) ;
#65842=CARTESIAN_POINT ( 'NONE',  ( 12.20341915910182351, 2.330389505238763093, -13.70797212924216701 ) ) ;
#65844=CARTESIAN_POINT ( 'NONE',  ( 12.15805955570366592, 2.854826764633444203, 12.27308055910813600 ) ) ;
#65847=CARTESIAN_POINT ( 'NONE',  ( 12.08004253349364454, -0.01140630886273803594, -14.00000041621361291 ) ) ;
#65851=CARTESIAN_POINT ( 'NONE',  ( 4.599999999999999645, -3.199751711897561357, 12.18694338143115452 ) ) ;
#65856=CARTESIAN_POINT ( 'NONE',  ( 18.07092639204458706, 2.147008627175521323, -13.74201915664823659 ) ) ;
#65863=CARTESIAN_POINT ( 'NONE',  ( 18.02801395604344847, 0.4085932599149181832, -12.69115266610270254 ) ) ;
#65867=CARTESIAN_POINT ( 'NONE',  ( 18.06394506373647602, -2.862992422157873751, -13.58968849268030965 ) ) ;
#65868=CARTESIAN_POINT ( 'NONE',  ( 7.100000000000000533, 12.50865771883999855, -2.924687089724999911 ) ) ;
#65873=CARTESIAN_POINT ( 'NONE',  ( 18.10980516112012495, -2.943705546998118816, -12.25131356140272132 ) ) ;
#65885=CARTESIAN_POINT ( 'NONE',  ( 12.44779487374910332, 3.012931620461074100, -13.55119122998581460 ) ) ;
#65888=CARTESIAN_POINT ( 'NONE',  ( 17.72054635526678013, -0.7113363331415086810, 13.98191770012929780 ) ) ;
#65893=CARTESIAN_POINT ( 'NONE',  ( 12.37275480852669318, -0.4515881961619166440, 13.89013012615365028 ) ) ;
#65894=CARTESIAN_POINT ( 'NONE',  ( 12.61467092246319055, -0.5953860544347909789, -13.88283270324647845 ) ) ;
#65895=LINE ( 'NONE', #28516, #31472 ) ;
#65897=EDGE_CURVE ( 'NONE', #48158, #4266, #17198, .T. ) ;
#65903=FACE_OUTER_BOUND ( 'NONE', #2316, .T. ) ;
#65906=CARTESIAN_POINT ( 'NONE',  ( 12.71012435279160435, -0.7254930141058675286, 13.98119259374225365 ) ) ;
#65910=CARTESIAN_POINT ( 'NONE',  ( 17.98440366585430539, -2.954302470114323675, -12.33403020158385743 ) ) ;
#65913=CARTESIAN_POINT ( 'NONE',  ( 12.43656315535333867, -1.853531805844372604, -12.46297683056140926 ) ) ;
#65922=CARTESIAN_POINT ( 'NONE',  ( 12.08961557973414358, 0.1170514037749880998, -12.59946170170351465 ) ) ;
#65923=DIRECTION ( 'NONE',  ( 0.000000000000000000, -1.000000000000000000, 0.000000000000000000 ) ) ;
#65938=CARTESIAN_POINT ( 'NONE',  ( 17.86760510161943927, -0.5416168188285630514, -13.88579828294357554 ) ) ;
#65955=CARTESIAN_POINT ( 'NONE',  ( 4.599999999999999645, 3.125000000000000000, -13.52084414783465682 ) ) ;
#65961=CARTESIAN_POINT ( 'NONE',  ( 17.55505043854147118, -3.125000000000000000, 12.28374638332999780 ) ) ;
#65993=CARTESIAN_POINT ( 'NONE',  ( 18.25518009351764093, 2.707823354518788417, 13.73564093574334244 ) ) ;
#66006=CARTESIAN_POINT ( 'NONE',  ( 17.88835954937810158, -3.166508787604182196, -13.63720117115729558 ) ) ;
#66028=CARTESIAN_POINT ( 'NONE',  ( 12.58267958641583739, 1.915804698272715489, -12.56868422206431113 ) ) ;
#66038=CARTESIAN_POINT ( 'NONE',  ( 12.54683914358776597, -1.807964460291309861, -12.46961431371563300 ) ) ;
#66045=CARTESIAN_POINT ( 'NONE',  ( 12.21287994455109605, -2.700912243963290660, -13.62875716402589887 ) ) ;
#66047=CARTESIAN_POINT ( 'NONE',  ( 18.11564574962620000, 0.2765170649790828494, -12.69595318831094666 ) ) ;
#66055=( NAMED_UNIT ( * ) PLANE_ANGLE_UNIT ( ) SI_UNIT ( $, .RADIAN. ) );
#66059=CARTESIAN_POINT ( 'NONE',  ( 18.09858302120873574, 2.191289104517298636, 12.51814558466706195 ) ) ;
#66060=AXIS2_PLACEMENT_3D ( 'NONE', #54618, #33993, #29104 ) ;
#66066=CARTESIAN_POINT ( 'NONE',  ( 12.20998423544387457, -2.691370015539682914, 12.40494896326797658 ) ) ;
#66071=CARTESIAN_POINT ( 'NONE',  ( 12.75722706473759693, -0.7178228174669247785, 12.57953618971562548 ) ) ;
#66074=CARTESIAN_POINT ( 'NONE',  ( 12.55381283423606043, 1.927626388171776783, 12.56664888159295934 ) ) ;
#66087=CARTESIAN_POINT ( 'NONE',  ( 17.80428133516622680, -0.5732558493148650625, -12.68257967785424967 ) ) ;
#66090=CARTESIAN_POINT ( 'NONE',  ( 17.75978284916825345, -3.091857219538878709, 13.52996931830918825 ) ) ;
#66102=CARTESIAN_POINT ( 'NONE',  ( 17.59562484692321149, -0.6250000000000004441, 13.88107975066923494 ) ) ;
#66111=DIRECTION ( 'NONE',  ( 1.000000000000000000, 0.000000000000000000, 0.000000000000000000 ) ) ;
#66114=CARTESIAN_POINT ( 'NONE',  ( 12.33505003437499958, -2.912475392678309571, 12.34587402705970405 ) ) ;
#66115=ORIENTED_EDGE ( 'NONE', *, *, #7227, .F. ) ;
#66119=CARTESIAN_POINT ( 'NONE',  ( 17.83374359992753000, -3.059519611938945172, 13.53873550554769878 ) ) ;
#66123=FACE_OUTER_BOUND ( 'NONE', #41446, .T. ) ;
#66144=CARTESIAN_POINT ( 'NONE',  ( 12.78422741110790284, 1.875000586273901426, 13.78627160872174251 ) ) ;
#66148=CARTESIAN_POINT ( 'NONE',  ( 12.17676779642100371, 0.3651687365794410445, 13.99525266148724256 ) ) ;
#66192=CARTESIAN_POINT ( 'NONE',  ( 12.49249577546344625, 0.5416168188285649387, -13.88579828294357554 ) ) ;
#66193=DIRECTION ( 'NONE',  ( -1.000000000000000000, -1.776356839400000238E-14, 0.000000000000000000 ) ) ;
#66197=CARTESIAN_POINT ( 'NONE',  ( 5.563312991732289881, 12.16892724394992875, -3.760371626685871771 ) ) ;
#66200=CARTESIAN_POINT ( 'NONE',  ( 17.99219435089537811, 2.053195051521780723, -13.75813171417237868 ) ) ;
#66206=CARTESIAN_POINT ( 'NONE',  ( 17.74403704562415740, 1.812651413143276713, -13.88215924362446074 ) ) ;
#66211=EDGE_CURVE ( 'NONE', #13672, #24349, #55601, .T. ) ;
#66213=CARTESIAN_POINT ( 'NONE',  ( 18.08671416527213438, -2.828730077929408893, -13.59817001275034443 ) ) ;
#66221=CARTESIAN_POINT ( 'NONE',  ( 18.13320831056635285, -2.045970293963736975, -12.43278322311362238 ) ) ;
#66234=CARTESIAN_POINT ( 'NONE',  ( 12.27426597077010051, 3.015840035300827893, -13.67132055224443477 ) ) ;
#66239=CARTESIAN_POINT ( 'NONE',  ( 17.87656099625190009, -0.6549277419692610680, 13.98467727287826889 ) ) ;
#66244=CARTESIAN_POINT ( 'NONE',  ( 12.64261640812602039, -0.6049408601398774676, 13.88227884472451557 ) ) ;
#66245=CARTESIAN_POINT ( 'NONE',  ( 12.20071655346993111, -2.340273578591448356, 13.70604138523078142 ) ) ;
#66257=CARTESIAN_POINT ( 'NONE',  ( 12.29147016622806809, -0.3563519072604388049, 12.69327554148123660 ) ) ;
#66258=CARTESIAN_POINT ( 'NONE',  ( 18.15919311585273377, -2.661142132628769641, -12.41257606618384557 ) ) ;
#66259=EDGE_LOOP ( 'NONE', ( #58074, #20111, #53389 ) ) ;
#66265=B_SPLINE_CURVE_WITH_KNOTS ( 'NONE', 3,
 ( #27985, #44762, #55589, #65719, #18529, #50342, #23425, #45101, #22721, #66410, #49997, #49294, #65370, #7336, #39856, #13296 ),
 .UNSPECIFIED., .F., .F.,
 ( 4, 2, 2, 2, 2, 2, 2, 4 ),
 ( 0.000000000000000000, 0.06249999999999904243, 0.1249999999999980849, 0.2499999999999983347, 0.4999999999999988898, 0.7499999999999993339, 0.8749999999999996669, 1.000000000000000000 ),
 .UNSPECIFIED. ) ;
#66270=CARTESIAN_POINT ( 'NONE',  ( 12.22921692136009320, 0.4376617689587208315, -12.59240970319242514 ) ) ;
#66286=CARTESIAN_POINT ( 'NONE',  ( 18.27393099755801487, -0.09542514088231193736, -13.99967976774382272 ) ) ;
#66290=PLANE ( 'NONE',  #20325 ) ;
#66295=EDGE_CURVE ( 'NONE', #11762, #33164, #51214, .T. ) ;
#66300=CARTESIAN_POINT ( 'NONE',  ( 12.75598008708079512, -3.248071441111094693, 13.61800396221869391 ) ) ;
#66303=CONICAL_SURFACE ( 'NONE', #59618, 13.94999927503000059, 0.7853981058017837080 ) ;
#66305=DIRECTION ( 'NONE',  ( -1.000000000000000000, 5.085933197601780420E-15, -5.275114267344730344E-15 ) ) ;
#66308=CARTESIAN_POINT ( 'NONE',  ( 12.20981157025896735, -0.1908382484571562454, -13.89824168789394854 ) ) ;
#66309=CARTESIAN_POINT ( 'NONE',  ( 17.96930180488791606, -2.968443477542578979, 12.33001868694671010 ) ) ;
#66313=CARTESIAN_POINT ( 'NONE',  ( 17.72017830080754663, 1.875000000000000000, 13.78627079974493164 ) ) ;
#66332=CARTESIAN_POINT ( 'NONE',  ( 18.13005353941770181, -0.4382646521645844340, 12.59237917444261434 ) ) ;
#66338=CARTESIAN_POINT ( 'NONE',  ( 17.79045811871160865, 1.826948899878884314, 13.88028486463507249 ) ) ;
#66344=VECTOR ( 'NONE', #20540, 1000.000000000000000 ) ;
#66364=ORIENTED_EDGE ( 'NONE', *, *, #41136, .F. ) ;
#66374=CARTESIAN_POINT ( 'NONE',  ( 12.66183496498643635, 1.891282299343450379, -12.57277654391869071 ) ) ;
#66384=CARTESIAN_POINT ( 'NONE',  ( 17.64997652428802510, 0.7254930141063502536, 13.98119259374222700 ) ) ;
#66385=VERTEX_POINT ( 'NONE', #16205 ) ;
#66387=CARTESIAN_POINT ( 'NONE',  ( 12.56929374240178987, -1.799893664886396349, -12.47078182885977604 ) ) ;
#66393=CARTESIAN_POINT ( 'NONE',  ( 12.18091821863274049, -2.461361028094613435, -13.68154568029715179 ) ) ;
#66394=CARTESIAN_POINT ( 'NONE',  ( 18.05145864173985260, -0.3802890292809140704, -12.69234946364261241 ) ) ;
#66406=CARTESIAN_POINT ( 'NONE',  ( 17.71825832218063468, 1.896331189961580455, 12.57190091395960607 ) ) ;
#66410=CARTESIAN_POINT ( 'NONE',  ( 12.07990771228650750, 0.1878083608151937256, -12.60000737103648660 ) ) ;
#66412=CARTESIAN_POINT ( 'NONE',  ( 12.22227632225713734, -2.273941840405719006, 12.50139599066422846 ) ) ;
#66417=CARTESIAN_POINT ( 'NONE',  ( 12.39285676950935766, 0.4699213205053948128, 12.68829855189361844 ) ) ;
#66421=CARTESIAN_POINT ( 'NONE',  ( 12.18001225342674232, 2.492635468222105022, 12.45327835951381168 ) ) ;
#66432=CARTESIAN_POINT ( 'NONE',  ( 18.05193840052253407, -0.3791517837728508589, -12.69238281682625136 ) ) ;
#66435=CARTESIAN_POINT ( 'NONE',  ( 17.93700172732586395, -2.995132885274008228, 13.55589876081949186 ) ) ;
#66439=CARTESIAN_POINT ( 'NONE',  ( 17.65854462812411185, -1.883284865257428775, -13.78503182716600683 ) ) ;
#66447=CARTESIAN_POINT ( 'NONE',  ( 18.05387017991211707, 2.121311586892751677, -13.74657283404811992 ) ) ;
#66448=LINE ( 'NONE', #24498, #59355 ) ;
#66458=DIRECTION ( 'NONE',  ( -1.000000000000000000, 0.000000000000000000, 0.000000000000000000 ) ) ;
#66460=CARTESIAN_POINT ( 'NONE',  ( 12.42339251327461369, -2.995356603774978144, 12.32227076303473368 ) ) ;
#66463=CARTESIAN_POINT ( 'NONE',  ( 18.27395862148971162, -2.614931059283422954, 13.75364391642198747 ) ) ;
#66470=FACE_OUTER_BOUND ( 'NONE', #28294, .T. ) ;
#66485=CARTESIAN_POINT ( 'NONE',  ( 12.56988000877536749, 3.209076157321550049, 13.62724777954567656 ) ) ;
#66490=CARTESIAN_POINT ( 'NONE',  ( 12.38195926868453789, 0.4608195498121803735, -12.68876479732302265 ) ) ;
#66491=CARTESIAN_POINT ( 'NONE',  ( 12.12622056954396221, 0.2566959043864855405, 13.99765098363215365 ) ) ;
#66494=CARTESIAN_POINT ( 'NONE',  ( 12.80505043854144276, -0.7192913403693027563, 12.57945229203838267 ) ) ;
#66502=DIRECTION ( 'NONE',  ( 0.000000000000000000, -0.000000000000000000, 1.000000000000000000 ) ) ;
#66503=CARTESIAN_POINT ( 'NONE',  ( 12.40985643288212614, 3.083578315866612574, 12.21685683184790783 ) ) ;
#66519=CARTESIAN_POINT ( 'NONE',  ( 12.42368232297765829, 2.995580128734607328, 13.55572452362623714 ) ) ;
#66521=ORIENTED_EDGE ( 'NONE', *, *, #42230, .F. ) ;
#66526=CARTESIAN_POINT ( 'NONE',  ( 18.14791645918231566, 2.065340611094592216, -12.42959220787597197 ) ) ;
#66531=DIRECTION ( 'NONE',  ( 0.7071074108313172291, -0.7071061515412171428, 4.731348483750111872E-09 ) ) ;
#66536=CARTESIAN_POINT ( 'NONE',  ( 12.30894494036361309, -0.5330308249010426991, -13.98985951701901698 ) ) ;
#66544=CIRCLE ( 'NONE', #8512, 12.59999999999999964 ) ;
#66546=CARTESIAN_POINT ( 'NONE',  ( 18.08776130068894972, 2.172968270232229937, -13.73740491327006552 ) ) ;
#66550=VECTOR ( 'NONE', #19537, 1000.000000000000000 ) ;
#66555=DIRECTION ( 'NONE',  ( 1.000000000000000000, 0.000000000000000000, 0.000000000000000000 ) ) ;
#66556=ORIENTED_EDGE ( 'NONE', *, *, #558, .T. ) ;
#66558=CARTESIAN_POINT ( 'NONE',  ( 17.83309906208979001, -3.060119824108007425, -13.53852211359039792 ) ) ;
#66565=CARTESIAN_POINT ( 'NONE',  ( 18.26132062505690712, -2.644858796842617821, -12.31930452622237127 ) ) ;
#66577=CARTESIAN_POINT ( 'NONE',  ( 12.24916914324843376, 2.049138926831458818, -13.84922804760273607 ) ) ;
#66581=CARTESIAN_POINT ( 'NONE',  ( 18.20553441509223802, -0.3226776716457260274, 13.99628514671256241 ) ) ;
#66582=VECTOR ( 'NONE', #67654, 1000.000000000000000 ) ;
#66588=CARTESIAN_POINT ( 'NONE',  ( 12.33198418666045626, -2.089544947732335789, 13.75203186102260311 ) ) ;
#66596=ORIENTED_EDGE ( 'NONE', *, *, #26750, .T. ) ;
#66601=CARTESIAN_POINT ( 'NONE',  ( 12.26182617418671938, -0.3097617571853261698, 12.69493148512415637 ) ) ;
#66615=CARTESIAN_POINT ( 'NONE',  ( 12.29127437512780219, -0.3560396104572045028, -12.69328656575056691 ) ) ;
#66635=AXIS2_PLACEMENT_3D ( 'NONE', #31484, #42328, #63630 ) ;
#66636=CARTESIAN_POINT ( 'NONE',  ( 18.08498662421418857, 0.4989076128645600350, -13.99111800451625243 ) ) ;
#66637=ORIENTED_EDGE ( 'NONE', *, *, #9919, .F. ) ;
#66645=CARTESIAN_POINT ( 'NONE',  ( 12.64199182499459262, -3.104696382831371615, -13.52638422211150093 ) ) ;
#66649=CARTESIAN_POINT ( 'NONE',  ( 12.35713445931583010, -3.099811329677685467, 13.65268841750260620 ) ) ;
#66650=ORIENTED_EDGE ( 'NONE', *, *, #57826, .T. ) ;
#66657=CARTESIAN_POINT ( 'NONE',  ( 12.24422661137779045, 0.2766185922798737873, -13.89631150889695732 ) ) ;
#66658=CARTESIAN_POINT ( 'NONE',  ( 18.00740283128408947, -2.068595914410284120, 12.54170588102538275 ) ) ;
#66679=CARTESIAN_POINT ( 'NONE',  ( 18.01033200807250978, -0.5598083480993575334, 12.58755849294668394 ) ) ;
#66688=CARTESIAN_POINT ( 'NONE',  ( 18.21732822554148257, 2.220719680094977555, 13.82275391900495798 ) ) ;
#66715=VERTEX_POINT ( 'NONE', #56727 ) ;
#66716=EDGE_CURVE ( 'NONE', #6955, #52670, #67885, .T. ) ;
#66718=VERTEX_POINT ( 'NONE', #57736 ) ;
#66723=CARTESIAN_POINT ( 'NONE',  ( 12.19628620791406348, 2.642962752853494024, -12.41715721841834608 ) ) ;
#66726=ORIENTED_EDGE ( 'NONE', *, *, #489, .F. ) ;
#66730=CARTESIAN_POINT ( 'NONE',  ( 12.80505043854146940, -3.125000000000000000, -13.52078605991414761 ) ) ;
#66732=CARTESIAN_POINT ( 'NONE',  ( 12.08558010717403164, -2.390021230702592092, -12.37125449870878846 ) ) ;
#66736=LINE ( 'NONE', #69140, #11449 ) ;
#66743=CARTESIAN_POINT ( 'NONE',  ( 17.55505043854147118, -3.199751711897561801, 12.18694338143115452 ) ) ;
#66749=CARTESIAN_POINT ( 'NONE',  ( 17.55505043854144276, -0.7302158263239199032, -13.98094363220830871 ) ) ;
#66752=CARTESIAN_POINT ( 'NONE',  ( 17.81550493765275789, 1.931762299006052119, 12.56594712229140498 ) ) ;
#66759=CARTESIAN_POINT ( 'NONE',  ( 12.80505043854146940, -3.199751711897561801, 12.18694338143115452 ) ) ;
#66762=CARTESIAN_POINT ( 'NONE',  ( 21.49999863197000138, 0.000000000000000000, 0.000000000000000000 ) ) ;
#66766=CARTESIAN_POINT ( 'NONE',  ( 12.78440276244763041, 0.6249994333735301444, 12.67928921956170996 ) ) ;
#66769=CARTESIAN_POINT ( 'NONE',  ( 12.54434846374635626, 1.931873423426545777, 12.56592826555434073 ) ) ;
#66783=CARTESIAN_POINT ( 'NONE',  ( 18.16417820190392618, -0.1413121815030540240, -12.69896133444535735 ) ) ;
#66789=CARTESIAN_POINT ( 'NONE',  ( 17.71877800696621108, -1.896477791912290822, -13.78304299653506959 ) ) ;
#66791=LINE ( 'NONE', #33951, #34415 ) ;
#66796=CARTESIAN_POINT ( 'NONE',  ( 18.14066966380178769, 2.280775195392830579, -13.71753029190285389 ) ) ;
#66800=ORIENTED_EDGE ( 'NONE', *, *, #14161, .T. ) ;
#66814=CARTESIAN_POINT ( 'NONE',  ( 17.74765434492531213, -1.905326452124538550, 13.78174529102851587 ) ) ;
#66825=CARTESIAN_POINT ( 'NONE',  ( 18.08442823429788504, 0.4920215530101138546, -12.59040071882420797 ) ) ;
#66835=CARTESIAN_POINT ( 'NONE',  ( 12.17999522571488846, 2.481546339243234200, 13.67732359575999368 ) ) ;
#66839=CARTESIAN_POINT ( 'NONE',  ( 12.32623905011267240, 0.4017251370869492910, -12.69144801866011640 ) ) ;
#66840=CARTESIAN_POINT ( 'NONE',  ( 12.54683519492311916, -0.5695321295966300212, 13.88429381145915720 ) ) ;
#66846=B_SPLINE_CURVE_WITH_KNOTS ( 'NONE', 3,
 ( #27840, #1256, #60333, #28174, #18720, #55781, #7193, #39354, #33771, #65218, #28884, #12439, #40055, #65910, #59981, #33076, #54390, #6493, #7886, #1952, #60675, #55086, #44954, #34118, #28529, #54741, #34470, #49145, #23274, #55436, #12093, #18379, #49490, #22571, #50193, #2293, #66258, #39701, #43914, #17333, #38662, #1601, #19748, #41070, #9585, #29575, #20427, #35151, #40381, #62390, #56814, #62721, #66944 ),
 .UNSPECIFIED., .F., .F.,
 ( 4, 2, 2, 2, 2, 2, 2, 2, 2, 2, 2, 2, 2, 1, 2, 2, 2, 2, 2, 2, 2, 2, 2, 2, 1, 1, 2, 4 ),
 ( 0.000000000000000000, 0.06264497286387624153, 0.1252899457277524831, 0.1566124321596882862, 0.1879349185916240339, 0.2192574050235598371, 0.2349186482395275166, 0.2505798914554951962, 0.2819023778874309438, 0.2975636211033985679, 0.3132248643193661919, 0.3288861075353337604, 0.3445473507513013844, 0.3602085939672690640, 0.3680392155752531536, 0.3758698371832371876, 0.3915310803992061439, 0.3993617020071908441, 0.4071923236151755443, 0.4228535668311456663, 0.4306841884391316433, 0.4385148100471176202, 0.4541760532630899072, 0.4698372964790621942, 0.4854985396950344811, 0.4933291613030210687, 0.4972444721070140017, 0.5011597829110069346 ),
 .UNSPECIFIED. ) ;
#66848=CARTESIAN_POINT ( 'NONE',  ( 4.599999999999999645, 0.000000000000000000, 0.000000000000000000 ) ) ;
#66869=ORIENTED_EDGE ( 'NONE', *, *, #52792, .F. ) ;
#66873=CARTESIAN_POINT ( 'NONE',  ( 18.11163387652230483, 2.018964330316874722, -12.43719698804479101 ) ) ;
#66877=AXIS2_PLACEMENT_3D ( 'NONE', #9225, #8896, #24973 ) ;
#66881=CARTESIAN_POINT ( 'NONE',  ( 18.00383897971137515, 1.936685752045136821, -13.86556672038938309 ) ) ;
#66882=CARTESIAN_POINT ( 'NONE',  ( 12.78109998040213213, 0.7302151644511238882, -13.98094363559787467 ) ) ;
#66884=CARTESIAN_POINT ( 'NONE',  ( 18.17891100654625092, -2.457162529596722766, -13.68241659861169701 ) ) ;
#66890=CARTESIAN_POINT ( 'NONE',  ( 18.25550288558782341, 2.707593611552285395, -13.73570038168180218 ) ) ;
#66906=EDGE_LOOP ( 'NONE', ( #42896, #52601, #14935, #39684 ) ) ;
#66908=CARTESIAN_POINT ( 'NONE',  ( 17.72206310054082934, -3.180756431682054242, -12.19191584669666462 ) ) ;
#66920=CARTESIAN_POINT ( 'NONE',  ( 12.53658830138314784, 3.196304600777675642, -13.63024796167575126 ) ) ;
#66924=CARTESIAN_POINT ( 'NONE',  ( 17.85458012075704559, 0.6654101994098620132, 13.98418081573739258 ) ) ;
#66930=CARTESIAN_POINT ( 'NONE',  ( 12.19673284948622793, -2.643529259147591404, 13.64196713071253164 ) ) ;
#66937=CARTESIAN_POINT ( 'NONE',  ( 12.80505043854143388, 3.149899482173124987, 12.25147293255931125 ) ) ;
#66942=CARTESIAN_POINT ( 'NONE',  ( 17.95964167607823470, 0.4764818960106712575, 12.68796903437992540 ) ) ;
#66943=CARTESIAN_POINT ( 'NONE',  ( 12.34510720040652032, -0.4232991628857526445, 12.69050643263297573 ) ) ;
#66944=CARTESIAN_POINT ( 'NONE',  ( 18.18005044388383240, -2.499999700414728743, -12.45156116530568902 ) ) ;
#66957=CARTESIAN_POINT ( 'NONE',  ( 12.64343166449435962, -0.6040886362899388073, -12.68065483099175417 ) ) ;
#66974=CARTESIAN_POINT ( 'NONE',  ( 18.27048575441379796, 0.1188263301541416239, -13.99950072926553979 ) ) ;
#66980=CARTESIAN_POINT ( 'NONE',  ( 18.01273579185514961, -2.926031893951825058, 12.34206213438603150 ) ) ;
#66983=CARTESIAN_POINT ( 'NONE',  ( 12.18211070746583680, -2.551853945028482951, -13.66227842076493104 ) ) ;
#66994=CARTESIAN_POINT ( 'NONE',  ( 12.72272221947698689, -0.6198980793944590673, -13.88138779565238501 ) ) ;
#66995=EDGE_CURVE ( 'NONE', #42472, #62494, #17153, .T. ) ;
#66996=CARTESIAN_POINT ( 'NONE',  ( 18.11762593468203875, -2.227530255644428525, 12.51091528569613409 ) ) ;
#67008=DIRECTION ( 'NONE',  ( 0.000000000000000000, 0.000000000000000000, -1.000000000000000000 ) ) ;
#67022=CARTESIAN_POINT ( 'NONE',  ( 17.99148514253576892, -0.5743932053697962115, 12.58690132123599525 ) ) ;
#67028=CARTESIAN_POINT ( 'NONE',  ( 17.98066499537650742, 1.926393605117485919, 13.86683778668631462 ) ) ;
#67030=CARTESIAN_POINT ( 'NONE',  ( 4.599999999999999645, 1.787816316115923509, -13.88537766212462898 ) ) ;
#67037=ORIENTED_EDGE ( 'NONE', *, *, #40361, .T. ) ;
#67039=CARTESIAN_POINT ( 'NONE',  ( 18.12392562323104173, -2.970749524062575642, -13.68118179967287951 ) ) ;
#67062=CARTESIAN_POINT ( 'NONE',  ( 12.23374516775628784, 2.245741837849041911, -12.50722324768529781 ) ) ;
#67068=LINE ( 'NONE', #66730, #39113 ) ;
#67069=ORIENTED_EDGE ( 'NONE', *, *, #46319, .T. ) ;
#67070=CARTESIAN_POINT ( 'NONE',  ( 12.11312973616749034, -2.264845417406519346, -12.39478132878350358 ) ) ;
#67076=CARTESIAN_POINT ( 'NONE',  ( 12.75679378108278961, -3.246933784478224450, -13.61827548339043403 ) ) ;
#67087=CARTESIAN_POINT ( 'NONE',  ( 17.94485468269862238, 2.989306481654914194, 13.55738131293089666 ) ) ;
#67090=CARTESIAN_POINT ( 'NONE',  ( 18.05338926791294440, 2.122656057830398790, 12.53150860927892296 ) ) ;
#67097=CARTESIAN_POINT ( 'NONE',  ( 12.44669855353773080, -1.987833209345829300, 12.55628527126821226 ) ) ;
#67104=CARTESIAN_POINT ( 'NONE',  ( 12.18532624936141673, 0.08167875237852871562, 12.69965198491186342 ) ) ;
#67107=CARTESIAN_POINT ( 'NONE',  ( 12.20865459317944435, 2.312811904845647248, 12.49320495213146032 ) ) ;
#67118=CARTESIAN_POINT ( 'NONE',  ( 17.94287612687506694, -0.4902485962753033166, -12.68726381690838778 ) ) ;
#67139=CONICAL_SURFACE ( 'NONE', #45940, 1.900023899775999947, 0.7853981633972997312 ) ;
#67142=CARTESIAN_POINT ( 'NONE',  ( 17.91964795130429877, 0.5080432161604431229, -13.88750743611951144 ) ) ;
#67147=CARTESIAN_POINT ( 'NONE',  ( 17.77706283214427785, -1.915668542326107726, 13.78016448532189386 ) ) ;
#67148=CARTESIAN_POINT ( 'NONE',  ( 17.59634971246090984, 3.125000000000000000, -13.52084437902332681 ) ) ;
#67151=CARTESIAN_POINT ( 'NONE',  ( 17.55505043854143565, 2.500000000000000000, -25.00000000000000000 ) ) ;
#67159=CARTESIAN_POINT ( 'NONE',  ( 18.13088395572279765, -0.4376617689587271043, -12.59240970319242514 ) ) ;
#67171=CARTESIAN_POINT ( 'NONE',  ( 12.33410680267662762, 3.073228032305981738, 13.65852590327789784 ) ) ;
#67174=CARTESIAN_POINT ( 'NONE',  ( 12.32512882958489797, 0.4004146478932060216, -12.69150435581204661 ) ) ;
#67175=CARTESIAN_POINT ( 'NONE',  ( 12.18940025506974401, -0.3858260082455265971, 13.99468631105251859 ) ) ;
#67187=CARTESIAN_POINT ( 'NONE',  ( 12.60431942020948526, 3.171686099353042909, 12.19427817519220092 ) ) ;
#67188=DIRECTION ( 'NONE',  ( -1.000000000000000000, 0.000000000000000000, 0.000000000000000000 ) ) ;
#67193=LINE ( 'NONE', #13730, #3997 ) ;
#67194=CARTESIAN_POINT ( 'NONE',  ( 12.41685245958457884, 2.003519757588521522, 12.55365090554869134 ) ) ;
#67204=DIRECTION ( 'NONE',  ( -1.000000000000000000, 0.000000000000000000, 0.000000000000000000 ) ) ;
#67211=CARTESIAN_POINT ( 'NONE',  ( 18.20249588168626786, 2.156032850912784404, -12.41417075669994219 ) ) ;
#67216=CARTESIAN_POINT ( 'NONE',  ( 12.33541982639859036, 2.912513636879463075, -13.57727066180432196 ) ) ;
#67224=CARTESIAN_POINT ( 'NONE',  ( 18.17813554646084029, 2.450019327289897575, 12.46306814184580425 ) ) ;
#67227=ORIENTED_EDGE ( 'NONE', *, *, #36325, .T. ) ;
#67229=CARTESIAN_POINT ( 'NONE',  ( 18.03491643637239150, 3.065379368238251079, -13.66028979695642853 ) ) ;
#67230=ORIENTED_EDGE ( 'NONE', *, *, #46883, .F. ) ;
#67244=AXIS2_PLACEMENT_3D ( 'NONE', #44884, #51491, #35087 ) ;
#67246=EDGE_CURVE ( 'NONE', #1476, #33164, #37332, .T. ) ;
#67249=CARTESIAN_POINT ( 'NONE',  ( 17.89634705932800074, -1.976313534945129291, -12.55826774113815425 ) ) ;
#67258=CARTESIAN_POINT ( 'NONE',  ( 12.08891106753597633, 2.402099963521329595, -13.79240636836165201 ) ) ;
#67261=CARTESIAN_POINT ( 'NONE',  ( 18.27048575441378375, -0.1188263301541328115, 13.99950072926553446 ) ) ;
#67282=B_SPLINE_CURVE_WITH_KNOTS ( 'NONE', 3,
 ( #11375, #43899, #59969, #33758, #1587, #44603, #23259, #65894, #55073, #64505, #38999, #16962, #54028, #16626, #49475, #49132, #54727, #7178, #22903, #27827, #11719, #37951, #32716, #6130, #27467, #48794, #28514, #44257, #65203, #903, #33061, #1244, #38295, #22216, #54375, #22557, #17320, #17676, #65553, #60318, #37836, #21748, #27010, #64734, #22094, #57781, #43081, #43439, #9893, #64387, #21074, #31233, #68609, #59158, #4637, #16850, #52540, #16508, #11262, #58473, #90, #63712, #58816, #58134, #47650, #25976, #32599, #47305, #53913, #10923, #26675, #31917, #64046, #20729, #5669, #42058, #32265, #63362, #15489, #42404, #48328, #36816, #53576, #21408, #5330, #6013, #27352, #53231, #433, #47988, #42742, #37491, #4988 ),
 .UNSPECIFIED., .F., .F.,
 ( 4, 2, 2, 2, 2, 2, 2, 2, 2, 1, 1, 2, 2, 2, 2, 2, 2, 2, 2, 2, 2, 2, 2, 2, 2, 2, 2, 2, 2, 2, 2, 2, 2, 1, 1, 2, 2, 2, 2, 1, 2, 2, 2, 2, 2, 2, 2, 2, 4 ),
 ( 0.000000000000000000, 0.03125000000000013878, 0.06250000000000027756, 0.09375000000000041633, 0.1093750000000004441, 0.1250000000000004718, 0.1562499999999978628, 0.1718749999999965583, 0.1874999999999952816, 0.2031249999999939770, 0.2109374999999943934, 0.2148437499999936162, 0.2187499999999929223, 0.2499999999999870659, 0.2656249999999834577, 0.2734374999999816258, 0.2812499999999797384, 0.2968749999999760192, 0.3124999999999722444, 0.3437499999999646949, 0.3593749999999609201, 0.3749999999999570899, 0.4062499999999493738, 0.4374999999999417133, 0.4999999999999258371, 0.5312499999999178435, 0.5624999999999098499, 0.5937499999999019673, 0.6093749999998983036, 0.6249999999998947509, 0.6562499999998887557, 0.6718749999998858691, 0.6874999999998828715, 0.7031249999998799849, 0.7109374999998784306, 0.7148437499998785416, 0.7187499999998785416, 0.7499999999998901989, 0.7656249999998960831, 0.7734374999998989697, 0.7773437499999016342, 0.7812499999999042988, 0.7968749999999096278, 0.8124999999999148459, 0.8437499999999256151, 0.8593749999999320544, 0.8749999999999386047, 0.9374999999999692468, 1.000000000000000000 ),
 .UNSPECIFIED. ) ;
#67294=CARTESIAN_POINT ( 'NONE',  ( 12.39285676950935766, -0.4699213205053973663, -12.68829855189362732 ) ) ;
#67295=CARTESIAN_POINT ( 'NONE',  ( 12.19705744667298575, -2.644897761314413565, -12.41662195506803634 ) ) ;
#67303=CARTESIAN_POINT ( 'NONE',  ( 17.91802421031557913, 0.5088992769509088632, 12.68627498207978377 ) ) ;
#67312=CARTESIAN_POINT ( 'NONE',  ( 18.02418602114746093, -0.5568603909045894973, -13.98892293345219962 ) ) ;
#67321=CARTESIAN_POINT ( 'NONE',  ( 12.18817138783093768, -2.600938394370665208, -13.65148521156285533 ) ) ;
#67332=CARTESIAN_POINT ( 'NONE',  ( 12.44045292577858142, -0.5080432161604421237, -13.88750743611951144 ) ) ;
#67333=CARTESIAN_POINT ( 'NONE',  ( 18.17231130205940204, -2.401422691383821917, 12.47401593597049718 ) ) ;
#67353=CARTESIAN_POINT ( 'NONE',  ( 12.80505043854143388, 1.787816316115912185, -13.88537766212463254 ) ) ;
#67357=CARTESIAN_POINT ( 'NONE',  ( 18.26845433917839756, 0.1286734328892390478, 12.59934825840596595 ) ) ;
#67365=CARTESIAN_POINT ( 'NONE',  ( 5.700000000000000178, 12.03770622561999915, 3.722046322334000124 ) ) ;
#67374=EDGE_CURVE ( 'NONE', #44202, #53037, #18688, .T. ) ;
#67376=CARTESIAN_POINT ( 'NONE',  ( 18.15197774836041589, -2.932501865601731428, -13.68943155935733991 ) ) ;
#67382=ADVANCED_FACE ( 'NONE', ( #65273 ), #6460, .T. ) ;
#67399=CARTESIAN_POINT ( 'NONE',  ( 12.26151780194100382, 2.191289199348897654, -12.51818198400761517 ) ) ;
#67408=CARTESIAN_POINT ( 'NONE',  ( 12.80505043854146940, -3.125000000000000444, -12.28373071562070074 ) ) ;
#67414=CARTESIAN_POINT ( 'NONE',  ( 12.30764200008710496, -3.049303773002894680, -13.66388724637008778 ) ) ;
#67424=CARTESIAN_POINT ( 'NONE',  ( 17.75984001012010438, 3.091833346853859688, 13.52991597407626223 ) ) ;
#67426=FACE_BOUND ( 'NONE', #37947, .T. ) ;
#67427=CARTESIAN_POINT ( 'NONE',  ( 17.55505043854143565, 3.125000000000000000, 12.28373071562070074 ) ) ;
#67433=CARTESIAN_POINT ( 'NONE',  ( 12.54459593125683625, -1.931762302728656122, 12.56598641381995307 ) ) ;
#67440=CARTESIAN_POINT ( 'NONE',  ( 12.37769715316224506, 0.4561785182478241829, 12.68897339690746762 ) ) ;
#67444=CARTESIAN_POINT ( 'NONE',  ( 12.18947222198076652, 2.391413182808838744, 12.47619792628429636 ) ) ;
#67454=ORIENTED_EDGE ( 'NONE', *, *, #46319, .F. ) ;
#67456=CARTESIAN_POINT ( 'NONE',  ( 17.55505043854144276, -0.6250000000000001110, -12.67928921589118474 ) ) ;
#67461=CARTESIAN_POINT ( 'NONE',  ( 12.53658830138318159, -3.196304600777688076, 13.63024796167574948 ) ) ;
#67480=DIRECTION ( 'NONE',  ( 0.000000000000000000, 0.000000000000000000, 1.000000000000000000 ) ) ;
#67485=CARTESIAN_POINT ( 'NONE',  ( 12.80505043854144276, 0.6600719421079733751, -13.91436771118225302 ) ) ;
#67492=CARTESIAN_POINT ( 'NONE',  ( 17.90989566141533018, -3.154773125069390449, 13.63992084652273817 ) ) ;
#67493=CARTESIAN_POINT ( 'NONE',  ( 7.100000000000000533, -12.50865771883999855, -2.924687089723999822 ) ) ;
#67498=DIRECTION ( 'NONE',  ( 0.000000000000000000, 0.9586353287342648244, -0.2846371488448895537 ) ) ;
#67505=CARTESIAN_POINT ( 'NONE',  ( 18.22927867710215111, 0.2646961475753863979, -12.59722401988189588 ) ) ;
#67513=CARTESIAN_POINT ( 'NONE',  ( 17.72120476622713880, 1.779652109340961408, 12.47368672373264076 ) ) ;
#67515=CARTESIAN_POINT ( 'NONE',  ( 12.08136008892999591, 2.567386246332872712, 13.76259835127842024 ) ) ;
#67518=CARTESIAN_POINT ( 'NONE',  ( 12.31443506008844579, 0.3873604450494987361, -12.69205253629085028 ) ) ;
#67520=ORIENTED_EDGE ( 'NONE', *, *, #34589, .F. ) ;
#67530=CARTESIAN_POINT ( 'NONE',  ( 12.63902032760542937, 3.180686373181415671, 12.19193352998605739 ) ) ;
#67531=CARTESIAN_POINT ( 'NONE',  ( 17.55505043854144276, 0.6250000000000001110, 13.88107975066923316 ) ) ;
#67537=CARTESIAN_POINT ( 'NONE',  ( 12.19317846012505591, 2.372225799402258417, 12.48041235930111981 ) ) ;
#67554=CARTESIAN_POINT ( 'NONE',  ( 17.79082714041176772, 1.799831594964171888, -12.47079078729191259 ) ) ;
#67557=CARTESIAN_POINT ( 'NONE',  ( 12.18127175123626493, 2.459544125670197090, -13.68195797701648253 ) ) ;
#67567=FACE_OUTER_BOUND ( 'NONE', #35924, .T. ) ;
#67570=CARTESIAN_POINT ( 'NONE',  ( 18.27395862148967609, 2.614931059283417181, -13.75364391642199280 ) ) ;
#67590=CARTESIAN_POINT ( 'NONE',  ( 17.79060029153385969, -3.161091907734806750, -12.19703033907565981 ) ) ;
#67594=ORIENTED_EDGE ( 'NONE', *, *, #50189, .T. ) ;
#67598=CARTESIAN_POINT ( 'NONE',  ( 12.09915596617137723, 2.684647274610783452, -13.74018952919733394 ) ) ;
#67599=CARTESIAN_POINT ( 'NONE',  ( 17.96742444759810908, 0.6007076874295131930, 13.98710814480368292 ) ) ;
#67613=CARTESIAN_POINT ( 'NONE',  ( 5.500000000000000000, 12.22293997673000021, -3.800173559029999648 ) ) ;
#67632=FACE_BOUND ( 'NONE', #30366, .T. ) ;
#67635=CARTESIAN_POINT ( 'NONE',  ( 12.54926746055851439, 0.6731412448965065076, -12.58200685883812930 ) ) ;
#67636=CARTESIAN_POINT ( 'NONE',  ( 12.21194436379302317, -2.301855881702226991, -12.49553541603750695 ) ) ;
#67642=CARTESIAN_POINT ( 'NONE',  ( 17.59562594671659497, 0.6250000000000000000, 12.67928921589118119 ) ) ;
#67648=VERTEX_POINT ( 'NONE', #68590 ) ;
#67649=EDGE_CURVE ( 'NONE', #24123, #17996, #27335, .T. ) ;
#67652=CARTESIAN_POINT ( 'NONE',  ( 18.27886422513981302, -0.04806343339260844838, -13.99993753789457962 ) ) ;
#67654=DIRECTION ( 'NONE',  ( -1.000000000000000000, 0.000000000000000000, 0.000000000000000000 ) ) ;
#67658=CARTESIAN_POINT ( 'NONE',  ( 17.99289217961977627, -2.946103266178389024, 12.33638055411116241 ) ) ;
#67661=CARTESIAN_POINT ( 'NONE',  ( 12.20137260048311312, -2.663020829440327475, -13.63749600572422871 ) ) ;
#67664=CARTESIAN_POINT ( 'NONE',  ( 5.699996624164000103, -12.50864642754000045, -2.924703664565999617 ) ) ;
#67672=CARTESIAN_POINT ( 'NONE',  ( 12.18402495282434295, -0.07112389991331875827, -13.89976024287834910 ) ) ;
#67673=CARTESIAN_POINT ( 'NONE',  ( 17.89701680218578517, -1.976751596789643850, 12.55823001632907499 ) ) ;
#67680=AXIS2_PLACEMENT_3D ( 'NONE', #61208, #39537, #3160 ) ;
#67688=ORIENTED_EDGE ( 'NONE', *, *, #58887, .F. ) ;
#67699=CARTESIAN_POINT ( 'NONE',  ( 18.27044763842722830, -0.1172743548790616819, 12.59945959730644027 ) ) ;
#67705=CARTESIAN_POINT ( 'NONE',  ( 18.03520353647598995, 3.065561386738592020, 13.66025540057654553 ) ) ;
#67706=FACE_BOUND ( 'NONE', #11735, .T. ) ;
#67716=CARTESIAN_POINT ( 'NONE',  ( 17.92259505138777698, -3.107618780086669918, 12.21081961728240195 ) ) ;
#67726=AXIS2_PLACEMENT_3D ( 'NONE', #3746, #52682, #25082 ) ;
#67739=CARTESIAN_POINT ( 'NONE',  ( 12.25653845796823482, 2.200227119461481529, -12.51640343681226142 ) ) ;
#67743=CARTESIAN_POINT ( 'NONE',  ( 4.649999478197480052, 2.033928581112999763E-13, -2.806643806251999915E-13 ) ) ;
#67747=CARTESIAN_POINT ( 'NONE',  ( 12.42670498308437210, -2.997500030636913060, -12.32161918487003582 ) ) ;
#67753=CARTESIAN_POINT ( 'NONE',  ( 12.80505043854146763, -3.248147246781389885, -13.61798588129780896 ) ) ;
#67757=FACE_OUTER_BOUND ( 'NONE', #50463, .T. ) ;
#67760=CARTESIAN_POINT ( 'NONE',  ( 12.71012435277331853, 0.7254930141035413893, -13.98119259374237444 ) ) ;
#67763=CARTESIAN_POINT ( 'NONE',  ( 17.99248396117510751, 2.946503669282361404, 13.56850299727437736 ) ) ;
#67765=DIRECTION ( 'NONE',  ( 0.000000000000000000, 1.000000000000000000, 0.000000000000000000 ) ) ;
#67767=CARTESIAN_POINT ( 'NONE',  ( 18.06437450929126243, 2.862796250983955737, 12.35961424106609208 ) ) ;
#67786=CARTESIAN_POINT ( 'NONE',  ( 12.29717897459458875, 0.3644117276601258060, 12.69296657371243953 ) ) ;
#67795=CARTESIAN_POINT ( 'NONE',  ( 17.93834580300581649, 2.005905130196157238, 13.76587868752632460 ) ) ;
#67806=CARTESIAN_POINT ( 'NONE',  ( 18.13779378220194971, -2.273859756726421377, -13.71877938508614037 ) ) ;
#67834=CARTESIAN_POINT ( 'NONE',  ( 18.13175260058829963, -2.961013189755323349, 13.68330200419956988 ) ) ;
#67835=CARTESIAN_POINT ( 'NONE',  ( 17.81487012556099359, 3.068783844977785336, -13.53623303301527159 ) ) ;
#67839=EDGE_LOOP ( 'NONE', ( #45955, #53973, #10368, #48760 ) ) ;
#67846=CARTESIAN_POINT ( 'NONE',  ( 18.27886405737313069, 0.04734719685816928675, -12.59993264914401401 ) ) ;
#67857=CARTESIAN_POINT ( 'NONE',  ( 12.33310466175876741, 1.963577280744727149, 13.86161695422964435 ) ) ;
#67860=CARTESIAN_POINT ( 'NONE',  ( 12.23148815955158142, 0.2485241243229640573, -12.69673260777818946 ) ) ;
#67863=CARTESIAN_POINT ( 'NONE',  ( 12.53842061970401822, -0.6791475903684007775, 13.98351814429473094 ) ) ;
#67866=CARTESIAN_POINT ( 'NONE',  ( 12.19289742234822072, -2.094552964378148641, 12.42468808284045245 ) ) ;
#67873=CYLINDRICAL_SURFACE ( 'NONE', #47673, 13.17499999999999893 ) ;
#67876=CARTESIAN_POINT ( 'NONE',  ( 12.24851426484563177, 2.019008278824861335, 12.43718985311489966 ) ) ;
#67880=CARTESIAN_POINT ( 'NONE',  ( 12.80505043854144276, 0.6249999999999994449, -12.67928921589118652 ) ) ;
#67881=EDGE_CURVE ( 'NONE', #36489, #31711, #46775, .T. ) ;
#67885=LINE ( 'NONE', #46577, #47530 ) ;
#67895=CARTESIAN_POINT ( 'NONE',  ( 12.25784352200408200, 2.802116367125526253, 13.60467368965351120 ) ) ;
#67903=CARTESIAN_POINT ( 'NONE',  ( 18.26259847173841422, 2.320949922530730181, -12.38441499264346390 ) ) ;
#67905=CARTESIAN_POINT ( 'NONE',  ( 18.01268549161953914, 2.926083040867999863, 12.34202569327310250 ) ) ;
#67906=CARTESIAN_POINT ( 'NONE',  ( 12.42225203016886148, 3.001455243200948253, -13.55441486462863665 ) ) ;
#67911=CARTESIAN_POINT ( 'NONE',  ( 12.12629894760562621, 0.2577288767859165497, -13.99764474128114777 ) ) ;
#67919=CARTESIAN_POINT ( 'NONE',  ( 18.03598133453868968, 1.971494603937298917, -13.86049335245054159 ) ) ;
#67932=VERTEX_POINT ( 'NONE', #36977 ) ;
#67938=CARTESIAN_POINT ( 'NONE',  ( 17.77742128654740839, -1.915804696728240941, -12.56864479336926088 ) ) ;
#67950=CARTESIAN_POINT ( 'NONE',  ( 12.75695158412489150, 3.246897126047498361, -13.61828421767944164 ) ) ;
#67951=CARTESIAN_POINT ( 'NONE',  ( 18.25212991285166808, 0.2010519787742756082, 13.99856097495847607 ) ) ;
#67961=ADVANCED_FACE ( 'NONE', ( #11768 ), #5146, .F. ) ;
#67971=CARTESIAN_POINT ( 'NONE',  ( 18.18005043799237086, -2.500000011518549670, 12.45159158845318359 ) ) ;
#67982=CARTESIAN_POINT ( 'NONE',  ( 12.60420289721210985, -0.5919389804100259056, -12.68142457171642690 ) ) ;
#67983=CARTESIAN_POINT ( 'NONE',  ( 12.21947784592275354, -2.718529665895031311, -12.39796232698949652 ) ) ;
#68001=EDGE_CURVE ( 'NONE', #66715, #59809, #44305, .T. ) ;
#68010=CARTESIAN_POINT ( 'NONE',  ( 12.25784352200452787, -2.802116367126311403, -13.60467368965330337 ) ) ;
#68023=CARTESIAN_POINT ( 'NONE',  ( 18.18008862603428710, -2.492635669256735298, 12.45330984115723361 ) ) ;
#68025=ADVANCED_FACE ( 'NONE', ( #49522 ), #6173, .F. ) ;
#68028=ORIENTED_EDGE ( 'NONE', *, *, #67881, .T. ) ;
#68044=FACE_OUTER_BOUND ( 'NONE', #20486, .T. ) ;
#68047=CARTESIAN_POINT ( 'NONE',  ( 12.80505043854146940, -3.174834474598374090, 12.21921104873077013 ) ) ;
#68049=CARTESIAN_POINT ( 'NONE',  ( 18.20545956023470779, 0.3178346465811124899, 12.59599179195193663 ) ) ;
#68084=CARTESIAN_POINT ( 'NONE',  ( 12.20882029558151949, 2.312280790556523247, -12.49335225873939770 ) ) ;
#68094=CARTESIAN_POINT ( 'NONE',  ( 12.75673482301077932, -1.762409409947525374, -12.47613375359912524 ) ) ;
#68100=CARTESIAN_POINT ( 'NONE',  ( 12.27233953995990134, -2.172968329541576704, -13.73735571485410745 ) ) ;
#68108=DIRECTION ( 'NONE',  ( -1.000000000000000000, 0.000000000000000000, 0.000000000000000000 ) ) ;
#68110=CARTESIAN_POINT ( 'NONE',  ( 18.17514039568614237, 2.578830838032381223, 13.65637626280583561 ) ) ;
#68113=FACE_BOUND ( 'NONE', #53075, .T. ) ;
#68114=CARTESIAN_POINT ( 'NONE',  ( 17.88765289689606064, 3.029249243711964468, 12.31236272700674839 ) ) ;
#68120=CARTESIAN_POINT ( 'NONE',  ( 12.23541831425122872, -2.757387829712826033, 12.38789221355391312 ) ) ;
#68129=CARTESIAN_POINT ( 'NONE',  ( 12.42410782380136780, -0.4959072410923938690, 12.68697406334525368 ) ) ;
#68149=CARTESIAN_POINT ( 'NONE',  ( 18.18012160401611155, -2.482106737233723326, -13.67720576235794816 ) ) ;
#68167=EDGE_CURVE ( 'NONE', #7389, #32586, #47731, .T. ) ;
#68174=CARTESIAN_POINT ( 'NONE',  ( 18.06209397514829718, -1.995989992690351933, 13.85698731868970413 ) ) ;
#68180=FILL_AREA_STYLE ('',( #52106 ) ) ;
#68187=CARTESIAN_POINT ( 'NONE',  ( 18.18883553772844763, 0.3494793053307434505, -12.59515668824706580 ) ) ;
#68188=CARTESIAN_POINT ( 'NONE',  ( 12.60033281150904472, 3.091857377016624220, -12.29379371307818225 ) ) ;
#68196=CARTESIAN_POINT ( 'NONE',  ( 12.36102515544322600, 1.940652449090402021, 13.86484480881333070 ) ) ;
#68199=CARTESIAN_POINT ( 'NONE',  ( 12.15449479986287251, -0.3231860383015694449, 13.99628497142876249 ) ) ;
#68201=CARTESIAN_POINT ( 'NONE',  ( 12.70926349491446672, -1.766754859226808305, 12.47551934520473260 ) ) ;
#68206=EDGE_CURVE ( 'NONE', #48764, #38102, #51121, .T. ) ;
#68211=CARTESIAN_POINT ( 'NONE',  ( 12.32336322858527744, 1.942450600934330085, 12.44937554728605100 ) ) ;
#68219=CARTESIAN_POINT ( 'NONE',  ( 12.30490414476351013, 2.123060221900641587, 12.53148904350137016 ) ) ;
#68223=CARTESIAN_POINT ( 'NONE',  ( 12.43800415128889725, -0.5060493095660281160, 12.68643001347753518 ) ) ;
#68230=CARTESIAN_POINT ( 'NONE',  ( 12.72264977853956580, -3.119885623323980894, 13.52225790872755873 ) ) ;
#68238=CARTESIAN_POINT ( 'NONE',  ( 17.91266776300914643, 3.012678901972745571, -12.31722829471395997 ) ) ;
#68240=CARTESIAN_POINT ( 'NONE',  ( 18.04518119037968660, 2.887943935962514086, 12.35267345330769473 ) ) ;
#68242=CARTESIAN_POINT ( 'NONE',  ( 12.64149076269671923, 3.109019952263742947, -13.52530492583441024 ) ) ;
#68251=CARTESIAN_POINT ( 'NONE',  ( 17.72046959774372965, 1.875000000000000444, 12.57541560742027364 ) ) ;
#68257=CARTESIAN_POINT ( 'NONE',  ( 17.94049251029957048, 1.899108762321197963, -13.87060088084272813 ) ) ;
#68265=EDGE_LOOP ( 'NONE', ( #47344, #10102, #43094, #27167 ) ) ;
#68266=CARTESIAN_POINT ( 'NONE',  ( 43.76123417800000226, -11.06886219213000011, 1.536526853569999851 ) ) ;
#68275=CARTESIAN_POINT ( 'NONE',  ( 18.11779302252799440, -2.227307244339886250, -12.51093773244153873 ) ) ;
#68279=CARTESIAN_POINT ( 'NONE',  ( 18.16429560770317408, -2.358968865818011018, -12.48332026670070860 ) ) ;
#68286=CARTESIAN_POINT ( 'NONE',  ( 17.60274960888721552, 0.7290235424212095916, 13.98100605002522734 ) ) ;
#68307=CARTESIAN_POINT ( 'NONE',  ( 4.599999999999999645, 3.125000000000000000, 13.52078605991414939 ) ) ;
#68319=CARTESIAN_POINT ( 'NONE',  ( 12.50079267818768258, 0.5460377805369034387, -12.68419612078312042 ) ) ;
#68320=CARTESIAN_POINT ( 'NONE',  ( 12.25843860534618202, -2.803243370077761476, -12.37572767902445925 ) ) ;
#68322=DIRECTION ( 'NONE',  ( -1.000000000000000000, 0.000000000000000000, 0.000000000000000000 ) ) ;
#68325=PLANE ( 'NONE',  #44461 ) ;
#68328=EDGE_CURVE ( 'NONE', #20140, #40405, #26976, .T. ) ;
#68348=CARTESIAN_POINT ( 'NONE',  ( 12.19231142703039339, -2.623190749633721897, -13.64650702417935157 ) ) ;
#68374=CARTESIAN_POINT ( 'NONE',  ( 18.02801947735587618, 0.4085868565813729480, 13.89191718360218353 ) ) ;
#68376=CARTESIAN_POINT ( 'NONE',  ( 12.80505043854144276, 0.6249999999999994449, 13.88107975066923316 ) ) ;
#68382=CARTESIAN_POINT ( 'NONE',  ( 12.07940096941472241, 2.330761819168849502, -13.80597083265678826 ) ) ;
#68387=CARTESIAN_POINT ( 'NONE',  ( 18.22055608408778937, 0.2856017019952105662, 12.59676745213710625 ) ) ;
#68391=ORIENTED_EDGE ( 'NONE', *, *, #23539, .F. ) ;
#68393=CARTESIAN_POINT ( 'NONE',  ( 18.10159474502872357, 2.998280829653924506, 13.67518427740799680 ) ) ;
#68395=ORIENTED_EDGE ( 'NONE', *, *, #52164, .T. ) ;
#68421=CARTESIAN_POINT ( 'NONE',  ( 18.08617702649035763, 0.3300666952397346421, -13.89473968862477449 ) ) ;
#68431=CONICAL_SURFACE ( 'NONE', #20434, 13.22499948080999843, 0.7853981240402999608 ) ;
#68435=CARTESIAN_POINT ( 'NONE',  ( 12.37577160951054367, -2.954704321271699907, -12.33392404961604072 ) ) ;
#68441=CARTESIAN_POINT ( 'NONE',  ( 12.52647507922624115, -1.940423270478297768, -13.77628945559398588 ) ) ;
#68444=CARTESIAN_POINT ( 'NONE',  ( 17.88886072129112748, -3.119102935781168817, 12.20783478086260487 ) ) ;
#68451=CARTESIAN_POINT ( 'NONE',  ( 17.96133816917716786, 2.975035784927402727, 12.32810058309831014 ) ) ;
#68454=EDGE_LOOP ( 'NONE', ( #41339, #44965, #47534, #16677 ) ) ;
#68456=EDGE_LOOP ( 'NONE', ( #7542, #47299, #36719, #59506 ) ) ;
#68457=CARTESIAN_POINT ( 'NONE',  ( 12.36494524852001398, -2.943800415886788979, 12.33703218264930079 ) ) ;
#68463=CIRCLE ( 'NONE', #58446, 2.200000000000001954 ) ;
#68466=CARTESIAN_POINT ( 'NONE',  ( 12.46581852961811698, -0.5250240499537052186, 12.68539034781188413 ) ) ;
#68476=CARTESIAN_POINT ( 'NONE',  ( 12.43753697068043884, -3.107573092003766746, -12.21083123506395118 ) ) ;
#68482=CARTESIAN_POINT ( 'NONE',  ( 5.655092287087765790, -12.08052032219203831, 3.735600122826553182 ) ) ;
#68490=CARTESIAN_POINT ( 'NONE',  ( 18.16473232272958427, -2.360987313248031683, -13.70192779769509528 ) ) ;
#68492=CARTESIAN_POINT ( 'NONE',  ( 4.599999999999999645, 0.7192913403693006469, 12.57945229203838444 ) ) ;
#68500=DIRECTION ( 'NONE',  ( -1.000000000000000000, 0.000000000000000000, 0.000000000000000000 ) ) ;
#68509=ORIENTED_EDGE ( 'NONE', *, *, #20125, .F. ) ;
#68511=CARTESIAN_POINT ( 'NONE',  ( 12.40905465428145504, 1.877469967418645247, -12.45933993000109119 ) ) ;
#68516=CARTESIAN_POINT ( 'NONE',  ( 18.27122651615335158, -2.402315819361985572, 13.79236889726217186 ) ) ;
#68529=CARTESIAN_POINT ( 'NONE',  ( 17.55505043854144276, 0.6250000000000001110, -12.67928921589118652 ) ) ;
#68538=AXIS2_PLACEMENT_3D ( 'NONE', #58747, #63980, #366 ) ;
#68540=CARTESIAN_POINT ( 'NONE',  ( 12.09886375431303485, 2.684759089869686477, 13.74018286504951192 ) ) ;
#68542=CARTESIAN_POINT ( 'NONE',  ( 12.40638932695447672, -0.4813547430241597036, -12.68771948605803424 ) ) ;
#68544=CARTESIAN_POINT ( 'NONE',  ( 12.71024384884961833, -0.7243378955761884397, 13.98124959093732400 ) ) ;
#68552=EDGE_CURVE ( 'NONE', #57647, #20309, #36118, .T. ) ;
#68556=CARTESIAN_POINT ( 'NONE',  ( 12.07989974639899167, 2.471827770301481042, 12.35516928474874554 ) ) ;
#68564=CARTESIAN_POINT ( 'NONE',  ( 12.72293129229312747, 3.125000000000000444, 12.28373127578716328 ) ) ;
#68566=EDGE_LOOP ( 'NONE', ( #22230, #15656, #66726, #29179 ) ) ;
#68573=CARTESIAN_POINT ( 'NONE',  ( 12.23409240334736658, -2.245563803222850652, 13.72414218390522223 ) ) ;
#68574=CARTESIAN_POINT ( 'NONE',  ( 5.500000000000000000, 13.17499999999999893, 0.000000000000000000 ) ) ;
#68582=CARTESIAN_POINT ( 'NONE',  ( 18.05208962242102189, 2.879457400869559702, -12.35505085550156323 ) ) ;
#68585=CARTESIAN_POINT ( 'NONE',  ( 17.59643454745089386, 3.125000000000000444, 12.28373095898682621 ) ) ;
#68590=CARTESIAN_POINT ( 'NONE',  ( 17.55505043854143565, 3.125000000000000000, 12.28373071562070074 ) ) ;
#68609=CARTESIAN_POINT ( 'NONE',  ( 12.20071588509496863, 0.1606973242730105611, -13.89876784138466626 ) ) ;
#68619=VERTEX_POINT ( 'NONE', #62343 ) ;
#68621=CARTESIAN_POINT ( 'NONE',  ( 18.02661896923965656, -2.910306870311579974, -12.34644497411517250 ) ) ;
#68642=CARTESIAN_POINT ( 'NONE',  ( 12.72306420252713544, -3.125000000000000888, 13.52084465375506461 ) ) ;
#68656=CARTESIAN_POINT ( 'NONE',  ( 18.16752965492863936, 2.624502287304359527, -12.42171427742621859 ) ) ;
#68667=ORIENTED_EDGE ( 'NONE', *, *, #28754, .T. ) ;
#68668=CARTESIAN_POINT ( 'NONE',  ( 12.24904276456879160, -0.2856309244984034379, -12.69568149856438311 ) ) ;
#68669=CARTESIAN_POINT ( 'NONE',  ( 12.80505043854146940, -3.125000000000000000, -12.28373071562070074 ) ) ;
#68688=CARTESIAN_POINT ( 'NONE',  ( 17.60274960888721552, -0.7290235424212396786, -13.98100605002522734 ) ) ;
#68704=CARTESIAN_POINT ( 'NONE',  ( 17.88386803568321426, 0.5319881936868626759, -13.88630234897434690 ) ) ;
#68709=CARTESIAN_POINT ( 'NONE',  ( 12.23542143184359965, 2.757395375068925514, 13.61543998564091140 ) ) ;
#68711=VERTEX_POINT ( 'NONE', #11598 ) ;
#68717=CARTESIAN_POINT ( 'NONE',  ( 12.42175510762288404, 2.005905104281934914, -13.76592701692033138 ) ) ;
#68719=CARTESIAN_POINT ( 'NONE',  ( 18.14710216240463581, -0.2005085131878108218, 13.89805835524349931 ) ) ;
#68723=CARTESIAN_POINT ( 'NONE',  ( 12.43800705108280802, 0.5060514261277413439, 13.88760251447654781 ) ) ;
#68735=FACE_OUTER_BOUND ( 'NONE', #17609, .T. ) ;
#68737=CARTESIAN_POINT ( 'NONE',  ( 18.27538032657185951, -0.08234928811777071644, 12.59973629603894096 ) ) ;
#68743=CARTESIAN_POINT ( 'NONE',  ( 18.12392562323100265, 2.970749524062570313, 13.68118179967288128 ) ) ;
#68765=CARTESIAN_POINT ( 'NONE',  ( 17.55505043854144276, 0.6250000000000001110, -12.67928921589118474 ) ) ;
#68769=CARTESIAN_POINT ( 'NONE',  ( 17.86832607310548582, 0.5412024733746048089, -13.88582008197801976 ) ) ;
#68775=LINE ( 'NONE', #4800, #56550 ) ;
#68786=CARTESIAN_POINT ( 'NONE',  ( 12.67197039647513535, -3.110753821461599067, -12.28805851341190980 ) ) ;
#68789=DIRECTION ( 'NONE',  ( 1.000000000000000000, 0.000000000000000000, 0.000000000000000000 ) ) ;
#68790=CARTESIAN_POINT ( 'NONE',  ( 12.15975302296895499, -2.850959433913118346, -13.70664605376239287 ) ) ;
#68793=CARTESIAN_POINT ( 'NONE',  ( 18.28026264019201363, -2.471821293434737665, 12.35517058147370761 ) ) ;
#68797=LINE ( 'NONE', #41215, #40299 ) ;
#68801=CARTESIAN_POINT ( 'NONE',  ( 18.15889616939339035, 2.662482328103963791, 12.41224410776442966 ) ) ;
#68806=ADVANCED_FACE ( 'NONE', ( #66470 ), #33984, .F. ) ;
#68808=CARTESIAN_POINT ( 'NONE',  ( 12.52601681438820869, -3.059349880828010626, 12.30349483713085057 ) ) ;
#68838=CARTESIAN_POINT ( 'NONE',  ( 18.14470825305572532, -2.707255376881378961, 13.62731588230026070 ) ) ;
#68841=CARTESIAN_POINT ( 'NONE',  ( 18.17891560871130707, -2.542711950176887559, -13.66427582110434713 ) ) ;
#68850=DIRECTION ( 'NONE',  ( 0.000000000000000000, 0.9553735099700838562, -0.2954005017724949944 ) ) ;
#68859=CARTESIAN_POINT ( 'NONE',  ( 12.70926349491442764, 1.766754859226804086, -12.47551934520473083 ) ) ;
#68864=CARTESIAN_POINT ( 'NONE',  ( 18.15341532599041230, -2.105586285009643177, 13.84075898842494468 ) ) ;
#68871=SURFACE_STYLE_FILL_AREA ( #68180 ) ;
#68874=CARTESIAN_POINT ( 'NONE',  ( 6.166666667118732015, -12.50864712907674381, 2.924698073458500414 ) ) ;
#68879=CARTESIAN_POINT ( 'NONE',  ( 18.10066919781365513, -0.4738025322793328886, -12.59109159930368627 ) ) ;
#68893=CARTESIAN_POINT ( 'NONE',  ( 12.37275785088829316, -0.4515912411692236117, -12.68919663782859963 ) ) ;
#68898=EDGE_CURVE ( 'NONE', #59588, #7219, #57797, .T. ) ;
#68903=EDGE_CURVE ( 'NONE', #7230, #3060, #52108, .T. ) ;
#68904=CARTESIAN_POINT ( 'NONE',  ( 12.17712767754846759, 0.3597466176220713852, 12.59486741915706531 ) ) ;
#68907=CARTESIAN_POINT ( 'NONE',  ( 12.08117318674009688, 2.436835578774657396, 12.36211850556986569 ) ) ;
#68919=CARTESIAN_POINT ( 'NONE',  ( 12.40293124239839173, 0.4784650741312070354, 12.68786664693105593 ) ) ;
#68927=CARTESIAN_POINT ( 'NONE',  ( 12.22230712497533034, -2.273859679217654861, 13.71882920742291745 ) ) ;
#68928=CARTESIAN_POINT ( 'NONE',  ( 12.18211070746967728, 2.551853945066973939, 13.66227842075671184 ) ) ;
#68936=CARTESIAN_POINT ( 'NONE',  ( 18.17829451895831738, 2.452078260301032042, -12.46263202712694707 ) ) ;
#68938=CARTESIAN_POINT ( 'NONE',  ( 18.13624051175171203, 2.730018211965808295, 12.39499564928988207 ) ) ;
#68943=CARTESIAN_POINT ( 'NONE',  ( 12.43745875767134734, 1.881346041122103907, 13.87306493545927033 ) ) ;
#68946=FACE_OUTER_BOUND ( 'NONE', #40949, .T. ) ;
#68967=AXIS2_PLACEMENT_3D ( 'NONE', #54092, #21927, #43265 ) ;
#68970=AXIS2_PLACEMENT_3D ( 'NONE', #15809, #417, #58119 ) ;
#68974=CARTESIAN_POINT ( 'NONE',  ( 18.12879050829621619, -2.748092781515380167, -12.39029782533441804 ) ) ;
#68976=CIRCLE ( 'NONE', #31017, 13.17499999999999538 ) ;
#68977=CARTESIAN_POINT ( 'NONE',  ( 18.14750831225986261, -2.299919533022120710, -12.49594326303513370 ) ) ;
#68983=CIRCLE ( 'NONE', #32172, 13.89999852641999922 ) ;
#69015=CARTESIAN_POINT ( 'NONE',  ( 18.28081516007887330, 2.296096720429526616, 12.39048987307994842 ) ) ;
#69018=CARTESIAN_POINT ( 'NONE',  ( 12.26342954938197316, 0.3125562302819458460, -12.69484091569604089 ) ) ;
#69036=CARTESIAN_POINT ( 'NONE',  ( 17.69878333211497434, 3.108595074582393369, -13.52536937155546504 ) ) ;
#69046=CARTESIAN_POINT ( 'NONE',  ( 18.14887404798968618, 0.1995702674084748607, -12.69797248607429374 ) ) ;
#69048=EDGE_CURVE ( 'NONE', #62522, #7389, #40939, .T. ) ;
#69060=CARTESIAN_POINT ( 'NONE',  ( 17.91028475965239153, -1.853043856158717029, -12.46299565389693242 ) ) ;
#69061=CARTESIAN_POINT ( 'NONE',  ( 17.60655599801540561, -0.6229596466635308749, -12.67942438339646749 ) ) ;
#69063=CARTESIAN_POINT ( 'NONE',  ( 5.700000000000000178, 13.94845324556000143, -4.312847325879000770 ) ) ;
#69071=CARTESIAN_POINT ( 'NONE',  ( 12.60210251410535420, 1.908512130997219725, -13.78126077419328332 ) ) ;
#69078=CARTESIAN_POINT ( 'NONE',  ( 12.66331021901985032, 0.6090267839138837624, 13.88203573366629762 ) ) ;
#69089=CARTESIAN_POINT ( 'NONE',  ( 17.81315952985430684, -0.5693054069933379813, 12.68281928773556366 ) ) ;
#69090=B_SPLINE_SURFACE_WITH_KNOTS ( 'NONE', 1, 3, ( 
 ( #55687, #50784, #51124, #45198, #3558, #2533, #67530, #45877, #67187, #8475, #18964, #14069, #19299, #35393, #56719, #8814, #7784, #13724, #46222, #50430, #35053, #34710, #66503, #18624, #19652, #39953, #61271, #13388, #2879, #24202, #45544, #40290, #5279, #10187, #36068, #58084, #37105, #57383, #36763, #52140, #31517, #53181, #21024, #58763, #42358, #10869, #52839, #15775, #42690, #63659, #58419, #9488, #10524, #68556, #3898, #68907, #14750, #31864, #26621, #42009, #4934, #46909, #47940, #30830, #4243, #47253, #15438, #25582, #25233, #25923, #32214, #46567, #21360, #62625, #26273, #67876, #19996, #63310, #41320, #40, #4585, #68211, #47599, #20330, #41658, #9839, #62962, #63998, #16116, #20678, #37442, #15090, #36414, #57728, #31184, #52489, #381, #22392, #65730, #5620, #60494, #28339, #43729, #59799, #59451, #17853, #26961, #53528 ),
 ( #38124, #11901, #53863, #60154, #32550, #49658, #54560, #33239, #17144, #48971, #22734, #49307, #1419, #44083, #38476, #64337, #65027, #6657, #12603, #27998, #64688, #23085, #44432, #65382, #12258, #5964, #39171, #17503, #16455, #38826, #27650, #54904, #33587, #37787, #7007, #1767, #59108, #48275, #27302, #21697, #43033, #11214, #48626, #729, #22041, #43388, #16796, #11549, #32892, #54202, #6303, #1077, #8046, #66421, #7349, #2796, #34970, #13309, #29389, #55253, #67444, #56630, #13986, #67107, #23435, #2453, #55602, #44774, #61188, #62211, #19215, #39517, #51040, #51378, #33934, #45113, #39869, #56287, #34281, #23778, #28694, #8733, #2118, #30078, #8392, #24122, #50699, #34630, #55943, #40542, #45457, #66769, #66074, #24813, #18887, #45794, #40212, #18542, #61528, #61866, #29737, #19567, #3477, #13643, #7703, #35312, #3141, #24470 ) ),
 .UNSPECIFIED., .F., .F., .F.,
 ( 2, 2 ),
 ( 4, 2, 2, 2, 2, 2, 2, 2, 2, 2, 2, 2, 2, 2, 2, 2, 2, 2, 2, 2, 2, 2, 2, 2, 2, 2, 2, 2, 2, 2, 2, 2, 2, 2, 2, 2, 2, 2, 2, 2, 2, 2, 2, 2, 2, 2, 2, 2, 2, 2, 2, 2, 2, 4 ),
 ( 0.000000000000000000, 1.000000000000000000 ),
 ( 0.000000000000000000, 7.156607294609336489E-05, 0.0001431321458921867298, 0.0001789151823652334054, 0.0002146982188382801082, 0.0002325897370748034325, 0.0002504812553113267568, 0.0002862642917843734596, 0.0003220473282574201623, 0.0003578303647304668109, 0.0003936134012035135137, 0.0004293964376765602164, 0.0004651794741496068650, 0.0004830709923861301893, 0.0005009625106226535136, 0.0005725285835687469191, 0.0006440946565148403247, 0.0007156607294609336218, 0.0007872268024070270273, 0.0008587928753531204329, 0.0008945759118261670815, 0.0009303589482992137300, 0.0009661419847722603786, 0.001001925021245307027, 0.001037708057718353784, 0.001073491094191400541, 0.001145057167137493838, 0.001180840203610540595, 0.001216623240083587135, 0.001252406276556633892, 0.001288189313029680649, 0.001359755385975773946, 0.001395538422448820703, 0.001431321458921867244, 0.001467104495394914001, 0.001502887531867960758, 0.001574453604814054055, 0.001646019677760147352, 0.001681802714233194109, 0.001717585750706240866, 0.001753368787179287406, 0.001789151823652334163, 0.001860717896598427460, 0.001896500933071474000, 0.001932283969544520757, 0.001968067006017567514, 0.002003850042490614054, 0.002039633078963661028, 0.002075416115436707568, 0.002146982188382801082, 0.002182765224855847622, 0.002218548261328894163, 0.002254331297801941136, 0.002290114334274987676 ),
 .UNSPECIFIED. ) ;
#69100=B_SPLINE_CURVE_WITH_KNOTS ( 'NONE', 3,
 ( #28394, #44825, #1817, #28046, #12307, #27351, #38526, #59848, #54253, #48674, #39221, #6012, #12654, #55304, #1125, #43438 ),
 .UNSPECIFIED., .F., .F.,
 ( 4, 2, 2, 2, 2, 2, 2, 4 ),
 ( 0.000000000000000000, 0.06249999999999879263, 0.1249999999999975853, 0.2499999999999972800, 0.4999999999999981126, 0.7499999999999987788, 0.8749999999999994449, 1.000000000000000000 ),
 .UNSPECIFIED. ) ;
#69105=CARTESIAN_POINT ( 'NONE',  ( 12.51647491292534120, -0.6599616342124140500, -12.58270523616455350 ) ) ;
#69107=CARTESIAN_POINT ( 'NONE',  ( 18.13174941159750730, 2.917101476509660785, -12.25768593326185574 ) ) ;
#69138=CARTESIAN_POINT ( 'NONE',  ( 12.18370898482675280, -2.431702807279748413, -12.46721300078355554 ) ) ;
#69140=CARTESIAN_POINT ( 'NONE',  ( 17.55505043854147118, -1.875000000000000000, -12.57541666120755863 ) ) ;
#69142=CARTESIAN_POINT ( 'NONE',  ( 12.25717089523538483, -2.039201503940136551, -13.85070424198620742 ) ) ;
#69145=CARTESIAN_POINT ( 'NONE',  ( 18.18591139755470820, -2.124730565513616831, 12.41957995629783440 ) ) ;
#69157=CARTESIAN_POINT ( 'NONE',  ( 18.20346453091165273, -2.853274009397274380, -12.27345743255177446 ) ) ;
#69160=CARTESIAN_POINT ( 'NONE',  ( 12.33348197901556276, -2.910306952023486549, 12.34646687328217141 ) ) ;
#69161=DIRECTION ( 'NONE',  ( 0.000000000000000000, 1.000000000000000000, 0.000000000000000000 ) ) ;
#69165=CARTESIAN_POINT ( 'NONE',  ( 12.21985383964851657, -0.2197131112048753554, 12.69744725510431493 ) ) ;
#69166=CARTESIAN_POINT ( 'NONE',  ( 5.648274849241648354, -12.08704511044963326, -3.737576519652977769 ) ) ;
#69185=CARTESIAN_POINT ( 'NONE',  ( 18.10189407302238607, -2.802802817710309480, -13.60450747121971204 ) ) ;
ENDSEC;
END-ISO-10303-21;
